ISO-10303-21;
HEADER;
FILE_DESCRIPTION (('STEP AP203'),
    '1' );
FILE_NAME ('Plastic Part 2.step',
    '2026-10-08T23:54:15',
    ( '' ),
    ( '' ),
    'SwSTEP 2.0',
    'SolidWorks 2024',
    '' );
FILE_SCHEMA (( 'AUTOMOTIVE_DESIGN' ));
ENDSEC;

DATA;
#9=ORIENTED_EDGE ( 'NONE', *, *, #75672, .F. ) ;
#19=ORIENTED_EDGE ( 'NONE', *, *, #7474, .F. ) ;
#26=CARTESIAN_POINT ( 'NONE',  ( 25.13610348050010757, -5.148720480136078415, -8.780752235156151997 ) ) ;
#33=EDGE_LOOP ( 'NONE', ( #82636, #82631 ) ) ;
#34=ORIENTED_EDGE ( 'NONE', *, *, #61187, .T. ) ;
#39=ORIENTED_EDGE ( 'NONE', *, *, #46353, .T. ) ;
#55=CARTESIAN_POINT ( 'NONE',  ( 0.000000000000000000, -4.056774720514426669, 0.000000000000000000 ) ) ;
#56=ADVANCED_FACE ( 'NONE', ( #60747 ), #53135, .F. ) ;
#66=ORIENTED_EDGE ( 'NONE', *, *, #66534, .T. ) ;
#70=CARTESIAN_POINT ( 'NONE',  ( 14.43441819135929194, -3.316774720514426456, -28.36222020317710957 ) ) ;
#85=SHAPE_DEFINITION_REPRESENTATION ( #13430, #26923 ) ;
#91=CARTESIAN_POINT ( 'NONE',  ( -1.836964591723098117, -5.876774720514410966, 19.23384392940399223 ) ) ;
#106=CARTESIAN_POINT ( 'NONE',  ( 0.000000000000000000, -6.376774720514426953, 0.000000000000000000 ) ) ;
#109=ORIENTED_EDGE ( 'NONE', *, *, #9060, .T. ) ;
#112=CARTESIAN_POINT ( 'NONE',  ( -8.978253834636468866, -6.376774720514426953, 0.000000000000000000 ) ) ;
#119=CIRCLE ( 'NONE', #69815, 6.000000000000000888 ) ;
#123=ORIENTED_EDGE ( 'NONE', *, *, #75034, .F. ) ;
#126=DIRECTION ( 'NONE',  ( 0.000000000000000000, 0.000000000000000000, 1.000000000000000000 ) ) ;
#129=EDGE_LOOP ( 'NONE', ( #2287, #83763, #40797, #42125 ) ) ;
#131=LINE ( 'NONE', #46818, #56738 ) ;
#142=ORIENTED_EDGE ( 'NONE', *, *, #69534, .F. ) ;
#143=CARTESIAN_POINT ( 'NONE',  ( 32.98210467718394767, -3.587965230352024193, -12.99284425914657604 ) ) ;
#156=EDGE_LOOP ( 'NONE', ( #85113, #7630, #40085, #37423 ) ) ;
#160=CARTESIAN_POINT ( 'NONE',  ( -7.586742644780859912, -6.376774720514413630, 19.78730719034165020 ) ) ;
#167=CARTESIAN_POINT ( 'NONE',  ( 7.479587785762670471, -5.876774720514418071, 20.73799387832858088 ) ) ;
#176=CARTESIAN_POINT ( 'NONE',  ( -10.24059822343752479, -5.876774720514426953, -2.394817856121274864E-14 ) ) ;
#180=CARTESIAN_POINT ( 'NONE',  ( 30.77564450787170003, 1.477225279485574028, -9.689394075852829857 ) ) ;
#184=ORIENTED_EDGE ( 'NONE', *, *, #85046, .F. ) ;
#190=CARTESIAN_POINT ( 'NONE',  ( 3.475076759263674209, -5.876774720514402084, 18.20843037655054530 ) ) ;
#195=ADVANCED_FACE ( 'NONE', ( #77436 ), #54627, .F. ) ;
#202=LINE ( 'NONE', #46883, #26152 ) ;
#206=CARTESIAN_POINT ( 'NONE',  ( 4.518955212990007908, -6.376774720514422512, 20.94857968174986951 ) ) ;
#213=DIRECTION ( 'NONE',  ( -0.000000000000000000, 1.000000000000000000, -0.000000000000000000 ) ) ;
#215=CARTESIAN_POINT ( 'NONE',  ( -0.4362980769230789257, -5.876774720514411854, 19.46153846153846345 ) ) ;
#220=CARTESIAN_POINT ( 'NONE',  ( 11.98973536156539943, -4.132774720514426292, -26.26140391504922178 ) ) ;
#222=DIRECTION ( 'NONE',  ( -0.000000000000000000, -1.000000000000000000, -0.000000000000000000 ) ) ;
#223=ADVANCED_FACE ( 'NONE', ( #39891 ), #24162, .F. ) ;
#240=DIRECTION ( 'NONE',  ( -0.000000000000000000, 1.000000000000000000, -0.000000000000000000 ) ) ;
#245=LINE ( 'NONE', #62665, #68980 ) ;
#249=CARTESIAN_POINT ( 'NONE',  ( 4.886128916861816052, -6.376774720514411854, 19.14085035285361514 ) ) ;
#262=FACE_OUTER_BOUND ( 'NONE', #1139, .T. ) ;
#265=CARTESIAN_POINT ( 'NONE',  ( -1.358974358974357921, -5.876774720514419847, 20.75510817307693046 ) ) ;
#266=ORIENTED_EDGE ( 'NONE', *, *, #94468, .T. ) ;
#268=DIRECTION ( 'NONE',  ( 1.286817348990133655E-16, 0.000000000000000000, -1.000000000000000000 ) ) ;
#281=CARTESIAN_POINT ( 'NONE',  ( 8.476323908314187250, -3.316774720514010788, -27.09030197646909599 ) ) ;
#289=ORIENTED_EDGE ( 'NONE', *, *, #88515, .T. ) ;
#296=VECTOR ( 'NONE', #83307, 1000.000000000000000 ) ;
#301=CARTESIAN_POINT ( 'NONE',  ( 32.06540688909005610, 6.475225279485576024, -12.44045471929206137 ) ) ;
#308=ORIENTED_EDGE ( 'NONE', *, *, #56022, .T. ) ;
#320=LINE ( 'NONE', #47507, #53904 ) ;
#329=CARTESIAN_POINT ( 'NONE',  ( -65.05438548721848235, 6.475225279485573360, 0.7300228001186309656 ) ) ;
#342=CARTESIAN_POINT ( 'NONE',  ( 2.708118538500707828, -6.376774720514424288, 20.94830092343283212 ) ) ;
#365=PLANE ( 'NONE',  #20104 ) ;
#404=VERTEX_POINT ( 'NONE', #20055 ) ;
#405=CARTESIAN_POINT ( 'NONE',  ( 4.588387839717440464, -6.376774720514401196, 18.52756237589653665 ) ) ;
#409=CARTESIAN_POINT ( 'NONE',  ( 13.10664265030973930, -0.3587747205144256601, -28.18129937523770678 ) ) ;
#412=CARTESIAN_POINT ( 'NONE',  ( 6.586338672804227024, -6.376774720514415407, 20.10086663068103618 ) ) ;
#417=EDGE_CURVE ( 'NONE', #44756, #35967, #96677, .T. ) ;
#418=FACE_OUTER_BOUND ( 'NONE', #18116, .T. ) ;
#429=EDGE_CURVE ( 'NONE', #17186, #23237, #19052, .T. ) ;
#431=DIRECTION ( 'NONE',  ( 0.000000000000000000, 0.000000000000000000, -1.000000000000000000 ) ) ;
#448=CARTESIAN_POINT ( 'NONE',  ( 6.259688558337090036, -6.376774720514413630, 19.73360741988579292 ) ) ;
#451=VERTEX_POINT ( 'NONE', #89074 ) ;
#452=DIRECTION ( 'NONE',  ( -1.000000000000000000, -0.000000000000000000, 0.000000000000000000 ) ) ;
#483=VECTOR ( 'NONE', #28798, 1000.000000000000000 ) ;
#490=DIRECTION ( 'NONE',  ( 0.000000000000000000, 0.000000000000000000, 1.000000000000000000 ) ) ;
#496=ADVANCED_FACE ( 'NONE', ( #26678 ), #64262, .F. ) ;
#497=VERTEX_POINT ( 'NONE', #65759 ) ;
#510=AXIS2_PLACEMENT_3D ( 'NONE', #90538, #91038, #83925 ) ;
#511=ORIENTED_EDGE ( 'NONE', *, *, #19314, .F. ) ;
#531=EDGE_LOOP ( 'NONE', ( #4697, #60989, #55794, #22828 ) ) ;
#532=EDGE_LOOP ( 'NONE', ( #32047, #70301, #41788, #57216 ) ) ;
#533=EDGE_CURVE ( 'NONE', #69177, #58343, #27177, .T. ) ;
#534=VERTEX_POINT ( 'NONE', #2346 ) ;
#537=ORIENTED_EDGE ( 'NONE', *, *, #81268, .F. ) ;
#552=CARTESIAN_POINT ( 'NONE',  ( 31.63587494018430135, -3.477878053198200536, 27.33969830395653844 ) ) ;
#554=LINE ( 'NONE', #43992, #61943 ) ;
#568=ORIENTED_EDGE ( 'NONE', *, *, #24222, .F. ) ;
#574=VECTOR ( 'NONE', #95324, 1000.000000000000114 ) ;
#581=ORIENTED_EDGE ( 'NONE', *, *, #67321, .F. ) ;
#602=CARTESIAN_POINT ( 'NONE',  ( -3.035630128403670192, -5.876774720514413630, 19.71630089903357685 ) ) ;
#604=CARTESIAN_POINT ( 'NONE',  ( 5.541369867593821219, -5.876774720514425177, 21.42815349816763160 ) ) ;
#613=ADVANCED_FACE ( 'NONE', ( #67746 ), #98663, .F. ) ;
#636=ORIENTED_EDGE ( 'NONE', *, *, #46341, .F. ) ;
#638=CARTESIAN_POINT ( 'NONE',  ( 2.834823996951755465, -5.876774720514406525, 18.76222163777333307 ) ) ;
#641=DIRECTION ( 'NONE',  ( 0.000000000000000000, -0.000000000000000000, 1.000000000000000000 ) ) ;
#645=B_SPLINE_CURVE_WITH_KNOTS ( 'NONE', 3,
 ( #31561, #54913, #56430, #2635, #32062, #40689 ),
 .UNSPECIFIED., .F., .F.,
 ( 4, 2, 4 ),
 ( 0.000000000000000000, 0.0005049716539041804782, 0.001009943307808368112 ),
 .UNSPECIFIED. ) ;
#650=ORIENTED_EDGE ( 'NONE', *, *, #19881, .T. ) ;
#653=EDGE_CURVE ( 'NONE', #30045, #37372, #13928, .T. ) ;
#657=CARTESIAN_POINT ( 'NONE',  ( -7.338700834008208496, -6.376774720514410077, 19.35116211686183263 ) ) ;
#659=DIRECTION ( 'NONE',  ( 0.000000000000000000, 0.000000000000000000, 1.000000000000000000 ) ) ;
#661=CARTESIAN_POINT ( 'NONE',  ( 6.480733632922428988, -5.876774720514425177, 21.47849199606610782 ) ) ;
#666=ORIENTED_EDGE ( 'NONE', *, *, #32067, .F. ) ;
#667=EDGE_CURVE ( 'NONE', #75528, #29344, #20541, .T. ) ;
#678=DIRECTION ( 'NONE',  ( 0.000000000000000000, -1.000000000000000000, 0.000000000000000000 ) ) ;
#688=CARTESIAN_POINT ( 'NONE',  ( 4.780030342074717886, -6.376774720514424288, 21.16398229115527130 ) ) ;
#691=CARTESIAN_POINT ( 'NONE',  ( -29.49875734969026198, 5.965225279485572685, 10.11402280011862587 ) ) ;
#694=CARTESIAN_POINT ( 'NONE',  ( -28.98875734969026396, -6.376774720514426953, -0.08597719988137648983 ) ) ;
#705=CARTESIAN_POINT ( 'NONE',  ( 5.642884982650352654, -6.376774720514426065, 20.85668005806743608 ) ) ;
#710=CARTESIAN_POINT ( 'NONE',  ( 32.25249349869195470, 1.477225279485574028, -12.65342752644894553 ) ) ;
#712=CARTESIAN_POINT ( 'NONE',  ( 0.3908843598833069422, -5.876774720514419847, 20.63520656483649773 ) ) ;
#720=ORIENTED_EDGE ( 'NONE', *, *, #23043, .T. ) ;
#721=ADVANCED_FACE ( 'NONE', ( #54500 ), #56013, .F. ) ;
#723=LINE ( 'NONE', #93064, #9580 ) ;
#729=CARTESIAN_POINT ( 'NONE',  ( 30.09341516180546350, 1.477225279485574028, -11.39311774897855933 ) ) ;
#730=ADVANCED_FACE ( 'NONE', ( #69730 ), #16418, .F. ) ;
#740=ORIENTED_EDGE ( 'NONE', *, *, #89907, .T. ) ;
#741=EDGE_CURVE ( 'NONE', #6280, #91104, #48516, .T. ) ;
#748=ORIENTED_EDGE ( 'NONE', *, *, #93099, .F. ) ;
#757=CARTESIAN_POINT ( 'NONE',  ( -4.358143420448500116, -6.376774720514413630, 19.75705121608222115 ) ) ;
#761=ORIENTED_EDGE ( 'NONE', *, *, #9232, .T. ) ;
#768=CARTESIAN_POINT ( 'NONE',  ( -1.649669150391666506, -5.876774720514411854, 19.67464842890028365 ) ) ;
#769=EDGE_CURVE ( 'NONE', #68993, #8748, #86444, .T. ) ;
#777=ORIENTED_EDGE ( 'NONE', *, *, #8668, .F. ) ;
#784=CARTESIAN_POINT ( 'NONE',  ( 11.32388168880214074, -5.356774720514423827, -25.00917421515942962 ) ) ;
#798=VECTOR ( 'NONE', #16545, 1000.000000000000000 ) ;
#807=EDGE_CURVE ( 'NONE', #15795, #18354, #1717, .T. ) ;
#817=ORIENTED_EDGE ( 'NONE', *, *, #100163, .F. ) ;
#819=CARTESIAN_POINT ( 'NONE',  ( -2.794793911895765870, -5.876774720514415407, 20.33046051580616265 ) ) ;
#820=CARTESIAN_POINT ( 'NONE',  ( 22.02124265030973760, 7.743225279485574042, 13.95402280011862395 ) ) ;
#822=LINE ( 'NONE', #56131, #34201 ) ;
#824=AXIS2_PLACEMENT_3D ( 'NONE', #32054, #1622, #63528 ) ;
#826=FACE_OUTER_BOUND ( 'NONE', #14399, .T. ) ;
#831=CARTESIAN_POINT ( 'NONE',  ( 22.81105451610979173, 8.475225279485572472, -17.31691820600746823 ) ) ;
#834=CARTESIAN_POINT ( 'NONE',  ( -24.90875734969025501, -3.316774720514426456, 26.43402280011862615 ) ) ;
#861=CARTESIAN_POINT ( 'NONE',  ( -2.794871794871795156, -6.376774720514417183, 20.36318108974359475 ) ) ;
#862=EDGE_CURVE ( 'NONE', #94971, #29990, #58017, .T. ) ;
#863=ORIENTED_EDGE ( 'NONE', *, *, #769, .F. ) ;
#875=CARTESIAN_POINT ( 'NONE',  ( -5.596556251055551101, -5.876774720514411854, 19.35667676486397681 ) ) ;
#881=VERTEX_POINT ( 'NONE', #41793 ) ;
#883=EDGE_LOOP ( 'NONE', ( #19897, #19757, #32178, #74503 ) ) ;
#885=ORIENTED_EDGE ( 'NONE', *, *, #55746, .F. ) ;
#894=CARTESIAN_POINT ( 'NONE',  ( 3.903461913076534451, -6.376774720514404748, 18.52532880998198905 ) ) ;
#901=AXIS2_PLACEMENT_3D ( 'NONE', #66757, #28172, #59131 ) ;
#910=CARTESIAN_POINT ( 'NONE',  ( -5.850750514176234596, -5.876774720514412742, 19.74039977944280366 ) ) ;
#920=CARTESIAN_POINT ( 'NONE',  ( 6.727829057902616761, -6.376774720514417183, 20.13865202822440281 ) ) ;
#926=EDGE_CURVE ( 'NONE', #39625, #82409, #57518, .T. ) ;
#930=CARTESIAN_POINT ( 'NONE',  ( 27.53860345374808105, 1.477225279485574028, 19.84760796525321425 ) ) ;
#944=VECTOR ( 'NONE', #15821, 1000.000000000000114 ) ;
#946=CARTESIAN_POINT ( 'NONE',  ( -17.66201745896767505, -0.3587747205144061202, -23.06272557202527906 ) ) ;
#949=DIRECTION ( 'NONE',  ( 0.000000000000000000, 0.000000000000000000, 1.000000000000000000 ) ) ;
#955=CARTESIAN_POINT ( 'NONE',  ( 5.327901167172695907, -6.376774720514418959, 20.73192761314082233 ) ) ;
#957=CYLINDRICAL_SURFACE ( 'NONE', #40692, 15.00000000000000178 ) ;
#960=CARTESIAN_POINT ( 'NONE',  ( -6.720452724358975338, -5.876774720514411854, 19.46153846153846700 ) ) ;
#971=AXIS2_PLACEMENT_3D ( 'NONE', #59783, #12083, #52157 ) ;
#980=CARTESIAN_POINT ( 'NONE',  ( -1.022535880784302353, -6.376774720514415407, 19.99258394656883908 ) ) ;
#986=CIRCLE ( 'NONE', #64243, 28.96799999999999287 ) ;
#987=EDGE_CURVE ( 'NONE', #54720, #90018, #13072, .T. ) ;
#993=EDGE_CURVE ( 'NONE', #81513, #4283, #67618, .T. ) ;
#998=DIRECTION ( 'NONE',  ( 0.7512896232465891000, 0.000000000000000000, 0.6599726524652351767 ) ) ;
#1006=CARTESIAN_POINT ( 'NONE',  ( -7.294102189209645815, -5.876774720514413630, 19.89644244529368677 ) ) ;
#1008=ORIENTED_EDGE ( 'NONE', *, *, #52103, .F. ) ;
#1013=ORIENTED_EDGE ( 'NONE', *, *, #9905, .F. ) ;
#1020=VERTEX_POINT ( 'NONE', #99033 ) ;
#1024=DIRECTION ( 'NONE',  ( 0.6177208787939497681, 0.000000000000000000, 0.7863974287229267279 ) ) ;
#1027=ADVANCED_FACE ( 'NONE', ( #74222 ), #19924, .F. ) ;
#1031=VECTOR ( 'NONE', #20783, 1000.000000000000114 ) ;
#1035=CARTESIAN_POINT ( 'NONE',  ( 4.819673832743241348, -5.876774720514421624, 21.07066438048017076 ) ) ;
#1040=B_SPLINE_CURVE_WITH_KNOTS ( 'NONE', 3,
 ( #7269, #70178, #76768, #9271 ),
 .UNSPECIFIED., .F., .F.,
 ( 4, 4 ),
 ( 0.001505373688938434684, 0.001772001984008341434 ),
 .UNSPECIFIED. ) ;
#1041=EDGE_CURVE ( 'NONE', #71460, #94222, #85959, .T. ) ;
#1054=CARTESIAN_POINT ( 'NONE',  ( 3.025806405283164136, -6.376774720514420736, 20.84867811309776542 ) ) ;
#1061=VECTOR ( 'NONE', #9585, 1000.000000000000000 ) ;
#1062=CARTESIAN_POINT ( 'NONE',  ( 29.72095141006403196, -6.296447751620394939, 26.96056093718771152 ) ) ;
#1063=FACE_OUTER_BOUND ( 'NONE', #36465, .T. ) ;
#1078=DIRECTION ( 'NONE',  ( -0.000000000000000000, 0.000000000000000000, -1.000000000000000000 ) ) ;
#1082=CARTESIAN_POINT ( 'NONE',  ( -2.794871794871791604, -6.376774720514427841, 21.75000000000001066 ) ) ;
#1096=LINE ( 'NONE', #22405, #90649 ) ;
#1100=EDGE_CURVE ( 'NONE', #65855, #79408, #1096, .T. ) ;
#1104=TOROIDAL_SURFACE ( 'NONE', #25364, 80.18232118519038920, 8.160000000000000142 ) ;
#1107=EDGE_CURVE ( 'NONE', #68694, #33348, #54517, .T. ) ;
#1116=AXIS2_PLACEMENT_3D ( 'NONE', #81771, #19857, #64077 ) ;
#1117=EDGE_LOOP ( 'NONE', ( #16397, #1638, #88766, #59303 ) ) ;
#1134=ORIENTED_EDGE ( 'NONE', *, *, #56098, .T. ) ;
#1139=EDGE_LOOP ( 'NONE', ( #55624, #82005, #26037, #95401 ) ) ;
#1142=CARTESIAN_POINT ( 'NONE',  ( -0.001774553997815280816, -6.376774720514413630, 19.59623724171353487 ) ) ;
#1146=ORIENTED_EDGE ( 'NONE', *, *, #3873, .T. ) ;
#1158=VERTEX_POINT ( 'NONE', #78691 ) ;
#1162=EDGE_CURVE ( 'NONE', #13059, #68694, #93933, .T. ) ;
#1170=DIRECTION ( 'NONE',  ( 4.251773225433346808E-15, 0.000000000000000000, -1.000000000000000000 ) ) ;
#1178=AXIS2_PLACEMENT_3D ( 'NONE', #59730, #45004, #75923 ) ;
#1189=EDGE_CURVE ( 'NONE', #54238, #76045, #40157, .T. ) ;
#1193=EDGE_LOOP ( 'NONE', ( #61323, #11249, #53370, #4307, #94744 ) ) ;
#1200=ORIENTED_EDGE ( 'NONE', *, *, #18607, .F. ) ;
#1201=CARTESIAN_POINT ( 'NONE',  ( 4.966987340572156739, -5.876774720514417183, 20.16530235339958210 ) ) ;
#1204=EDGE_CURVE ( 'NONE', #7479, #61485, #73937, .T. ) ;
#1216=CARTESIAN_POINT ( 'NONE',  ( 6.546094359317672584, -6.376774720514411854, 19.73546617144828375 ) ) ;
#1223=EDGE_CURVE ( 'NONE', #98531, #71754, #51619, .T. ) ;
#1226=ORIENTED_EDGE ( 'NONE', *, *, #78966, .F. ) ;
#1242=CARTESIAN_POINT ( 'NONE',  ( 32.16024265030974050, 5.965225279485572685, 16.27760796525321751 ) ) ;
#1246=EDGE_CURVE ( 'NONE', #44958, #35328, #87838, .T. ) ;
#1266=CARTESIAN_POINT ( 'NONE',  ( 3.769940963823357638, -6.376774720514402972, 18.16074422543206879 ) ) ;
#1267=ORIENTED_EDGE ( 'NONE', *, *, #93453, .F. ) ;
#1270=DIRECTION ( 'NONE',  ( 7.994117400814786717E-16, 0.000000000000000000, -1.000000000000000000 ) ) ;
#1272=CARTESIAN_POINT ( 'NONE',  ( -4.194375271223358403, -6.376774720514417183, 20.09898898868106087 ) ) ;
#1282=VERTEX_POINT ( 'NONE', #49790 ) ;
#1284=DIRECTION ( 'NONE',  ( -0.2488812114211667037, 0.000000000000000000, -0.9685340172660599212 ) ) ;
#1287=DIRECTION ( 'NONE',  ( 0.6599726524652350657, 0.000000000000000000, -0.7512896232465892110 ) ) ;
#1289=EDGE_LOOP ( 'NONE', ( #77277, #33087, #83521, #33162, #33804, #78860, #58280, #20417, #73763, #77798, #100157, #5747, #24089, #27868, #8227, #81213 ) ) ;
#1295=CARTESIAN_POINT ( 'NONE',  ( -5.891025641025637860, -6.376774720514427841, 21.75000000000000711 ) ) ;
#1302=DIRECTION ( 'NONE',  ( 0.000000000000000000, 1.064096645546785541E-13, -1.000000000000000000 ) ) ;
#1306=DIRECTION ( 'NONE',  ( -0.000000000000000000, -1.000000000000000000, -0.000000000000000000 ) ) ;
#1309=FACE_OUTER_BOUND ( 'NONE', #15010, .T. ) ;
#1310=EDGE_CURVE ( 'NONE', #58916, #71424, #75858, .T. ) ;
#1314=CARTESIAN_POINT ( 'NONE',  ( 14.56569730433575138, -3.366897624368339059, -28.38594530802194882 ) ) ;
#1317=ORIENTED_EDGE ( 'NONE', *, *, #68324, .T. ) ;
#1319=CARTESIAN_POINT ( 'NONE',  ( -4.223504350552545361, -5.876774720514411854, 19.52341893546492813 ) ) ;
#1343=DIRECTION ( 'NONE',  ( 0.000000000000000000, 0.000000000000000000, 1.000000000000000000 ) ) ;
#1345=CARTESIAN_POINT ( 'NONE',  ( -10.54059822343757880, -5.876774720514426953, 22.82308057603841078 ) ) ;
#1354=ADVANCED_FACE ( 'NONE', ( #67013 ), #82212, .T. ) ;
#1359=CARTESIAN_POINT ( 'NONE',  ( 2.589743589743596086, -6.376774720514415407, 20.00140224358974095 ) ) ;
#1361=FACE_OUTER_BOUND ( 'NONE', #49208, .T. ) ;
#1369=DIRECTION ( 'NONE',  ( -0.000000000000000000, 1.000000000000000000, -0.000000000000000000 ) ) ;
#1370=CARTESIAN_POINT ( 'NONE',  ( 15.00914443175702573, -3.504414796833706713, -27.32709449451501982 ) ) ;
#1372=ADVANCED_FACE ( 'NONE', ( #20299 ), #97442, .T. ) ;
#1381=DIRECTION ( 'NONE',  ( -1.526034937513432889E-15, 7.121496375062686157E-15, -1.000000000000000000 ) ) ;
#1386=CARTESIAN_POINT ( 'NONE',  ( -5.530932042872791499, -6.376774720514410077, 19.30497968945844534 ) ) ;
#1389=VERTEX_POINT ( 'NONE', #97924 ) ;
#1391=DIRECTION ( 'NONE',  ( -0.000000000000000000, -1.000000000000000000, -0.000000000000000000 ) ) ;
#1406=CARTESIAN_POINT ( 'NONE',  ( 4.413617546364139166, -6.376774720514406525, 18.86076033669171181 ) ) ;
#1408=EDGE_LOOP ( 'NONE', ( #69793, #49827, #66585, #25732 ) ) ;
#1434=CYLINDRICAL_SURFACE ( 'NONE', #78097, 1.149999999999998135 ) ;
#1448=CARTESIAN_POINT ( 'NONE',  ( -29.49875734969026198, 5.965225279485572685, 10.11402280011862587 ) ) ;
#1453=DIRECTION ( 'NONE',  ( 0.000000000000000000, 1.000000000000000000, 0.000000000000000000 ) ) ;
#1466=CIRCLE ( 'NONE', #58180, 3.349999999999998757 ) ;
#1469=ORIENTED_EDGE ( 'NONE', *, *, #69482, .T. ) ;
#1512=VERTEX_POINT ( 'NONE', #37038 ) ;
#1526=CARTESIAN_POINT ( 'NONE',  ( -6.636054160061366503, -6.376774720514411854, 19.15289935703627933 ) ) ;
#1528=VERTEX_POINT ( 'NONE', #98927 ) ;
#1531=ORIENTED_EDGE ( 'NONE', *, *, #27283, .F. ) ;
#1533=CARTESIAN_POINT ( 'NONE',  ( 0.000000000000000000, 0.000000000000000000, 0.000000000000000000 ) ) ;
#1536=CARTESIAN_POINT ( 'NONE',  ( 25.90238399655805424, -5.165317243602335573, -7.576880152980976391 ) ) ;
#1539=AXIS2_PLACEMENT_3D ( 'NONE', #3296, #82877, #51450 ) ;
#1542=FACE_OUTER_BOUND ( 'NONE', #9586, .T. ) ;
#1547=VERTEX_POINT ( 'NONE', #52769 ) ;
#1548=CARTESIAN_POINT ( 'NONE',  ( 30.76755528059980804, -5.112846897994270279, -0.3209731499739113536 ) ) ;
#1550=AXIS2_PLACEMENT_3D ( 'NONE', #4421, #21116, #66832 ) ;
#1560=CARTESIAN_POINT ( 'NONE',  ( 2.935461252226840401, -5.876774720514419847, 20.47627681611744777 ) ) ;
#1563=ORIENTED_EDGE ( 'NONE', *, *, #34195, .F. ) ;
#1565=EDGE_CURVE ( 'NONE', #12606, #15278, #66525, .T. ) ;
#1569=CARTESIAN_POINT ( 'NONE',  ( 29.60459817610514932, -4.854569207680477838, 28.81138945959710185 ) ) ;
#1578=DIRECTION ( 'NONE',  ( -0.9952638024365005887, 0.000000000000000000, -0.09721092304694052555 ) ) ;
#1585=DIRECTION ( 'NONE',  ( 1.000000000000000000, -4.088963247170718308E-15, 0.000000000000000000 ) ) ;
#1588=VERTEX_POINT ( 'NONE', #99909 ) ;
#1590=DIRECTION ( 'NONE',  ( -0.6599726524652352877, 0.000000000000000000, 0.7512896232465892110 ) ) ;
#1612=AXIS2_PLACEMENT_3D ( 'NONE', #15470, #91600, #22078 ) ;
#1613=CARTESIAN_POINT ( 'NONE',  ( 10.86929179853872007, -4.313324117933219348, -26.78630334068696683 ) ) ;
#1617=AXIS2_PLACEMENT_3D ( 'NONE', #35698, #42821, #90475 ) ;
#1622=DIRECTION ( 'NONE',  ( -0.000000000000000000, 1.000000000000000000, -0.000000000000000000 ) ) ;
#1637=CARTESIAN_POINT ( 'NONE',  ( 6.944081373883786767, -5.876774720514424288, 21.27829155525578031 ) ) ;
#1638=ORIENTED_EDGE ( 'NONE', *, *, #39342, .F. ) ;
#1647=CARTESIAN_POINT ( 'NONE',  ( 7.087697398486194622, -5.876774720514418071, 20.45710073441444621 ) ) ;
#1648=CARTESIAN_POINT ( 'NONE',  ( 29.73860345376319003, 1.477225279485574028, 19.84760796525321425 ) ) ;
#1653=CARTESIAN_POINT ( 'NONE',  ( 2.710830299132254595, -5.876774720514410966, 19.05039662921485544 ) ) ;
#1665=ORIENTED_EDGE ( 'NONE', *, *, #86622, .F. ) ;
#1672=AXIS2_PLACEMENT_3D ( 'NONE', #11370, #57563, #88500 ) ;
#1683=EDGE_LOOP ( 'NONE', ( #83248, #93624, #3389, #39960, #41208, #59557 ) ) ;
#1689=CARTESIAN_POINT ( 'NONE',  ( 7.480769230769231726, -6.376774720514420736, 20.77403846153845635 ) ) ;
#1698=ORIENTED_EDGE ( 'NONE', *, *, #40048, .F. ) ;
#1701=CARTESIAN_POINT ( 'NONE',  ( 31.63207147031214106, -3.934018429836814601, 27.19231918963763661 ) ) ;
#1705=CARTESIAN_POINT ( 'NONE',  ( 4.910384361841649614, -5.876774720514419847, 20.73924463800384643 ) ) ;
#1707=CARTESIAN_POINT ( 'NONE',  ( 11.62916340711181284, -0.3587747205144265483, 28.75961759920349792 ) ) ;
#1710=ORIENTED_EDGE ( 'NONE', *, *, #76950, .F. ) ;
#1715=CARTESIAN_POINT ( 'NONE',  ( 4.487249349319938574, -6.376774720514420736, 21.01618089687719504 ) ) ;
#1717=LINE ( 'NONE', #9820, #11057 ) ;
#1718=CARTESIAN_POINT ( 'NONE',  ( 5.727631217150810805, -6.376774720514422512, 21.11407618546790133 ) ) ;
#1726=EDGE_CURVE ( 'NONE', #35033, #10968, #71419, .T. ) ;
#1731=VECTOR ( 'NONE', #34361, 1000.000000000000000 ) ;
#1756=VERTEX_POINT ( 'NONE', #82951 ) ;
#1758=CYLINDRICAL_SURFACE ( 'NONE', #23351, 2.499999999999995115 ) ;
#1759=CARTESIAN_POINT ( 'NONE',  ( 5.271800844963591359, -6.376774720514426953, -28.56638892015329034 ) ) ;
#1764=DIRECTION ( 'NONE',  ( -0.000000000000000000, 1.000000000000000000, -0.000000000000000000 ) ) ;
#1772=DIRECTION ( 'NONE',  ( 0.000000000000000000, -1.000000000000000000, 0.000000000000000000 ) ) ;
#1777=PLANE ( 'NONE',  #19270 ) ;
#1782=LINE ( 'NONE', #47960, #73331 ) ;
#1789=CARTESIAN_POINT ( 'NONE',  ( 5.251006604497604258, -6.376774720514426953, -25.47015536487705489 ) ) ;
#1790=CARTESIAN_POINT ( 'NONE',  ( 5.097264368844747651, -3.299463065352477908, -27.56135813788838718 ) ) ;
#1801=CARTESIAN_POINT ( 'NONE',  ( 29.80070917940689768, -3.316774720514426456, 27.39560796525317343 ) ) ;
#1808=CARTESIAN_POINT ( 'NONE',  ( 10.24059822343757808, -5.876774720514426953, 22.08128695274315945 ) ) ;
#1814=ORIENTED_EDGE ( 'NONE', *, *, #51149, .F. ) ;
#1817=B_SPLINE_CURVE_WITH_KNOTS ( 'NONE', 3,
 ( #51353, #72200, #35632, #11288, #82294, #26521, #33631, #97517, #12273, #80806, #18893, #95526, #73688, #12772 ),
 .UNSPECIFIED., .F., .F.,
 ( 4, 2, 2, 2, 2, 2, 4 ),
 ( 0.000000000000000000, 0.002392375077555367480, 0.003588562616333051004, 0.004784750155110734093, 0.005980937693888416749, 0.007177125232666099405, 0.009569500310221466452 ),
 .UNSPECIFIED. ) ;
#1819=ORIENTED_EDGE ( 'NONE', *, *, #48420, .T. ) ;
#1820=ORIENTED_EDGE ( 'NONE', *, *, #75680, .F. ) ;
#1829=CARTESIAN_POINT ( 'NONE',  ( -5.053929855541893446, -5.876774720514408301, 19.14848118821636547 ) ) ;
#1839=CARTESIAN_POINT ( 'NONE',  ( 7.089543269230769162, -6.376774720514413630, 19.75741185897435415 ) ) ;
#1848=CARTESIAN_POINT ( 'NONE',  ( -4.495793269230770939, -6.376774720514410077, 19.27714342948718595 ) ) ;
#1855=DIRECTION ( 'NONE',  ( 0.000000000000000000, 0.000000000000000000, 1.000000000000000000 ) ) ;
#1875=DIRECTION ( 'NONE',  ( 1.000000000000000000, 0.000000000000000000, 0.000000000000000000 ) ) ;
#1881=DIRECTION ( 'NONE',  ( -0.000000000000000000, -1.000000000000000000, -0.000000000000000000 ) ) ;
#1885=ORIENTED_EDGE ( 'NONE', *, *, #82355, .T. ) ;
#1890=ORIENTED_EDGE ( 'NONE', *, *, #23545, .T. ) ;
#1896=VERTEX_POINT ( 'NONE', #43911 ) ;
#1902=CIRCLE ( 'NONE', #11584, 2.249999999999998668 ) ;
#1904=CARTESIAN_POINT ( 'NONE',  ( 4.653515142448186204, -6.376774720514413630, 19.86181745814487343 ) ) ;
#1920=CARTESIAN_POINT ( 'NONE',  ( -5.923037968371668072, -5.876774720514414518, 19.62288733224861303 ) ) ;
#1934=ADVANCED_FACE ( 'NONE', ( #9327 ), #55020, .F. ) ;
#1935=AXIS2_PLACEMENT_3D ( 'NONE', #45851, #76770, #7779 ) ;
#1936=EDGE_CURVE ( 'NONE', #35496, #42575, #20808, .T. ) ;
#1943=CARTESIAN_POINT ( 'NONE',  ( -7.312991930324885814, -5.876774720514413630, 20.02088365235844947 ) ) ;
#1944=DIRECTION ( 'NONE',  ( -0.000000000000000000, 1.000000000000000000, -0.000000000000000000 ) ) ;
#1948=ORIENTED_EDGE ( 'NONE', *, *, #29490, .T. ) ;
#1949=CARTESIAN_POINT ( 'NONE',  ( -5.533628790199073499, -6.376774720514417183, 19.87297243748313491 ) ) ;
#1953=LINE ( 'NONE', #92528, #99744 ) ;
#1966=CARTESIAN_POINT ( 'NONE',  ( 27.53860345374808105, -4.772774720514425972, -8.321925749325261634 ) ) ;
#1979=TOROIDAL_SURFACE ( 'NONE', #39249, 25.90800000000000125, 3.060000000000000053 ) ;
#1980=EDGE_LOOP ( 'NONE', ( #35560, #60896, #54666, #76639 ) ) ;
#1990=DIRECTION ( 'NONE',  ( -0.000000000000000000, 1.000000000000000000, -0.000000000000000000 ) ) ;
#2006=FACE_OUTER_BOUND ( 'NONE', #59724, .T. ) ;
#2012=ADVANCED_FACE ( 'NONE', ( #69741 ), #30347, .T. ) ;
#2017=ADVANCED_FACE ( 'NONE', ( #10842 ), #88969, .T. ) ;
#2019=CARTESIAN_POINT ( 'NONE',  ( 13.10664265030973930, 5.965225279485574461, -28.18129937516157568 ) ) ;
#2026=ORIENTED_EDGE ( 'NONE', *, *, #14356, .T. ) ;
#2034=CARTESIAN_POINT ( 'NONE',  ( 0.1309051665272248643, -6.376774720514413630, 19.34190049657482291 ) ) ;
#2045=DIRECTION ( 'NONE',  ( -0.000000000000000000, 0.000000000000000000, -1.000000000000000000 ) ) ;
#2048=FACE_OUTER_BOUND ( 'NONE', #90624, .T. ) ;
#2055=ORIENTED_EDGE ( 'NONE', *, *, #92519, .T. ) ;
#2059=AXIS2_PLACEMENT_3D ( 'NONE', #61741, #84552, #69841 ) ;
#2062=CARTESIAN_POINT ( 'NONE',  ( 32.74409430444596580, -4.661791533294295853, -3.688467650546950249 ) ) ;
#2075=CARTESIAN_POINT ( 'NONE',  ( 29.62673903083957683, -5.344535611318891988, 28.45872576146958011 ) ) ;
#2081=EDGE_CURVE ( 'NONE', #7066, #1588, #98605, .T. ) ;
#2083=CARTESIAN_POINT ( 'NONE',  ( 10.75273025779354263, -5.876774720514426953, 16.96478738960562893 ) ) ;
#2100=DIRECTION ( 'NONE',  ( 0.9872275723272648795, 0.000000000000000000, 0.1593164160933056017 ) ) ;
#2101=LINE ( 'NONE', #31144, #77086 ) ;
#2107=CARTESIAN_POINT ( 'NONE',  ( 5.697397333356354565, -5.876774720514418959, 20.51730809691671809 ) ) ;
#2108=EDGE_LOOP ( 'NONE', ( #76754, #92993, #30196, #47183, #19230 ) ) ;
#2121=CARTESIAN_POINT ( 'NONE',  ( 11.22434917415779054, -4.132774715458839232, -26.87660878605755599 ) ) ;
#2134=AXIS2_PLACEMENT_3D ( 'NONE', #26644, #27643, #20016 ) ;
#2149=VERTEX_POINT ( 'NONE', #30546 ) ;
#2161=VECTOR ( 'NONE', #73780, 1000.000000000000227 ) ;
#2163=CARTESIAN_POINT ( 'NONE',  ( 2.628295812946869425, -5.876774720514411854, 19.40849182188139110 ) ) ;
#2175=PLANE ( 'NONE',  #94065 ) ;
#2183=CARTESIAN_POINT ( 'NONE',  ( 6.365284455128204399, -5.876774720514413630, 19.73076923076922640 ) ) ;
#2205=ORIENTED_EDGE ( 'NONE', *, *, #49340, .F. ) ;
#2207=CARTESIAN_POINT ( 'NONE',  ( -5.486124437288584232, -6.376774720514417183, 19.74568812963598319 ) ) ;
#2217=LINE ( 'NONE', #80324, #78069 ) ;
#2221=CARTESIAN_POINT ( 'NONE',  ( 3.063121397228215859, -5.876774720514419847, 20.95210102656095685 ) ) ;
#2247=DIRECTION ( 'NONE',  ( 0.000000000000000000, 0.000000000000000000, 1.000000000000000000 ) ) ;
#2249=EDGE_CURVE ( 'NONE', #67044, #71424, #63002, .T. ) ;
#2252=DIRECTION ( 'NONE',  ( -0.000000000000000000, -0.000000000000000000, 1.000000000000000000 ) ) ;
#2258=DIRECTION ( 'NONE',  ( 0.000000000000000000, -1.000000000000000000, 0.000000000000000000 ) ) ;
#2270=CARTESIAN_POINT ( 'NONE',  ( 2.993128331772667572, -6.376774720514402972, 18.53171057923899312 ) ) ;
#2272=VECTOR ( 'NONE', #45015, 1000.000000000000000 ) ;
#2275=LINE ( 'NONE', #25084, #81052 ) ;
#2276=LINE ( 'NONE', #18481, #59977 ) ;
#2282=CARTESIAN_POINT ( 'NONE',  ( 6.457852148677970305, -5.876774720514416295, 20.09052163342618158 ) ) ;
#2286=CARTESIAN_POINT ( 'NONE',  ( -1.394533802543915124, -5.876774720514414518, 20.19722303762275573 ) ) ;
#2287=ORIENTED_EDGE ( 'NONE', *, *, #63312, .F. ) ;
#2291=ORIENTED_EDGE ( 'NONE', *, *, #85679, .F. ) ;
#2292=PLANE ( 'NONE',  #8497 ) ;
#2297=EDGE_LOOP ( 'NONE', ( #36569, #72728, #19210, #94236 ) ) ;
#2298=DIRECTION ( 'NONE',  ( -0.000000000000000000, 1.000000000000000000, -0.000000000000000000 ) ) ;
#2309=ORIENTED_EDGE ( 'NONE', *, *, #66338, .F. ) ;
#2311=CARTESIAN_POINT ( 'NONE',  ( -6.181720432442950219, -6.376774720514410077, 19.67464842890028720 ) ) ;
#2316=CARTESIAN_POINT ( 'NONE',  ( 31.30917625415073502, -4.464831821618584051, 0.9454093304329914682 ) ) ;
#2325=ORIENTED_EDGE ( 'NONE', *, *, #32578, .T. ) ;
#2343=CARTESIAN_POINT ( 'NONE',  ( -2.732037236150805626, -5.876774720514412742, 19.78976258633487717 ) ) ;
#2345=DIRECTION ( 'NONE',  ( 0.000000000000000000, 1.000000000000000000, 0.000000000000000000 ) ) ;
#2346=CARTESIAN_POINT ( 'NONE',  ( 14.76093561896379214, -3.316774720514426456, -27.37148769130089931 ) ) ;
#2351=EDGE_CURVE ( 'NONE', #53050, #83993, #31042, .T. ) ;
#2361=LINE ( 'NONE', #41930, #93390 ) ;
#2363=EDGE_LOOP ( 'NONE', ( #82334, #32170, #99242, #71654 ) ) ;
#2370=DIRECTION ( 'NONE',  ( 1.000000000000000000, 0.000000000000000000, -2.168404344971008868E-16 ) ) ;
#2391=ORIENTED_EDGE ( 'NONE', *, *, #1204, .T. ) ;
#2395=CYLINDRICAL_SURFACE ( 'NONE', #80979, 28.96799999999999642 ) ;
#2402=PLANE ( 'NONE',  #20171 ) ;
#2405=CARTESIAN_POINT ( 'NONE',  ( 4.127614219445591814, -5.876774720514409189, 18.60403502951120558 ) ) ;
#2420=CARTESIAN_POINT ( 'NONE',  ( -6.775140224358976226, -5.876774720514409189, 19.14743589743590846 ) ) ;
#2424=VERTEX_POINT ( 'NONE', #25440 ) ;
#2431=VECTOR ( 'NONE', #14573, 1000.000000000000000 ) ;
#2438=CARTESIAN_POINT ( 'NONE',  ( -6.720452724358975338, -5.876774720514411854, 19.46153846153846700 ) ) ;
#2444=CARTESIAN_POINT ( 'NONE',  ( -5.514838905578028694, -6.376774720514410077, 19.81240905262003338 ) ) ;
#2449=LINE ( 'NONE', #47127, #76100 ) ;
#2469=LINE ( 'NONE', #48150, #5852 ) ;
#2477=EDGE_CURVE ( 'NONE', #44429, #47230, #81059, .T. ) ;
#2485=CARTESIAN_POINT ( 'NONE',  ( 7.479587785762670471, -6.376774720514417183, 20.73799387832858088 ) ) ;
#2486=CARTESIAN_POINT ( 'NONE',  ( -4.568292318365942073, 5.965225279485572685, 30.06720597538392425 ) ) ;
#2496=FACE_OUTER_BOUND ( 'NONE', #56686, .T. ) ;
#2506=CARTESIAN_POINT ( 'NONE',  ( 24.71017632900190719, -5.356774720514427379, -0.3523920347467662806 ) ) ;
#2508=ORIENTED_EDGE ( 'NONE', *, *, #11711, .F. ) ;
#2514=EDGE_CURVE ( 'NONE', #44951, #75496, #81230, .T. ) ;
#2515=AXIS2_PLACEMENT_3D ( 'NONE', #86016, #16493, #16999 ) ;
#2519=AXIS2_PLACEMENT_3D ( 'NONE', #87109, #1391, #23702 ) ;
#2523=DIRECTION ( 'NONE',  ( -1.000000000000000000, 0.000000000000000000, 0.000000000000000000 ) ) ;
#2530=CARTESIAN_POINT ( 'NONE',  ( -6.499903988472228278, -6.376774720514408301, 19.18381548539529646 ) ) ;
#2545=DIRECTION ( 'NONE',  ( 0.000000000000000000, 0.000000000000000000, 1.000000000000000000 ) ) ;
#2554=ORIENTED_EDGE ( 'NONE', *, *, #81857, .T. ) ;
#2559=APPLICATION_CONTEXT ( 'configuration controlled 3d designs of mechanical parts and assemblies' ) ;
#2578=EDGE_CURVE ( 'NONE', #39283, #69177, #20310, .T. ) ;
#2579=CARTESIAN_POINT ( 'NONE',  ( -3.108974358974359475, -6.376774720514417183, 20.36458333333334281 ) ) ;
#2580=ORIENTED_EDGE ( 'NONE', *, *, #22477, .F. ) ;
#2581=VECTOR ( 'NONE', #13758, 1000.000000000000000 ) ;
#2582=B_SPLINE_CURVE_WITH_KNOTS ( 'NONE', 3,
 ( #68242, #53026, #81970, #67254, #99171, #22044, #90572, #43908, #90081, #21051, #13441, #75837, #52022, #73858, #91563, #83956, #20556, #51525, #44415 ),
 .UNSPECIFIED., .F., .F.,
 ( 4, 1, 1, 1, 1, 1, 1, 1, 1, 1, 1, 1, 1, 1, 1, 1, 4 ),
 ( 0.000000000000000000, 0.08252970382206505084, 0.1587788549175693509, 0.2277380621151788020, 0.2899456527966750574, 0.3454988386981356352, 0.3938963373401225820, 0.4363737851900879039, 0.4721222744615228839, 0.5363836155048278265, 0.5990779017254967975, 0.6619482340244574603, 0.7263105423531552862, 0.7917711030502098124, 0.8586473037978579192, 0.9273053338076842067, 1.000000000000000000 ),
 .UNSPECIFIED. ) ;
#2589=VERTEX_POINT ( 'NONE', #97933 ) ;
#2590=AXIS2_PLACEMENT_3D ( 'NONE', #85676, #61855, #15658 ) ;
#2595=EDGE_CURVE ( 'NONE', #47215, #35163, #75104, .T. ) ;
#2597=AXIS2_PLACEMENT_3D ( 'NONE', #78234, #54420, #32073 ) ;
#2600=CARTESIAN_POINT ( 'NONE',  ( -5.265981236333618470E-16, -2.056774720514426669, -4.299999999999999822 ) ) ;
#2603=EDGE_CURVE ( 'NONE', #32855, #62667, #29932, .T. ) ;
#2605=CARTESIAN_POINT ( 'NONE',  ( -7.243541020599075786, -5.876774720514409189, 19.27798293355755632 ) ) ;
#2610=CARTESIAN_POINT ( 'NONE',  ( 29.77147767949874435, -4.540774720514427543, 26.15915692125050995 ) ) ;
#2611=DIRECTION ( 'NONE',  ( -1.334402673828313586E-16, 0.000000000000000000, 1.000000000000000000 ) ) ;
#2615=CARTESIAN_POINT ( 'NONE',  ( 13.91401389203221406, 6.475225279485573360, 27.75920385068456042 ) ) ;
#2620=CARTESIAN_POINT ( 'NONE',  ( -41.32836283488544638, -4.132774720514426292, 39.26872235229541985 ) ) ;
#2621=LINE ( 'NONE', #16827, #78805 ) ;
#2628=ORIENTED_EDGE ( 'NONE', *, *, #60832, .T. ) ;
#2631=ORIENTED_EDGE ( 'NONE', *, *, #37859, .T. ) ;
#2633=VECTOR ( 'NONE', #87073, 1000.000000000000000 ) ;
#2635=CARTESIAN_POINT ( 'NONE',  ( 31.20850673110457763, -5.144960210277549351, -4.610511713824573476 ) ) ;
#2647=ORIENTED_EDGE ( 'NONE', *, *, #45047, .T. ) ;
#2654=CARTESIAN_POINT ( 'NONE',  ( 6.365284455128204399, -6.376774720514413630, 19.73076923076922640 ) ) ;
#2667=CARTESIAN_POINT ( 'NONE',  ( 12.17309066428871667, -5.143895418987112222, -26.49515656621686333 ) ) ;
#2668=ORIENTED_EDGE ( 'NONE', *, *, #87344, .F. ) ;
#2679=CARTESIAN_POINT ( 'NONE',  ( 5.873458226074941280, -5.876774720514414518, 19.84669099281175164 ) ) ;
#2681=CARTESIAN_POINT ( 'NONE',  ( 7.153659783701941777, -5.876774720514421624, 20.92502190304499265 ) ) ;
#2687=DIRECTION ( 'NONE',  ( 0.000000000000000000, -1.000000000000000000, 0.000000000000000000 ) ) ;
#2689=CARTESIAN_POINT ( 'NONE',  ( 30.53060340732036693, -4.132774720514426292, -2.322449884495168870 ) ) ;
#2692=DIRECTION ( 'NONE',  ( 0.000000000000000000, -1.000000000000000000, 0.000000000000000000 ) ) ;
#2700=EDGE_CURVE ( 'NONE', #3925, #53709, #36051, .T. ) ;
#2702=CARTESIAN_POINT ( 'NONE',  ( -5.063563723219555612, -6.376774720514408301, 19.46509473978807847 ) ) ;
#2704=CARTESIAN_POINT ( 'NONE',  ( 13.91401389203221406, -3.316774720514426456, 27.24920385068457662 ) ) ;
#2705=EDGE_LOOP ( 'NONE', ( #68137, #77377, #63466, #71904 ) ) ;
#2711=DIRECTION ( 'NONE',  ( 0.000000000000000000, -1.000000000000000000, 0.000000000000000000 ) ) ;
#2720=CARTESIAN_POINT ( 'NONE',  ( 3.045412351277957175, -5.876774720514421624, 20.90433128744512814 ) ) ;
#2721=CARTESIAN_POINT ( 'NONE',  ( 33.74607884027702909, 5.965225279485572685, -4.999864028243830916 ) ) ;
#2725=TOROIDAL_SURFACE ( 'NONE', #99955, 253.2618649670780826, 0.8159999999999999476 ) ;
#2733=ORIENTED_EDGE ( 'NONE', *, *, #11745, .T. ) ;
#2734=VECTOR ( 'NONE', #94311, 1000.000000000000000 ) ;
#2737=CARTESIAN_POINT ( 'NONE',  ( 0.06697178475903577122, -6.376774720514410077, 19.29815762497054976 ) ) ;
#2738=CARTESIAN_POINT ( 'NONE',  ( 8.817327481837082814, -3.316774720514257702, -28.08864864913269699 ) ) ;
#2745=CYLINDRICAL_SURFACE ( 'NONE', #14415, 6.000000000000000888 ) ;
#2748=CARTESIAN_POINT ( 'NONE',  ( 7.478911390063968767, -6.376774720514422512, 20.82112274756839199 ) ) ;
#2762=EDGE_CURVE ( 'NONE', #98254, #92450, #32439, .T. ) ;
#2765=B_SPLINE_CURVE_WITH_KNOTS ( 'NONE', 3,
 ( #70657, #76740, #78248, #7242, #61558, #92477, #15353, #15854, #46317, #46825, #8257, #8759, #39697, #39195, #70153, #638, #62551, #72169, #1653, #18865, #57455, #2163, #49338, #87885, #55946, #32589, #95494 ),
 .UNSPECIFIED., .F., .F.,
 ( 4, 1, 1, 1, 1, 1, 1, 1, 1, 1, 1, 1, 1, 1, 1, 1, 1, 1, 1, 1, 1, 1, 1, 1, 4 ),
 ( 0.000000000000000000, 0.03378811616271038681, 0.06719393237388025797, 0.09986241085682510954, 0.1325666121262582542, 0.1651511732547865374, 0.1979131873557924692, 0.2313190035669614730, 0.2650832782673732679, 0.2992553087581151794, 0.3343985665049788447, 0.3699428235093072392, 0.4062835607000603866, 0.4440638196985079444, 0.4829977068727749345, 0.5233544466133041029, 0.5655365896041484319, 0.6096129240658189063, 0.6563908113764170826, 0.7058854949364568032, 0.7583245002617304831, 0.8138317829411497728, 0.8727945590393887398, 0.9347222295400740011, 1.000000000000000000 ),
 .UNSPECIFIED. ) ;
#2767=LINE ( 'NONE', #48939, #54171 ) ;
#2770=CARTESIAN_POINT ( 'NONE',  ( 2.936453026386435017, -6.376774720514406525, 18.60215244312560401 ) ) ;
#2778=VERTEX_POINT ( 'NONE', #85726 ) ;
#2786=EDGE_LOOP ( 'NONE', ( #1665, #80195, #83007, #82612 ) ) ;
#2787=PLANE ( 'NONE',  #64733 ) ;
#2790=VERTEX_POINT ( 'NONE', #30435 ) ;
#2792=DIRECTION ( 'NONE',  ( 5.238131417152343399E-15, 0.000000000000000000, 1.000000000000000000 ) ) ;
#2798=VERTEX_POINT ( 'NONE', #15710 ) ;
#2801=DIRECTION ( 'NONE',  ( -0.000000000000000000, 0.000000000000000000, -1.000000000000000000 ) ) ;
#2809=ORIENTED_EDGE ( 'NONE', *, *, #79106, .T. ) ;
#2814=CARTESIAN_POINT ( 'NONE',  ( -13.89275734969026566, 5.965225279485572685, 30.51402280011862089 ) ) ;
#2821=ADVANCED_FACE ( 'NONE', ( #47175 ), #31438, .T. ) ;
#2830=AXIS2_PLACEMENT_3D ( 'NONE', #92371, #93366, #24365 ) ;
#2862=CARTESIAN_POINT ( 'NONE',  ( 15.14080536460163984, -5.152774720514426754, -26.62908960815042292 ) ) ;
#2863=CARTESIAN_POINT ( 'NONE',  ( 32.50838937279093699, -2.682774720514426559, -10.74666623472941573 ) ) ;
#2868=CARTESIAN_POINT ( 'NONE',  ( 4.281508569253434260, -6.376774720514422512, 21.28700241941785265 ) ) ;
#2876=VECTOR ( 'NONE', #19769, 1000.000000000000114 ) ;
#2879=CARTESIAN_POINT ( 'NONE',  ( -2.780940648273603433, -6.376774720514413630, 20.02088365235843881 ) ) ;
#2884=FACE_OUTER_BOUND ( 'NONE', #28070, .T. ) ;
#2897=CARTESIAN_POINT ( 'NONE',  ( -0.005606649364735081555, -5.876774720514410077, 19.25713806424188235 ) ) ;
#2898=ORIENTED_EDGE ( 'NONE', *, *, #5944, .F. ) ;
#2902=ORIENTED_EDGE ( 'NONE', *, *, #23112, .F. ) ;
#2920=EDGE_LOOP ( 'NONE', ( #72097, #9257 ) ) ;
#2925=CARTESIAN_POINT ( 'NONE',  ( 31.79364159983995464, 5.965225279485572685, -11.59305536555894278 ) ) ;
#2926=CARTESIAN_POINT ( 'NONE',  ( 5.326923076923078426, -6.376774720514420736, 20.76772836538461320 ) ) ;
#2928=VERTEX_POINT ( 'NONE', #89225 ) ;
#2935=VECTOR ( 'NONE', #98158, 1000.000000000000114 ) ;
#2938=ORIENTED_EDGE ( 'NONE', *, *, #90090, .F. ) ;
#2939=ORIENTED_EDGE ( 'NONE', *, *, #14356, .F. ) ;
#2941=AXIS2_PLACEMENT_3D ( 'NONE', #65196, #48951, #66192 ) ;
#2942=DIRECTION ( 'NONE',  ( 0.000000000000000000, -1.000000000000000000, 0.000000000000000000 ) ) ;
#2945=CARTESIAN_POINT ( 'NONE',  ( 29.76216731806157867, -5.356774720514427379, 26.42665638500616154 ) ) ;
#2950=EDGE_CURVE ( 'NONE', #22734, #39283, #45201, .T. ) ;
#2951=ORIENTED_EDGE ( 'NONE', *, *, #82704, .F. ) ;
#2952=FACE_OUTER_BOUND ( 'NONE', #27000, .T. ) ;
#2956=CARTESIAN_POINT ( 'NONE',  ( 26.73860345374794178, 1.477225279485574028, -1.272392034746785860 ) ) ;
#2960=PLANE ( 'NONE',  #45023 ) ;
#2961=CARTESIAN_POINT ( 'NONE',  ( -0.7614568544629641833, -5.876774720514408301, 19.18727597066020962 ) ) ;
#2972=DIRECTION ( 'NONE',  ( 0.000000000000000000, -1.000000000000000000, 0.000000000000000000 ) ) ;
#2998=AXIS2_PLACEMENT_3D ( 'NONE', #19182, #50644, #47269 ) ;
#3028=VERTEX_POINT ( 'NONE', #45056 ) ;
#3033=CARTESIAN_POINT ( 'NONE',  ( -5.850750514176234596, -6.376774720514411854, 19.74039977944280366 ) ) ;
#3034=CARTESIAN_POINT ( 'NONE',  ( 3.121233215686890272, -5.876774720514405637, 18.93204046835445808 ) ) ;
#3037=EDGE_LOOP ( 'NONE', ( #81822, #51213 ) ) ;
#3038=CARTESIAN_POINT ( 'NONE',  ( 12.99736557111424595, 6.475225279485574248, -27.13536621820933448 ) ) ;
#3044=EDGE_CURVE ( 'NONE', #52189, #91108, #56592, .T. ) ;
#3049=DIRECTION ( 'NONE',  ( 0.000000000000000000, -1.000000000000000000, 0.000000000000000000 ) ) ;
#3061=VECTOR ( 'NONE', #74120, 1000.000000000000000 ) ;
#3062=CARTESIAN_POINT ( 'NONE',  ( 29.73860345376319714, 1.477225279485574028, -8.849814207987165560 ) ) ;
#3063=AXIS2_PLACEMENT_3D ( 'NONE', #65182, #59044, #35206 ) ;
#3082=DIRECTION ( 'NONE',  ( -0.4725087886537609472, 0.000000000000000000, -0.8813259582271223413 ) ) ;
#3105=DIRECTION ( 'NONE',  ( 0.000000000000000000, -1.000000000000000000, 0.000000000000000000 ) ) ;
#3110=CARTESIAN_POINT ( 'NONE',  ( -6.901944873432418248, -5.876774720514410966, 19.15221817653406688 ) ) ;
#3112=VERTEX_POINT ( 'NONE', #6979 ) ;
#3117=DIRECTION ( 'NONE',  ( 0.000000000000000000, -1.000000000000000000, 0.000000000000000000 ) ) ;
#3118=LINE ( 'NONE', #27444, #30035 ) ;
#3131=AXIS2_PLACEMENT_3D ( 'NONE', #74977, #4498, #60285 ) ;
#3147=EDGE_CURVE ( 'NONE', #50923, #42247, #15086, .T. ) ;
#3157=CARTESIAN_POINT ( 'NONE',  ( 6.853365600657045142, -6.376774720514415407, 20.20310688689519196 ) ) ;
#3158=CARTESIAN_POINT ( 'NONE',  ( 6.329711958793041049, -6.376774720514411854, 19.73172534246499765 ) ) ;
#3172=CARTESIAN_POINT ( 'NONE',  ( 13.35520464978777788, -3.511397109468809674, -28.20545335007043164 ) ) ;
#3177=ORIENTED_EDGE ( 'NONE', *, *, #77143, .F. ) ;
#3194=EDGE_CURVE ( 'NONE', #3328, #58613, #88113, .T. ) ;
#3200=FACE_OUTER_BOUND ( 'NONE', #15248, .T. ) ;
#3202=VECTOR ( 'NONE', #11055, 1000.000000000000000 ) ;
#3210=FACE_OUTER_BOUND ( 'NONE', #43603, .T. ) ;
#3215=CARTESIAN_POINT ( 'NONE',  ( 4.189750619059152470, -5.876774720514426953, 21.76591699724029283 ) ) ;
#3224=AXIS2_PLACEMENT_3D ( 'NONE', #24463, #47811, #56440 ) ;
#3237=CYLINDRICAL_SURFACE ( 'NONE', #22990, 84.48086791635432746 ) ;
#3238=DIRECTION ( 'NONE',  ( -0.000000000000000000, 1.000000000000000000, -0.000000000000000000 ) ) ;
#3246=CARTESIAN_POINT ( 'NONE',  ( 10.74487964110493188, -6.376774720514429617, -24.99341878722455235 ) ) ;
#3248=CARTESIAN_POINT ( 'NONE',  ( -7.586742644780859912, -6.376774720514413630, 19.78730719034165020 ) ) ;
#3258=CARTESIAN_POINT ( 'NONE',  ( -4.568292318365942073, -0.3587747205144265483, 30.06720597538392425 ) ) ;
#3265=CARTESIAN_POINT ( 'NONE',  ( 9.032095062437601740, 5.965225279485574461, -28.07116626896318579 ) ) ;
#3270=ORIENTED_EDGE ( 'NONE', *, *, #25349, .F. ) ;
#3273=DIRECTION ( 'NONE',  ( 0.000000000000000000, 0.000000000000000000, 1.000000000000000000 ) ) ;
#3276=ORIENTED_EDGE ( 'NONE', *, *, #73571, .T. ) ;
#3280=CARTESIAN_POINT ( 'NONE',  ( 14.43441819135929727, 5.965225279485572685, -28.36222020317710246 ) ) ;
#3296=CARTESIAN_POINT ( 'NONE',  ( 4.784292611718075072, -3.316774720514426456, -25.54547254883186014 ) ) ;
#3299=CIRCLE ( 'NONE', #16230, 0.3000000000000016542 ) ;
#3321=DIRECTION ( 'NONE',  ( 0.000000000000000000, 0.000000000000000000, -1.000000000000000000 ) ) ;
#3322=EDGE_CURVE ( 'NONE', #47722, #46585, #35326, .T. ) ;
#3328=VERTEX_POINT ( 'NONE', #97213 ) ;
#3333=LINE ( 'NONE', #81437, #50361 ) ;
#3339=DIRECTION ( 'NONE',  ( 1.000000000000000000, 0.000000000000000000, 0.000000000000000000 ) ) ;
#3341=ADVANCED_FACE ( 'NONE', ( #29200 ), #35817, .T. ) ;
#3348=CARTESIAN_POINT ( 'NONE',  ( 32.25183987940364005, 5.965225279485572685, 2.026414261721653176 ) ) ;
#3364=CARTESIAN_POINT ( 'NONE',  ( -2.188401442307694289, -5.876774720514411854, 19.46153846153846700 ) ) ;
#3389=ORIENTED_EDGE ( 'NONE', *, *, #57873, .F. ) ;
#3394=CARTESIAN_POINT ( 'NONE',  ( 30.77564450787169648, -4.772774720514425972, -9.689394075852828081 ) ) ;
#3398=CARTESIAN_POINT ( 'NONE',  ( -10.75273025779354263, -5.876774720514426953, 16.96478738960562893 ) ) ;
#3406=DIRECTION ( 'NONE',  ( 0.3133898629642186684, 7.885106708985488048E-16, -0.9496245541219267006 ) ) ;
#3408=LINE ( 'NONE', #40952, #81137 ) ;
#3412=CARTESIAN_POINT ( 'NONE',  ( -1.044871794871793602, -5.876774720514418071, 20.44941907051282115 ) ) ;
#3422=EDGE_CURVE ( 'NONE', #60099, #45760, #7344, .T. ) ;
#3429=CARTESIAN_POINT ( 'NONE',  ( 32.59332756141814258, -2.682774720514426559, -11.41404606144462086 ) ) ;
#3437=DIRECTION ( 'NONE',  ( 0.000000000000000000, -0.7071067811865525687, 0.7071067811865425767 ) ) ;
#3440=VERTEX_POINT ( 'NONE', #71635 ) ;
#3449=CARTESIAN_POINT ( 'NONE',  ( -7.326695514711824231, -6.376774720514417183, 20.26757654895259719 ) ) ;
#3454=DIRECTION ( 'NONE',  ( -1.000000000000000000, 0.000000000000000000, 0.000000000000000000 ) ) ;
#3455=CARTESIAN_POINT ( 'NONE',  ( 29.73860345376319003, -14.82721238576461609, -4.021180035027960287 ) ) ;
#3457=PLANE ( 'NONE',  #8103 ) ;
#3465=EDGE_CURVE ( 'NONE', #95862, #42749, #60665, .T. ) ;
#3471=LINE ( 'NONE', #19665, #31043 ) ;
#3478=DIRECTION ( 'NONE',  ( 0.7689940216596069522, 5.365801633547218220E-16, -0.6392559695863496705 ) ) ;
#3497=CARTESIAN_POINT ( 'NONE',  ( 4.332134589405623792, -6.376774720514427841, 21.69242924468134959 ) ) ;
#3510=ORIENTED_EDGE ( 'NONE', *, *, #25660, .T. ) ;
#3527=EDGE_CURVE ( 'NONE', #57212, #93999, #38299, .T. ) ;
#3529=VERTEX_POINT ( 'NONE', #53048 ) ;
#3530=AXIS2_PLACEMENT_3D ( 'NONE', #42623, #19257, #58346 ) ;
#3536=CARTESIAN_POINT ( 'NONE',  ( 282.9764569301858046, -3.316774720514426900, 20.79159422840526616 ) ) ;
#3546=ORIENTED_EDGE ( 'NONE', *, *, #17964, .F. ) ;
#3557=CARTESIAN_POINT ( 'NONE',  ( 33.00535138976609062, -6.376774720514426953, -12.97242311383962310 ) ) ;
#3558=CARTESIAN_POINT ( 'NONE',  ( 24.71017632900190719, -5.356774720514427379, 1.647607965253213624 ) ) ;
#3563=ORIENTED_EDGE ( 'NONE', *, *, #48534, .T. ) ;
#3579=CARTESIAN_POINT ( 'NONE',  ( -19.69812919673063689, 5.965225279485592225, -22.00173861453435720 ) ) ;
#3582=DIRECTION ( 'NONE',  ( 4.015954566446630556E-15, 1.000000000000000000, 1.297050502119899750E-15 ) ) ;
#3591=CARTESIAN_POINT ( 'NONE',  ( -28.98875734969026041, 5.965225279485572685, 15.62202280011862321 ) ) ;
#3595=FACE_OUTER_BOUND ( 'NONE', #91005, .T. ) ;
#3596=CARTESIAN_POINT ( 'NONE',  ( -10.21384395349174490, -3.316774720514427344, 29.49402280011862487 ) ) ;
#3601=CARTESIAN_POINT ( 'NONE',  ( -7.603582339867426043, -5.876774720514417183, 19.86545874326176175 ) ) ;
#3603=VECTOR ( 'NONE', #60225, 1000.000000000000000 ) ;
#3606=CARTESIAN_POINT ( 'NONE',  ( 22.81105451610979173, 6.475225279485573360, -16.21691820600746681 ) ) ;
#3607=CARTESIAN_POINT ( 'NONE',  ( -19.77875734969026311, -5.356774720514425603, 0.7300228001186309656 ) ) ;
#3608=CARTESIAN_POINT ( 'NONE',  ( 5.271800844963591359, -3.316774720514426011, -28.56638892015329034 ) ) ;
#3613=ORIENTED_EDGE ( 'NONE', *, *, #72932, .F. ) ;
#3620=AXIS2_PLACEMENT_3D ( 'NONE', #14800, #74223, #20918 ) ;
#3624=LINE ( 'NONE', #26948, #66388 ) ;
#3627=ORIENTED_EDGE ( 'NONE', *, *, #47805, .T. ) ;
#3641=EDGE_LOOP ( 'NONE', ( #61447, #62910, #24123, #82420 ) ) ;
#3645=CARTESIAN_POINT ( 'NONE',  ( 17.47419131657910540, -6.376774720514426953, 28.31804950686278843 ) ) ;
#3652=CARTESIAN_POINT ( 'NONE',  ( 5.963731207934512391, -5.876774720514413630, 19.80418863844947097 ) ) ;
#3661=LINE ( 'NONE', #49342, #49740 ) ;
#3668=CARTESIAN_POINT ( 'NONE',  ( -65.05438548721848235, -3.316774720514426456, 27.45402280011862572 ) ) ;
#3688=AXIS2_PLACEMENT_3D ( 'NONE', #5937, #61746, #54131 ) ;
#3697=EDGE_CURVE ( 'NONE', #1512, #71460, #46762, .T. ) ;
#3698=CARTESIAN_POINT ( 'NONE',  ( 30.53060340732037048, -2.682774720514426559, -2.322449884495168870 ) ) ;
#3701=CARTESIAN_POINT ( 'NONE',  ( -5.063563723219555612, -5.876774720514406525, 19.46509473978807847 ) ) ;
#3703=ORIENTED_EDGE ( 'NONE', *, *, #4079, .T. ) ;
#3716=AXIS2_PLACEMENT_3D ( 'NONE', #35908, #4961, #53146 ) ;
#3719=ORIENTED_EDGE ( 'NONE', *, *, #96841, .T. ) ;
#3724=DIRECTION ( 'NONE',  ( -2.000709955812756421E-15, 6.669033186042521139E-15, -1.000000000000000000 ) ) ;
#3733=DIRECTION ( 'NONE',  ( 0.000000000000000000, -1.000000000000000000, 0.000000000000000000 ) ) ;
#3737=CARTESIAN_POINT ( 'NONE',  ( 8.616046215355789073, -6.376774720514426065, -25.03514012577542758 ) ) ;
#3749=CARTESIAN_POINT ( 'NONE',  ( 7.475222833218381879, -6.376774720514418959, 20.91460388675487891 ) ) ;
#3760=CARTESIAN_POINT ( 'NONE',  ( -5.891025641025637860, -6.376774720514427841, 21.75000000000000711 ) ) ;
#3766=EDGE_CURVE ( 'NONE', #6469, #98127, #9798, .T. ) ;
#3782=VECTOR ( 'NONE', #25291, 1000.000000000000000 ) ;
#3783=CARTESIAN_POINT ( 'NONE',  ( 29.70566059910618861, -3.975162330554212531, 28.10075438475601928 ) ) ;
#3798=CARTESIAN_POINT ( 'NONE',  ( 5.326923076923078426, -6.376774720514420736, 20.76772836538461320 ) ) ;
#3799=CARTESIAN_POINT ( 'NONE',  ( 6.546094359317672584, -5.876774720514411854, 19.73546617144828375 ) ) ;
#3803=CARTESIAN_POINT ( 'NONE',  ( 7.311104923646705167, -5.876774720514415407, 20.13320233724603980 ) ) ;
#3805=CARTESIAN_POINT ( 'NONE',  ( 5.271800844963591359, -3.316774720514426456, -28.56638892015329745 ) ) ;
#3810=CARTESIAN_POINT ( 'NONE',  ( 7.155337544004596317, -6.376774720514417183, 20.64714842558261765 ) ) ;
#3834=VERTEX_POINT ( 'NONE', #98825 ) ;
#3848=DIRECTION ( 'NONE',  ( 1.232047923278981953E-16, 1.000000000000000000, 0.000000000000000000 ) ) ;
#3849=EDGE_CURVE ( 'NONE', #83993, #17395, #14085, .T. ) ;
#3863=CARTESIAN_POINT ( 'NONE',  ( 2.932009311892267434, -6.376774720514410077, 19.53174284846577891 ) ) ;
#3866=LINE ( 'NONE', #10966, #23793 ) ;
#3873=EDGE_CURVE ( 'NONE', #68993, #94137, #53675, .T. ) ;
#3879=CARTESIAN_POINT ( 'NONE',  ( 0.3908843598833069422, -6.376774720514420736, 20.63520656483649773 ) ) ;
#3885=ORIENTED_EDGE ( 'NONE', *, *, #56485, .F. ) ;
#3906=ORIENTED_EDGE ( 'NONE', *, *, #24513, .F. ) ;
#3907=CARTESIAN_POINT ( 'NONE',  ( -24.90875734969025501, -3.316774720514426456, 26.43402280011862615 ) ) ;
#3908=CARTESIAN_POINT ( 'NONE',  ( -10.16634758543296613, 5.965225279485572685, 30.00402280011862288 ) ) ;
#3923=DIRECTION ( 'NONE',  ( 0.000000000000000000, -1.000000000000000000, 0.000000000000000000 ) ) ;
#3925=VERTEX_POINT ( 'NONE', #69887 ) ;
#3936=ORIENTED_EDGE ( 'NONE', *, *, #37973, .F. ) ;
#3938=DIRECTION ( 'NONE',  ( 0.000000000000000000, -1.000000000000000000, 0.000000000000000000 ) ) ;
#3941=CARTESIAN_POINT ( 'NONE',  ( -7.318926569091948942, -6.376774720514417183, 20.09505574050193033 ) ) ;
#3953=CARTESIAN_POINT ( 'NONE',  ( -1.267404104715736279, -5.876774720514411854, 19.66076420632889921 ) ) ;
#3957=CIRCLE ( 'NONE', #70362, 10.20000000000000107 ) ;
#3976=CARTESIAN_POINT ( 'NONE',  ( 27.53860345374808105, 1.477225279485574028, -6.982392034746241372 ) ) ;
#3980=CARTESIAN_POINT ( 'NONE',  ( -27.25988310792305214, -0.3587747205144265483, 30.32664379231667695 ) ) ;
#3985=DIRECTION ( 'NONE',  ( 1.000000000000000000, -4.218136541796977197E-15, 0.000000000000000000 ) ) ;
#3994=B_SPLINE_CURVE_WITH_KNOTS ( 'NONE', 3,
 ( #61095, #16393, #69189, #31122, #30122, #70193, #100109, #7787, #21999, #38732 ),
 .UNSPECIFIED., .F., .F.,
 ( 4, 2, 2, 2, 4 ),
 ( 0.002505011693330810862, 0.003215057662361453343, 0.003925103631392095824, 0.004635149600422737437, 0.005345195569453379918 ),
 .UNSPECIFIED. ) ;
#4003=ORIENTED_EDGE ( 'NONE', *, *, #51609, .F. ) ;
#4025=AXIS2_PLACEMENT_3D ( 'NONE', #46041, #54159, #21670 ) ;
#4027=EDGE_CURVE ( 'NONE', #25694, #21553, #16240, .T. ) ;
#4028=CARTESIAN_POINT ( 'NONE',  ( 3.749014282529493869, -5.876774720514404748, 18.52125941707705792 ) ) ;
#4032=CARTESIAN_POINT ( 'NONE',  ( 5.851028665930490646, -3.316774720514426011, -27.43979700150094558 ) ) ;
#4046=ORIENTED_EDGE ( 'NONE', *, *, #12707, .F. ) ;
#4048=ORIENTED_EDGE ( 'NONE', *, *, #4774, .F. ) ;
#4079=EDGE_CURVE ( 'NONE', #54223, #78100, #72975, .T. ) ;
#4081=ORIENTED_EDGE ( 'NONE', *, *, #15057, .F. ) ;
#4088=PLANE ( 'NONE',  #46307 ) ;
#4093=ORIENTED_EDGE ( 'NONE', *, *, #26438, .T. ) ;
#4098=VECTOR ( 'NONE', #90810, 1000.000000000000000 ) ;
#4100=ORIENTED_EDGE ( 'NONE', *, *, #89703, .T. ) ;
#4101=LINE ( 'NONE', #43660, #65370 ) ;
#4107=EDGE_CURVE ( 'NONE', #11869, #3328, #20089, .T. ) ;
#4111=CIRCLE ( 'NONE', #96450, 129.7684398600581517 ) ;
#4119=ORIENTED_EDGE ( 'NONE', *, *, #97259, .T. ) ;
#4121=ORIENTED_EDGE ( 'NONE', *, *, #69016, .T. ) ;
#4122=EDGE_CURVE ( 'NONE', #40241, #59933, #10481, .T. ) ;
#4144=DIRECTION ( 'NONE',  ( 1.000000000000000000, 0.000000000000000000, 0.000000000000000000 ) ) ;
#4146=CARTESIAN_POINT ( 'NONE',  ( 14.74815398954873835, -3.719725396296209574, -28.39563063676373389 ) ) ;
#4155=DIRECTION ( 'NONE',  ( 0.000000000000000000, -1.000000000000000000, 0.000000000000000000 ) ) ;
#4160=VERTEX_POINT ( 'NONE', #66797 ) ;
#4175=CARTESIAN_POINT ( 'NONE',  ( 6.763596848542221984, -6.376774720514426065, 21.40271460634751577 ) ) ;
#4184=CARTESIAN_POINT ( 'NONE',  ( 30.53060340732035982, -4.594240983522013266, 19.84760796525321425 ) ) ;
#4206=CARTESIAN_POINT ( 'NONE',  ( 3.025806405283164136, -5.876774720514420736, 20.84867811309776542 ) ) ;
#4210=LINE ( 'NONE', #82323, #79172 ) ;
#4216=DIRECTION ( 'NONE',  ( 0.000000000000000000, 1.000000000000000000, 0.000000000000000000 ) ) ;
#4223=PLANE ( 'NONE',  #11887 ) ;
#4227=CARTESIAN_POINT ( 'NONE',  ( 7.822518687475809251, -6.376774720513926908, -28.18023264526767591 ) ) ;
#4229=CARTESIAN_POINT ( 'NONE',  ( -7.603582339867426043, -5.876774720514417183, 19.86545874326176175 ) ) ;
#4231=VECTOR ( 'NONE', #20082, 1000.000000000000000 ) ;
#4243=VECTOR ( 'NONE', #57659, 1000.000000000000000 ) ;
#4248=CARTESIAN_POINT ( 'NONE',  ( -2.104002878010082789, -6.376774720514410077, 19.15289935703627222 ) ) ;
#4251=CARTESIAN_POINT ( 'NONE',  ( 30.54789914928607786, 0.2637885907592373291, 23.75907673500034178 ) ) ;
#4252=FACE_OUTER_BOUND ( 'NONE', #72560, .T. ) ;
#4262=ORIENTED_EDGE ( 'NONE', *, *, #94255, .F. ) ;
#4269=ORIENTED_EDGE ( 'NONE', *, *, #44279, .T. ) ;
#4273=FACE_OUTER_BOUND ( 'NONE', #52947, .T. ) ;
#4279=CARTESIAN_POINT ( 'NONE',  ( 3.362030615038681169, -5.876774720514424288, 21.34376340489846413 ) ) ;
#4282=CARTESIAN_POINT ( 'NONE',  ( 15.32643653063178668, -3.582999323269832725, -27.14485409495428314 ) ) ;
#4283=VERTEX_POINT ( 'NONE', #41705 ) ;
#4303=EDGE_CURVE ( 'NONE', #87149, #18629, #39306, .T. ) ;
#4307=ORIENTED_EDGE ( 'NONE', *, *, #24780, .F. ) ;
#4310=DIRECTION ( 'NONE',  ( -0.000000000000000000, 1.000000000000000000, -0.000000000000000000 ) ) ;
#4311=CARTESIAN_POINT ( 'NONE',  ( 16.04662828278931741, -3.608091531752042336, -27.86986495919489215 ) ) ;
#4314=LINE ( 'NONE', #35266, #11762 ) ;
#4326=AXIS2_PLACEMENT_3D ( 'NONE', #68863, #30290, #53653 ) ;
#4335=CARTESIAN_POINT ( 'NONE',  ( 31.02038118199824268, -5.152774720514427642, -4.893189986691015569 ) ) ;
#4345=CARTESIAN_POINT ( 'NONE',  ( -28.84663072490566194, -0.3587747205144265483, 28.73989617533406715 ) ) ;
#4348=CARTESIAN_POINT ( 'NONE',  ( -28.98875734969026396, 5.965225279485572685, 2.362022800118626531 ) ) ;
#4354=CARTESIAN_POINT ( 'NONE',  ( 16.15056352287345476, -3.622774720514426949, -27.77856273171767398 ) ) ;
#4355=EDGE_CURVE ( 'NONE', #69249, #49812, #11726, .T. ) ;
#4361=DIRECTION ( 'NONE',  ( 0.000000000000000000, -1.000000000000000000, 0.000000000000000000 ) ) ;
#4364=VERTEX_POINT ( 'NONE', #28952 ) ;
#4365=CARTESIAN_POINT ( 'NONE',  ( -1.036876607668611117, -5.876774720514417183, 20.14881673916291405 ) ) ;
#4368=CARTESIAN_POINT ( 'NONE',  ( -2.702089344534958304, -6.376774720514413630, 19.72789237585158162 ) ) ;
#4370=CIRCLE ( 'NONE', #49800, 251.9358649670780892 ) ;
#4392=ORIENTED_EDGE ( 'NONE', *, *, #25073, .F. ) ;
#4404=ORIENTED_EDGE ( 'NONE', *, *, #90288, .F. ) ;
#4410=DIRECTION ( 'NONE',  ( -0.000000000000000000, 1.000000000000000000, -0.000000000000000000 ) ) ;
#4412=ADVANCED_FACE ( 'NONE', ( #21324 ), #88872, .F. ) ;
#4415=CARTESIAN_POINT ( 'NONE',  ( 5.085443162053245203, -3.316774720514426456, -27.56355752155217331 ) ) ;
#4421=CARTESIAN_POINT ( 'NONE',  ( 22.02124265030973760, -5.356774720514425603, 16.20402280011862217 ) ) ;
#4432=ORIENTED_EDGE ( 'NONE', *, *, #70652, .T. ) ;
#4436=CARTESIAN_POINT ( 'NONE',  ( -10.11875734969026119, -3.519249775642004696, 30.51402280011862445 ) ) ;
#4440=CARTESIAN_POINT ( 'NONE',  ( 5.359050311451609261, -5.876774720514419847, 21.05346524168807676 ) ) ;
#4454=CARTESIAN_POINT ( 'NONE',  ( -1.122631020312409245, -5.876774720514411854, 19.41635569784906679 ) ) ;
#4458=EDGE_CURVE ( 'NONE', #34695, #70182, #27471, .T. ) ;
#4462=DIRECTION ( 'NONE',  ( 7.904402583950632871E-14, 0.000000000000000000, -1.000000000000000000 ) ) ;
#4473=CARTESIAN_POINT ( 'NONE',  ( -5.023036858974361252, -6.376774720514410077, 19.14743589743590846 ) ) ;
#4481=CARTESIAN_POINT ( 'NONE',  ( -53.01255352321339842, -2.682774720514426559, 35.59556822165056644 ) ) ;
#4482=CARTESIAN_POINT ( 'NONE',  ( 10.54059822343757880, -5.876774720514426953, 22.82308057603841078 ) ) ;
#4486=DIRECTION ( 'NONE',  ( -0.000000000000000000, 0.000000000000000000, -1.000000000000000000 ) ) ;
#4489=ORIENTED_EDGE ( 'NONE', *, *, #26293, .F. ) ;
#4490=CARTESIAN_POINT ( 'NONE',  ( 5.771117285127500551, -6.376774720514417183, 20.39900056875960388 ) ) ;
#4498=DIRECTION ( 'NONE',  ( 0.000000000000000000, -1.000000000000000000, 0.000000000000000000 ) ) ;
#4519=LINE ( 'NONE', #35467, #65932 ) ;
#4533=CIRCLE ( 'NONE', #40158, 1.700000000000000178 ) ;
#4535=CARTESIAN_POINT ( 'NONE',  ( 6.620851319379956301, 6.475225279485576024, -27.30756699305372592 ) ) ;
#4539=EDGE_CURVE ( 'NONE', #99974, #4160, #26958, .T. ) ;
#4545=CARTESIAN_POINT ( 'NONE',  ( 5.654871928786437074, -6.376774720514420736, 20.64717925217163952 ) ) ;
#4548=CARTESIAN_POINT ( 'NONE',  ( 1.175186991919848989, 5.965225279485572685, 28.89597625626659649 ) ) ;
#4555=CARTESIAN_POINT ( 'NONE',  ( 0.1309051665272248643, -6.376774720514413630, 19.34190049657482291 ) ) ;
#4559=CARTESIAN_POINT ( 'NONE',  ( 2.591664760199015927, -6.376774720514417183, 20.15921530338947321 ) ) ;
#4565=CARTESIAN_POINT ( 'NONE',  ( -3.108425644221024520, -6.376774720514415407, 20.25188360057253334 ) ) ;
#4569=ADVANCED_FACE ( 'NONE', ( #37065 ), #22322, .F. ) ;
#4580=ORIENTED_EDGE ( 'NONE', *, *, #91840, .F. ) ;
#4581=CARTESIAN_POINT ( 'NONE',  ( 4.653726706778644306, -5.876774720514415407, 20.04674869880385302 ) ) ;
#4592=VECTOR ( 'NONE', #19048, 1000.000000000000227 ) ;
#4603=CARTESIAN_POINT ( 'NONE',  ( 5.766314450391940127, -5.876774720514423400, 21.17177008079512035 ) ) ;
#4614=ORIENTED_EDGE ( 'NONE', *, *, #57654, .F. ) ;
#4619=DIRECTION ( 'NONE',  ( 0.7512896232465891000, 0.000000000000000000, 0.6599726524652351767 ) ) ;
#4637=CARTESIAN_POINT ( 'NONE',  ( 6.944081373883786767, -6.376774720514424288, 21.27829155525578031 ) ) ;
#4645=CARTESIAN_POINT ( 'NONE',  ( 15.37486457892753400, -3.577890193782784500, -28.28298033016822899 ) ) ;
#4665=ORIENTED_EDGE ( 'NONE', *, *, #77473, .T. ) ;
#4674=CARTESIAN_POINT ( 'NONE',  ( -28.98875734969026396, 5.965225279485572685, -0.08597719988137648983 ) ) ;
#4676=CARTESIAN_POINT ( 'NONE',  ( 3.787259615384621192, -6.376774720514426065, 21.48076923076922640 ) ) ;
#4678=ADVANCED_FACE ( 'NONE', ( #16724 ), #10118, .F. ) ;
#4679=CARTESIAN_POINT ( 'NONE',  ( 29.67488939790761648, -5.972177877498852538, 27.69255262365155801 ) ) ;
#4697=ORIENTED_EDGE ( 'NONE', *, *, #6536, .T. ) ;
#4708=ORIENTED_EDGE ( 'NONE', *, *, #34887, .F. ) ;
#4714=AXIS2_PLACEMENT_3D ( 'NONE', #59667, #27211, #58165 ) ;
#4720=DIRECTION ( 'NONE',  ( -0.000000000000000000, -1.000000000000000000, -0.000000000000000000 ) ) ;
#4722=EDGE_LOOP ( 'NONE', ( #83104, #17806, #68796, #28133 ) ) ;
#4724=DIRECTION ( 'NONE',  ( 0.7071067811865442421, 0.000000000000000000, -0.7071067811865507924 ) ) ;
#4726=CARTESIAN_POINT ( 'NONE',  ( 10.86431179148764770, -6.376774720514934991, -28.05678185045468709 ) ) ;
#4734=CARTESIAN_POINT ( 'NONE',  ( 30.53060340732036693, -4.484471217129241793, -4.073950328685796762 ) ) ;
#4735=CARTESIAN_POINT ( 'NONE',  ( 6.371704462700114924, -6.376774720514427841, 21.83798798526824214 ) ) ;
#4737=AXIS2_PLACEMENT_3D ( 'NONE', #42573, #51169, #82115 ) ;
#4740=CARTESIAN_POINT ( 'NONE',  ( 282.9764569301858046, -2.682774720514426559, 20.79159422840526616 ) ) ;
#4741=CARTESIAN_POINT ( 'NONE',  ( -25.92875734969025814, -5.356774720514425603, 26.43402280011862615 ) ) ;
#4765=LINE ( 'NONE', #96118, #38057 ) ;
#4769=CARTESIAN_POINT ( 'NONE',  ( 32.53346577320676403, -1.682774720514426114, -11.93731717363829681 ) ) ;
#4774=EDGE_CURVE ( 'NONE', #99954, #24488, #62929, .T. ) ;
#4779=ORIENTED_EDGE ( 'NONE', *, *, #52740, .T. ) ;
#4789=CARTESIAN_POINT ( 'NONE',  ( 7.275731542451676859, -5.876774720514415407, 20.06332870126568224 ) ) ;
#4795=CARTESIAN_POINT ( 'NONE',  ( -19.77875734969026311, -5.356774720514426491, 27.45402280011862217 ) ) ;
#4796=CARTESIAN_POINT ( 'NONE',  ( -20.27875734969026311, 7.743225279485574042, 24.00402280011862288 ) ) ;
#4815=CARTESIAN_POINT ( 'NONE',  ( 3.160575456146155204, -5.876774720514408301, 18.86877352677795372 ) ) ;
#4816=CARTESIAN_POINT ( 'NONE',  ( 2.677564053859940341, -6.376774720514406525, 19.16116138973293559 ) ) ;
#4835=DIRECTION ( 'NONE',  ( 0.000000000000000000, 0.000000000000000000, -1.000000000000000000 ) ) ;
#4836=CARTESIAN_POINT ( 'NONE',  ( -4.141439336867657417, -5.876774720514418071, 20.56083401959468304 ) ) ;
#4838=DIRECTION ( 'NONE',  ( 0.000000000000000000, 0.000000000000000000, 1.000000000000000000 ) ) ;
#4844=CYLINDRICAL_SURFACE ( 'NONE', #84782, 2.249999999999998668 ) ;
#4846=CARTESIAN_POINT ( 'NONE',  ( 7.477175500793984853, -6.376774720514417183, 20.66439772633092176 ) ) ;
#4852=ORIENTED_EDGE ( 'NONE', *, *, #28818, .F. ) ;
#4853=LINE ( 'NONE', #81977, #12221 ) ;
#4858=CARTESIAN_POINT ( 'NONE',  ( 32.88562546571903056, 5.965225279485572685, -5.083907541707159972 ) ) ;
#4873=CIRCLE ( 'NONE', #61598, 0.3000000000000016542 ) ;
#4880=FACE_OUTER_BOUND ( 'NONE', #20010, .T. ) ;
#4887=EDGE_CURVE ( 'NONE', #57623, #21668, #96858, .T. ) ;
#4906=EDGE_CURVE ( 'NONE', #64208, #29097, #97361, .T. ) ;
#4925=ORIENTED_EDGE ( 'NONE', *, *, #89907, .F. ) ;
#4935=FACE_OUTER_BOUND ( 'NONE', #49117, .T. ) ;
#4942=CARTESIAN_POINT ( 'NONE',  ( -0.9988807608215116707, -5.876774720514410077, 19.30497968945844889 ) ) ;
#4950=CARTESIAN_POINT ( 'NONE',  ( 13.91401389203221406, -0.3587747205144265483, 158.0376437107427137 ) ) ;
#4961=DIRECTION ( 'NONE',  ( -0.000000000000000000, -1.000000000000000000, -0.000000000000000000 ) ) ;
#4975=EDGE_CURVE ( 'NONE', #31243, #34608, #80016, .T. ) ;
#4978=ADVANCED_FACE ( 'NONE', ( #71921 ), #5179, .T. ) ;
#4983=DIRECTION ( 'NONE',  ( -1.000000000000000000, -8.503546450866701308E-16, 0.000000000000000000 ) ) ;
#4992=DIRECTION ( 'NONE',  ( 1.000000000000000000, -3.639832272653110612E-15, 0.000000000000000000 ) ) ;
#5015=EDGE_CURVE ( 'NONE', #45647, #56694, #97242, .T. ) ;
#5016=ORIENTED_EDGE ( 'NONE', *, *, #23171, .F. ) ;
#5020=CARTESIAN_POINT ( 'NONE',  ( -25.92875734969026169, -5.356774720514426491, 24.50402280011861933 ) ) ;
#5069=CARTESIAN_POINT ( 'NONE',  ( 14.85605547803280402, -2.682774720514425670, -27.37236044627089271 ) ) ;
#5075=CARTESIAN_POINT ( 'NONE',  ( -10.22357262723052784, -3.975302591317960044, 29.38944064375215248 ) ) ;
#5078=VECTOR ( 'NONE', #18547, 1000.000000000000000 ) ;
#5079=VERTEX_POINT ( 'NONE', #66815 ) ;
#5083=CARTESIAN_POINT ( 'NONE',  ( 6.251785340501501587, -5.876774720514423400, 21.46941214867599612 ) ) ;
#5089=EDGE_CURVE ( 'NONE', #57696, #14282, #38327, .T. ) ;
#5115=CARTESIAN_POINT ( 'NONE',  ( 32.45853543194704116, 5.965225279485572685, 9.169203677920338080 ) ) ;
#5123=VECTOR ( 'NONE', #41404, 1000.000000000000000 ) ;
#5127=CARTESIAN_POINT ( 'NONE',  ( 5.184553252003285984, 5.965225279485572685, -28.06387035751381731 ) ) ;
#5134=CARTESIAN_POINT ( 'NONE',  ( 30.53060340732035982, -1.682774720514426114, -1.272392034746785860 ) ) ;
#5144=LINE ( 'NONE', #36096, #93475 ) ;
#5151=VERTEX_POINT ( 'NONE', #76870 ) ;
#5155=EDGE_LOOP ( 'NONE', ( #9423, #27310, #68711, #72820 ) ) ;
#5158=PLANE ( 'NONE',  #41485 ) ;
#5167=CARTESIAN_POINT ( 'NONE',  ( 29.59852343658945983, -4.673870278164355518, 28.90818992718861224 ) ) ;
#5178=CIRCLE ( 'NONE', #45674, 3.570000000000003837 ) ;
#5179=B_SPLINE_SURFACE_WITH_KNOTS ( 'NONE', 3, 1, ( 
 ( #24719, #32847 ),
 ( #93731, #54690 ),
 ( #1904, #63316 ),
 ( #72421, #70916 ),
 ( #71413, #39955 ),
 ( #17112, #31339 ),
 ( #48080, #55198 ),
 ( #10501, #40961 ),
 ( #32340, #17619 ),
 ( #63823, #64326 ),
 ( #86128, #94736 ),
 ( #8507, #93230 ),
 ( #23720, #16109 ),
 ( #1406, #94234 ),
 ( #79514, #79006 ),
 ( #9504, #55700 ),
 ( #47080, #95243 ),
 ( #56705, #16604 ),
 ( #39458, #2405 ),
 ( #77995, #70408 ),
 ( #894, #48591 ),
 ( #47581, #56201 ),
 ( #25730, #87127 ) ),
 .UNSPECIFIED., .F., .F., .F.,
 ( 4, 1, 1, 1, 1, 1, 1, 1, 1, 1, 1, 1, 1, 1, 1, 1, 1, 1, 1, 1, 4 ),
 ( 2, 2 ),
 ( 0.000000000000000000, 0.07330213563861354142, 0.1422863278392666464, 0.2062532954491644865, 0.2660167794074391745, 0.3216117904407559402, 0.3725324599732942055, 0.4194969815799879376, 0.4623979521337304721, 0.5028252778726873817, 0.5414888117388608757, 0.5790338027738967108, 0.6151434188814435267, 0.6502976044497242869, 0.6849123758493420588, 0.7187008999567505718, 0.7521889702416487689, 0.8172453813748596918, 0.8791167514140035832, 0.9396133806889377382, 1.000000000000000000 ),
 ( 0.000000000000000000, 1.000000000000000000 ),
 .UNSPECIFIED. ) ;
#5192=AXIS2_PLACEMENT_3D ( 'NONE', #72122, #49792, #2611 ) ;
#5193=LINE ( 'NONE', #13293, #296 ) ;
#5194=CARTESIAN_POINT ( 'NONE',  ( 2.904244945035652670, -5.876774720514416295, 20.04207437776001299 ) ) ;
#5199=CARTESIAN_POINT ( 'NONE',  ( 4.967948717948723392, -6.376774720514415407, 20.00140224358974095 ) ) ;
#5200=PLANE ( 'NONE',  #11784 ) ;
#5214=CARTESIAN_POINT ( 'NONE',  ( 4.612744205187371271, -6.376774720514418959, 20.61169588237105188 ) ) ;
#5222=CARTESIAN_POINT ( 'NONE',  ( 10.24059822343757808, -5.876774720514426953, 17.17691942396160698 ) ) ;
#5226=CARTESIAN_POINT ( 'NONE',  ( 6.132272708306365949, -5.876774720514423400, 21.80683391321003839 ) ) ;
#5230=CARTESIAN_POINT ( 'NONE',  ( 13.74975846015576586, 6.475225279485573360, -27.72022515045486557 ) ) ;
#5235=CARTESIAN_POINT ( 'NONE',  ( -2.104002878010082789, -5.876774720514409189, 19.15289935703627222 ) ) ;
#5248=ORIENTED_EDGE ( 'NONE', *, *, #90467, .F. ) ;
#5267=VERTEX_POINT ( 'NONE', #94108 ) ;
#5269=FACE_OUTER_BOUND ( 'NONE', #61727, .T. ) ;
#5282=CARTESIAN_POINT ( 'NONE',  ( 9.315600972258339496, -6.376774720514426953, 28.35070303307545458 ) ) ;
#5286=FACE_OUTER_BOUND ( 'NONE', #77334, .T. ) ;
#5289=ORIENTED_EDGE ( 'NONE', *, *, #3322, .T. ) ;
#5295=CARTESIAN_POINT ( 'NONE',  ( 30.64109437917162637, -3.603390417177663174, 28.31981403122773955 ) ) ;
#5303=CIRCLE ( 'NONE', #15005, 0.3000000000000016542 ) ;
#5305=CARTESIAN_POINT ( 'NONE',  ( 3.051095722660301934, -6.376774720514410077, 19.07493897947323092 ) ) ;
#5312=ORIENTED_EDGE ( 'NONE', *, *, #14124, .F. ) ;
#5328=CARTESIAN_POINT ( 'NONE',  ( -4.358143420448500116, -5.876774720514413630, 19.75705121608222115 ) ) ;
#5333=EDGE_CURVE ( 'NONE', #94842, #70772, #45429, .T. ) ;
#5339=AXIS2_PLACEMENT_3D ( 'NONE', #5442, #36394, #75437 ) ;
#5341=DESIGN_CONTEXT ( 'detailed design', #2559, 'design' ) ;
#5343=CARTESIAN_POINT ( 'NONE',  ( -1.438454482798693146, -6.376774720514410077, 19.55848054040323092 ) ) ;
#5353=EDGE_CURVE ( 'NONE', #54462, #31713, #19484, .T. ) ;
#5358=VECTOR ( 'NONE', #90438, 1000.000000000000000 ) ;
#5370=DIRECTION ( 'NONE',  ( 0.000000000000000000, 0.000000000000000000, 1.000000000000000000 ) ) ;
#5372=VECTOR ( 'NONE', #3733, 1000.000000000000000 ) ;
#5382=CARTESIAN_POINT ( 'NONE',  ( 30.58729439590577570, -4.540774720514427543, 26.14186284044645703 ) ) ;
#5386=CARTESIAN_POINT ( 'NONE',  ( -2.492070857093962921, -5.876774720514407413, 19.17707164986947177 ) ) ;
#5406=CARTESIAN_POINT ( 'NONE',  ( 13.91401389203221406, 6.475225279485573360, 158.0376437107427137 ) ) ;
#5407=LINE ( 'NONE', #67316, #95553 ) ;
#5412=LINE ( 'NONE', #52091, #54423 ) ;
#5416=VECTOR ( 'NONE', #36411, 1000.000000000000000 ) ;
#5427=PLANE ( 'NONE',  #36229 ) ;
#5435=CARTESIAN_POINT ( 'NONE',  ( -2.780940648273603433, -6.376774720514413630, 20.02088365235843881 ) ) ;
#5442=CARTESIAN_POINT ( 'NONE',  ( 29.80070917940689412, -6.376774720514426953, 27.39560796525321607 ) ) ;
#5444=DIRECTION ( 'NONE',  ( 2.910297583984928910E-15, 1.000000000000000000, -3.056206645085457922E-15 ) ) ;
#5453=FACE_OUTER_BOUND ( 'NONE', #54802, .T. ) ;
#5458=EDGE_CURVE ( 'NONE', #5619, #49448, #34228, .T. ) ;
#5460=DIRECTION ( 'NONE',  ( -1.000000000000000000, 0.000000000000000000, 0.000000000000000000 ) ) ;
#5464=DIRECTION ( 'NONE',  ( 1.743630241030147080E-15, -6.974520964120588319E-15, 1.000000000000000000 ) ) ;
#5477=CARTESIAN_POINT ( 'NONE',  ( 3.448102555317568374, -6.376774720514424288, 21.39871091031772110 ) ) ;
#5494=VERTEX_POINT ( 'NONE', #11876 ) ;
#5521=CARTESIAN_POINT ( 'NONE',  ( 5.771117285127500551, -5.876774720514417183, 20.39900056875960388 ) ) ;
#5525=ORIENTED_EDGE ( 'NONE', *, *, #25723, .F. ) ;
#5529=ADVANCED_FACE ( 'NONE', ( #50953 ), #2725, .F. ) ;
#5537=DIRECTION ( 'NONE',  ( 0.000000000000000000, 0.000000000000000000, 1.000000000000000000 ) ) ;
#5539=CARTESIAN_POINT ( 'NONE',  ( -1.304987980769231948, -5.876774720514413630, 19.76512419871795245 ) ) ;
#5543=CARTESIAN_POINT ( 'NONE',  ( -3.085512303079157359, -6.376774720514415407, 19.95084900476495093 ) ) ;
#5545=CARTESIAN_POINT ( 'NONE',  ( 19.75748517575715368, 5.965225279485572685, 28.87153971905864580 ) ) ;
#5562=CARTESIAN_POINT ( 'NONE',  ( 2.589743589743596086, -5.876774720514419847, 20.00140224358974095 ) ) ;
#5576=DIRECTION ( 'NONE',  ( 0.000000000000000000, 0.000000000000000000, -1.000000000000000000 ) ) ;
#5583=CARTESIAN_POINT ( 'NONE',  ( 33.64447732616053344, -3.738877066258443627, -11.77943383154337376 ) ) ;
#5586=B_SPLINE_SURFACE_WITH_KNOTS ( 'NONE', 3, 1, ( 
 ( #11847, #42818 ),
 ( #82356, #73749 ),
 ( #4248, #5235 ),
 ( #36192, #58536 ),
 ( #35197, #66169 ),
 ( #97087, #27586 ),
 ( #89477, #48698 ),
 ( #86734, #55306 ),
 ( #25336, #63426 ),
 ( #17222, #30056 ),
 ( #32959, #86237 ),
 ( #68139, #8617 ),
 ( #79621, #6723 ),
 ( #56314, #10113 ),
 ( #16719, #37677 ) ),
 .UNSPECIFIED., .F., .F., .F.,
 ( 4, 1, 1, 1, 1, 1, 1, 1, 1, 1, 1, 1, 4 ),
 ( 2, 2 ),
 ( 0.000000000000000000, 0.1183849129606691086, 0.2344384882140508886, 0.3525851839391771492, 0.4731673593536172007, 0.5350581108286732723, 0.5975237332646006205, 0.6605170696247792961, 0.7251603465314735431, 0.7908841475025376599, 0.8587744642336311296, 0.9282339358416605846, 1.000000000000000000 ),
 ( 0.000000000000000000, 1.000000000000000000 ),
 .UNSPECIFIED. ) ;
#5596=EDGE_CURVE ( 'NONE', #63330, #79616, #21964, .T. ) ;
#5601=CARTESIAN_POINT ( 'NONE',  ( 29.68479148105952703, -1.682774720514426114, -9.431263391055123790 ) ) ;
#5602=CARTESIAN_POINT ( 'NONE',  ( 6.110660513271839456, -5.876774720514422512, 21.43053473047838509 ) ) ;
#5604=CARTESIAN_POINT ( 'NONE',  ( 5.271800844963591359, -6.376774720514426953, -28.56638892015329745 ) ) ;
#5611=CARTESIAN_POINT ( 'NONE',  ( -10.54059822343757880, -5.876774720514426953, 23.12308057603841149 ) ) ;
#5612=VECTOR ( 'NONE', #69900, 1000.000000000000114 ) ;
#5613=VERTEX_POINT ( 'NONE', #29590 ) ;
#5619=VERTEX_POINT ( 'NONE', #52946 ) ;
#5625=CARTESIAN_POINT ( 'NONE',  ( 30.93860345374796594, 6.475225279485573360, 20.86760796525322093 ) ) ;
#5629=DIRECTION ( 'NONE',  ( 0.000000000000000000, -1.000000000000000000, 0.000000000000000000 ) ) ;
#5641=LINE ( 'NONE', #13742, #85766 ) ;
#5643=CIRCLE ( 'NONE', #67234, 1.399999999999998579 ) ;
#5644=VERTEX_POINT ( 'NONE', #74765 ) ;
#5645=ORIENTED_EDGE ( 'NONE', *, *, #77506, .T. ) ;
#5650=VERTEX_POINT ( 'NONE', #44338 ) ;
#5655=CARTESIAN_POINT ( 'NONE',  ( 15.00349586803797486, -3.316774720514427344, -27.42854230132123305 ) ) ;
#5661=ADVANCED_FACE ( 'NONE', ( #28602 ), #36716, .T. ) ;
#5676=ORIENTED_EDGE ( 'NONE', *, *, #57042, .F. ) ;
#5685=VECTOR ( 'NONE', #6239, 1000.000000000000000 ) ;
#5691=DIRECTION ( 'NONE',  ( 0.000000000000000000, -1.000000000000000000, 0.000000000000000000 ) ) ;
#5693=EDGE_CURVE ( 'NONE', #54115, #35328, #92981, .T. ) ;
#5697=DIRECTION ( 'NONE',  ( -0.7863974287229266169, -5.639749025771352497E-15, 0.6177208787939496570 ) ) ;
#5700=DIRECTION ( 'NONE',  ( -0.6451914333552730696, 0.000000000000000000, -0.7640209514960754067 ) ) ;
#5708=CARTESIAN_POINT ( 'NONE',  ( -16.89397143409390623, -5.876774720514426953, 16.89397143409405899 ) ) ;
#5711=EDGE_CURVE ( 'NONE', #79973, #96474, #54439, .T. ) ;
#5728=ORIENTED_EDGE ( 'NONE', *, *, #79331, .F. ) ;
#5743=FACE_OUTER_BOUND ( 'NONE', #2363, .T. ) ;
#5746=AXIS2_PLACEMENT_3D ( 'NONE', #34639, #42274, #51861 ) ;
#5747=ORIENTED_EDGE ( 'NONE', *, *, #15829, .T. ) ;
#5754=ORIENTED_EDGE ( 'NONE', *, *, #91820, .F. ) ;
#5774=ADVANCED_FACE ( 'NONE', ( #94492 ), #47828, .T. ) ;
#5775=DIRECTION ( 'NONE',  ( 1.000000000000000000, 0.000000000000000000, 0.000000000000000000 ) ) ;
#5778=CARTESIAN_POINT ( 'NONE',  ( 7.344278919687202922, -5.876774720514417183, 20.19896341048075783 ) ) ;
#5786=ORIENTED_EDGE ( 'NONE', *, *, #23619, .F. ) ;
#5795=CARTESIAN_POINT ( 'NONE',  ( 30.60993360729056079, -4.065030569019225659, 27.12046991540520580 ) ) ;
#5800=ORIENTED_EDGE ( 'NONE', *, *, #57280, .F. ) ;
#5804=CARTESIAN_POINT ( 'NONE',  ( 3.787259615384621636, -5.876774720514404748, 18.51923076923076650 ) ) ;
#5805=CARTESIAN_POINT ( 'NONE',  ( 3.797776442307698286, -6.376774720514401196, 18.16025641025640525 ) ) ;
#5807=CARTESIAN_POINT ( 'NONE',  ( 26.73860345374794178, -5.161986642477099707, -6.453784975055922857 ) ) ;
#5811=ORIENTED_EDGE ( 'NONE', *, *, #18163, .F. ) ;
#5814=LINE ( 'NONE', #44393, #95042 ) ;
#5820=LINE ( 'NONE', #44900, #87215 ) ;
#5825=AXIS2_PLACEMENT_3D ( 'NONE', #63338, #94256, #78015 ) ;
#5829=CARTESIAN_POINT ( 'NONE',  ( 29.73860345376319003, -4.772782019468681192, -4.021180035027960287 ) ) ;
#5831=VECTOR ( 'NONE', #85170, 1000.000000000000000 ) ;
#5838=DIRECTION ( 'NONE',  ( 0.000000000000000000, 0.000000000000000000, 1.000000000000000000 ) ) ;
#5852=VECTOR ( 'NONE', #63386, 1000.000000000000000 ) ;
#5854=ORIENTED_EDGE ( 'NONE', *, *, #54318, .F. ) ;
#5855=CARTESIAN_POINT ( 'NONE',  ( -0.3982818654701407723, -5.876774720514410077, 19.46306892155547530 ) ) ;
#5868=LINE ( 'NONE', #36825, #86532 ) ;
#5869=DIRECTION ( 'NONE',  ( 0.000000000000000000, -1.000000000000000000, 0.000000000000000000 ) ) ;
#5870=ORIENTED_EDGE ( 'NONE', *, *, #58819, .F. ) ;
#5875=DIRECTION ( 'NONE',  ( -2.313651251573816365E-16, -1.000000000000000000, -8.068660792749104624E-16 ) ) ;
#5880=CARTESIAN_POINT ( 'NONE',  ( -3.085512303079157359, -5.876774720514414518, 19.95084900476495093 ) ) ;
#5886=CARTESIAN_POINT ( 'NONE',  ( -10.40290173325841216, -5.356774720514425603, 27.45402280011861862 ) ) ;
#5889=VERTEX_POINT ( 'NONE', #42730 ) ;
#5890=CARTESIAN_POINT ( 'NONE',  ( 4.328803674008796065, -6.376774720514406525, 18.75671216747623049 ) ) ;
#5900=AXIS2_PLACEMENT_3D ( 'NONE', #66193, #81888, #12365 ) ;
#5901=CARTESIAN_POINT ( 'NONE',  ( -4.886549725601808447, -5.876774720514410077, 19.15251819062245175 ) ) ;
#5908=AXIS2_PLACEMENT_3D ( 'NONE', #64785, #18567, #57652 ) ;
#5909=EDGE_CURVE ( 'NONE', #50658, #7479, #18869, .T. ) ;
#5914=ADVANCED_FACE ( 'NONE', ( #73170 ), #49846, .F. ) ;
#5915=CYLINDRICAL_SURFACE ( 'NONE', #53161, 84.48086791635432746 ) ;
#5918=ORIENTED_EDGE ( 'NONE', *, *, #75191, .F. ) ;
#5925=DIRECTION ( 'NONE',  ( 0.000000000000000000, 0.000000000000000000, -1.000000000000000000 ) ) ;
#5926=AXIS2_PLACEMENT_3D ( 'NONE', #89502, #57575, #80893 ) ;
#5931=CARTESIAN_POINT ( 'NONE',  ( -2.791950601096355733, -6.376774720514417183, 20.17732409774492552 ) ) ;
#5937=CARTESIAN_POINT ( 'NONE',  ( 11.62916340711181284, -0.3587747205144265483, 28.75961759920349792 ) ) ;
#5944=EDGE_CURVE ( 'NONE', #96134, #1389, #3661, .T. ) ;
#5947=CARTESIAN_POINT ( 'NONE',  ( -4.537657931416015700, -6.376774720514410077, 19.25713806424188235 ) ) ;
#5954=CARTESIAN_POINT ( 'NONE',  ( 3.714529970114099022, -6.376774720514426065, 21.83853177191107520 ) ) ;
#5960=EDGE_CURVE ( 'NONE', #32849, #47463, #65081, .T. ) ;
#5963=VECTOR ( 'NONE', #68807, 1000.000000000000000 ) ;
#5974=CARTESIAN_POINT ( 'NONE',  ( 3.787259615384621192, -6.376774720514426065, 21.48076923076922640 ) ) ;
#5982=CARTESIAN_POINT ( 'NONE',  ( 7.478911390063968767, -5.876774720514421624, 20.82112274756839199 ) ) ;
#5986=PLANE ( 'NONE',  #61456 ) ;
#5998=VECTOR ( 'NONE', #60942, 1000.000000000000000 ) ;
#6004=ORIENTED_EDGE ( 'NONE', *, *, #99966, .F. ) ;
#6013=CARTESIAN_POINT ( 'NONE',  ( 4.959895098850171102, -6.376774720514411854, 19.67755022954121813 ) ) ;
#6027=ADVANCED_FACE ( 'NONE', ( #47097 ), #82267, .F. ) ;
#6028=ORIENTED_EDGE ( 'NONE', *, *, #63541, .T. ) ;
#6050=CARTESIAN_POINT ( 'NONE',  ( 14.76093561896379214, 5.965225279485572685, -27.88148769130088667 ) ) ;
#6054=DIRECTION ( 'NONE',  ( 1.000000000000000000, 0.000000000000000000, 0.000000000000000000 ) ) ;
#6059=CARTESIAN_POINT ( 'NONE',  ( 3.787259615384621192, -5.876774720514425177, 21.48076923076922640 ) ) ;
#6066=CARTESIAN_POINT ( 'NONE',  ( 14.73434868161571920, -2.682774720514425670, -27.37990131745768707 ) ) ;
#6077=EDGE_LOOP ( 'NONE', ( #73628, #15986, #6004, #10856, #32353 ) ) ;
#6085=DIRECTION ( 'NONE',  ( -1.000000000000000000, -0.000000000000000000, -0.000000000000000000 ) ) ;
#6087=CARTESIAN_POINT ( 'NONE',  ( 3.509873074917118085, -0.3587747205144265483, 29.15869884040363758 ) ) ;
#6102=LINE ( 'NONE', #21811, #12188 ) ;
#6111=LINE ( 'NONE', #76112, #46117 ) ;
#6121=ORIENTED_EDGE ( 'NONE', *, *, #12306, .F. ) ;
#6125=ORIENTED_EDGE ( 'NONE', *, *, #24330, .T. ) ;
#6137=LINE ( 'NONE', #61443, #5998 ) ;
#6138=ORIENTED_EDGE ( 'NONE', *, *, #88764, .T. ) ;
#6150=DIRECTION ( 'NONE',  ( 0.06486421869277853025, 0.000000000000000000, -0.9978940991575084851 ) ) ;
#6153=CARTESIAN_POINT ( 'NONE',  ( 15.00349588318476712, -3.443263483566525007, -27.42854228801664007 ) ) ;
#6154=CARTESIAN_POINT ( 'NONE',  ( -28.49194798280534968, -0.3587747205144265483, 28.38521343323375490 ) ) ;
#6169=CARTESIAN_POINT ( 'NONE',  ( 15.99992875909482137, -3.579156900695799060, -27.91088829768895963 ) ) ;
#6183=CARTESIAN_POINT ( 'NONE',  ( -41.32836283488544638, 2.803225279485573207, 39.26872235229541985 ) ) ;
#6190=CARTESIAN_POINT ( 'NONE',  ( 33.61713288457014670, -3.416362262365323144, -11.96006463429725564 ) ) ;
#6191=DIRECTION ( 'NONE',  ( -0.000000000000000000, -1.000000000000000000, -0.000000000000000000 ) ) ;
#6194=EDGE_LOOP ( 'NONE', ( #77645, #12340, #96844, #39597, #18121 ) ) ;
#6197=LINE ( 'NONE', #61499, #32897 ) ;
#6199=CARTESIAN_POINT ( 'NONE',  ( 22.81105451610979173, 1.477225279485574028, -18.46691820600746681 ) ) ;
#6206=FACE_OUTER_BOUND ( 'NONE', #7010, .T. ) ;
#6207=DIRECTION ( 'NONE',  ( -4.472869286569340140E-16, 1.000000000000000000, 7.102795889480464408E-16 ) ) ;
#6208=CARTESIAN_POINT ( 'NONE',  ( -12.64432969575899968, -0.3587747205143967943, -26.13179214487285407 ) ) ;
#6212=CARTESIAN_POINT ( 'NONE',  ( -1.371775545366004545, -5.876774720514413630, 20.39230070883894186 ) ) ;
#6215=LINE ( 'NONE', #68129, #73808 ) ;
#6222=EDGE_CURVE ( 'NONE', #94651, #21242, #29741, .T. ) ;
#6227=CARTESIAN_POINT ( 'NONE',  ( 10.86264265031000775, 1.324225279485583551, -28.05717073599341660 ) ) ;
#6234=CARTESIAN_POINT ( 'NONE',  ( 22.81105451610979173, -1.682774720514426114, -18.46691820600746681 ) ) ;
#6239=DIRECTION ( 'NONE',  ( 0.000000000000000000, 0.000000000000000000, 1.000000000000000000 ) ) ;
#6244=CARTESIAN_POINT ( 'NONE',  ( 22.65031661608482594, -1.684774720501991618, -20.71116937900383448 ) ) ;
#6246=CARTESIAN_POINT ( 'NONE',  ( -0.1037292527911751056, -6.376774720514413630, 19.53657742262743824 ) ) ;
#6258=CARTESIAN_POINT ( 'NONE',  ( 32.16024265030974050, 5.965225279485572685, 16.27760796525321751 ) ) ;
#6270=ORIENTED_EDGE ( 'NONE', *, *, #23171, .T. ) ;
#6280=VERTEX_POINT ( 'NONE', #99727 ) ;
#6283=CARTESIAN_POINT ( 'NONE',  ( 32.34323322234308051, -6.036341485554500785, 0.7979233379450167973 ) ) ;
#6284=EDGE_CURVE ( 'NONE', #67077, #37098, #14005, .T. ) ;
#6285=ORIENTED_EDGE ( 'NONE', *, *, #40097, .F. ) ;
#6286=EDGE_CURVE ( 'NONE', #13745, #27602, #68309, .T. ) ;
#6287=ORIENTED_EDGE ( 'NONE', *, *, #98913, .T. ) ;
#6306=CARTESIAN_POINT ( 'NONE',  ( 2.920210193027767076, -6.376774720514413630, 19.64065332113010243 ) ) ;
#6308=DIRECTION ( 'NONE',  ( -1.000000000000000000, -0.000000000000000000, -7.994117400814786717E-16 ) ) ;
#6317=CARTESIAN_POINT ( 'NONE',  ( 3.797776442307698286, -5.876774720514402084, 18.16025641025640525 ) ) ;
#6325=CARTESIAN_POINT ( 'NONE',  ( -29.49875734969025842, -0.3587747205144265483, 17.86602280011862476 ) ) ;
#6326=CIRCLE ( 'NONE', #54928, 132.8284398600581824 ) ;
#6327=CARTESIAN_POINT ( 'NONE',  ( -4.635780534842457001, -5.876774720514410077, 19.53657742262743113 ) ) ;
#6331=CYLINDRICAL_SURFACE ( 'NONE', #45218, 1.836000000000000743 ) ;
#6336=DIRECTION ( 'NONE',  ( 1.333806637208504346E-15, 0.000000000000000000, 1.000000000000000000 ) ) ;
#6345=CARTESIAN_POINT ( 'NONE',  ( 0.03625801282051022839, -5.876774720514410077, 19.27714342948718240 ) ) ;
#6358=CARTESIAN_POINT ( 'NONE',  ( 0.3376760108279234784, -6.376774720514417183, 20.09898898868105732 ) ) ;
#6382=EDGE_CURVE ( 'NONE', #1528, #51970, #8397, .T. ) ;
#6384=CARTESIAN_POINT ( 'NONE',  ( -2.369893591381136755, -6.376774720514410077, 19.15221817653405623 ) ) ;
#6389=EDGE_CURVE ( 'NONE', #27315, #80744, #46458, .T. ) ;
#6399=ORIENTED_EDGE ( 'NONE', *, *, #59316, .T. ) ;
#6401=ORIENTED_EDGE ( 'NONE', *, *, #85445, .T. ) ;
#6402=EDGE_LOOP ( 'NONE', ( #39396, #89291, #7255, #51192 ) ) ;
#6419=CARTESIAN_POINT ( 'NONE',  ( -10.14776687836540070, -4.675267808546679227, 30.20327419389746382 ) ) ;
#6427=ORIENTED_EDGE ( 'NONE', *, *, #59308, .T. ) ;
#6430=CARTESIAN_POINT ( 'NONE',  ( 27.53860345374771867, -1.682774720514426114, -9.482392034746242260 ) ) ;
#6437=CARTESIAN_POINT ( 'NONE',  ( -2.702089344534958304, -6.376774720514413630, 19.72789237585158162 ) ) ;
#6449=CARTESIAN_POINT ( 'NONE',  ( 22.02124265030973760, 7.743225279485574042, 16.20402280011862217 ) ) ;
#6459=ORIENTED_EDGE ( 'NONE', *, *, #70975, .T. ) ;
#6460=VECTOR ( 'NONE', #34061, 1000.000000000000000 ) ;
#6462=CARTESIAN_POINT ( 'NONE',  ( 3.474198977381013798, -6.376774720514426065, 21.79108561604954986 ) ) ;
#6464=CARTESIAN_POINT ( 'NONE',  ( 3.794707603699265519E-15, -5.876774720514426953, 17.50000000000000000 ) ) ;
#6467=CIRCLE ( 'NONE', #35659, 25.90800000000000125 ) ;
#6468=EDGE_CURVE ( 'NONE', #29344, #12604, #77291, .T. ) ;
#6469=VERTEX_POINT ( 'NONE', #70307 ) ;
#6481=ADVANCED_FACE ( 'NONE', ( #87533 ), #56090, .F. ) ;
#6482=CARTESIAN_POINT ( 'NONE',  ( -5.115065434581078208, -6.376774720514408301, 19.15054976246387497 ) ) ;
#6499=VERTEX_POINT ( 'NONE', #3805 ) ;
#6506=CARTESIAN_POINT ( 'NONE',  ( -7.999999999999996447, -6.376774720514426953, 0.000000000000000000 ) ) ;
#6514=ORIENTED_EDGE ( 'NONE', *, *, #41198, .F. ) ;
#6518=ORIENTED_EDGE ( 'NONE', *, *, #18937, .F. ) ;
#6521=CARTESIAN_POINT ( 'NONE',  ( 4.263585034174699473, -5.876774720514401196, 18.26968045024142739 ) ) ;
#6529=CARTESIAN_POINT ( 'NONE',  ( 5.981014360695730225, -6.376774720514426065, 21.36744920115099333 ) ) ;
#6536=EDGE_CURVE ( 'NONE', #19444, #61919, #7631, .T. ) ;
#6547=CARTESIAN_POINT ( 'NONE',  ( -0.6735982426299428338, -5.876774720514410077, 19.16400979764068069 ) ) ;
#6557=FACE_OUTER_BOUND ( 'NONE', #44600, .T. ) ;
#6562=EDGE_CURVE ( 'NONE', #64622, #57117, #73310, .T. ) ;
#6565=CARTESIAN_POINT ( 'NONE',  ( 4.127208352283176396, -5.876774720514423400, 21.39624840817692686 ) ) ;
#6571=DIRECTION ( 'NONE',  ( -0.000000000000000000, -1.000000000000000000, -0.000000000000000000 ) ) ;
#6591=EDGE_CURVE ( 'NONE', #25405, #18886, #11898, .T. ) ;
#6603=CARTESIAN_POINT ( 'NONE',  ( 5.641025641025643189, -5.876774720514419847, 20.78665865384615330 ) ) ;
#6605=LINE ( 'NONE', #37556, #92284 ) ;
#6606=ORIENTED_EDGE ( 'NONE', *, *, #57607, .F. ) ;
#6626=CARTESIAN_POINT ( 'NONE',  ( 3.251543564379332008, -5.876774720514424288, 21.68810402963413964 ) ) ;
#6642=ORIENTED_EDGE ( 'NONE', *, *, #23179, .F. ) ;
#6649=CARTESIAN_POINT ( 'NONE',  ( -5.960145391809922089, -5.876774720514416295, 20.04104409779160534 ) ) ;
#6657=LINE ( 'NONE', #58472, #12953 ) ;
#6666=CARTESIAN_POINT ( 'NONE',  ( 15.98199071239991120, -3.493868136757070975, -27.92664602931597884 ) ) ;
#6682=DIRECTION ( 'NONE',  ( 0.000000000000000000, 0.000000000000000000, -1.000000000000000000 ) ) ;
#6696=CARTESIAN_POINT ( 'NONE',  ( -6.720452724358975338, -6.376774720514411854, 19.46153846153846700 ) ) ;
#6698=DIRECTION ( 'NONE',  ( 0.000000000000000000, 0.000000000000000000, -1.000000000000000000 ) ) ;
#6709=AXIS2_PLACEMENT_3D ( 'NONE', #53521, #6819, #61129 ) ;
#6710=EDGE_CURVE ( 'NONE', #30746, #13059, #91193, .T. ) ;
#6714=CARTESIAN_POINT ( 'NONE',  ( 5.402409956206937203, -6.376774720514424288, 21.18719775722114917 ) ) ;
#6718=EDGE_CURVE ( 'NONE', #69295, #35481, #70678, .T. ) ;
#6720=CARTESIAN_POINT ( 'NONE',  ( 30.53060340732035982, -4.594240983522013266, 19.84760796525321425 ) ) ;
#6723=CARTESIAN_POINT ( 'NONE',  ( -1.345681049247692940, -5.876774720514409189, 19.69174559449348294 ) ) ;
#6734=CARTESIAN_POINT ( 'NONE',  ( 14.76093561896379214, -3.316774720514426456, -26.55548769130089681 ) ) ;
#6746=ORIENTED_EDGE ( 'NONE', *, *, #92973, .T. ) ;
#6750=CARTESIAN_POINT ( 'NONE',  ( 282.9764569301858046, -4.132774720514426292, 20.79159422840526616 ) ) ;
#6754=CARTESIAN_POINT ( 'NONE',  ( 6.546094359317672584, -5.876774720514411854, 19.73546617144828375 ) ) ;
#6759=EDGE_LOOP ( 'NONE', ( #39088, #99453, #60552, #59873 ) ) ;
#6764=LINE ( 'NONE', #91006, #41407 ) ;
#6767=CARTESIAN_POINT ( 'NONE',  ( -7.641025641025641413, -6.376774720514418959, 20.36458333333334636 ) ) ;
#6773=ORIENTED_EDGE ( 'NONE', *, *, #81654, .F. ) ;
#6776=CARTESIAN_POINT ( 'NONE',  ( 32.23945434255342235, -4.540774721353955989, 2.150384428877208709 ) ) ;
#6779=ORIENTED_EDGE ( 'NONE', *, *, #95384, .F. ) ;
#6783=DIRECTION ( 'NONE',  ( 0.000000000000000000, 0.000000000000000000, 1.000000000000000000 ) ) ;
#6796=CARTESIAN_POINT ( 'NONE',  ( 3.797776442307698286, -5.876774720514402084, 18.16025641025640525 ) ) ;
#6800=CARTESIAN_POINT ( 'NONE',  ( 26.73860345374794534, -5.058662225110310828, -7.113848178280766099 ) ) ;
#6806=ADVANCED_FACE ( 'NONE', ( #69683 ), #23040, .T. ) ;
#6819=DIRECTION ( 'NONE',  ( 1.000000000000000000, 0.000000000000000000, -2.439088438507244272E-15 ) ) ;
#6820=B_SPLINE_CURVE_WITH_KNOTS ( 'NONE', 3,
 ( #67148, #59521, #51910, #13319, #44299, #70119, #93951, #8727, #46785, #46280, #602, #32555, #77712, #63026, #38662, #8225, #31551, #79223, #17330 ),
 .UNSPECIFIED., .F., .F.,
 ( 4, 1, 1, 1, 1, 1, 1, 1, 1, 1, 1, 1, 1, 1, 1, 1, 4 ),
 ( 0.000000000000000000, 0.07560433049574548370, 0.1479650154827359954, 0.2187969985237009085, 0.2894704453213758910, 0.3597242180874983819, 0.4297077387530445769, 0.5004965198485837874, 0.5744290198679491422, 0.6139472962286710578, 0.6571552698261118319, 0.7039727697209380297, 0.7549389848168008843, 0.8097066112894878431, 0.8688329536985502921, 0.9323854739325977414, 1.000000000000000000 ),
 .UNSPECIFIED. ) ;
#6821=CARTESIAN_POINT ( 'NONE',  ( 30.09341516180546350, -2.682774720514426559, -11.39311774897855933 ) ) ;
#6835=CONICAL_SURFACE ( 'NONE', #42506, 2.999999999999999112, 0.7853981633974412846 ) ;
#6838=CARTESIAN_POINT ( 'NONE',  ( -29.49875734969025842, 5.965225279485572685, 17.86602280011862476 ) ) ;
#6847=EDGE_CURVE ( 'NONE', #78994, #65732, #26002, .T. ) ;
#6848=ORIENTED_EDGE ( 'NONE', *, *, #667, .F. ) ;
#6849=CARTESIAN_POINT ( 'NONE',  ( 0.3376760108279234784, -5.876774720514417183, 20.09898898868105732 ) ) ;
#6852=EDGE_CURVE ( 'NONE', #68551, #5650, #80292, .T. ) ;
#6865=CARTESIAN_POINT ( 'NONE',  ( 4.263585034174699473, -6.376774720514402972, 18.26968045024142739 ) ) ;
#6876=DIRECTION ( 'NONE',  ( 0.000000000000000000, -1.000000000000000000, 0.000000000000000000 ) ) ;
#6881=CYLINDRICAL_SURFACE ( 'NONE', #67508, 91.74549126261076992 ) ;
#6883=ORIENTED_EDGE ( 'NONE', *, *, #28067, .T. ) ;
#6884=DIRECTION ( 'NONE',  ( 0.000000000000000000, 0.000000000000000000, -1.000000000000000000 ) ) ;
#6888=ORIENTED_EDGE ( 'NONE', *, *, #21469, .F. ) ;
#6906=CARTESIAN_POINT ( 'NONE',  ( 26.73860345374794178, -1.682774720514426114, -1.272392034746785860 ) ) ;
#6926=EDGE_CURVE ( 'NONE', #80766, #2778, #82287, .T. ) ;
#6931=EDGE_CURVE ( 'NONE', #42578, #75743, #44731, .T. ) ;
#6943=CARTESIAN_POINT ( 'NONE',  ( 33.10875634548599322, 6.475225279485573360, -11.42349945801155719 ) ) ;
#6946=EDGE_CURVE ( 'NONE', #78995, #74863, #38103, .T. ) ;
#6964=VECTOR ( 'NONE', #71993, 1000.000000000000000 ) ;
#6969=CARTESIAN_POINT ( 'NONE',  ( 14.61581676223891613, -3.316774720514426900, -27.35847991879931485 ) ) ;
#6970=VECTOR ( 'NONE', #88293, 1000.000000000000114 ) ;
#6978=DIRECTION ( 'NONE',  ( 1.000000000000000000, 0.000000000000000000, 0.000000000000000000 ) ) ;
#6979=CARTESIAN_POINT ( 'NONE',  ( 13.91401389203221406, -3.316774720514426456, 28.26920385068457264 ) ) ;
#6984=CARTESIAN_POINT ( 'NONE',  ( -5.205649524681222218, -5.876774720514406525, 19.16400979764067714 ) ) ;
#6989=VERTEX_POINT ( 'NONE', #75168 ) ;
#6991=( BOUNDED_SURFACE ( )  B_SPLINE_SURFACE ( 3, 2, ( 
 ( #94402, #40122, #78159 ),
 ( #79173, #24388, #31498 ),
 ( #71580, #53850, #552 ),
 ( #54855, #40628, #62976 ),
 ( #55863, #8672, #9672 ),
 ( #30997, #61965, #85283 ),
 ( #1569, #86787, #38613 ),
 ( #85794, #39613, #17280 ),
 ( #2075, #69573, #47739 ),
 ( #33013, #15771, #62461 ),
 ( #63988, #46737, #84781 ),
 ( #77661, #15268, #8168 ),
 ( #46227, #70064, #16275 ),
 ( #1062, #77161, #70565 ),
 ( #93391, #93899, #7664 ),
 ( #39109, #23880, #55356 ) ),
 .UNSPECIFIED., .F., .F., .T. ) 
 B_SPLINE_SURFACE_WITH_KNOTS ( ( 4, 2, 2, 2, 2, 2, 2, 4 ),
 ( 3, 3 ),
 ( 5.963111948670274387E-19, 0.0002402527847056124086, 0.0004805055694112242209, 0.0007207583541168360603, 0.0009610111388224478997, 0.001201263923528059739, 0.001441516708233671470, 0.001922022277644895149 ),
 ( 0.000000000000000000, 1.000000000000000000 ),
 .UNSPECIFIED. ) 
 GEOMETRIC_REPRESENTATION_ITEM ( )  RATIONAL_B_SPLINE_SURFACE ( (
 ( 1.000000000000000000, 0.6532382444175202085, 1.000000000000000000),
 ( 1.000000000000000000, 0.6532394276814369460, 1.000000000000000000),
 ( 1.000000000000000000, 0.6536213453767286685, 1.000000000000000000),
 ( 1.000000000000000000, 0.6551141999105375424, 1.000000000000000000),
 ( 1.000000000000000000, 0.6562426621441458385, 1.000000000000000000),
 ( 1.000000000000000000, 0.6591574828660696772, 1.000000000000000000),
 ( 1.000000000000000000, 0.6609310395923536641, 1.000000000000000000),
 ( 1.000000000000000000, 0.6650742797341039347, 1.000000000000000000),
 ( 1.000000000000000000, 0.6674600455424170020, 1.000000000000000000),
 ( 1.000000000000000000, 0.6725980719960679144, 1.000000000000000000),
 ( 1.000000000000000000, 0.6753708636379929242, 1.000000000000000000),
 ( 1.000000000000000000, 0.6813027919944147914, 1.000000000000000000),
 ( 1.000000000000000000, 0.6844015431888567091, 1.000000000000000000),
 ( 1.000000000000000000, 0.6938890553659712301, 1.000000000000000000),
 ( 1.000000000000000000, 0.7006220437376852184, 1.000000000000000000),
 ( 1.000000000000000000, 0.7071067811865475727, 1.000000000000000000) ) ) 
 REPRESENTATION_ITEM ( '' )  SURFACE ( )  );
#6993=ORIENTED_EDGE ( 'NONE', *, *, #54265, .T. ) ;
#7002=CARTESIAN_POINT ( 'NONE',  ( 5.097264368844747651, -3.299463065352477908, -27.56135813788838718 ) ) ;
#7010=EDGE_LOOP ( 'NONE', ( #35681, #93467, #99571, #93739 ) ) ;
#7013=FACE_OUTER_BOUND ( 'NONE', #65807, .T. ) ;
#7015=CARTESIAN_POINT ( 'NONE',  ( 15.32643653063177958, -3.577630190450218350, -27.14485409495429380 ) ) ;
#7017=CARTESIAN_POINT ( 'NONE',  ( 4.948119756536996761, -5.876774720514408301, 19.52858994054604125 ) ) ;
#7027=ORIENTED_EDGE ( 'NONE', *, *, #95038, .T. ) ;
#7028=ORIENTED_EDGE ( 'NONE', *, *, #34887, .T. ) ;
#7040=CARTESIAN_POINT ( 'NONE',  ( 14.76093561896379214, 5.965225279485572685, -28.39148769130089889 ) ) ;
#7047=FACE_OUTER_BOUND ( 'NONE', #86258, .T. ) ;
#7051=LINE ( 'NONE', #75050, #38188 ) ;
#7056=CARTESIAN_POINT ( 'NONE',  ( -27.96875734969026084, -3.316774720514426456, 23.50402280011861933 ) ) ;
#7061=ORIENTED_EDGE ( 'NONE', *, *, #13673, .T. ) ;
#7063=DIRECTION ( 'NONE',  ( 0.000000000000000000, 0.000000000000000000, -1.000000000000000000 ) ) ;
#7066=VERTEX_POINT ( 'NONE', #85274 ) ;
#7068=VECTOR ( 'NONE', #47102, 1000.000000000000000 ) ;
#7099=CARTESIAN_POINT ( 'NONE',  ( 6.377880655330028681, -5.876774720514424288, 21.48000012937543346 ) ) ;
#7110=EDGE_LOOP ( 'NONE', ( #95330, #98715, #97541, #67051 ) ) ;
#7122=DIRECTION ( 'NONE',  ( 0.000000000000000000, -1.000000000000000000, 0.000000000000000000 ) ) ;
#7123=VERTEX_POINT ( 'NONE', #31997 ) ;
#7137=LINE ( 'NONE', #38087, #100371 ) ;
#7149=CARTESIAN_POINT ( 'NONE',  ( 9.566520649354789185, -3.316774720514426011, -27.03026789950428110 ) ) ;
#7173=DIRECTION ( 'NONE',  ( 0.000000000000000000, 0.000000000000000000, -1.000000000000000000 ) ) ;
#7175=ORIENTED_EDGE ( 'NONE', *, *, #30050, .F. ) ;
#7185=ORIENTED_EDGE ( 'NONE', *, *, #36612, .F. ) ;
#7189=CARTESIAN_POINT ( 'NONE',  ( -29.49875734969025842, 5.965225279485572685, 25.61802280011862720 ) ) ;
#7194=EDGE_CURVE ( 'NONE', #5494, #93024, #15867, .T. ) ;
#7198=VERTEX_POINT ( 'NONE', #47712 ) ;
#7205=CARTESIAN_POINT ( 'NONE',  ( -1.380763273332680896, -6.376774720514418959, 20.28973052848695602 ) ) ;
#7206=CYLINDRICAL_SURFACE ( 'NONE', #75452, 1.399999999999999911 ) ;
#7208=CARTESIAN_POINT ( 'NONE',  ( 5.359050311451609261, -6.376774720514420736, 21.05346524168807676 ) ) ;
#7213=FACE_OUTER_BOUND ( 'NONE', #33224, .T. ) ;
#7227=CYLINDRICAL_SURFACE ( 'NONE', #12005, 0.8160000000000007248 ) ;
#7229=CARTESIAN_POINT ( 'NONE',  ( 9.150000000000003908, -5.876774720514426953, 11.88602120139451834 ) ) ;
#7237=CARTESIAN_POINT ( 'NONE',  ( 0.1739078616027790736, -6.376774720514415407, 19.75705121608222115 ) ) ;
#7242=CARTESIAN_POINT ( 'NONE',  ( 3.632744579681756569, -5.876774720514403860, 18.17103827887095946 ) ) ;
#7248=CARTESIAN_POINT ( 'NONE',  ( 6.727764423076923350, -5.876774720514413630, 19.76442307692307665 ) ) ;
#7255=ORIENTED_EDGE ( 'NONE', *, *, #75443, .T. ) ;
#7262=CARTESIAN_POINT ( 'NONE',  ( -7.536766146225033047, -6.376774720514411854, 19.63296556618507438 ) ) ;
#7264=CARTESIAN_POINT ( 'NONE',  ( 7.402957069319889172, -5.876774720514418071, 20.34212842306459024 ) ) ;
#7269=CARTESIAN_POINT ( 'NONE',  ( 11.22434917415779054, -4.132774715458839232, -26.87660878605755599 ) ) ;
#7281=EDGE_CURVE ( 'NONE', #71450, #36701, #96573, .T. ) ;
#7283=CARTESIAN_POINT ( 'NONE',  ( 16.09831413233135677, -3.622774720514429614, -27.82446136760824018 ) ) ;
#7286=CARTESIAN_POINT ( 'NONE',  ( 26.25551457520356635, -1.682774720514426114, -10.59759736550662446 ) ) ;
#7293=CARTESIAN_POINT ( 'NONE',  ( 3.475076759263674209, -6.376774720514401196, 18.20843037655054530 ) ) ;
#7300=CIRCLE ( 'NONE', #25125, 1.325999999999990298 ) ;
#7312=CARTESIAN_POINT ( 'NONE',  ( 22.02124265030973760, 7.743225279485574042, 18.45402280011862217 ) ) ;
#7344=LINE ( 'NONE', #45438, #25790 ) ;
#7362=CARTESIAN_POINT ( 'NONE',  ( -12.64432969575900323, 5.965225279485592225, -26.13179214487284696 ) ) ;
#7366=CARTESIAN_POINT ( 'NONE',  ( -3.071531057816138333, -5.876774720514412742, 19.86545874326175110 ) ) ;
#7372=CARTESIAN_POINT ( 'NONE',  ( -4.743266218460161276, -6.376774720514413630, 19.49357334786887108 ) ) ;
#7379=ORIENTED_EDGE ( 'NONE', *, *, #9893, .T. ) ;
#7387=PLANE ( 'NONE',  #77294 ) ;
#7395=EDGE_LOOP ( 'NONE', ( #58564, #62674, #90943, #12069 ) ) ;
#7399=ORIENTED_EDGE ( 'NONE', *, *, #60163, .F. ) ;
#7406=EDGE_LOOP ( 'NONE', ( #58456, #19362 ) ) ;
#7410=AXIS2_PLACEMENT_3D ( 'NONE', #73833, #10429, #41390 ) ;
#7417=PLANE ( 'NONE',  #29541 ) ;
#7419=VECTOR ( 'NONE', #95825, 1000.000000000000000 ) ;
#7420=EDGE_CURVE ( 'NONE', #83680, #92224, #69425, .T. ) ;
#7435=CARTESIAN_POINT ( 'NONE',  ( 3.797776442307698286, -5.876774720514402084, 18.16025641025640525 ) ) ;
#7441=CARTESIAN_POINT ( 'NONE',  ( -1.358974358974357921, -6.376774720514420736, 20.75510817307693046 ) ) ;
#7453=SHAPE_REPRESENTATION_RELATIONSHIP ( 'NONE' , 'NONE' ,  #26923, #64713 ) ;
#7472=CARTESIAN_POINT ( 'NONE',  ( -5.378122165843598701, -6.376774720514411854, 19.21968329462762526 ) ) ;
#7473=TOROIDAL_SURFACE ( 'NONE', #64227, 253.2618649670780826, 1.835999999999999854 ) ;
#7474=EDGE_CURVE ( 'NONE', #34973, #14282, #14628, .T. ) ;
#7475=CYLINDRICAL_SURFACE ( 'NONE', #65752, 1.149999999999998135 ) ;
#7479=VERTEX_POINT ( 'NONE', #409 ) ;
#7491=CIRCLE ( 'NONE', #47993, 252.4458649670781085 ) ;
#7493=ADVANCED_FACE ( 'NONE', ( #78518, #8527, #9026, #77521, #8020 ), #37971, .T. ) ;
#7514=CARTESIAN_POINT ( 'NONE',  ( 3.960454120839856706, -5.876774720514401196, 18.17119035270509997 ) ) ;
#7521=TOROIDAL_SURFACE ( 'NONE', #70683, 80.18232118519038920, 9.179999999999999716 ) ;
#7523=CARTESIAN_POINT ( 'NONE',  ( 5.471383689419962337, 5.965225279485594001, -29.02273493113403902 ) ) ;
#7526=EDGE_CURVE ( 'NONE', #71823, #44958, #99847, .T. ) ;
#7539=DIRECTION ( 'NONE',  ( 0.6599726524652347326, 0.000000000000000000, -0.7512896232465895441 ) ) ;
#7546=CARTESIAN_POINT ( 'NONE',  ( -20.27875734969026311, 6.143225279485574397, 24.00402280011862288 ) ) ;
#7550=EDGE_CURVE ( 'NONE', #15460, #69866, #71944, .T. ) ;
#7557=DIRECTION ( 'NONE',  ( 0.7512896232465892110, 0.000000000000000000, 0.6599726524652351767 ) ) ;
#7563=CARTESIAN_POINT ( 'NONE',  ( -24.90875734969025501, 5.965225279485572685, 19.84760796525321780 ) ) ;
#7569=CARTESIAN_POINT ( 'NONE',  ( -6.181720432442950219, -5.876774720514410077, 19.67464842890028720 ) ) ;
#7582=ORIENTED_EDGE ( 'NONE', *, *, #15332, .F. ) ;
#7584=DIRECTION ( 'NONE',  ( 0.000000000000000000, 0.000000000000000000, -1.000000000000000000 ) ) ;
#7587=CARTESIAN_POINT ( 'NONE',  ( -0.8502773128684013582, -5.876774720514413630, 19.61227901093089798 ) ) ;
#7592=AXIS2_PLACEMENT_3D ( 'NONE', #81395, #27107, #97607 ) ;
#7610=LINE ( 'NONE', #47187, #66385 ) ;
#7615=VECTOR ( 'NONE', #36378, 1000.000000000000000 ) ;
#7616=DIRECTION ( 'NONE',  ( -0.000000000000000000, 1.000000000000000000, -0.000000000000000000 ) ) ;
#7621=ORIENTED_EDGE ( 'NONE', *, *, #26435, .T. ) ;
#7626=VERTEX_POINT ( 'NONE', #98750 ) ;
#7630=ORIENTED_EDGE ( 'NONE', *, *, #83330, .F. ) ;
#7631=CIRCLE ( 'NONE', #64383, 1.399999999999999911 ) ;
#7640=CARTESIAN_POINT ( 'NONE',  ( 25.20501588964928885, -4.845993637035629575, -10.40696522542261171 ) ) ;
#7645=CARTESIAN_POINT ( 'NONE',  ( -32.30247028140506416, -1.684774720514426560, 27.60502002861223048 ) ) ;
#7647=EDGE_CURVE ( 'NONE', #89693, #59659, #5412, .T. ) ;
#7661=CYLINDRICAL_SURFACE ( 'NONE', #99939, 0.3000000000000016542 ) ;
#7664=CARTESIAN_POINT ( 'NONE',  ( 31.61046577166746374, -4.540774708561928108, 26.28065669267635585 ) ) ;
#7673=CARTESIAN_POINT ( 'NONE',  ( -5.000686017310577824, -5.876774720514411854, 19.46274624311237034 ) ) ;
#7681=DIRECTION ( 'NONE',  ( -6.217671308086683664E-14, 0.000000000000000000, -1.000000000000000000 ) ) ;
#7699=CARTESIAN_POINT ( 'NONE',  ( -1.488488975859286523, -5.876774720514411854, 19.49847411603315095 ) ) ;
#7721=AXIS2_PLACEMENT_3D ( 'NONE', #89517, #58091, #27631 ) ;
#7734=EDGE_LOOP ( 'NONE', ( #15362, #49646, #49473, #73429 ) ) ;
#7741=ORIENTED_EDGE ( 'NONE', *, *, #97312, .F. ) ;
#7742=CARTESIAN_POINT ( 'NONE',  ( -2.188401442307694289, -6.376774720514411854, 19.46153846153846700 ) ) ;
#7744=CARTESIAN_POINT ( 'NONE',  ( 0.3910256410256418569, -6.376774720514420736, 20.67377804487180271 ) ) ;
#7751=AXIS2_PLACEMENT_3D ( 'NONE', #23650, #54623, #55128 ) ;
#7752=EDGE_CURVE ( 'NONE', #2928, #31571, #82886, .T. ) ;
#7770=CARTESIAN_POINT ( 'NONE',  ( -7.421417143192116761, -6.376774720514411854, 19.43823095447975291 ) ) ;
#7776=ORIENTED_EDGE ( 'NONE', *, *, #59886, .F. ) ;
#7777=DIRECTION ( 'NONE',  ( 0.000000000000000000, -1.000000000000000000, 0.000000000000000000 ) ) ;
#7779=DIRECTION ( 'NONE',  ( 0.000000000000000000, 0.000000000000000000, 1.000000000000000000 ) ) ;
#7781=VERTEX_POINT ( 'NONE', #77897 ) ;
#7787=CARTESIAN_POINT ( 'NONE',  ( 20.65876267092793128, -4.278775337050348959, -17.77048666223835127 ) ) ;
#7790=B_SPLINE_CURVE_WITH_KNOTS ( 'NONE', 3,
 ( #82381, #58560, #82871, #12860, #43828, #44831, #44334 ),
 .UNSPECIFIED., .F., .F.,
 ( 4, 1, 1, 1, 4 ),
 ( 0.000000000000000000, 0.2835948081386949760, 0.5433948405759660982, 0.7806456291745647036, 1.000000000000000000 ),
 .UNSPECIFIED. ) ;
#7793=EDGE_LOOP ( 'NONE', ( #30952, #89238, #1317, #47045 ) ) ;
#7805=B_SPLINE_SURFACE_WITH_KNOTS ( 'NONE', 3, 1, ( 
 ( #64624, #65616 ),
 ( #56499, #41770 ),
 ( #2702, #3701 ),
 ( #87930, #40751 ),
 ( #94532, #18414 ),
 ( #10804, #17919 ),
 ( #27028, #95036 ),
 ( #49886, #71709 ),
 ( #2207, #78792 ),
 ( #96534, #64116 ),
 ( #49382, #25527 ),
 ( #57997, #9800 ),
 ( #25016, #80314 ),
 ( #9290, #72713 ),
 ( #34152, #41259 ),
 ( #71205, #40255 ),
 ( #73213, #18906 ),
 ( #65119, #96039 ),
 ( #26533, #17413 ) ),
 .UNSPECIFIED., .F., .F., .F.,
 ( 4, 1, 1, 1, 1, 1, 1, 1, 1, 1, 1, 1, 1, 1, 1, 1, 4 ),
 ( 2, 2 ),
 ( 0.000000000000000000, 0.07269466619231546023, 0.1413526962021423028, 0.2082288969497897435, 0.2736894576468444917, 0.3380517659755423177, 0.4009220982745038686, 0.4636163844951728397, 0.5278777255384772271, 0.5636262148099121516, 0.6061036626598776955, 0.6545011613018618668, 0.7100543472033251646, 0.7722619378848213367, 0.8412211450824307324, 0.9174702961779349630, 1.000000000000000000 ),
 ( 0.000000000000000000, 1.000000000000000000 ),
 .UNSPECIFIED. ) ;
#7826=CARTESIAN_POINT ( 'NONE',  ( 0.3180806761505774460, -5.876774720514415407, 20.02963804100705403 ) ) ;
#7827=CARTESIAN_POINT ( 'NONE',  ( 33.96422015159436114, 5.965225279485572685, -7.233236000911337449 ) ) ;
#7844=EDGE_LOOP ( 'NONE', ( #2309, #70142, #65286, #85719 ) ) ;
#7857=LINE ( 'NONE', #56051, #67331 ) ;
#7859=EDGE_LOOP ( 'NONE', ( #91303, #10786, #58487, #18127, #84528, #98235 ) ) ;
#7861=FACE_OUTER_BOUND ( 'NONE', #61913, .T. ) ;
#7864=EDGE_LOOP ( 'NONE', ( #1820, #51676, #76599, #97515 ) ) ;
#7867=FACE_OUTER_BOUND ( 'NONE', #37829, .T. ) ;
#7876=CARTESIAN_POINT ( 'NONE',  ( -4.854568188115255367, -6.376774720514410077, 19.46611907402017394 ) ) ;
#7877=CARTESIAN_POINT ( 'NONE',  ( -1.845912073933368536, -5.876774720514409189, 19.53740760792477360 ) ) ;
#7879=DIRECTION ( 'NONE',  ( 0.000000000000000000, 0.000000000000000000, 1.000000000000000000 ) ) ;
#7886=LINE ( 'NONE', #76390, #82769 ) ;
#7892=AXIS2_PLACEMENT_3D ( 'NONE', #69447, #15651, #8546 ) ;
#7903=PLANE ( 'NONE',  #95985 ) ;
#7904=ORIENTED_EDGE ( 'NONE', *, *, #57831, .F. ) ;
#7906=EDGE_LOOP ( 'NONE', ( #97873, #75706, #57661, #27596 ) ) ;
#7908=DIRECTION ( 'NONE',  ( 0.000000000000000000, 0.000000000000000000, -1.000000000000000000 ) ) ;
#7915=CARTESIAN_POINT ( 'NONE',  ( 14.97946386127337881, -3.496757005395663587, -28.37921330198104641 ) ) ;
#7935=CARTESIAN_POINT ( 'NONE',  ( -2.780940648273603433, -5.876774720514414518, 20.02088365235843881 ) ) ;
#7937=CARTESIAN_POINT ( 'NONE',  ( 14.23870388848190771, -5.152774720514427642, -26.44223458220801248 ) ) ;
#7939=CARTESIAN_POINT ( 'NONE',  ( 4.115763745420833786, -5.876774720514403860, 18.20859014712428348 ) ) ;
#7952=CARTESIAN_POINT ( 'NONE',  ( 2.745953332610513442, -6.376774720514418959, 21.05053573504278575 ) ) ;
#7962=CIRCLE ( 'NONE', #100287, 2.040000000000000036 ) ;
#7989=ORIENTED_EDGE ( 'NONE', *, *, #17995, .F. ) ;
#7996=ORIENTED_EDGE ( 'NONE', *, *, #62015, .F. ) ;
#8010=VECTOR ( 'NONE', #98162, 1000.000000000000000 ) ;
#8012=CARTESIAN_POINT ( 'NONE',  ( -1.714505518806294145E-16, -4.056774720514426669, 1.399999999999999911 ) ) ;
#8016=CARTESIAN_POINT ( 'NONE',  ( 4.886128916861816052, -6.376774720514411854, 19.14085035285361514 ) ) ;
#8020=FACE_BOUND ( 'NONE', #23826, .T. ) ;
#8048=CARTESIAN_POINT ( 'NONE',  ( 12.29742213896087932, -2.682774720514425670, -27.09288434420517433 ) ) ;
#8055=CYLINDRICAL_SURFACE ( 'NONE', #22737, 6.000000000000000888 ) ;
#8059=VECTOR ( 'NONE', #27749, 1000.000000000000000 ) ;
#8064=CARTESIAN_POINT ( 'NONE',  ( 6.365284455128204399, -6.376774720514413630, 19.73076923076922640 ) ) ;
#8068=CARTESIAN_POINT ( 'NONE',  ( -6.602379858799704238, -6.376774720514410077, 19.46575348430202723 ) ) ;
#8074=ADVANCED_FACE ( 'NONE', ( #56603 ), #71314, .F. ) ;
#8078=ADVANCED_FACE ( 'NONE', ( #96152, #80418 ), #9901, .F. ) ;
#8085=CARTESIAN_POINT ( 'NONE',  ( 29.73860345376319003, 1.477225279485574028, -1.272392034746785860 ) ) ;
#8098=EDGE_LOOP ( 'NONE', ( #83327, #35208, #41224, #32020 ) ) ;
#8103=AXIS2_PLACEMENT_3D ( 'NONE', #19154, #50123, #81064 ) ;
#8105=B_SPLINE_CURVE_WITH_KNOTS ( 'NONE', 3,
 ( #2183, #94510, #78268, #24991, #25502, #9774, #2679, #33618, #35623, #73679, #11276, #58468, #89403, #49360, #26511, #26000, #18390, #89901, #81289 ),
 .UNSPECIFIED., .F., .F.,
 ( 4, 1, 1, 1, 1, 1, 1, 1, 1, 1, 1, 1, 1, 1, 1, 1, 4 ),
 ( 0.000000000000000000, 0.06523080374203017728, 0.1284048960032230235, 0.1900670715964783708, 0.2509433657682806351, 0.3115458328521427123, 0.3728628021568293205, 0.4350236738562381356, 0.4990717247070431406, 0.5630910750496627148, 0.6255101063303755149, 0.6866800359296488798, 0.7472825030135124003, 0.8085634952159584943, 0.8707421035159862432, 0.9343409515059130088, 1.000000000000000000 ),
 .UNSPECIFIED. ) ;
#8106=DIRECTION ( 'NONE',  ( -0.9994733861282923959, 0.000000000000000000, -0.03244919754393515293 ) ) ;
#8110=VECTOR ( 'NONE', #4144, 1000.000000000000000 ) ;
#8112=ORIENTED_EDGE ( 'NONE', *, *, #22043, .F. ) ;
#8123=VECTOR ( 'NONE', #1944, 1000.000000000000000 ) ;
#8133=ORIENTED_EDGE ( 'NONE', *, *, #79102, .T. ) ;
#8134=ORIENTED_EDGE ( 'NONE', *, *, #24360, .F. ) ;
#8151=CARTESIAN_POINT ( 'NONE',  ( 4.400426145423703694, -5.876774720514425177, 21.64763382324305852 ) ) ;
#8153=EDGE_LOOP ( 'NONE', ( #84540, #69806, #83811, #87875, #7904 ) ) ;
#8161=CARTESIAN_POINT ( 'NONE',  ( 2.905029696106983916, -6.376774720514415407, 20.12486936895525957 ) ) ;
#8168=CARTESIAN_POINT ( 'NONE',  ( 31.62080439023052492, -4.380055315099236957, 26.73348078282562668 ) ) ;
#8173=DIRECTION ( 'NONE',  ( 0.000000000000000000, 1.000000000000000000, 0.000000000000000000 ) ) ;
#8177=CARTESIAN_POINT ( 'NONE',  ( -5.514838905578028694, -5.876774720514410966, 19.81240905262003338 ) ) ;
#8179=EDGE_CURVE ( 'NONE', #27420, #54063, #5178, .T. ) ;
#8193=ADVANCED_FACE ( 'NONE', ( #28628 ), #35253, .T. ) ;
#8197=VECTOR ( 'NONE', #75880, 1000.000000000000000 ) ;
#8200=CIRCLE ( 'NONE', #48712, 1.399999999999988143 ) ;
#8206=CARTESIAN_POINT ( 'NONE',  ( 30.53060340732036337, 1.477225279485574028, -8.442346167188910400 ) ) ;
#8208=B_SPLINE_CURVE_WITH_KNOTS ( 'NONE', 3,
 ( #44174, #7099, #75105, #68013, #98942, #5602, #30436, #36546, #67513, #52283, #60412, #91332, #29933, #99927, #52785, #21809, #83722, #14199, #6603 ),
 .UNSPECIFIED., .F., .F.,
 ( 4, 1, 1, 1, 1, 1, 1, 1, 1, 1, 1, 1, 1, 1, 1, 1, 4 ),
 ( 0.000000000000000000, 0.06796237149445635839, 0.1332834028675231042, 0.1978352977570558280, 0.2608919865309880515, 0.3233765044831760083, 0.3863500754690888384, 0.4496377310517142845, 0.5147953269783583918, 0.5792399132410295248, 0.6418141777582890839, 0.7013585647860598460, 0.7607267659857199771, 0.8192220679243895631, 0.8787161693846299304, 0.9381473540533086242, 1.000000000000000000 ),
 .UNSPECIFIED. ) ;
#8225=CARTESIAN_POINT ( 'NONE',  ( -3.103301570662693187, -5.876774720514418071, 20.14409848895067512 ) ) ;
#8227=ORIENTED_EDGE ( 'NONE', *, *, #40647, .T. ) ;
#8251=CARTESIAN_POINT ( 'NONE',  ( 0.3849403830293018358, -6.376774720514418959, 20.45311193189268906 ) ) ;
#8257=CARTESIAN_POINT ( 'NONE',  ( 3.116263380642223968, -5.876774720514401196, 18.40799819116699609 ) ) ;
#8260=CARTESIAN_POINT ( 'NONE',  ( -5.891025641025637860, -5.876774720514426953, 21.75000000000000711 ) ) ;
#8279=ORIENTED_EDGE ( 'NONE', *, *, #46869, .F. ) ;
#8289=CARTESIAN_POINT ( 'NONE',  ( -25.92875734969025814, -3.316774720514426456, -0.08597719988137648983 ) ) ;
#8301=ORIENTED_EDGE ( 'NONE', *, *, #26743, .F. ) ;
#8302=EDGE_CURVE ( 'NONE', #18512, #82889, #44861, .T. ) ;
#8303=FACE_OUTER_BOUND ( 'NONE', #532, .T. ) ;
#8317=DIRECTION ( 'NONE',  ( 0.000000000000000000, 0.000000000000000000, -1.000000000000000000 ) ) ;
#8318=CARTESIAN_POINT ( 'NONE',  ( 4.595037417369686850, -6.376774720514420736, 20.70846556543617467 ) ) ;
#8327=CARTESIAN_POINT ( 'NONE',  ( 0.2885822020289898759, -5.876774720514416295, 19.94806476610988710 ) ) ;
#8328=VECTOR ( 'NONE', #59359, 1000.000000000000000 ) ;
#8329=DIRECTION ( 'NONE',  ( -0.000000000000000000, -1.000000000000000000, -0.000000000000000000 ) ) ;
#8333=CARTESIAN_POINT ( 'NONE',  ( -7.635352852713973348, -6.376774720514415407, 20.14409848895066091 ) ) ;
#8339=VERTEX_POINT ( 'NONE', #61589 ) ;
#8341=DIRECTION ( 'NONE',  ( 0.000000000000000000, -1.000000000000000000, 0.000000000000000000 ) ) ;
#8343=ORIENTED_EDGE ( 'NONE', *, *, #14807, .F. ) ;
#8356=ADVANCED_FACE ( 'NONE', ( #32495 ), #86706, .T. ) ;
#8357=DIRECTION ( 'NONE',  ( -0.4009304992412300317, 6.845827386180410961E-16, -0.9161084732596779245 ) ) ;
#8365=VERTEX_POINT ( 'NONE', #92510 ) ;
#8371=CARTESIAN_POINT ( 'NONE',  ( -4.177535645411178500, -6.376774720514415407, 20.17598923696320767 ) ) ;
#8376=CARTESIAN_POINT ( 'NONE',  ( 32.98733314340959311, -0.3587747205144265483, 2.074222136288530027 ) ) ;
#8388=VERTEX_POINT ( 'NONE', #45360 ) ;
#8397=LINE ( 'NONE', #48480, #43284 ) ;
#8404=EDGE_CURVE ( 'NONE', #73995, #32487, #19725, .T. ) ;
#8422=FACE_OUTER_BOUND ( 'NONE', #93995, .T. ) ;
#8424=FACE_BOUND ( 'NONE', #8631, .T. ) ;
#8426=ADVANCED_FACE ( 'NONE', ( #18270 ), #91902, .T. ) ;
#8430=CARTESIAN_POINT ( 'NONE',  ( -5.293508136514246232, -5.876774720514409189, 19.18727597066021318 ) ) ;
#8434=LINE ( 'NONE', #820, #67528 ) ;
#8436=DIRECTION ( 'NONE',  ( 0.000000000000000000, -1.000000000000000000, 0.000000000000000000 ) ) ;
#8458=LINE ( 'NONE', #92185, #72668 ) ;
#8462=CIRCLE ( 'NONE', #71627, 1.325999999999990298 ) ;
#8468=DIRECTION ( 'NONE',  ( 0.000000000000000000, 0.000000000000000000, -1.000000000000000000 ) ) ;
#8471=LINE ( 'NONE', #53160, #82042 ) ;
#8474=AXIS2_PLACEMENT_3D ( 'NONE', #55, #15269, #79174 ) ;
#8486=EDGE_CURVE ( 'NONE', #87540, #93259, #42436, .T. ) ;
#8487=CARTESIAN_POINT ( 'NONE',  ( -5.023036858974360364, -6.376774720514410077, 19.14743589743590491 ) ) ;
#8496=ORIENTED_EDGE ( 'NONE', *, *, #66338, .T. ) ;
#8497=AXIS2_PLACEMENT_3D ( 'NONE', #24104, #2792, #48962 ) ;
#8499=VERTEX_POINT ( 'NONE', #34000 ) ;
#8503=ORIENTED_EDGE ( 'NONE', *, *, #15491, .T. ) ;
#8507=CARTESIAN_POINT ( 'NONE',  ( 4.486687842132109694, -6.376774720514410077, 18.98221446873611029 ) ) ;
#8509=EDGE_LOOP ( 'NONE', ( #20117, #33294, #68422, #52588 ) ) ;
#8527=FACE_OUTER_BOUND ( 'NONE', #11812, .T. ) ;
#8530=LINE ( 'NONE', #69926, #7068 ) ;
#8537=LINE ( 'NONE', #16639, #49016 ) ;
#8538=ORIENTED_EDGE ( 'NONE', *, *, #43491, .F. ) ;
#8546=DIRECTION ( 'NONE',  ( 2.501730345825856573E-15, 0.000000000000000000, 1.000000000000000000 ) ) ;
#8548=ORIENTED_EDGE ( 'NONE', *, *, #23556, .T. ) ;
#8570=CARTESIAN_POINT ( 'NONE',  ( 6.156881756163101294, -6.376774720514413630, 19.74809127057764968 ) ) ;
#8571=CIRCLE ( 'NONE', #2134, 2.500000000000000444 ) ;
#8577=CARTESIAN_POINT ( 'NONE',  ( -5.926585084595196840, -5.876774720514415407, 20.19722303762275573 ) ) ;
#8593=CARTESIAN_POINT ( 'NONE',  ( -1.012926118674504883, -6.376774720514415407, 19.92818918856637822 ) ) ;
#8597=AXIS2_PLACEMENT_3D ( 'NONE', #47214, #16747, #20244 ) ;
#8615=ORIENTED_EDGE ( 'NONE', *, *, #39342, .T. ) ;
#8617=CARTESIAN_POINT ( 'NONE',  ( -1.390986686320385468, -5.876774720514412742, 19.62288733224860948 ) ) ;
#8621=AXIS2_PLACEMENT_3D ( 'NONE', #85825, #86822, #62495 ) ;
#8631=EDGE_LOOP ( 'NONE', ( #4269, #72139 ) ) ;
#8637=ORIENTED_EDGE ( 'NONE', *, *, #35762, .F. ) ;
#8650=CARTESIAN_POINT ( 'NONE',  ( 4.189750619059152470, -5.876774720514427841, 21.76591699724029283 ) ) ;
#8655=EDGE_LOOP ( 'NONE', ( #80781, #60055, #52556, #65517 ) ) ;
#8666=ORIENTED_EDGE ( 'NONE', *, *, #35312, .F. ) ;
#8668=EDGE_CURVE ( 'NONE', #26207, #98742, #68438, .T. ) ;
#8672=CARTESIAN_POINT ( 'NONE',  ( 31.68607835968417064, -4.403148666511627951, 29.28367637967570758 ) ) ;
#8677=DIRECTION ( 'NONE',  ( -0.000000000000000000, 1.000000000000000000, -0.000000000000000000 ) ) ;
#8685=EDGE_LOOP ( 'NONE', ( #92222, #23945, #57445, #56071 ) ) ;
#8691=CARTESIAN_POINT ( 'NONE',  ( 14.56700794487395534, -4.079493581517788847, -28.22524715676654594 ) ) ;
#8697=EDGE_CURVE ( 'NONE', #18133, #12639, #60841, .T. ) ;
#8704=AXIS2_PLACEMENT_3D ( 'NONE', #23781, #64385, #31903 ) ;
#8710=FACE_OUTER_BOUND ( 'NONE', #78899, .T. ) ;
#8711=CARTESIAN_POINT ( 'NONE',  ( -1.318699232124953324, -5.876774720514411854, 19.74039977944280722 ) ) ;
#8719=B_SPLINE_CURVE_WITH_KNOTS ( 'NONE', 3,
 ( #62985, #77668, #31507, #56376, #86296, #25401, #54862, #62469, #46745, #8177, #54360, #9679, #87297, #85292, #24397, #46237, #93398, #7673, #15779 ),
 .UNSPECIFIED., .F., .F.,
 ( 4, 1, 1, 1, 1, 1, 1, 1, 1, 1, 1, 1, 1, 1, 1, 1, 4 ),
 ( 0.000000000000000000, 0.08252970382206502309, 0.1587788549175692676, 0.2277380621151786910, 0.2899456527966748909, 0.3454988386981381332, 0.3938963373401223600, 0.4363737851900878484, 0.4721222744615228284, 0.5363836155048271603, 0.5990779017254961314, 0.6619482340244576823, 0.7263105423531555083, 0.7917711030502102565, 0.8586473037978576972, 0.9273053338076845398, 1.000000000000000000 ),
 .UNSPECIFIED. ) ;
#8727=CARTESIAN_POINT ( 'NONE',  ( -2.889365861140832159, -5.876774720514410966, 19.43823095447973870 ) ) ;
#8731=FACE_OUTER_BOUND ( 'NONE', #39071, .T. ) ;
#8747=CARTESIAN_POINT ( 'NONE',  ( 22.81105451610979173, 6.475225279485573360, -20.71691820600746681 ) ) ;
#8748=VERTEX_POINT ( 'NONE', #40493 ) ;
#8750=VERTEX_POINT ( 'NONE', #70440 ) ;
#8752=CARTESIAN_POINT ( 'NONE',  ( 6.792576760808763936, -6.376774720514415407, 20.16775508794004779 ) ) ;
#8753=CARTESIAN_POINT ( 'NONE',  ( 0.2428503871269292180, -6.376774720514413630, 19.85590024959437017 ) ) ;
#8756=ORIENTED_EDGE ( 'NONE', *, *, #27309, .T. ) ;
#8759=CARTESIAN_POINT ( 'NONE',  ( 3.052815417670126319, -5.876774720514407413, 18.46676085997033923 ) ) ;
#8762=ADVANCED_FACE ( 'NONE', ( #69931 ), #1434, .T. ) ;
#8771=ORIENTED_EDGE ( 'NONE', *, *, #53566, .F. ) ;
#8781=CARTESIAN_POINT ( 'NONE',  ( 6.403846153846157740, -6.376774720514426065, 21.48076923076922995 ) ) ;
#8782=ORIENTED_EDGE ( 'NONE', *, *, #5333, .F. ) ;
#8788=EDGE_CURVE ( 'NONE', #43715, #34477, #14941, .T. ) ;
#8794=DIRECTION ( 'NONE',  ( -0.000000000000000000, 1.000000000000000000, -0.000000000000000000 ) ) ;
#8796=EDGE_CURVE ( 'NONE', #23800, #37700, #58710, .T. ) ;
#8811=EDGE_CURVE ( 'NONE', #86043, #63083, #8537, .T. ) ;
#8815=ORIENTED_EDGE ( 'NONE', *, *, #41531, .T. ) ;
#8818=DIRECTION ( 'NONE',  ( -0.6599726524652352877, 0.000000000000000000, 0.7512896232465891000 ) ) ;
#8824=DIRECTION ( 'NONE',  ( 0.000000000000000000, 0.000000000000000000, 1.000000000000000000 ) ) ;
#8831=CARTESIAN_POINT ( 'NONE',  ( -0.1037292527911751056, -5.876774720514413630, 19.53657742262743824 ) ) ;
#8839=ORIENTED_EDGE ( 'NONE', *, *, #1310, .F. ) ;
#8842=ORIENTED_EDGE ( 'NONE', *, *, #50341, .F. ) ;
#8864=CARTESIAN_POINT ( 'NONE',  ( 3.183477995988301945, -6.376774720514404748, 18.35601591497023577 ) ) ;
#8866=ORIENTED_EDGE ( 'NONE', *, *, #44279, .F. ) ;
#8869=CARTESIAN_POINT ( 'NONE',  ( -25.92875734969025814, -3.316774720514426456, 23.50402280011861933 ) ) ;
#8889=CARTESIAN_POINT ( 'NONE',  ( 0.03625801282051022839, -6.376774720514410077, 19.27714342948718240 ) ) ;
#8890=ORIENTED_EDGE ( 'NONE', *, *, #93486, .F. ) ;
#8895=CARTESIAN_POINT ( 'NONE',  ( 5.717391271363888805, -6.376774720514426953, -25.39218285751184467 ) ) ;
#8897=DIRECTION ( 'NONE',  ( 0.000000000000000000, 0.000000000000000000, 1.000000000000000000 ) ) ;
#8908=ORIENTED_EDGE ( 'NONE', *, *, #99060, .T. ) ;
#8910=CIRCLE ( 'NONE', #34852, 2.499999999999996891 ) ;
#8911=LINE ( 'NONE', #301, #58024 ) ;
#8917=ORIENTED_EDGE ( 'NONE', *, *, #653, .F. ) ;
#8928=ORIENTED_EDGE ( 'NONE', *, *, #76342, .T. ) ;
#8932=CARTESIAN_POINT ( 'NONE',  ( 0.000000000000000000, -4.056774720514426669, 3.500000000000000000 ) ) ;
#8934=CARTESIAN_POINT ( 'NONE',  ( 31.84105487026623393, -5.152774720514427642, -11.95870468328481806 ) ) ;
#8944=CARTESIAN_POINT ( 'NONE',  ( 26.73860345374794178, 1.477225279485574028, -1.272392034746785860 ) ) ;
#8955=CARTESIAN_POINT ( 'NONE',  ( 9.278253834636473130, -5.876774720514426953, 21.78128695274316229 ) ) ;
#8958=CARTESIAN_POINT ( 'NONE',  ( 4.487249349319938574, -5.876774720514419847, 21.01618089687719504 ) ) ;
#8963=FACE_OUTER_BOUND ( 'NONE', #12111, .T. ) ;
#8972=CARTESIAN_POINT ( 'NONE',  ( 4.593956459244529889, -5.876774720514410077, 19.29001220640957115 ) ) ;
#8977=VERTEX_POINT ( 'NONE', #42507 ) ;
#8980=CARTESIAN_POINT ( 'NONE',  ( 11.62916340711181284, 5.965225279485572685, 28.75961759920349792 ) ) ;
#8985=CYLINDRICAL_SURFACE ( 'NONE', #100309, 1.325999999999990298 ) ;
#8989=VERTEX_POINT ( 'NONE', #17649 ) ;
#8991=ORIENTED_EDGE ( 'NONE', *, *, #56789, .F. ) ;
#8992=EDGE_LOOP ( 'NONE', ( #67059, #85478, #48107, #23002, #79787 ) ) ;
#8997=ORIENTED_EDGE ( 'NONE', *, *, #75443, .F. ) ;
#9000=EDGE_CURVE ( 'NONE', #67804, #26531, #16534, .T. ) ;
#9008=ORIENTED_EDGE ( 'NONE', *, *, #99589, .F. ) ;
#9016=DIRECTION ( 'NONE',  ( 0.000000000000000000, -1.000000000000000000, 0.000000000000000000 ) ) ;
#9026=FACE_BOUND ( 'NONE', #64000, .T. ) ;
#9034=ORIENTED_EDGE ( 'NONE', *, *, #74757, .T. ) ;
#9036=CARTESIAN_POINT ( 'NONE',  ( -0.4362980769230789257, -6.376774720514411854, 19.46153846153846345 ) ) ;
#9043=ADVANCED_FACE ( 'NONE', ( #57729 ), #25255, .F. ) ;
#9046=DIRECTION ( 'NONE',  ( -0.000000000000000000, 1.000000000000000000, -0.000000000000000000 ) ) ;
#9050=CARTESIAN_POINT ( 'NONE',  ( 26.73860345374794534, -1.682774720514426114, -7.113848178280766099 ) ) ;
#9057=FACE_OUTER_BOUND ( 'NONE', #51176, .T. ) ;
#9060=EDGE_CURVE ( 'NONE', #94938, #43985, #41494, .T. ) ;
#9069=ADVANCED_FACE ( 'NONE', ( #34877 ), #6835, .F. ) ;
#9070=CARTESIAN_POINT ( 'NONE',  ( -5.912814555383966386, -6.376774720514418959, 20.28973052848695602 ) ) ;
#9094=AXIS2_PLACEMENT_3D ( 'NONE', #61157, #91083, #76834 ) ;
#9097=ORIENTED_EDGE ( 'NONE', *, *, #35807, .F. ) ;
#9099=PLANE ( 'NONE',  #85263 ) ;
#9111=CARTESIAN_POINT ( 'NONE',  ( -7.264088518202086675, -5.876774720514411854, 19.78976258633487717 ) ) ;
#9112=ORIENTED_EDGE ( 'NONE', *, *, #12545, .F. ) ;
#9113=VECTOR ( 'NONE', #31410, 1000.000000000000000 ) ;
#9118=ORIENTED_EDGE ( 'NONE', *, *, #33925, .T. ) ;
#9124=VERTEX_POINT ( 'NONE', #90653 ) ;
#9132=ADVANCED_FACE ( 'NONE', ( #97766 ), #43984, .T. ) ;
#9140=CARTESIAN_POINT ( 'NONE',  ( 4.261846905714947731, -5.876774720514426953, 21.73176331363731251 ) ) ;
#9141=EDGE_LOOP ( 'NONE', ( #24212, #4614, #18758, #2939, #15469, #53947, #10299, #73177, #98853, #14794, #41463 ) ) ;
#9153=CIRCLE ( 'NONE', #39943, 0.3000000000000016542 ) ;
#9154=CARTESIAN_POINT ( 'NONE',  ( 2.922108196329484375, -5.876774720514417183, 20.36383711510645256 ) ) ;
#9160=CARTESIAN_POINT ( 'NONE',  ( -9.278253834636469577, -5.876774720514426953, 21.48128695274316158 ) ) ;
#9165=DIRECTION ( 'NONE',  ( 0.1489078231574183508, 6.454799914155188842E-16, -0.9888510809027409865 ) ) ;
#9189=CIRCLE ( 'NONE', #41669, 252.4458649670781085 ) ;
#9198=DIRECTION ( 'NONE',  ( 0.000000000000000000, -7.805083003223303470E-15, 1.000000000000000000 ) ) ;
#9201=CARTESIAN_POINT ( 'NONE',  ( 3.252401863874210264, 5.965225279485592225, -29.35688408629928858 ) ) ;
#9203=ORIENTED_EDGE ( 'NONE', *, *, #35701, .T. ) ;
#9204=ADVANCED_FACE ( 'NONE', ( #98253 ), #21133, .F. ) ;
#9218=CARTESIAN_POINT ( 'NONE',  ( 0.7051282051282083962, -6.376774720514427841, 21.75000000000000000 ) ) ;
#9226=EDGE_CURVE ( 'NONE', #75580, #79185, #98758, .T. ) ;
#9228=CARTESIAN_POINT ( 'NONE',  ( 7.081057417352553784, -5.876774720514423400, 21.11453472826393352 ) ) ;
#9229=VERTEX_POINT ( 'NONE', #91150 ) ;
#9232=EDGE_CURVE ( 'NONE', #9229, #2928, #22125, .T. ) ;
#9233=CARTESIAN_POINT ( 'NONE',  ( 5.271800844963591359, -3.316774720514426456, -28.56638892015329034 ) ) ;
#9236=ORIENTED_EDGE ( 'NONE', *, *, #96779, .T. ) ;
#9240=CARTESIAN_POINT ( 'NONE',  ( 6.259688558337090036, -5.876774720514413630, 19.73360741988579292 ) ) ;
#9255=ORIENTED_EDGE ( 'NONE', *, *, #6562, .T. ) ;
#9257=ORIENTED_EDGE ( 'NONE', *, *, #89257, .T. ) ;
#9269=CARTESIAN_POINT ( 'NONE',  ( -1.222978892338334012, -6.376774720514411854, 19.56655654527324373 ) ) ;
#9271=CARTESIAN_POINT ( 'NONE',  ( 10.95759398273795249, -4.132774720514426292, -26.86884997114579932 ) ) ;
#9277=DIRECTION ( 'NONE',  ( 0.1311553622875919756, 0.000000000000000000, 0.9913618264504692190 ) ) ;
#9282=CARTESIAN_POINT ( 'NONE',  ( -28.98875734969026396, 5.965225279485572685, -0.08597719988137648983 ) ) ;
#9288=ORIENTED_EDGE ( 'NONE', *, *, #21399, .F. ) ;
#9290=CARTESIAN_POINT ( 'NONE',  ( -5.563047341353722253, -6.376774720514413630, 20.06599527532950589 ) ) ;
#9294=CARTESIAN_POINT ( 'NONE',  ( 4.854822496258163866, -6.376774720514422512, 20.96950945262037891 ) ) ;
#9296=CARTESIAN_POINT ( 'NONE',  ( 22.02124265030973760, -4.776774720514394446, 14.80402280011863425 ) ) ;
#9299=ORIENTED_EDGE ( 'NONE', *, *, #42290, .F. ) ;
#9308=CARTESIAN_POINT ( 'NONE',  ( -29.49875734969026198, -0.3587747205144262708, 7.870022800118625206 ) ) ;
#9324=LINE ( 'NONE', #24047, #24815 ) ;
#9326=VECTOR ( 'NONE', #6571, 1000.000000000000000 ) ;
#9327=FACE_OUTER_BOUND ( 'NONE', #37322, .T. ) ;
#9339=DIRECTION ( 'NONE',  ( 0.000000000000000000, 0.000000000000000000, -1.000000000000000000 ) ) ;
#9349=DIRECTION ( 'NONE',  ( -0.000000000000000000, 0.000000000000000000, -1.000000000000000000 ) ) ;
#9352=AXIS2_PLACEMENT_3D ( 'NONE', #48328, #40207, #72665 ) ;
#9357=CARTESIAN_POINT ( 'NONE',  ( 6.547257265821404104, -6.376774720514411854, 19.73960610265399396 ) ) ;
#9360=EDGE_LOOP ( 'NONE', ( #14522, #6287, #5754, #27565 ) ) ;
#9361=VECTOR ( 'NONE', #56254, 1000.000000000000000 ) ;
#9365=FACE_OUTER_BOUND ( 'NONE', #89757, .T. ) ;
#9373=EDGE_CURVE ( 'NONE', #42816, #46766, #85030, .T. ) ;
#9382=CARTESIAN_POINT ( 'NONE',  ( 4.712727796232550226, -3.316774720514426456, -25.55789472434992859 ) ) ;
#9388=VERTEX_POINT ( 'NONE', #54597 ) ;
#9390=DIRECTION ( 'NONE',  ( 0.000000000000000000, 0.000000000000000000, 1.000000000000000000 ) ) ;
#9391=CARTESIAN_POINT ( 'NONE',  ( 7.491841679052118508, -5.356774720514426491, -25.13395656343690021 ) ) ;
#9392=CARTESIAN_POINT ( 'NONE',  ( 9.150000000000000355, -5.876774720514426953, -15.70000000000000284 ) ) ;
#9403=CARTESIAN_POINT ( 'NONE',  ( -5.926585084595196840, -6.376774720514415407, 20.19722303762275573 ) ) ;
#9405=ORIENTED_EDGE ( 'NONE', *, *, #43023, .F. ) ;
#9417=LINE ( 'NONE', #80440, #14111 ) ;
#9423=ORIENTED_EDGE ( 'NONE', *, *, #58422, .F. ) ;
#9430=AXIS2_PLACEMENT_3D ( 'NONE', #74235, #95208, #71881 ) ;
#9441=EDGE_CURVE ( 'NONE', #70995, #86012, #10921, .T. ) ;
#9457=DIRECTION ( 'NONE',  ( -0.8368789961609474082, 0.000000000000000000, 0.5473879298857851072 ) ) ;
#9485=DIRECTION ( 'NONE',  ( 0.000000000000000000, 0.000000000000000000, -1.000000000000000000 ) ) ;
#9486=ORIENTED_EDGE ( 'NONE', *, *, #4887, .T. ) ;
#9487=LINE ( 'NONE', #62801, #67070 ) ;
#9503=CARTESIAN_POINT ( 'NONE',  ( 1.140932434931746582E-13, -5.876774720514426953, 21.78128695274321203 ) ) ;
#9504=CARTESIAN_POINT ( 'NONE',  ( 4.328803674008796065, -6.376774720514406525, 18.75671216747623049 ) ) ;
#9514=ORIENTED_EDGE ( 'NONE', *, *, #75882, .T. ) ;
#9541=CARTESIAN_POINT ( 'NONE',  ( -7.641025641025638748, -5.876774720514426953, 21.75000000000001066 ) ) ;
#9545=CARTESIAN_POINT ( 'NONE',  ( 15.58962545129234911, -1.684774720514426560, -26.91365498785467025 ) ) ;
#9547=DIRECTION ( 'NONE',  ( 0.000000000000000000, 0.000000000000000000, -1.000000000000000000 ) ) ;
#9549=CARTESIAN_POINT ( 'NONE',  ( 11.92939068485097209, -2.682774720514424782, -27.07380692790804488 ) ) ;
#9557=EDGE_CURVE ( 'NONE', #59937, #32327, #57609, .T. ) ;
#9561=CARTESIAN_POINT ( 'NONE',  ( 6.329711958793041049, -6.376774720514411854, 19.73172534246499765 ) ) ;
#9569=CARTESIAN_POINT ( 'NONE',  ( -5.941268476065055815, -5.876774720514417183, 20.11414146978959749 ) ) ;
#9570=EDGE_CURVE ( 'NONE', #28435, #4160, #26895, .T. ) ;
#9578=VERTEX_POINT ( 'NONE', #56614 ) ;
#9580=VECTOR ( 'NONE', #39287, 1000.000000000000227 ) ;
#9585=DIRECTION ( 'NONE',  ( 0.000000000000000000, -1.000000000000000000, 0.000000000000000000 ) ) ;
#9586=EDGE_LOOP ( 'NONE', ( #96272, #41667, #6138, #19931, #15471, #29350 ) ) ;
#9590=VECTOR ( 'NONE', #66909, 1000.000000000000000 ) ;
#9596=LINE ( 'NONE', #33428, #7419 ) ;
#9609=ORIENTED_EDGE ( 'NONE', *, *, #99966, .T. ) ;
#9614=CARTESIAN_POINT ( 'NONE',  ( -7.326923076923076650, -5.876774720514418071, 20.36318108974359831 ) ) ;
#9628=CARTESIAN_POINT ( 'NONE',  ( -5.970505764849975527, -5.876774720514411854, 19.55848054040323802 ) ) ;
#9635=LINE ( 'NONE', #47205, #99794 ) ;
#9636=B_SPLINE_CURVE_WITH_KNOTS ( 'NONE', 3,
 ( #25485, #10263, #2667, #33602, #64586, #95500, #74652, #58946, #26992, #57959, #72673, #11263, #50335, #82270, #3172, #49849 ),
 .UNSPECIFIED., .F., .F.,
 ( 4, 2, 2, 2, 2, 2, 2, 4 ),
 ( 0.000000000000000000, 0.0004662014769087530121, 0.0009324029538175060243, 0.001398604430726259036, 0.001864805907635012049, 0.002331007384543765278, 0.002797208861452518073, 0.003729611815270027567 ),
 .UNSPECIFIED. ) ;
#9640=CARTESIAN_POINT ( 'NONE',  ( 25.12780715347580696, -4.914991111971125370, -10.18391567818362731 ) ) ;
#9649=EDGE_LOOP ( 'NONE', ( #87308, #38312, #51319, #81010 ) ) ;
#9659=DIRECTION ( 'NONE',  ( 0.000000000000000000, -1.000000000000000000, 0.000000000000000000 ) ) ;
#9664=( BOUNDED_SURFACE ( )  B_SPLINE_SURFACE ( 3, 2, ( 
 ( #85447, #94566, #25050 ),
 ( #26570, #49418, #58028 ),
 ( #81349, #12318, #95570 ),
 ( #10335, #4227, #97068 ),
 ( #96563, #88967, #48911 ),
 ( #19935, #35676, #19440 ),
 ( #2738, #43295, #3737 ),
 ( #35180, #74231, #59021 ),
 ( #50405, #42802, #50904 ),
 ( #72748, #11827, #73731 ),
 ( #27570, #89462, #96075 ),
 ( #66151, #65651, #3246 ),
 ( #27064, #4726, #81846 ),
 ( #49920, #72246, #58521 ),
 ( #89953, #66651, #73243 ),
 ( #57530, #97565, #57029 ),
 ( #28064, #80344, #88465 ),
 ( #18940, #79837, #34678 ) ),
 .UNSPECIFIED., .F., .F., .T. ) 
 B_SPLINE_SURFACE_WITH_KNOTS ( ( 4, 2, 2, 2, 2, 2, 2, 2, 4 ),
 ( 3, 3 ),
 ( -3.428680950268159222E-15, 0.002319258964652063781, 0.003478888446979810228, 0.004058703188143683235, 0.004638517929307556242, 0.005798147411635302256, 0.006377962152799175263, 0.006957776893963049138, 0.009277035858618542033 ),
 ( 0.000000000000000000, 1.000000000000000000 ),
 .UNSPECIFIED. ) 
 GEOMETRIC_REPRESENTATION_ITEM ( )  RATIONAL_B_SPLINE_SURFACE ( (
 ( 1.000000000000000000, 0.7071067811865475727, 1.000000000000000000),
 ( 1.000000000000000000, 0.7071067811865475727, 1.000000000000000000),
 ( 1.000000000000000000, 0.7071067811865471286, 1.000000000000000000),
 ( 1.000000000000000000, 0.7071067811865471286, 1.000000000000000000),
 ( 1.000000000000000000, 0.7071067811865473507, 1.000000000000000000),
 ( 1.000000000000000000, 0.7071067811865473507, 1.000000000000000000),
 ( 1.000000000000000000, 0.7071067811865475727, 1.000000000000000000),
 ( 1.000000000000000000, 0.7071067811865475727, 1.000000000000000000),
 ( 1.000000000000000000, 0.7071067811865476838, 1.000000000000000000),
 ( 1.000000000000000000, 0.7071067811865476838, 1.000000000000000000),
 ( 1.000000000000000000, 0.7071067811865473507, 1.000000000000000000),
 ( 1.000000000000000000, 0.7071067811865473507, 1.000000000000000000),
 ( 1.000000000000000000, 0.7071067811865471286, 1.000000000000000000),
 ( 1.000000000000000000, 0.7071067811865471286, 1.000000000000000000),
 ( 1.000000000000000000, 0.7071067811865471286, 1.000000000000000000),
 ( 1.000000000000000000, 0.7071067811865471286, 1.000000000000000000),
 ( 1.000000000000000000, 0.7071067811865475727, 1.000000000000000000),
 ( 1.000000000000000000, 0.7071067811865475727, 1.000000000000000000) ) ) 
 REPRESENTATION_ITEM ( '' )  SURFACE ( )  );
#9672=CARTESIAN_POINT ( 'NONE',  ( 31.63443928675788186, -3.712996582965905290, 27.28441363938236464 ) ) ;
#9674=CARTESIAN_POINT ( 'NONE',  ( 282.9764569301858046, 5.965225279485572685, 20.79159422840526616 ) ) ;
#9679=CARTESIAN_POINT ( 'NONE',  ( -5.439936175300728927, -5.876774720514410077, 19.67454710845353816 ) ) ;
#9684=CARTESIAN_POINT ( 'NONE',  ( 2.904396343079095111, -6.376774720514415407, 19.95793242748194984 ) ) ;
#9688=ORIENTED_EDGE ( 'NONE', *, *, #66428, .F. ) ;
#9700=CARTESIAN_POINT ( 'NONE',  ( -7.617563585130437076, -5.876774720514412742, 19.95084900476494383 ) ) ;
#9705=CARTESIAN_POINT ( 'NONE',  ( -7.641025641025638748, -6.376774720514427841, 21.75000000000001066 ) ) ;
#9708=VECTOR ( 'NONE', #87860, 1000.000000000000000 ) ;
#9715=ORIENTED_EDGE ( 'NONE', *, *, #24533, .F. ) ;
#9718=DIRECTION ( 'NONE',  ( 0.000000000000000000, 1.000000000000000000, 0.000000000000000000 ) ) ;
#9742=CARTESIAN_POINT ( 'NONE',  ( 7.166040305186291093, -6.376774720514420736, 20.81030863372915718 ) ) ;
#9745=ORIENTED_EDGE ( 'NONE', *, *, #9441, .F. ) ;
#9746=VERTEX_POINT ( 'NONE', #66231 ) ;
#9748=CARTESIAN_POINT ( 'NONE',  ( 6.727829057902616761, -5.876774720514417183, 20.13865202822440281 ) ) ;
#9749=CARTESIAN_POINT ( 'NONE',  ( 5.329826657887789310, -6.376774720514418959, 20.66144943787464783 ) ) ;
#9752=ORIENTED_EDGE ( 'NONE', *, *, #30514, .T. ) ;
#9758=ORIENTED_EDGE ( 'NONE', *, *, #6536, .F. ) ;
#9762=ORIENTED_EDGE ( 'NONE', *, *, #63312, .T. ) ;
#9769=ORIENTED_EDGE ( 'NONE', *, *, #3194, .F. ) ;
#9773=CARTESIAN_POINT ( 'NONE',  ( 7.343377932919765705, -6.376774720514422512, 21.31293098237466310 ) ) ;
#9774=CARTESIAN_POINT ( 'NONE',  ( 5.963731207934512391, -5.876774720514413630, 19.80418863844947097 ) ) ;
#9779=PLANE ( 'NONE',  #92887 ) ;
#9785=ORIENTED_EDGE ( 'NONE', *, *, #28062, .F. ) ;
#9790=CARTESIAN_POINT ( 'NONE',  ( 30.54125281784916268, -0.6647747205144264315, 23.11160796525322070 ) ) ;
#9794=VECTOR ( 'NONE', #7557, 1000.000000000000227 ) ;
#9797=ORIENTED_EDGE ( 'NONE', *, *, #91106, .F. ) ;
#9798=CIRCLE ( 'NONE', #85925, 3.349999999999998757 ) ;
#9800=CARTESIAN_POINT ( 'NONE',  ( -5.544977400725785266, -5.876774720514410077, 19.92818918856636401 ) ) ;
#9801=EDGE_CURVE ( 'NONE', #97499, #16640, #4314, .T. ) ;
#9804=DIRECTION ( 'NONE',  ( 0.000000000000000000, 0.000000000000000000, -1.000000000000000000 ) ) ;
#9816=CARTESIAN_POINT ( 'NONE',  ( 3.787259615384621192, -6.376774720514426065, 21.48076923076922640 ) ) ;
#9820=CARTESIAN_POINT ( 'NONE',  ( -1.044871794871790938, -6.376774720514427841, 21.75000000000000355 ) ) ;
#9821=CARTESIAN_POINT ( 'NONE',  ( 6.179707021866671646, -6.376774720514426065, 21.45334750074374242 ) ) ;
#9829=CARTESIAN_POINT ( 'NONE',  ( 22.02124265030973760, 6.143225279485574397, 19.55402280011862004 ) ) ;
#9845=DIRECTION ( 'NONE',  ( -0.000000000000000000, 1.000000000000000000, -0.000000000000000000 ) ) ;
#9847=AXIS2_PLACEMENT_3D ( 'NONE', #86039, #53612, #32251 ) ;
#9864=CARTESIAN_POINT ( 'NONE',  ( 3.632744579681756569, -6.376774720514402972, 18.17103827887095946 ) ) ;
#9865=ORIENTED_EDGE ( 'NONE', *, *, #37159, .F. ) ;
#9871=VERTEX_POINT ( 'NONE', #7286 ) ;
#9873=CARTESIAN_POINT ( 'NONE',  ( 6.586338672804227024, -5.876774720514415407, 20.10086663068103618 ) ) ;
#9877=CARTESIAN_POINT ( 'NONE',  ( -1.955883090540335045, -5.876774720514411854, 19.49432735726521315 ) ) ;
#9878=ORIENTED_EDGE ( 'NONE', *, *, #81083, .F. ) ;
#9879=CARTESIAN_POINT ( 'NONE',  ( 32.84232313084847732, -4.840274619473232676, -11.71291885348859196 ) ) ;
#9880=CARTESIAN_POINT ( 'NONE',  ( 3.787259615384621192, -5.876774720514425177, 21.48076923076922640 ) ) ;
#9886=VERTEX_POINT ( 'NONE', #11298 ) ;
#9889=EDGE_LOOP ( 'NONE', ( #50411, #68210, #37091, #77362 ) ) ;
#9893=EDGE_CURVE ( 'NONE', #9578, #54063, #33641, .T. ) ;
#9901=PLANE ( 'NONE',  #14868 ) ;
#9905=EDGE_CURVE ( 'NONE', #36332, #79116, #18903, .T. ) ;
#9906=CARTESIAN_POINT ( 'NONE',  ( -6.720452724358975338, -6.376774720514411854, 19.46153846153846700 ) ) ;
#9910=CARTESIAN_POINT ( 'NONE',  ( 31.13513474936813807, -5.356774720514427379, 3.331262582247329185 ) ) ;
#9918=ORIENTED_EDGE ( 'NONE', *, *, #27493, .F. ) ;
#9920=LINE ( 'NONE', #25646, #22300 ) ;
#9921=CARTESIAN_POINT ( 'NONE',  ( -4.223504350552545361, -6.376774720514411854, 19.52341893546492813 ) ) ;
#9925=VECTOR ( 'NONE', #8818, 1000.000000000000114 ) ;
#9932=CARTESIAN_POINT ( 'NONE',  ( -41.32836283488544638, -4.132774720514426292, 39.26872235229541985 ) ) ;
#9958=CARTESIAN_POINT ( 'NONE',  ( 2.589743589743596086, -5.876774720514416295, 20.00140224358974095 ) ) ;
#9960=CARTESIAN_POINT ( 'NONE',  ( -0.02075734969026423599, -3.316774720514426456, -0.08597719988137648983 ) ) ;
#9964=ORIENTED_EDGE ( 'NONE', *, *, #72035, .T. ) ;
#9988=ORIENTED_EDGE ( 'NONE', *, *, #99355, .T. ) ;
#9999=DIRECTION ( 'NONE',  ( 0.000000000000000000, 1.000000000000000000, 0.000000000000000000 ) ) ;
#10001=CIRCLE ( 'NONE', #21352, 84.76210982660168725 ) ;
#10030=EDGE_LOOP ( 'NONE', ( #74636, #93343, #86617, #6401 ) ) ;
#10035=CARTESIAN_POINT ( 'NONE',  ( 22.02124265030973760, -6.376774720514428729, 16.20402280011862217 ) ) ;
#10040=CARTESIAN_POINT ( 'NONE',  ( -6.752792875861700850, -5.876774720514411854, 19.46247113826586528 ) ) ;
#10045=VERTEX_POINT ( 'NONE', #98011 ) ;
#10064=DIRECTION ( 'NONE',  ( 0.000000000000000000, 0.000000000000000000, 1.000000000000000000 ) ) ;
#10067=LINE ( 'NONE', #58252, #52213 ) ;
#10071=CARTESIAN_POINT ( 'NONE',  ( -19.80875734969026425, 5.965225279485572685, 31.02402280011862246 ) ) ;
#10078=VECTOR ( 'NONE', #37421, 1000.000000000000000 ) ;
#10090=CARTESIAN_POINT ( 'NONE',  ( -1.044792363895550302, -6.376774720514417183, 20.41272575174754422 ) ) ;
#10096=CARTESIAN_POINT ( 'NONE',  ( 3.960462906497916435, -6.376774720514427841, 21.82884394085917279 ) ) ;
#10111=ORIENTED_EDGE ( 'NONE', *, *, #60389, .T. ) ;
#10113=CARTESIAN_POINT ( 'NONE',  ( -1.318699232124953324, -5.876774720514410966, 19.74039977944280722 ) ) ;
#10118=PLANE ( 'NONE',  #41549 ) ;
#10121=CIRCLE ( 'NONE', #70017, 0.3000000000000016542 ) ;
#10140=CARTESIAN_POINT ( 'NONE',  ( 5.097264368844747651, -3.299463065352477908, -27.56135813788838718 ) ) ;
#10147=CARTESIAN_POINT ( 'NONE',  ( 4.931367317174526477, -5.876774720514419847, 20.61012727089847019 ) ) ;
#10148=ORIENTED_EDGE ( 'NONE', *, *, #80046, .T. ) ;
#10155=AXIS2_PLACEMENT_3D ( 'NONE', #40887, #65748, #34780 ) ;
#10166=CIRCLE ( 'NONE', #66891, 91.74549126261076992 ) ;
#10169=CARTESIAN_POINT ( 'NONE',  ( -2.369893591381136755, -6.376774720514410077, 19.15221817653405623 ) ) ;
#10178=DIRECTION ( 'NONE',  ( 0.000000000000000000, 0.000000000000000000, 1.000000000000000000 ) ) ;
#10203=CARTESIAN_POINT ( 'NONE',  ( -7.024122139145243082, -5.876774720514408301, 19.17707164986947532 ) ) ;
#10226=ORIENTED_EDGE ( 'NONE', *, *, #16659, .T. ) ;
#10245=( BOUNDED_SURFACE ( )  B_SPLINE_SURFACE ( 3, 2, ( 
 ( #10918, #9910, #10411 ),
 ( #18522, #88544, #41371 ),
 ( #71825, #65235, #2316 ),
 ( #33246, #26647, #49495 ),
 ( #42390, #64226, #56611 ),
 ( #86534, #95154, #25638 ) ),
 .UNSPECIFIED., .F., .F., .T. ) 
 B_SPLINE_SURFACE_WITH_KNOTS ( ( 4, 2, 4 ),
 ( 3, 3 ),
 ( 0.04217399329892001364, 0.04576393237407583303, 0.04935387144923164549 ),
 ( 0.000000000000000000, 1.000000000000000000 ),
 .UNSPECIFIED. ) 
 GEOMETRIC_REPRESENTATION_ITEM ( )  RATIONAL_B_SPLINE_SURFACE ( (
 ( 1.000000000000000000, 0.7071067811865475727, 1.000000000000000000),
 ( 1.000000000000000000, 0.7325703083253984893, 1.000000000000000000),
 ( 1.000000000000000000, 0.7567337024450505600, 1.000000000000000000),
 ( 1.000000000000000000, 0.8025768260704856383, 1.000000000000000000),
 ( 1.000000000000000000, 0.8242588182985012280, 1.000000000000000000),
 ( 1.000000000000000000, 0.8446854842613638059, 1.000000000000000000) ) ) 
 REPRESENTATION_ITEM ( '' )  SURFACE ( )  );
#10249=CARTESIAN_POINT ( 'NONE',  ( 6.365284455128204399, -5.876774720514413630, 19.73076923076922640 ) ) ;
#10253=AXIS2_PLACEMENT_3D ( 'NONE', #95247, #16608, #87640 ) ;
#10256=CARTESIAN_POINT ( 'NONE',  ( 33.96422015159436114, -0.3587747205144265483, -7.233236000911337449 ) ) ;
#10261=ORIENTED_EDGE ( 'NONE', *, *, #68061, .F. ) ;
#10263=CARTESIAN_POINT ( 'NONE',  ( 12.28518416766336507, -5.152774720514428530, -26.38359849988869144 ) ) ;
#10267=ADVANCED_FACE ( 'NONE', ( #87809 ), #48254, .F. ) ;
#10278=DIRECTION ( 'NONE',  ( -0.000000000000000000, 1.000000000000000000, -0.000000000000000000 ) ) ;
#10281=ORIENTED_EDGE ( 'NONE', *, *, #48984, .T. ) ;
#10296=AXIS2_PLACEMENT_3D ( 'NONE', #72866, #87581, #34300 ) ;
#10299=ORIENTED_EDGE ( 'NONE', *, *, #78709, .F. ) ;
#10301=CARTESIAN_POINT ( 'NONE',  ( 31.63608488009069575, -3.478648800329905644, 27.34773273846989738 ) ) ;
#10306=CARTESIAN_POINT ( 'NONE',  ( 4.400426145423703694, -6.376774720514426065, 21.64763382324305852 ) ) ;
#10308=DIRECTION ( 'NONE',  ( -0.000000000000000000, 1.000000000000000000, -0.000000000000000000 ) ) ;
#10317=CARTESIAN_POINT ( 'NONE',  ( 3.249631081431332280, -6.376774720514424288, 21.24682042713427776 ) ) ;
#10332=AXIS2_PLACEMENT_3D ( 'NONE', #65367, #26775, #26275 ) ;
#10334=CARTESIAN_POINT ( 'NONE',  ( 30.53060340732036337, -2.682774720514426559, -8.442346167188910400 ) ) ;
#10335=CARTESIAN_POINT ( 'NONE',  ( 7.822518687389895753, -3.316774720514091168, -28.18023264461383448 ) ) ;
#10337=CARTESIAN_POINT ( 'NONE',  ( -6.775140224358976226, -5.876774720514408301, 19.14743589743590846 ) ) ;
#10342=CARTESIAN_POINT ( 'NONE',  ( 30.53060340732036337, -5.099191132445380248, -0.7211848363580904975 ) ) ;
#10343=CARTESIAN_POINT ( 'NONE',  ( 0.000000000000000000, -2.056774720514426669, 0.000000000000000000 ) ) ;
#10344=ORIENTED_EDGE ( 'NONE', *, *, #96217, .T. ) ;
#10346=CARTESIAN_POINT ( 'NONE',  ( 7.343377932919765705, -6.376774720514422512, 21.31293098237466310 ) ) ;
#10350=DIRECTION ( 'NONE',  ( -0.000000000000000000, 1.000000000000000000, -0.000000000000000000 ) ) ;
#10354=CARTESIAN_POINT ( 'NONE',  ( 5.271800844963591359, -0.3587747205143965168, -28.56638892015329745 ) ) ;
#10369=CARTESIAN_POINT ( 'NONE',  ( -4.930333147521421822, -6.376774720514410077, 19.46306892155547530 ) ) ;
#10378=CARTESIAN_POINT ( 'NONE',  ( 0.7051282051282083962, -5.876774720514426953, 21.75000000000000000 ) ) ;
#10379=EDGE_LOOP ( 'NONE', ( #47807, #69557, #40344, #5525 ) ) ;
#10380=CARTESIAN_POINT ( 'NONE',  ( 33.55334901790278224, -3.914284326356132659, -11.46592497341461758 ) ) ;
#10381=LINE ( 'NONE', #71291, #26421 ) ;
#10386=CARTESIAN_POINT ( 'NONE',  ( -0.3544984435505275644, -6.376774720514408301, 19.15251819062245531 ) ) ;
#10387=ORIENTED_EDGE ( 'NONE', *, *, #28575, .F. ) ;
#10392=CARTESIAN_POINT ( 'NONE',  ( 0.3910256410256418569, -6.376774720514420736, 20.67377804487180271 ) ) ;
#10398=DIRECTION ( 'NONE',  ( 0.000000000000000000, 7.440411327181627631E-14, -1.000000000000000000 ) ) ;
#10401=ADVANCED_FACE ( 'NONE', ( #73092 ), #74086, .F. ) ;
#10403=CARTESIAN_POINT ( 'NONE',  ( 21.97688922017995594, 1.477225279485574028, -18.55878510778118340 ) ) ;
#10407=LINE ( 'NONE', #26134, #39421 ) ;
#10410=ORIENTED_EDGE ( 'NONE', *, *, #88218, .F. ) ;
#10411=CARTESIAN_POINT ( 'NONE',  ( 31.13513474936813807, -4.540774720514427543, 3.331262582247328741 ) ) ;
#10429=DIRECTION ( 'NONE',  ( -1.000000000000000000, 0.000000000000000000, 1.250865172912931245E-15 ) ) ;
#10431=CARTESIAN_POINT ( 'NONE',  ( -1.358974358974355257, -6.376774720514427841, 21.75000000000000711 ) ) ;
#10434=ADVANCED_FACE ( 'NONE', ( #21637 ), #68338, .T. ) ;
#10440=DIRECTION ( 'NONE',  ( 0.000000000000000000, -1.000000000000000000, 0.000000000000000000 ) ) ;
#10446=CARTESIAN_POINT ( 'NONE',  ( -6.720452724358975338, -6.376774720514411854, 19.46153846153846700 ) ) ;
#10460=ORIENTED_EDGE ( 'NONE', *, *, #37901, .T. ) ;
#10470=LINE ( 'NONE', #12468, #51725 ) ;
#10481=LINE ( 'NONE', #81998, #15199 ) ;
#10501=CARTESIAN_POINT ( 'NONE',  ( 4.593956459244529889, -6.376774720514410077, 19.29001220640957115 ) ) ;
#10505=VECTOR ( 'NONE', #32915, 1000.000000000000114 ) ;
#10518=CARTESIAN_POINT ( 'NONE',  ( -6.369015873774380943, -5.876774720514413630, 19.23384392940399934 ) ) ;
#10519=DIRECTION ( 'NONE',  ( 0.000000000000000000, 0.000000000000000000, -1.000000000000000000 ) ) ;
#10523=ORIENTED_EDGE ( 'NONE', *, *, #14542, .F. ) ;
#10530=VERTEX_POINT ( 'NONE', #68836 ) ;
#10538=CARTESIAN_POINT ( 'NONE',  ( -7.188523146553190912, -5.876774720514413630, 19.66116880005639800 ) ) ;
#10546=CIRCLE ( 'NONE', #21890, 0.2999999999999981570 ) ;
#10554=CARTESIAN_POINT ( 'NONE',  ( -1.304987980769231948, -5.876774720514413630, 19.76512419871795245 ) ) ;
#10564=LINE ( 'NONE', #47643, #74719 ) ;
#10567=LINE ( 'NONE', #96807, #53973 ) ;
#10575=CARTESIAN_POINT ( 'NONE',  ( 29.80070917940689412, -0.6647747205144266536, 27.39560796525321607 ) ) ;
#10580=ORIENTED_EDGE ( 'NONE', *, *, #31784, .T. ) ;
#10583=CARTESIAN_POINT ( 'NONE',  ( 7.089543269230769162, -6.376774720514413630, 19.75741185897435415 ) ) ;
#10585=LINE ( 'NONE', #32932, #60857 ) ;
#10594=CARTESIAN_POINT ( 'NONE',  ( 4.780030342074717886, -6.376774720514424288, 21.16398229115527130 ) ) ;
#10613=B_SPLINE_CURVE_WITH_KNOTS ( 'NONE', 3,
 ( #6345, #76829, #36803, #13449, #67265, #74848, #90582 ),
 .UNSPECIFIED., .F., .F.,
 ( 4, 1, 1, 1, 4 ),
 ( 0.000000000000000000, 0.2537340756906609762, 0.5030351201318566945, 0.7500135973308793558, 1.000000000000000000 ),
 .UNSPECIFIED. ) ;
#10619=ORIENTED_EDGE ( 'NONE', *, *, #58290, .T. ) ;
#10631=EDGE_CURVE ( 'NONE', #95426, #42247, #26701, .T. ) ;
#10633=CARTESIAN_POINT ( 'NONE',  ( -5.923037968371668072, -5.876774720514413630, 19.62288733224861303 ) ) ;
#10647=EDGE_CURVE ( 'NONE', #13725, #26613, #52267, .T. ) ;
#10654=EDGE_LOOP ( 'NONE', ( #63493, #4580, #41701, #71296 ) ) ;
#10661=CARTESIAN_POINT ( 'NONE',  ( 0.03625801282051022839, -6.376774720514410077, 19.27714342948718240 ) ) ;
#10667=LINE ( 'NONE', #58841, #53545 ) ;
#10683=AXIS2_PLACEMENT_3D ( 'NONE', #89116, #11981, #42950 ) ;
#10694=AXIS2_PLACEMENT_3D ( 'NONE', #87732, #66903, #26823 ) ;
#10699=VECTOR ( 'NONE', #88481, 1000.000000000000000 ) ;
#10704=ORIENTED_EDGE ( 'NONE', *, *, #95849, .F. ) ;
#10706=CARTESIAN_POINT ( 'NONE',  ( 5.872047395031165351, -5.876774720514416295, 20.29192741308114734 ) ) ;
#10710=FACE_OUTER_BOUND ( 'NONE', #87007, .T. ) ;
#10712=DIRECTION ( 'NONE',  ( 0.000000000000000000, 0.000000000000000000, -1.000000000000000000 ) ) ;
#10722=ADVANCED_FACE ( 'NONE', ( #64755 ), #19037, .F. ) ;
#10736=ORIENTED_EDGE ( 'NONE', *, *, #77590, .T. ) ;
#10738=AXIS2_PLACEMENT_3D ( 'NONE', #23153, #62760, #14556 ) ;
#10740=ADVANCED_FACE ( 'NONE', ( #72843 ), #52334, .F. ) ;
#10746=ORIENTED_EDGE ( 'NONE', *, *, #83212, .F. ) ;
#10748=ORIENTED_EDGE ( 'NONE', *, *, #18826, .F. ) ;
#10753=ORIENTED_EDGE ( 'NONE', *, *, #72999, .T. ) ;
#10756=CARTESIAN_POINT ( 'NONE',  ( 7.010993867624484288, -5.876774720514417183, 20.34381700913260715 ) ) ;
#10761=ORIENTED_EDGE ( 'NONE', *, *, #50586, .F. ) ;
#10766=CARTESIAN_POINT ( 'NONE',  ( 22.81105451610979173, -4.772774720514425972, -18.46691820600746681 ) ) ;
#10767=DIRECTION ( 'NONE',  ( 0.000000000000000000, -1.000000000000000000, 0.000000000000000000 ) ) ;
#10782=CARTESIAN_POINT ( 'NONE',  ( 6.830155907162054341, -6.376774720514427841, 21.76451523534627341 ) ) ;
#10783=FACE_OUTER_BOUND ( 'NONE', #6077, .T. ) ;
#10786=ORIENTED_EDGE ( 'NONE', *, *, #12585, .F. ) ;
#10796=DIRECTION ( 'NONE',  ( 0.000000000000000000, 1.000000000000000000, 0.000000000000000000 ) ) ;
#10804=CARTESIAN_POINT ( 'NONE',  ( -5.314757719055156038, -6.376774720514411854, 19.55912026249540858 ) ) ;
#10814=DIRECTION ( 'NONE',  ( 0.000000000000000000, -1.000000000000000000, 0.000000000000000000 ) ) ;
#10816=AXIS2_PLACEMENT_3D ( 'NONE', #54874, #68590, #44758 ) ;
#10818=ORIENTED_EDGE ( 'NONE', *, *, #63163, .T. ) ;
#10819=FACE_OUTER_BOUND ( 'NONE', #60993, .T. ) ;
#10820=CARTESIAN_POINT ( 'NONE',  ( -1.845912073933368536, -6.376774720514408301, 19.53740760792477360 ) ) ;
#10827=LINE ( 'NONE', #58018, #39233 ) ;
#10839=LINE ( 'NONE', #98428, #94928 ) ;
#10842=FACE_OUTER_BOUND ( 'NONE', #10992, .T. ) ;
#10847=LINE ( 'NONE', #57538, #25195 ) ;
#10848=CYLINDRICAL_SURFACE ( 'NONE', #41981, 3.500000000000000000 ) ;
#10852=CARTESIAN_POINT ( 'NONE',  ( 12.16765770914787304, 5.965225279485572685, -27.57618308014988173 ) ) ;
#10856=ORIENTED_EDGE ( 'NONE', *, *, #15829, .F. ) ;
#10881=PLANE ( 'NONE',  #67476 ) ;
#10884=CARTESIAN_POINT ( 'NONE',  ( 29.70435979725210274, -3.845442984095253536, 28.14021868772163160 ) ) ;
#10887=DIRECTION ( 'NONE',  ( 0.000000000000000000, 0.000000000000000000, -1.000000000000000000 ) ) ;
#10901=CYLINDRICAL_SURFACE ( 'NONE', #48240, 0.3000000000000016542 ) ;
#10911=FACE_OUTER_BOUND ( 'NONE', #94296, .T. ) ;
#10914=EDGE_LOOP ( 'NONE', ( #90232, #23730, #66386, #33483 ) ) ;
#10918=CARTESIAN_POINT ( 'NONE',  ( 30.32108885906865936, -5.356774720514427379, 3.274824222184972822 ) ) ;
#10920=DIRECTION ( 'NONE',  ( -0.000000000000000000, 1.000000000000000000, -0.000000000000000000 ) ) ;
#10921=LINE ( 'NONE', #78915, #73270 ) ;
#10925=VERTEX_POINT ( 'NONE', #99145 ) ;
#10946=LINE ( 'NONE', #17553, #67753 ) ;
#10950=CARTESIAN_POINT ( 'NONE',  ( -19.80875734969026425, -0.3587747205144265483, 31.02402280011862246 ) ) ;
#10953=DIRECTION ( 'NONE',  ( 1.000000000000000000, 0.000000000000000000, 0.000000000000000000 ) ) ;
#10962=CARTESIAN_POINT ( 'NONE',  ( 3.296033061219842519, -6.376774720514406525, 18.71226942120119574 ) ) ;
#10965=VECTOR ( 'NONE', #65934, 1000.000000000000000 ) ;
#10966=CARTESIAN_POINT ( 'NONE',  ( 15.58962545129235799, 6.475225279485573360, -26.91365498785467025 ) ) ;
#10968=VERTEX_POINT ( 'NONE', #51995 ) ;
#10974=CARTESIAN_POINT ( 'NONE',  ( -2.732037236150805626, -6.376774720514411854, 19.78976258633487717 ) ) ;
#10989=ORIENTED_EDGE ( 'NONE', *, *, #84718, .T. ) ;
#10992=EDGE_LOOP ( 'NONE', ( #69818, #63675, #36079, #61795 ) ) ;
#11004=VECTOR ( 'NONE', #23870, 1000.000000000000000 ) ;
#11015=ORIENTED_EDGE ( 'NONE', *, *, #80822, .T. ) ;
#11020=DIRECTION ( 'NONE',  ( 0.000000000000000000, 0.000000000000000000, -1.000000000000000000 ) ) ;
#11030=B_SPLINE_CURVE_WITH_KNOTS ( 'NONE', 3,
 ( #25923, #19305, #25424, #55892, #64021, #2107, #65520, #40151, #48782, #10706, #50272, #71107, #79705, #18317, #41671, #11202, #49286, #63509, #24915 ),
 .UNSPECIFIED., .F., .F.,
 ( 4, 1, 1, 1, 1, 1, 1, 1, 1, 1, 1, 1, 1, 1, 1, 1, 4 ),
 ( 0.000000000000000000, 0.06113791491562318298, 0.1199938438512138800, 0.1782253215076183839, 0.2362564202618999687, 0.2949293769549112820, 0.3547157488097555933, 0.4167296639241647727, 0.4806644084708298625, 0.5458317702108677061, 0.6097581054261674849, 0.6729712284742227490, 0.7360168691676642894, 0.7998393981920319806, 0.8647753566655687063, 0.9310876232725688872, 1.000000000000000000 ),
 .UNSPECIFIED. ) ;
#11033=AXIS2_PLACEMENT_3D ( 'NONE', #58134, #28663, #43403 ) ;
#11041=DIRECTION ( 'NONE',  ( 0.000000000000000000, 1.000000000000000000, -0.000000000000000000 ) ) ;
#11054=CARTESIAN_POINT ( 'NONE',  ( -24.90875734969025501, -5.356774720514425603, 27.45402280011862572 ) ) ;
#11055=DIRECTION ( 'NONE',  ( -1.000000000000000000, 0.000000000000000000, 5.238131417152343399E-15 ) ) ;
#11057=VECTOR ( 'NONE', #3724, 1000.000000000000000 ) ;
#11059=CARTESIAN_POINT ( 'NONE',  ( -0.6735982426299428338, -6.376774720514411854, 19.16400979764068069 ) ) ;
#11069=DIRECTION ( 'NONE',  ( 0.000000000000000000, -1.000000000000000000, 0.000000000000000000 ) ) ;
#11070=EDGE_CURVE ( 'NONE', #45914, #71192, #47380, .T. ) ;
#11071=EDGE_LOOP ( 'NONE', ( #87359, #98959, #85884, #25926 ) ) ;
#11072=LINE ( 'NONE', #26298, #16941 ) ;
#11088=DIRECTION ( 'NONE',  ( -0.9685340172660600322, 0.000000000000000000, 0.2488812114211667037 ) ) ;
#11116=CARTESIAN_POINT ( 'NONE',  ( -0.02075734969026423599, -6.376774720514426953, -28.03397719988137382 ) ) ;
#11123=CARTESIAN_POINT ( 'NONE',  ( 6.555906488453394410, -5.876774720514426065, 21.46941147007026274 ) ) ;
#11131=CARTESIAN_POINT ( 'NONE',  ( -6.020540257910568904, -5.876774720514411854, 19.49847411603315095 ) ) ;
#11136=CARTESIAN_POINT ( 'NONE',  ( 5.097264368844749427, -3.316774720514425567, -27.56135813788841560 ) ) ;
#11147=ORIENTED_EDGE ( 'NONE', *, *, #86871, .T. ) ;
#11150=EDGE_CURVE ( 'NONE', #15127, #57287, #62310, .T. ) ;
#11153=CARTESIAN_POINT ( 'NONE',  ( 0.3910256410256394144, -6.376774720514411854, 19.63681891025641235 ) ) ;
#11157=CARTESIAN_POINT ( 'NONE',  ( 2.627412086454235851, -6.376774720514420736, 20.59155478446653831 ) ) ;
#11172=CARTESIAN_POINT ( 'NONE',  ( 32.25249349869195470, -1.682774720514426114, -12.65342752644894553 ) ) ;
#11175=DIRECTION ( 'NONE',  ( 0.000000000000000000, 1.000000000000000000, 0.000000000000000000 ) ) ;
#11190=EDGE_LOOP ( 'NONE', ( #24962, #4404, #10736, #22824 ) ) ;
#11202=CARTESIAN_POINT ( 'NONE',  ( 6.273728352332436309, -5.876774720514416295, 20.10092598260902008 ) ) ;
#11218=DIRECTION ( 'NONE',  ( -0.1311553622875928082, 6.454799914155188842E-16, -0.9913618264504692190 ) ) ;
#11221=CARTESIAN_POINT ( 'NONE',  ( -23.59123376470063960, -5.356774720514425603, 24.50402280011862288 ) ) ;
#11226=AXIS2_PLACEMENT_3D ( 'NONE', #22062, #100168, #37314 ) ;
#11232=ORIENTED_EDGE ( 'NONE', *, *, #15332, .T. ) ;
#11241=VECTOR ( 'NONE', #58699, 1000.000000000000000 ) ;
#11245=CARTESIAN_POINT ( 'NONE',  ( 30.32108885906865936, -4.540774720514427543, 3.274824222184972822 ) ) ;
#11248=EDGE_LOOP ( 'NONE', ( #80145, #45362, #46306, #37498 ) ) ;
#11249=ORIENTED_EDGE ( 'NONE', *, *, #82364, .F. ) ;
#11252=CARTESIAN_POINT ( 'NONE',  ( 5.327901167172695907, -5.876774720514418071, 20.73192761314082233 ) ) ;
#11257=DIRECTION ( 'NONE',  ( -0.9952638024365005887, 0.000000000000000000, -0.09721092304694052555 ) ) ;
#11261=ORIENTED_EDGE ( 'NONE', *, *, #29836, .T. ) ;
#11263=CARTESIAN_POINT ( 'NONE',  ( 12.67628326092776803, -4.091305608280291217, -27.97525530010125294 ) ) ;
#11264=ORIENTED_EDGE ( 'NONE', *, *, #29489, .F. ) ;
#11271=DIRECTION ( 'NONE',  ( -0.000000000000000000, -1.000000000000000000, -0.000000000000000000 ) ) ;
#11272=ADVANCED_FACE ( 'NONE', ( #47880 ), #85933, .F. ) ;
#11276=CARTESIAN_POINT ( 'NONE',  ( 5.557675543255346184, -5.876774720514415407, 20.10561748372801461 ) ) ;
#11278=CARTESIAN_POINT ( 'NONE',  ( 7.136624701378261548, -5.876774720514419847, 20.99078681144753844 ) ) ;
#11285=ADVANCED_FACE ( 'NONE', ( #73219 ), #56505, .T. ) ;
#11287=ORIENTED_EDGE ( 'NONE', *, *, #35592, .T. ) ;
#11288=CARTESIAN_POINT ( 'NONE',  ( 7.858420481369514654, 6.475225279485573360, -27.14867965659404092 ) ) ;
#11293=FACE_OUTER_BOUND ( 'NONE', #34753, .T. ) ;
#11298=CARTESIAN_POINT ( 'NONE',  ( 14.43441819135929194, -3.316774720514426456, -28.36222020317710957 ) ) ;
#11301=CARTESIAN_POINT ( 'NONE',  ( 31.63524360068765162, -3.637569336689931543, 27.31569296206930630 ) ) ;
#11308=AXIS2_PLACEMENT_3D ( 'NONE', #23610, #47975, #16005 ) ;
#11312=EDGE_CURVE ( 'NONE', #62112, #46432, #52036, .T. ) ;
#11313=CIRCLE ( 'NONE', #24279, 129.7684398600581517 ) ;
#11323=CARTESIAN_POINT ( 'NONE',  ( 32.66876533700882845, 5.965225279485572685, -12.58926540598385557 ) ) ;
#11332=ORIENTED_EDGE ( 'NONE', *, *, #1041, .T. ) ;
#11349=CARTESIAN_POINT ( 'NONE',  ( 7.072045900997899537, -6.376774720514427841, 21.62824307385093192 ) ) ;
#11350=CARTESIAN_POINT ( 'NONE',  ( 14.52511747680497933, 5.965225279485572685, -27.86035006098926559 ) ) ;
#11359=CARTESIAN_POINT ( 'NONE',  ( 32.16024265030974050, -0.3587747205144265483, 14.03360796525321774 ) ) ;
#11370=CARTESIAN_POINT ( 'NONE',  ( -65.05438548721848235, -3.316774720514426456, 27.45402280011862572 ) ) ;
#11371=CARTESIAN_POINT ( 'NONE',  ( -4.300916688315937542, -6.376774720514410077, 19.43951662020192828 ) ) ;
#11377=DIRECTION ( 'NONE',  ( 0.000000000000000000, 0.000000000000000000, 1.000000000000000000 ) ) ;
#11379=CARTESIAN_POINT ( 'NONE',  ( 32.15269211224249091, -4.540774720514427543, 3.401810532325273417 ) ) ;
#11396=LINE ( 'NONE', #58090, #98086 ) ;
#11402=CARTESIAN_POINT ( 'NONE',  ( 7.107139210497321002, -6.376774720514413630, 19.78447747620696617 ) ) ;
#11413=DIRECTION ( 'NONE',  ( 1.226388327005079762E-16, 0.000000000000000000, -1.000000000000000000 ) ) ;
#11414=ORIENTED_EDGE ( 'NONE', *, *, #19882, .T. ) ;
#11415=ORIENTED_EDGE ( 'NONE', *, *, #38917, .F. ) ;
#11419=CARTESIAN_POINT ( 'NONE',  ( 29.73860345376319358, -5.356514366711551567, 19.42370913944100863 ) ) ;
#11426=CARTESIAN_POINT ( 'NONE',  ( 2.598318274922708060, -5.876774720514414518, 19.68966562063331693 ) ) ;
#11436=AXIS2_PLACEMENT_3D ( 'NONE', #87900, #78759, #85005 ) ;
#11443=DIRECTION ( 'NONE',  ( 0.000000000000000000, 0.000000000000000000, 1.000000000000000000 ) ) ;
#11469=EDGE_LOOP ( 'NONE', ( #90461, #89530, #100281, #57501 ) ) ;
#11480=DIRECTION ( 'NONE',  ( 0.000000000000000000, 0.000000000000000000, -1.000000000000000000 ) ) ;
#11482=ORIENTED_EDGE ( 'NONE', *, *, #29490, .F. ) ;
#11485=ORIENTED_EDGE ( 'NONE', *, *, #32476, .T. ) ;
#11486=CARTESIAN_POINT ( 'NONE',  ( -9.278253834636473130, -5.876774720514426953, 18.21871304725684482 ) ) ;
#11504=ORIENTED_EDGE ( 'NONE', *, *, #40878, .F. ) ;
#11515=ADVANCED_FACE ( 'NONE', ( #78061 ), #87193, .T. ) ;
#11516=DIRECTION ( 'NONE',  ( -0.000000000000000000, 1.000000000000000000, -0.000000000000000000 ) ) ;
#11526=CIRCLE ( 'NONE', #40715, 28.96799999999999642 ) ;
#11531=CARTESIAN_POINT ( 'NONE',  ( -1.358974358974357921, -6.376774720514420736, 20.75510817307693046 ) ) ;
#11532=CARTESIAN_POINT ( 'NONE',  ( 32.40199294184733247, 6.475225279485576024, -12.82361242714783245 ) ) ;
#11535=CARTESIAN_POINT ( 'NONE',  ( -7.312991930324885814, -6.376774720514413630, 20.02088365235844947 ) ) ;
#11539=EDGE_CURVE ( 'NONE', #56847, #77894, #70979, .T. ) ;
#11541=CARTESIAN_POINT ( 'NONE',  ( -5.576923076923076650, -6.376774720514418959, 20.44941907051282470 ) ) ;
#11544=CARTESIAN_POINT ( 'NONE',  ( 29.73860345376319358, 1.477225279485574028, 7.190646357373898680E-15 ) ) ;
#11547=CARTESIAN_POINT ( 'NONE',  ( -1.064504969004270052, -6.376774720514410077, 19.35667676486395905 ) ) ;
#11572=EDGE_CURVE ( 'NONE', #77700, #69513, #5643, .T. ) ;
#11578=FACE_OUTER_BOUND ( 'NONE', #61923, .T. ) ;
#11579=CARTESIAN_POINT ( 'NONE',  ( -4.926336369345162502, -0.3587747205143967943, -28.61095484066305161 ) ) ;
#11584=AXIS2_PLACEMENT_3D ( 'NONE', #21294, #82206, #42672 ) ;
#11596=CARTESIAN_POINT ( 'NONE',  ( -7.999999999999996447, -5.876774720514426953, 17.50000000000000000 ) ) ;
#11603=ORIENTED_EDGE ( 'NONE', *, *, #46001, .T. ) ;
#11615=CARTESIAN_POINT ( 'NONE',  ( 6.697025426467099862, -5.876774720514423400, 21.43052570396496037 ) ) ;
#11622=CARTESIAN_POINT ( 'NONE',  ( 3.296033061219842519, -5.876774720514407413, 18.71226942120119574 ) ) ;
#11624=DIRECTION ( 'NONE',  ( 0.000000000000000000, 0.000000000000000000, -1.000000000000000000 ) ) ;
#11636=DIRECTION ( 'NONE',  ( -1.000000000000000000, 0.000000000000000000, 0.000000000000000000 ) ) ;
#11640=ORIENTED_EDGE ( 'NONE', *, *, #53566, .T. ) ;
#11643=LINE ( 'NONE', #88283, #67644 ) ;
#11644=ORIENTED_EDGE ( 'NONE', *, *, #56543, .T. ) ;
#11649=CARTESIAN_POINT ( 'NONE',  ( 2.933277810221831761, -6.376774720514424288, 21.39432064584807947 ) ) ;
#11656=EDGE_CURVE ( 'NONE', #32849, #67333, #89694, .T. ) ;
#11671=CARTESIAN_POINT ( 'NONE',  ( 4.518955212990007908, -5.876774720514422512, 20.94857968174986951 ) ) ;
#11675=ADVANCED_FACE ( 'NONE', ( #20666 ), #42039, .T. ) ;
#11679=LINE ( 'NONE', #42662, #15632 ) ;
#11681=CARTESIAN_POINT ( 'NONE',  ( -20.77875734969026311, 6.143225279485574397, 29.49402280011862487 ) ) ;
#11695=CARTESIAN_POINT ( 'NONE',  ( 29.80070917940689412, 6.475225279485573360, 27.39560796525321607 ) ) ;
#11696=CARTESIAN_POINT ( 'NONE',  ( 13.86067930680217586, -3.316774720512323693, -28.23766061184436538 ) ) ;
#11703=ORIENTED_EDGE ( 'NONE', *, *, #32936, .T. ) ;
#11707=CARTESIAN_POINT ( 'NONE',  ( -23.31187512739357359, -6.376774720514425177, -17.31005501743528541 ) ) ;
#11711=EDGE_CURVE ( 'NONE', #79539, #83635, #73473, .T. ) ;
#11715=EDGE_CURVE ( 'NONE', #7781, #36610, #47741, .T. ) ;
#11721=ORIENTED_EDGE ( 'NONE', *, *, #93676, .F. ) ;
#11723=EDGE_CURVE ( 'NONE', #56850, #4364, #11072, .T. ) ;
#11724=LINE ( 'NONE', #50806, #9708 ) ;
#11726=LINE ( 'NONE', #97949, #80431 ) ;
#11743=CARTESIAN_POINT ( 'NONE',  ( 14.74567117936146943, -4.687674228468594606, -27.80582190761124650 ) ) ;
#11745=EDGE_CURVE ( 'NONE', #54720, #100399, #27298, .T. ) ;
#11758=VERTEX_POINT ( 'NONE', #18673 ) ;
#11761=ORIENTED_EDGE ( 'NONE', *, *, #81530, .T. ) ;
#11762=VECTOR ( 'NONE', #36257, 1000.000000000000114 ) ;
#11775=CARTESIAN_POINT ( 'NONE',  ( 6.996935307331598075, -5.876774720514423400, 21.22729008382901128 ) ) ;
#11778=PLANE ( 'NONE',  #42725 ) ;
#11784=AXIS2_PLACEMENT_3D ( 'NONE', #90933, #28048, #14298 ) ;
#11788=DIRECTION ( 'NONE',  ( 0.000000000000000000, 1.478457507934778393E-16, -1.000000000000000000 ) ) ;
#11812=EDGE_LOOP ( 'NONE', ( #14673, #47595, #11264, #73112 ) ) ;
#11818=DIRECTION ( 'NONE',  ( -0.9978940991575084851, 0.000000000000000000, -0.06486421869277853025 ) ) ;
#11819=AXIS2_PLACEMENT_3D ( 'NONE', #90631, #21107, #82024 ) ;
#11827=CARTESIAN_POINT ( 'NONE',  ( 9.818046095181445665, -6.376774720513919803, -28.04791983960493695 ) ) ;
#11836=VERTEX_POINT ( 'NONE', #22649 ) ;
#11838=CARTESIAN_POINT ( 'NONE',  ( 7.478911390063968767, -5.876774720514422512, 20.82112274756839199 ) ) ;
#11847=CARTESIAN_POINT ( 'NONE',  ( -2.243088942307695177, -6.376774720514408301, 19.14743589743590491 ) ) ;
#11852=CARTESIAN_POINT ( 'NONE',  ( 9.948453975742596711, 5.965225279485574461, -28.04422933552663366 ) ) ;
#11861=ORIENTED_EDGE ( 'NONE', *, *, #77949, .T. ) ;
#11869=VERTEX_POINT ( 'NONE', #21654 ) ;
#11872=CARTESIAN_POINT ( 'NONE',  ( -28.98875734969026041, -0.3587747205144262708, 23.37402280011862743 ) ) ;
#11875=CARTESIAN_POINT ( 'NONE',  ( 29.71114493364435916, -4.339464138238508184, 27.93491297891351621 ) ) ;
#11876=CARTESIAN_POINT ( 'NONE',  ( 26.14999174255633463, -4.132774720517320866, -11.56127575336603286 ) ) ;
#11880=CARTESIAN_POINT ( 'NONE',  ( 3.206569032998081603, -5.876774720514424288, 21.19686455982786200 ) ) ;
#11887=AXIS2_PLACEMENT_3D ( 'NONE', #5708, #4724, #67135 ) ;
#11898=LINE ( 'NONE', #5282, #72473 ) ;
#11903=DIRECTION ( 'NONE',  ( -0.000000000000000000, -1.000000000000000000, -0.000000000000000000 ) ) ;
#11907=EDGE_CURVE ( 'NONE', #90367, #95277, #86571, .T. ) ;
#11921=DIRECTION ( 'NONE',  ( 0.000000000000000000, 0.000000000000000000, -1.000000000000000000 ) ) ;
#11922=VECTOR ( 'NONE', #75025, 1000.000000000000000 ) ;
#11925=CARTESIAN_POINT ( 'NONE',  ( 13.36367879947601445, -5.876774720514426953, 20.00000000000000355 ) ) ;
#11929=DIRECTION ( 'NONE',  ( 0.000000000000000000, 1.478457507934778393E-16, -1.000000000000000000 ) ) ;
#11954=DIRECTION ( 'NONE',  ( -1.000000000000000000, 0.000000000000000000, -0.000000000000000000 ) ) ;
#11957=ORIENTED_EDGE ( 'NONE', *, *, #40647, .F. ) ;
#11958=CARTESIAN_POINT ( 'NONE',  ( 10.86264265030973952, -0.3587747205144257157, -28.64597719988137570 ) ) ;
#11959=B_SPLINE_CURVE_WITH_KNOTS ( 'NONE', 3,
 ( #86208, #48670, #94815, #70489, #62378, #70994, #71998 ),
 .UNSPECIFIED., .F., .F.,
 ( 4, 1, 1, 1, 4 ),
 ( 0.3452202732246780759, 0.4949101844912719983, 0.6446000957578658097, 0.7942900070244596211, 0.9439799182910535436 ),
 .UNSPECIFIED. ) ;
#11971=CARTESIAN_POINT ( 'NONE',  ( 0.3910256410256418569, -6.376774720514420736, 20.67377804487180271 ) ) ;
#11981=DIRECTION ( 'NONE',  ( -0.000000000000000000, 1.000000000000000000, -0.000000000000000000 ) ) ;
#11983=VERTEX_POINT ( 'NONE', #70857 ) ;
#11990=ORIENTED_EDGE ( 'NONE', *, *, #98220, .T. ) ;
#11996=ORIENTED_EDGE ( 'NONE', *, *, #46800, .F. ) ;
#12005=AXIS2_PLACEMENT_3D ( 'NONE', #6734, #83357, #44817 ) ;
#12006=ORIENTED_EDGE ( 'NONE', *, *, #14721, .F. ) ;
#12008=B_SPLINE_CURVE_WITH_KNOTS ( 'NONE', 3,
 ( #6800, #5807, #99142, #44888, #53501, #43389 ),
 .UNSPECIFIED., .F., .F.,
 ( 4, 2, 4 ),
 ( 0.07707475098329773233, 0.07906619944496928731, 0.08105764790664082842 ),
 .UNSPECIFIED. ) ;
#12013=DIRECTION ( 'NONE',  ( -0.000000000000000000, 1.000000000000000000, -0.000000000000000000 ) ) ;
#12017=CARTESIAN_POINT ( 'NONE',  ( 10.86264265030973952, 5.965225279485574461, -27.62597719988137612 ) ) ;
#12018=LINE ( 'NONE', #98241, #11241 ) ;
#12029=ADVANCED_FACE ( 'NONE', ( #87070 ), #73730, .F. ) ;
#12041=CARTESIAN_POINT ( 'NONE',  ( -27.61845239340658154, -0.3587747205144057872, -10.37513603161905706 ) ) ;
#12057=DIRECTION ( 'NONE',  ( 0.000000000000000000, 0.000000000000000000, 1.000000000000000000 ) ) ;
#12059=VECTOR ( 'NONE', #47578, 1000.000000000000000 ) ;
#12061=LINE ( 'NONE', #27794, #59341 ) ;
#12069=ORIENTED_EDGE ( 'NONE', *, *, #44163, .T. ) ;
#12072=PLANE ( 'NONE',  #48491 ) ;
#12073=ADVANCED_FACE ( 'NONE', ( #96193 ), #26173, .T. ) ;
#12077=FACE_OUTER_BOUND ( 'NONE', #8992, .T. ) ;
#12081=CARTESIAN_POINT ( 'NONE',  ( 4.736659488006659480, -6.376774720514420736, 21.25082490164487581 ) ) ;
#12083=DIRECTION ( 'NONE',  ( -0.9952638024365006997, 0.000000000000000000, -0.09721092304694052555 ) ) ;
#12085=AXIS2_PLACEMENT_3D ( 'NONE', #62111, #69209, #77797 ) ;
#12091=CARTESIAN_POINT ( 'NONE',  ( -16.89397143409390623, -6.376774720514426953, 16.89397143409405899 ) ) ;
#12111=EDGE_LOOP ( 'NONE', ( #31612, #15653, #23246, #25701 ) ) ;
#12126=CIRCLE ( 'NONE', #15383, 129.7684398600581517 ) ;
#12131=CARTESIAN_POINT ( 'NONE',  ( 5.671814302646631667, -5.876774720514418071, 20.58085404595000512 ) ) ;
#12135=VERTEX_POINT ( 'NONE', #4348 ) ;
#12143=ORIENTED_EDGE ( 'NONE', *, *, #11539, .F. ) ;
#12146=CARTESIAN_POINT ( 'NONE',  ( 2.787364042957740651, -6.376774720514424288, 21.14548745790758488 ) ) ;
#12155=EDGE_CURVE ( 'NONE', #72161, #35495, #57529, .T. ) ;
#12156=CARTESIAN_POINT ( 'NONE',  ( -3.095730855174848362, -6.376774720514413630, 20.04377961306771638 ) ) ;
#12159=VECTOR ( 'NONE', #64647, 1000.000000000000114 ) ;
#12179=DIRECTION ( 'NONE',  ( -0.06283980576413537855, 0.000000000000000000, -0.9980236263794188822 ) ) ;
#12188=VECTOR ( 'NONE', #4619, 1000.000000000000227 ) ;
#12192=CARTESIAN_POINT ( 'NONE',  ( 11.95416678406013489, -5.152774720514426754, -26.25966023343078248 ) ) ;
#12194=CARTESIAN_POINT ( 'NONE',  ( 30.09341516180546350, -4.772774720514425972, -13.09311774897855862 ) ) ;
#12200=AXIS2_PLACEMENT_3D ( 'NONE', #24578, #38308, #100183 ) ;
#12205=EDGE_CURVE ( 'NONE', #99563, #42617, #89952, .T. ) ;
#12221=VECTOR ( 'NONE', #25311, 1000.000000000000114 ) ;
#12233=CARTESIAN_POINT ( 'NONE',  ( 15.76197349289645189, -3.603191427427929305, -28.09505689080105384 ) ) ;
#12244=DIRECTION ( 'NONE',  ( 1.000000000000000000, 2.464095846557964090E-17, 0.000000000000000000 ) ) ;
#12264=CARTESIAN_POINT ( 'NONE',  ( 7.153659783701941777, -6.376774720514422512, 20.92502190304499265 ) ) ;
#12265=VERTEX_POINT ( 'NONE', #5829 ) ;
#12269=AXIS2_PLACEMENT_3D ( 'NONE', #9233, #62038, #126 ) ;
#12273=CARTESIAN_POINT ( 'NONE',  ( 10.64801255963128668, 6.475225279485572472, -27.03041135669327488 ) ) ;
#12283=EDGE_LOOP ( 'NONE', ( #80396, #29602, #40102, #45072 ) ) ;
#12289=EDGE_CURVE ( 'NONE', #30492, #50183, #22034, .T. ) ;
#12291=DIRECTION ( 'NONE',  ( 0.000000000000000000, -3.055962005780221396E-15, -1.000000000000000000 ) ) ;
#12295=ORIENTED_EDGE ( 'NONE', *, *, #56022, .F. ) ;
#12297=CARTESIAN_POINT ( 'NONE',  ( 30.59431191903084013, -4.508530027678929741, 26.46517314890041916 ) ) ;
#12304=CARTESIAN_POINT ( 'NONE',  ( -7.264088518202086675, -6.376774720514411854, 19.78976258633487717 ) ) ;
#12305=DIRECTION ( 'NONE',  ( 7.994117400814786717E-16, 0.000000000000000000, -1.000000000000000000 ) ) ;
#12306=EDGE_CURVE ( 'NONE', #33323, #83635, #39677, .T. ) ;
#12314=CARTESIAN_POINT ( 'NONE',  ( 9.492487079130338401, -5.851656861456516978, -26.75003832473357690 ) ) ;
#12318=CARTESIAN_POINT ( 'NONE',  ( 6.783277368979140576, -6.376774720515435924, -28.31678455572487252 ) ) ;
#12321=EDGE_CURVE ( 'NONE', #86027, #94971, #85095, .T. ) ;
#12328=CARTESIAN_POINT ( 'NONE',  ( 6.420673076923079314, -6.376774720514427841, 21.83974358974358765 ) ) ;
#12330=VECTOR ( 'NONE', #56630, 1000.000000000000000 ) ;
#12334=EDGE_CURVE ( 'NONE', #20807, #89693, #64055, .T. ) ;
#12335=VECTOR ( 'NONE', #54368, 1000.000000000000000 ) ;
#12336=DIRECTION ( 'NONE',  ( 0.9888510809027408754, 5.365801633547220192E-16, 0.1489078231574191280 ) ) ;
#12337=VECTOR ( 'NONE', #82350, 1000.000000000000000 ) ;
#12340=ORIENTED_EDGE ( 'NONE', *, *, #89017, .T. ) ;
#12357=CARTESIAN_POINT ( 'NONE',  ( 10.95759398273795249, -4.132774720514426292, -26.86884997114579932 ) ) ;
#12364=AXIS2_PLACEMENT_3D ( 'NONE', #76422, #43994, #45009 ) ;
#12365=DIRECTION ( 'NONE',  ( -2.216313064514630605E-15, -0.000000000000000000, -1.000000000000000000 ) ) ;
#12394=CARTESIAN_POINT ( 'NONE',  ( 7.165897526731081157, -6.376774720514420736, 20.76279523443833597 ) ) ;
#12395=CARTESIAN_POINT ( 'NONE',  ( -24.90875734969025501, 6.475225279485573360, 26.43402280011862615 ) ) ;
#12397=CARTESIAN_POINT ( 'NONE',  ( 30.53060340732036337, 1.477225279485574028, 3.744237563515920634E-15 ) ) ;
#12416=EDGE_CURVE ( 'NONE', #61919, #35496, #73234, .T. ) ;
#12417=DIRECTION ( 'NONE',  ( -0.3133898629642186684, 0.000000000000000000, 0.9496245541219267006 ) ) ;
#12443=EDGE_CURVE ( 'NONE', #2424, #70415, #66140, .T. ) ;
#12444=FACE_OUTER_BOUND ( 'NONE', #82303, .T. ) ;
#12447=DIRECTION ( 'NONE',  ( 0.9978940991575084851, 0.000000000000000000, 0.06486421869277853025 ) ) ;
#12451=AXIS2_PLACEMENT_3D ( 'NONE', #79678, #41638, #40125 ) ;
#12453=EDGE_CURVE ( 'NONE', #40720, #17533, #8910, .T. ) ;
#12458=CARTESIAN_POINT ( 'NONE',  ( -10.75273025779354263, -5.876774720514426953, 16.96478738960562893 ) ) ;
#12463=CARTESIAN_POINT ( 'NONE',  ( -2.220741593810419801, -6.376774720514411854, 19.46247113826587238 ) ) ;
#12468=CARTESIAN_POINT ( 'NONE',  ( -65.05438548721849656, -5.356774720514425603, 24.50402280011859091 ) ) ;
#12471=EDGE_CURVE ( 'NONE', #75788, #90630, #64142, .T. ) ;
#12486=ORIENTED_EDGE ( 'NONE', *, *, #80614, .T. ) ;
#12487=VECTOR ( 'NONE', #61562, 1000.000000000000000 ) ;
#12490=VECTOR ( 'NONE', #48607, 1000.000000000000000 ) ;
#12497=DIRECTION ( 'NONE',  ( -0.000000000000000000, -1.000000000000000000, -0.000000000000000000 ) ) ;
#12511=EDGE_LOOP ( 'NONE', ( #54848, #55714, #77034, #100314 ) ) ;
#12515=CARTESIAN_POINT ( 'NONE',  ( -19.77875734969026311, 6.143225279485574397, 29.49402280011862487 ) ) ;
#12529=VERTEX_POINT ( 'NONE', #20413 ) ;
#12537=PLANE ( 'NONE',  #1178 ) ;
#12545=EDGE_CURVE ( 'NONE', #35590, #8339, #7300, .T. ) ;
#12548=CYLINDRICAL_SURFACE ( 'NONE', #58414, 1.399999999999998579 ) ;
#12559=CARTESIAN_POINT ( 'NONE',  ( 7.166666666666668739, -6.376774720514414518, 20.78665865384614975 ) ) ;
#12568=DIRECTION ( 'NONE',  ( 0.7512896232465892110, 0.000000000000000000, 0.6599726524652350657 ) ) ;
#12570=VERTEX_POINT ( 'NONE', #52387 ) ;
#12585=EDGE_CURVE ( 'NONE', #95752, #75373, #17020, .T. ) ;
#12590=LINE ( 'NONE', #34935, #90138 ) ;
#12603=VERTEX_POINT ( 'NONE', #32544 ) ;
#12604=VERTEX_POINT ( 'NONE', #24924 ) ;
#12606=VERTEX_POINT ( 'NONE', #61999 ) ;
#12619=VERTEX_POINT ( 'NONE', #100025 ) ;
#12639=VERTEX_POINT ( 'NONE', #69096 ) ;
#12644=EDGE_CURVE ( 'NONE', #51886, #84743, #94438, .T. ) ;
#12652=CARTESIAN_POINT ( 'NONE',  ( 14.76093561896378326, -3.316774720514426456, -26.55548769130088260 ) ) ;
#12658=DIRECTION ( 'NONE',  ( -0.000000000000000000, -1.000000000000000000, -0.000000000000000000 ) ) ;
#12671=DIRECTION ( 'NONE',  ( 1.000000000000000000, 0.000000000000000000, -1.611864046919725738E-15 ) ) ;
#12676=EDGE_LOOP ( 'NONE', ( #44347, #22570, #72070, #35851 ) ) ;
#12681=DIRECTION ( 'NONE',  ( 0.000000000000000000, 0.000000000000000000, 1.000000000000000000 ) ) ;
#12693=CARTESIAN_POINT ( 'NONE',  ( -11.64875734969026233, -0.3587747205144265483, 31.02402280011862246 ) ) ;
#12702=DIRECTION ( 'NONE',  ( 0.000000000000000000, -1.000000000000000000, 0.000000000000000000 ) ) ;
#12707=EDGE_CURVE ( 'NONE', #32707, #55189, #32042, .T. ) ;
#12714=VERTEX_POINT ( 'NONE', #31034 ) ;
#12720=ORIENTED_EDGE ( 'NONE', *, *, #46353, .F. ) ;
#12731=CARTESIAN_POINT ( 'NONE',  ( -4.993225604111835914, 5.965225279485592225, -29.11654937215278593 ) ) ;
#12733=CARTESIAN_POINT ( 'NONE',  ( 22.81105451610979173, 6.475225279485573360, -18.46691820600746681 ) ) ;
#12739=CARTESIAN_POINT ( 'NONE',  ( 30.09341516180546350, -2.682774720514426559, -11.39311774897855933 ) ) ;
#12742=CARTESIAN_POINT ( 'NONE',  ( 32.85081302853804885, -3.622774720514426949, -13.10817780685210643 ) ) ;
#12746=CARTESIAN_POINT ( 'NONE',  ( 27.86270917940689174, -0.3587747205144265483, 29.02104833056109001 ) ) ;
#12747=ORIENTED_EDGE ( 'NONE', *, *, #91106, .T. ) ;
#12755=DIRECTION ( 'NONE',  ( -0.9978940991575084851, -0.000000000000000000, -0.06486421869277853025 ) ) ;
#12760=CARTESIAN_POINT ( 'NONE',  ( 7.403636664866980688, -6.376774720514424288, 21.18544102487025782 ) ) ;
#12761=DIRECTION ( 'NONE',  ( -1.000000000000000000, 0.000000000000000000, 0.000000000000000000 ) ) ;
#12766=DIRECTION ( 'NONE',  ( 1.000000000000000000, 0.000000000000000000, 0.000000000000000000 ) ) ;
#12772=CARTESIAN_POINT ( 'NONE',  ( 14.61581670307174008, 6.475225279485573360, -27.35847990810646024 ) ) ;
#12782=ORIENTED_EDGE ( 'NONE', *, *, #60097, .T. ) ;
#12787=ORIENTED_EDGE ( 'NONE', *, *, #94896, .T. ) ;
#12789=CARTESIAN_POINT ( 'NONE',  ( -7.999999999999996447, -5.876774720514426953, 0.000000000000000000 ) ) ;
#12797=ORIENTED_EDGE ( 'NONE', *, *, #32537, .T. ) ;
#12803=AXIS2_PLACEMENT_3D ( 'NONE', #34936, #75472, #4983 ) ;
#12804=AXIS2_PLACEMENT_3D ( 'NONE', #34199, #97580, #66667 ) ;
#12805=CARTESIAN_POINT ( 'NONE',  ( 9.478389368232452483, -4.132774720514426292, -23.17485683983816003 ) ) ;
#12808=CARTESIAN_POINT ( 'NONE',  ( 26.25551457520358056, -4.772774720514425972, -10.59759736550660492 ) ) ;
#12813=CARTESIAN_POINT ( 'NONE',  ( 11.59154397149680626, -4.779967012825416361, -27.71550087055790712 ) ) ;
#12816=CARTESIAN_POINT ( 'NONE',  ( -28.98875734969026396, 5.965225279485572685, 0.1180228001186258285 ) ) ;
#12835=DIRECTION ( 'NONE',  ( -0.000000000000000000, 1.000000000000000000, -0.000000000000000000 ) ) ;
#12842=CARTESIAN_POINT ( 'NONE',  ( -27.96875734969026084, 6.475225279485573360, 0.7300228001186309656 ) ) ;
#12846=ORIENTED_EDGE ( 'NONE', *, *, #79169, .F. ) ;
#12847=CARTESIAN_POINT ( 'NONE',  ( 6.403846153846157740, -6.376774720514426065, 21.48076923076922995 ) ) ;
#12860=CARTESIAN_POINT ( 'NONE',  ( -4.312370003044874167, -6.376774720514408301, 19.42522865122897358 ) ) ;
#12864=ORIENTED_EDGE ( 'NONE', *, *, #69130, .F. ) ;
#12868=EDGE_LOOP ( 'NONE', ( #37875, #4852, #68043, #96780, #83024, #88678 ) ) ;
#12870=ORIENTED_EDGE ( 'NONE', *, *, #54648, .T. ) ;
#12871=ORIENTED_EDGE ( 'NONE', *, *, #30311, .F. ) ;
#12876=CARTESIAN_POINT ( 'NONE',  ( 6.666194146093591399, -5.876774720514413630, 19.75460921626947908 ) ) ;
#12885=ORIENTED_EDGE ( 'NONE', *, *, #75635, .F. ) ;
#12891=AXIS2_PLACEMENT_3D ( 'NONE', #68024, #61414, #60914 ) ;
#12894=AXIS2_PLACEMENT_3D ( 'NONE', #41685, #72630, #79719 ) ;
#12896=LINE ( 'NONE', #14392, #59501 ) ;
#12901=LINE ( 'NONE', #27146, #55045 ) ;
#12908=EDGE_CURVE ( 'NONE', #12604, #100201, #73122, .T. ) ;
#12910=CARTESIAN_POINT ( 'NONE',  ( 3.559170184186323915, -5.876774720514402972, 18.55412939673608719 ) ) ;
#12925=DIRECTION ( 'NONE',  ( -0.03244919754393515293, 0.000000000000000000, 0.9994733861282923959 ) ) ;
#12930=CARTESIAN_POINT ( 'NONE',  ( -4.141166922167975883, -5.876774720514419847, 20.63520656483649063 ) ) ;
#12940=CARTESIAN_POINT ( 'NONE',  ( 2.920210193027767076, -6.376774720514413630, 19.64065332113010243 ) ) ;
#12944=CARTESIAN_POINT ( 'NONE',  ( -32.30247028140506416, 6.475225279485573360, 27.60502002861223048 ) ) ;
#12952=DIRECTION ( 'NONE',  ( 0.000000000000000000, 0.000000000000000000, 1.000000000000000000 ) ) ;
#12953=VECTOR ( 'NONE', #97997, 1000.000000000000000 ) ;
#12955=EDGE_LOOP ( 'NONE', ( #95492, #32331, #54564, #48732 ) ) ;
#12956=CARTESIAN_POINT ( 'NONE',  ( 0.3906119451836247425, -5.876774720514418071, 20.56083401959467594 ) ) ;
#12959=VECTOR ( 'NONE', #59820, 1000.000000000000000 ) ;
#12968=EDGE_CURVE ( 'NONE', #64651, #27420, #3118, .T. ) ;
#12979=ORIENTED_EDGE ( 'NONE', *, *, #1246, .F. ) ;
#12985=CARTESIAN_POINT ( 'NONE',  ( -3.108974358974359475, -6.376774720514417183, 20.36458333333334281 ) ) ;
#12998=ORIENTED_EDGE ( 'NONE', *, *, #67328, .F. ) ;
#13002=ORIENTED_EDGE ( 'NONE', *, *, #80426, .F. ) ;
#13004=CARTESIAN_POINT ( 'NONE',  ( 13.59451591917074431, -3.316774720514426456, -28.23515841827053308 ) ) ;
#13009=EDGE_LOOP ( 'NONE', ( #84987, #68748, #5786, #66804 ) ) ;
#13014=EDGE_LOOP ( 'NONE', ( #77011, #20334, #67532, #76893 ) ) ;
#13030=ADVANCED_FACE ( 'NONE', ( #50782 ), #90328, .F. ) ;
#13036=VECTOR ( 'NONE', #34819, 1000.000000000000000 ) ;
#13038=CARTESIAN_POINT ( 'NONE',  ( -2.772696838893043747, -6.376774720514413630, 19.95463486386180207 ) ) ;
#13040=FACE_BOUND ( 'NONE', #35195, .T. ) ;
#13042=CIRCLE ( 'NONE', #43845, 2.999999999999999112 ) ;
#13059=VERTEX_POINT ( 'NONE', #43664 ) ;
#13065=CARTESIAN_POINT ( 'NONE',  ( 32.16024265030974050, -0.3587747205144265483, 14.03360796525321774 ) ) ;
#13066=VERTEX_POINT ( 'NONE', #14189 ) ;
#13071=EDGE_LOOP ( 'NONE', ( #1814, #63595, #14502, #50813 ) ) ;
#13072=B_SPLINE_CURVE_WITH_KNOTS ( 'NONE', 3,
 ( #68605, #90440, #21408, #75208, #20915, #59009, #13800, #14301, #36161, #12304, #45273, #36653, #20409, #89448, #51891, #28534, #67126, #76200, #6696 ),
 .UNSPECIFIED., .F., .F.,
 ( 4, 1, 1, 1, 1, 1, 1, 1, 1, 1, 1, 1, 1, 1, 1, 1, 4 ),
 ( 0.000000000000000000, 0.07834298519370234970, 0.1505633028794191031, 0.2161510566599780803, 0.2756797924514261533, 0.3287070503654628273, 0.3759044348322084228, 0.4173018977400322349, 0.4526927480535833936, 0.5172652917530119465, 0.5812165680623057051, 0.6453218939728029291, 0.7120244933797633680, 0.7801300447160454121, 0.8502182262116654288, 0.9226485217347378809, 1.000000000000000000 ),
 .UNSPECIFIED. ) ;
#13073=CARTESIAN_POINT ( 'NONE',  ( 5.930937628982182908, -6.376774720514417183, 20.24478033514397524 ) ) ;
#13091=EDGE_LOOP ( 'NONE', ( #94727, #84265, #51449, #30219, #93372, #40861, #91680, #90239, #54809, #85097, #54465, #48578, #19084, #93480, #19536, #63967, #54546, #96981, #64584, #94228, #16151, #77305, #65964, #23335 ) ) ;
#13094=ORIENTED_EDGE ( 'NONE', *, *, #4458, .T. ) ;
#13116=CARTESIAN_POINT ( 'NONE',  ( -2.794871794871791604, -5.876774720514426953, 21.75000000000001066 ) ) ;
#13126=CARTESIAN_POINT ( 'NONE',  ( 5.993553214355093139, -6.376774720514417183, 20.20316077874593930 ) ) ;
#13148=CARTESIAN_POINT ( 'NONE',  ( -2.492070857093962921, -6.376774720514408301, 19.17707164986947177 ) ) ;
#13162=VERTEX_POINT ( 'NONE', #46663 ) ;
#13163=CARTESIAN_POINT ( 'NONE',  ( 4.215004826710222474, -5.876774720514426953, 21.34072927444733381 ) ) ;
#13182=CYLINDRICAL_SURFACE ( 'NONE', #55472, 10.20000000000000107 ) ;
#13202=CARTESIAN_POINT ( 'NONE',  ( 4.712727796232550226, -6.376774720514426953, -25.55789472434992859 ) ) ;
#13207=ORIENTED_EDGE ( 'NONE', *, *, #18607, .T. ) ;
#13215=ADVANCED_FACE ( 'NONE', ( #53778 ), #89639, .T. ) ;
#13224=ORIENTED_EDGE ( 'NONE', *, *, #74532, .F. ) ;
#13226=CARTESIAN_POINT ( 'NONE',  ( 12.16765770914787304, 5.965225279485572685, -27.57618308014988173 ) ) ;
#13228=CARTESIAN_POINT ( 'NONE',  ( 3.632573734185411851, -5.876774720514429617, 21.82795992345630509 ) ) ;
#13256=FACE_OUTER_BOUND ( 'NONE', #52916, .T. ) ;
#13293=CARTESIAN_POINT ( 'NONE',  ( -5.576923076923074873, -6.376774720514427841, 21.75000000000000711 ) ) ;
#13294=CARTESIAN_POINT ( 'NONE',  ( 30.60443771307607008, -4.296120514312956828, 26.89827953497908908 ) ) ;
#13296=ORIENTED_EDGE ( 'NONE', *, *, #5333, .T. ) ;
#13303=DIRECTION ( 'NONE',  ( -0.000000000000000000, -1.000000000000000000, -0.000000000000000000 ) ) ;
#13309=CARTESIAN_POINT ( 'NONE',  ( 7.553089130262996775, -6.316227684668181297, -25.84264253713260828 ) ) ;
#13317=CARTESIAN_POINT ( 'NONE',  ( -1.955883090540335045, -6.376774720514411854, 19.49432735726521315 ) ) ;
#13319=CARTESIAN_POINT ( 'NONE',  ( -2.492070857093962921, -5.876774720514409189, 19.17707164986947177 ) ) ;
#13325=DIRECTION ( 'NONE',  ( 0.000000000000000000, -0.7071067811865513475, -0.7071067811865436870 ) ) ;
#13328=EDGE_CURVE ( 'NONE', #66516, #56847, #95328, .T. ) ;
#13338=EDGE_CURVE ( 'NONE', #50071, #38539, #10585, .T. ) ;
#13350=CYLINDRICAL_SURFACE ( 'NONE', #89168, 2.500000000000000444 ) ;
#13352=DIRECTION ( 'NONE',  ( 1.000000000000000000, 0.000000000000000000, 0.000000000000000000 ) ) ;
#13365=CARTESIAN_POINT ( 'NONE',  ( 30.09341516180546350, -2.682774720514426559, -11.39311774897855933 ) ) ;
#13389=VERTEX_POINT ( 'NONE', #94822 ) ;
#13390=EDGE_CURVE ( 'NONE', #66516, #6989, #4853, .T. ) ;
#13391=VECTOR ( 'NONE', #18795, 1000.000000000000000 ) ;
#13394=CARTESIAN_POINT ( 'NONE',  ( -10.24059822343757808, -5.876774720514426953, 17.91871304725684766 ) ) ;
#13395=DIRECTION ( 'NONE',  ( 0.000000000000000000, -1.000000000000000000, 0.000000000000000000 ) ) ;
#13402=ORIENTED_EDGE ( 'NONE', *, *, #32383, .T. ) ;
#13407=ORIENTED_EDGE ( 'NONE', *, *, #11723, .F. ) ;
#13408=CARTESIAN_POINT ( 'NONE',  ( 2.949406532984364393, -5.876774720514410077, 19.42899254576129664 ) ) ;
#13418=LINE ( 'NONE', #83937, #70783 ) ;
#13419=DIRECTION ( 'NONE',  ( 0.000000000000000000, -1.155373159085149695E-17, 1.000000000000000000 ) ) ;
#13428=CYLINDRICAL_SURFACE ( 'NONE', #52763, 0.2999999999999981570 ) ;
#13430=PRODUCT_DEFINITION_SHAPE ( 'NONE', 'NONE',  #94066 ) ;
#13431=LINE ( 'NONE', #35789, #37638 ) ;
#13441=CARTESIAN_POINT ( 'NONE',  ( -0.9540731552372990754, -6.376774720514411854, 19.74568812963596542 ) ) ;
#13442=CARTESIAN_POINT ( 'NONE',  ( -28.98875734969026041, 5.965225279485572685, 17.86602280011862476 ) ) ;
#13448=VERTEX_POINT ( 'NONE', #37796 ) ;
#13449=CARTESIAN_POINT ( 'NONE',  ( -0.2200237740140755516, -5.876774720514409189, 19.17724329193115551 ) ) ;
#13457=LINE ( 'NONE', #65295, #40425 ) ;
#13469=EDGE_CURVE ( 'NONE', #80664, #44878, #83460, .T. ) ;
#13472=VECTOR ( 'NONE', #23897, 1000.000000000000000 ) ;
#13474=CARTESIAN_POINT ( 'NONE',  ( 4.948119756536996761, -6.376774720514410077, 19.52858994054604125 ) ) ;
#13486=ORIENTED_EDGE ( 'NONE', *, *, #57280, .T. ) ;
#13487=DIRECTION ( 'NONE',  ( -0.000000000000000000, 1.000000000000000000, -0.000000000000000000 ) ) ;
#13493=DIRECTION ( 'NONE',  ( -0.000000000000000000, 1.000000000000000000, -0.000000000000000000 ) ) ;
#13499=CARTESIAN_POINT ( 'NONE',  ( 30.49880699021233710, -4.793320133135864580, 19.84760796525321425 ) ) ;
#13509=AXIS2_PLACEMENT_3D ( 'NONE', #10403, #55224, #26638 ) ;
#13513=EDGE_CURVE ( 'NONE', #47314, #10925, #61648, .T. ) ;
#13514=VECTOR ( 'NONE', #80851, 1000.000000000000000 ) ;
#13530=AXIS2_PLACEMENT_3D ( 'NONE', #48361, #64104, #16388 ) ;
#13533=CARTESIAN_POINT ( 'NONE',  ( -2.786875287040666560, -6.376774720514417183, 20.09505574050193388 ) ) ;
#13550=DIRECTION ( 'NONE',  ( 0.000000000000000000, -1.000000000000000000, 0.000000000000000000 ) ) ;
#13552=EDGE_CURVE ( 'NONE', #99423, #21858, #10613, .T. ) ;
#13560=LINE ( 'NONE', #67871, #33769 ) ;
#13561=CARTESIAN_POINT ( 'NONE',  ( 3.769931535195356620, -6.376774720514429617, 21.83933825178638699 ) ) ;
#13563=DIRECTION ( 'NONE',  ( 0.000000000000000000, 0.000000000000000000, -1.000000000000000000 ) ) ;
#13565=ORIENTED_EDGE ( 'NONE', *, *, #64222, .T. ) ;
#13576=CARTESIAN_POINT ( 'NONE',  ( 3.787259615384621636, -5.876774720514405637, 18.51923076923076650 ) ) ;
#13591=EDGE_LOOP ( 'NONE', ( #22412, #14413, #99665, #47668 ) ) ;
#13603=DIRECTION ( 'NONE',  ( 1.000000000000000000, 0.000000000000000000, 0.000000000000000000 ) ) ;
#13611=ORIENTED_EDGE ( 'NONE', *, *, #12321, .T. ) ;
#13613=ORIENTED_EDGE ( 'NONE', *, *, #40388, .F. ) ;
#13616=CARTESIAN_POINT ( 'NONE',  ( 3.879812756903532556, -5.876774720514399419, 18.16163344421570969 ) ) ;
#13623=CARTESIAN_POINT ( 'NONE',  ( 6.273728352332436309, -6.376774720514415407, 20.10092598260902008 ) ) ;
#13628=ORIENTED_EDGE ( 'NONE', *, *, #37915, .T. ) ;
#13631=AXIS2_PLACEMENT_3D ( 'NONE', #83316, #97550, #75698 ) ;
#13652=CARTESIAN_POINT ( 'NONE',  ( 14.82775695341588573, -5.152774720514427642, -26.90408793620859385 ) ) ;
#13660=CARTESIAN_POINT ( 'NONE',  ( 8.978253834636468866, -6.376774720514426953, 0.000000000000000000 ) ) ;
#13673=EDGE_CURVE ( 'NONE', #77609, #54376, #10847, .T. ) ;
#13680=VECTOR ( 'NONE', #57759, 1000.000000000000000 ) ;
#13687=CARTESIAN_POINT ( 'NONE',  ( 14.10331789288738236, -5.152774720514426754, -26.41276880515819769 ) ) ;
#13688=DIRECTION ( 'NONE',  ( 0.000000000000000000, 0.000000000000000000, 1.000000000000000000 ) ) ;
#13689=CARTESIAN_POINT ( 'NONE',  ( -41.32836283488544638, -4.132774720514426292, 39.26872235229541985 ) ) ;
#13711=EDGE_CURVE ( 'NONE', #15369, #3440, #29828, .T. ) ;
#13714=ORIENTED_EDGE ( 'NONE', *, *, #41768, .F. ) ;
#13718=EDGE_CURVE ( 'NONE', #67104, #57214, #41294, .T. ) ;
#13725=VERTEX_POINT ( 'NONE', #42319 ) ;
#13727=CARTESIAN_POINT ( 'NONE',  ( 7.462166178408539352, 5.965225279485572685, -27.67315496249664974 ) ) ;
#13742=CARTESIAN_POINT ( 'NONE',  ( -4.568292318365942073, 5.965225279485572685, 30.06720597538392425 ) ) ;
#13744=AXIS2_PLACEMENT_3D ( 'NONE', #6821, #45898, #52013 ) ;
#13745=VERTEX_POINT ( 'NONE', #88473 ) ;
#13756=CARTESIAN_POINT ( 'NONE',  ( 7.526024287269984292, 1.477225279485574028, 9.032262774691707463 ) ) ;
#13758=DIRECTION ( 'NONE',  ( -0.5630016722799275897, 4.164321980682959710E-15, 0.8264557562326038109 ) ) ;
#13759=ORIENTED_EDGE ( 'NONE', *, *, #17258, .F. ) ;
#13760=CARTESIAN_POINT ( 'NONE',  ( 29.64418490232317893, -5.621712738193696879, 28.18100406333994457 ) ) ;
#13781=VECTOR ( 'NONE', #86515, 1000.000000000000000 ) ;
#13782=ADVANCED_FACE ( 'NONE', ( #57036 ), #73250, .F. ) ;
#13790=ORIENTED_EDGE ( 'NONE', *, *, #41900, .T. ) ;
#13797=CARTESIAN_POINT ( 'NONE',  ( -1.363607173041644582, -6.376774720514420736, 20.50445910983877340 ) ) ;
#13800=CARTESIAN_POINT ( 'NONE',  ( -7.304748120944324796, -6.376774720514417183, 19.95463486386180563 ) ) ;
#13807=ORIENTED_EDGE ( 'NONE', *, *, #45836, .T. ) ;
#13813=DIRECTION ( 'NONE',  ( -0.4009304992412300317, 6.845827386180410961E-16, -0.9161084732596779245 ) ) ;
#13830=LINE ( 'NONE', #31053, #19329 ) ;
#13834=CARTESIAN_POINT ( 'NONE',  ( 30.54125281784916268, -0.6647747205144264315, 23.11160796525322070 ) ) ;
#13841=VECTOR ( 'NONE', #67163, 1000.000000000000000 ) ;
#13844=CARTESIAN_POINT ( 'NONE',  ( 33.00535138976610483, 5.965225279485572685, -12.97242311383961422 ) ) ;
#13845=ORIENTED_EDGE ( 'NONE', *, *, #49854, .F. ) ;
#13851=CARTESIAN_POINT ( 'NONE',  ( -4.568292318365942073, 5.965225279485572685, 30.06720597538392425 ) ) ;
#13856=VECTOR ( 'NONE', #48242, 1000.000000000000000 ) ;
#13865=EDGE_LOOP ( 'NONE', ( #21488, #38228, #48342 ) ) ;
#13877=CARTESIAN_POINT ( 'NONE',  ( 30.64697572893791744, -5.232796261063619170, 0.6042509527384705148 ) ) ;
#13880=CARTESIAN_POINT ( 'NONE',  ( -28.47875734969025885, 6.475225279485573360, -0.08597719988137117464 ) ) ;
#13894=CARTESIAN_POINT ( 'NONE',  ( 30.59299694858157892, -5.371884064401012182, 26.41087035901067637 ) ) ;
#13901=EDGE_CURVE ( 'NONE', #83680, #38147, #21426, .T. ) ;
#13905=CARTESIAN_POINT ( 'NONE',  ( 3.362850247043494001, -6.376774720514404748, 18.65880685207958223 ) ) ;
#13906=ADVANCED_FACE ( 'NONE', ( #52401 ), #7206, .F. ) ;
#13909=EDGE_CURVE ( 'NONE', #71272, #9388, #6215, .T. ) ;
#13916=LINE ( 'NONE', #83428, #22031 ) ;
#13922=CIRCLE ( 'NONE', #91706, 130.2784398600581710 ) ;
#13928=LINE ( 'NONE', #6325, #8010 ) ;
#13929=VECTOR ( 'NONE', #85650, 1000.000000000000000 ) ;
#13930=VECTOR ( 'NONE', #91049, 1000.000000000000114 ) ;
#13932=CARTESIAN_POINT ( 'NONE',  ( 0.000000000000000000, -7.835183881457442823, 0.000000000000000000 ) ) ;
#13938=AXIS2_PLACEMENT_3D ( 'NONE', #63405, #88228, #80600 ) ;
#13957=CARTESIAN_POINT ( 'NONE',  ( -0.3982818654701407723, -6.376774720514410077, 19.46306892155547530 ) ) ;
#13962=DIRECTION ( 'NONE',  ( 0.000000000000000000, -1.000000000000000000, 0.000000000000000000 ) ) ;
#13968=DIRECTION ( 'NONE',  ( 0.000000000000000000, -1.000000000000000000, 0.000000000000000000 ) ) ;
#13979=CARTESIAN_POINT ( 'NONE',  ( 13.91401389203221406, -3.316774720514426456, 158.0376437107427137 ) ) ;
#13982=ORIENTED_EDGE ( 'NONE', *, *, #44106, .T. ) ;
#13983=CARTESIAN_POINT ( 'NONE',  ( -0.8502773128684013582, -5.876774720514413630, 19.61227901093089798 ) ) ;
#13985=CARTESIAN_POINT ( 'NONE',  ( -4.177535645411178500, -6.376774720514415407, 20.17598923696320767 ) ) ;
#13999=CARTESIAN_POINT ( 'NONE',  ( 30.32108885906865936, -6.376774720514426953, 3.274824222184972822 ) ) ;
#14005=LINE ( 'NONE', #46465, #74059 ) ;
#14018=FACE_OUTER_BOUND ( 'NONE', #97366, .T. ) ;
#14024=DIRECTION ( 'NONE',  ( -2.000709955812756421E-15, 6.669033186042521139E-15, -1.000000000000000000 ) ) ;
#14032=CARTESIAN_POINT ( 'NONE',  ( -2.188401442307694289, -6.376774720514411854, 19.46153846153846700 ) ) ;
#14033=EDGE_CURVE ( 'NONE', #33348, #52199, #6820, .T. ) ;
#14035=LINE ( 'NONE', #60739, #99444 ) ;
#14043=PLANE ( 'NONE',  #57007 ) ;
#14047=CARTESIAN_POINT ( 'NONE',  ( 10.46399479596398052, -3.316774720514422903, -27.03001098546561209 ) ) ;
#14064=CARTESIAN_POINT ( 'NONE',  ( -2.768609665556983845, 5.965225279485594001, -29.41086200512614823 ) ) ;
#14085=LINE ( 'NONE', #37934, #22739 ) ;
#14095=ORIENTED_EDGE ( 'NONE', *, *, #23529, .T. ) ;
#14101=VECTOR ( 'NONE', #25983, 1000.000000000000000 ) ;
#14108=CARTESIAN_POINT ( 'NONE',  ( -20.77875734969026311, 6.143225279485574397, 27.31649921512899937 ) ) ;
#14111=VECTOR ( 'NONE', #42402, 1000.000000000000000 ) ;
#14114=FACE_OUTER_BOUND ( 'NONE', #89512, .T. ) ;
#14118=CARTESIAN_POINT ( 'NONE',  ( 4.403244164709623654, -6.376774720514404748, 18.35516266052912826 ) ) ;
#14119=VERTEX_POINT ( 'NONE', #69628 ) ;
#14124=EDGE_CURVE ( 'NONE', #63088, #45647, #24437, .T. ) ;
#14126=CARTESIAN_POINT ( 'NONE',  ( -23.29179552176161749, 5.965225279485594001, -17.29637630388738501 ) ) ;
#14128=CARTESIAN_POINT ( 'NONE',  ( 6.326958800731953048, -6.376774720514426065, 21.47849181751607972 ) ) ;
#14132=CARTESIAN_POINT ( 'NONE',  ( 0.000000000000000000, -5.356774720496559894, 19.84760796525321425 ) ) ;
#14148=CARTESIAN_POINT ( 'NONE',  ( -2.711489738547795625, -6.376774720514410077, 19.27798293355755632 ) ) ;
#14150=PLANE ( 'NONE',  #27459 ) ;
#14162=FACE_OUTER_BOUND ( 'NONE', #13591, .T. ) ;
#14168=CARTESIAN_POINT ( 'NONE',  ( 3.509873074917118085, -0.3587747205144265483, 29.15869884040363758 ) ) ;
#14174=CARTESIAN_POINT ( 'NONE',  ( 9.402885806365684829, 5.965225279485572685, 29.04108526060719342 ) ) ;
#14187=CARTESIAN_POINT ( 'NONE',  ( 22.02124265030973760, 7.743225279485574042, 16.20402280011862217 ) ) ;
#14189=CARTESIAN_POINT ( 'NONE',  ( 29.73860345376319358, -5.356774720496559894, -0.3523920347288969079 ) ) ;
#14199=CARTESIAN_POINT ( 'NONE',  ( 5.641653616409716854, -5.876774720514420736, 20.81030773351227481 ) ) ;
#14202=EDGE_CURVE ( 'NONE', #86782, #32836, #92942, .T. ) ;
#14211=EDGE_LOOP ( 'NONE', ( #9609, #56190, #35381, #39704 ) ) ;
#14221=EDGE_CURVE ( 'NONE', #70995, #69928, #49518, .T. ) ;
#14225=CARTESIAN_POINT ( 'NONE',  ( 3.181132013147180970, -5.876774720514426065, 21.64201922499777808 ) ) ;
#14234=CARTESIAN_POINT ( 'NONE',  ( 29.73860345376319003, -14.82721238576461609, -4.021180035027960287 ) ) ;
#14239=DIRECTION ( 'NONE',  ( 0.4009304992412300872, 0.000000000000000000, 0.9161084732596779245 ) ) ;
#14241=DIRECTION ( 'NONE',  ( 0.000000000000000000, 0.000000000000000000, 1.000000000000000000 ) ) ;
#14251=CARTESIAN_POINT ( 'NONE',  ( -6.720452724358975338, -5.876774720514411854, 19.46153846153846700 ) ) ;
#14257=CARTESIAN_POINT ( 'NONE',  ( -4.686006777320704586, -6.376774720514426953, 29.60911411231905888 ) ) ;
#14260=ADVANCED_FACE ( 'NONE', ( #74124 ), #73132, .T. ) ;
#14269=CARTESIAN_POINT ( 'NONE',  ( 14.44544951633968566, -3.759487683616679288, -28.33948095063585271 ) ) ;
#14282=VERTEX_POINT ( 'NONE', #72636 ) ;
#14283=ADVANCED_FACE ( 'NONE', ( #33066 ), #94957, .T. ) ;
#14287=CARTESIAN_POINT ( 'NONE',  ( 20.57455539870830208, -4.132774720514426292, -18.22080502500661581 ) ) ;
#14292=VERTEX_POINT ( 'NONE', #88859 ) ;
#14298=DIRECTION ( 'NONE',  ( 0.9952638024365005887, 0.000000000000000000, 0.09721092304694053943 ) ) ;
#14301=CARTESIAN_POINT ( 'NONE',  ( -7.294102189209645815, -6.376774720514413630, 19.89644244529368677 ) ) ;
#14308=ORIENTED_EDGE ( 'NONE', *, *, #27441, .T. ) ;
#14309=CARTESIAN_POINT ( 'NONE',  ( 6.184520403203634942, -6.376774720514426953, -25.32021290018218451 ) ) ;
#14315=CARTESIAN_POINT ( 'NONE',  ( -1.363607173041644582, -6.376774720514420736, 20.50445910983877340 ) ) ;
#14317=DIRECTION ( 'NONE',  ( 0.000000000000000000, 0.000000000000000000, -1.000000000000000000 ) ) ;
#14347=CARTESIAN_POINT ( 'NONE',  ( -5.576923076923074873, -5.876774720514426953, 21.75000000000000711 ) ) ;
#14356=EDGE_CURVE ( 'NONE', #30864, #45617, #6102, .T. ) ;
#14368=ORIENTED_EDGE ( 'NONE', *, *, #61154, .T. ) ;
#14377=CARTESIAN_POINT ( 'NONE',  ( 7.433267315672343223, -5.876774720514418071, 20.43888261666079842 ) ) ;
#14379=CARTESIAN_POINT ( 'NONE',  ( -0.6735982426299428338, -6.376774720514410077, 19.16400979764068069 ) ) ;
#14385=CARTESIAN_POINT ( 'NONE',  ( 32.51008598047019404, -5.548342165039966467, -1.163674249303449315 ) ) ;
#14388=EDGE_CURVE ( 'NONE', #6499, #97248, #90342, .T. ) ;
#14392=CARTESIAN_POINT ( 'NONE',  ( 2.589743589743596086, -6.376774720514415407, 20.00140224358974095 ) ) ;
#14399=EDGE_LOOP ( 'NONE', ( #50333, #23095, #25819, #50785 ) ) ;
#14401=DIRECTION ( 'NONE',  ( -0.000000000000000000, -1.000000000000000000, -0.000000000000000000 ) ) ;
#14405=CARTESIAN_POINT ( 'NONE',  ( 3.121233215686890272, -5.876774720514404748, 18.93204046835445808 ) ) ;
#14406=CARTESIAN_POINT ( 'NONE',  ( 3.769940963823357638, -6.376774720514402972, 18.16074422543206879 ) ) ;
#14413=ORIENTED_EDGE ( 'NONE', *, *, #429, .F. ) ;
#14415=AXIS2_PLACEMENT_3D ( 'NONE', #86961, #33176, #65163 ) ;
#14422=CARTESIAN_POINT ( 'NONE',  ( 22.81105451610979173, -2.682774720540237468, -18.46691820600746681 ) ) ;
#14423=DIRECTION ( 'NONE',  ( 2.313651251573820309E-16, 1.000000000000000000, 8.068660792749117443E-16 ) ) ;
#14427=AXIS2_PLACEMENT_3D ( 'NONE', #65167, #88980, #2247 ) ;
#14444=EDGE_LOOP ( 'NONE', ( #22312, #27575, #76560, #74144 ) ) ;
#14458=DIRECTION ( 'NONE',  ( 1.000000000000000000, 0.000000000000000000, 0.000000000000000000 ) ) ;
#14466=CARTESIAN_POINT ( 'NONE',  ( 4.856316114246853388, -6.376774720514408301, 19.03119074624055074 ) ) ;
#14472=CIRCLE ( 'NONE', #12804, 3.570000000000003837 ) ;
#14473=B_SPLINE_CURVE_WITH_KNOTS ( 'NONE', 3,
 ( #9906, #55096, #72825, #78407, #48488, #94643, #2311, #33242, #24619, #88044, #56607, #18518, #9403, #40364, #40857, #64734, #49491, #24126, #63213 ),
 .UNSPECIFIED., .F., .F.,
 ( 4, 1, 1, 1, 1, 1, 1, 1, 1, 1, 1, 1, 1, 1, 1, 1, 4 ),
 ( 0.000000000000000000, 0.06815824415599770758, 0.1347066022023564180, 0.2018649976035981897, 0.2707882662774624971, 0.3400242943604918633, 0.4080827390537212218, 0.4768131952581446398, 0.5473460643070942044, 0.5856397954238958814, 0.6288649531777639190, 0.6771532033637904791, 0.7308028113651051649, 0.7898066155325015325, 0.8543250087420142247, 0.9243651340575425035, 1.000000000000000000 ),
 .UNSPECIFIED. ) ;
#14478=CARTESIAN_POINT ( 'NONE',  ( -9.278253834636469577, -6.376774720514426953, 18.51871304725684553 ) ) ;
#14487=CARTESIAN_POINT ( 'NONE',  ( -4.213970605900704491, -6.376774720514415407, 20.02963804100705758 ) ) ;
#14491=VECTOR ( 'NONE', #39668, 1000.000000000000000 ) ;
#14502=ORIENTED_EDGE ( 'NONE', *, *, #46224, .T. ) ;
#14504=DIRECTION ( 'NONE',  ( -0.000000000000000000, 1.000000000000000000, -0.000000000000000000 ) ) ;
#14522=ORIENTED_EDGE ( 'NONE', *, *, #4079, .F. ) ;
#14525=VERTEX_POINT ( 'NONE', #62403 ) ;
#14536=CARTESIAN_POINT ( 'NONE',  ( -2.373828433815573735, -5.876774720514408301, 19.48240003225459915 ) ) ;
#14542=EDGE_CURVE ( 'NONE', #98254, #96767, #15212, .T. ) ;
#14544=CARTESIAN_POINT ( 'NONE',  ( -0.02075734969026423599, 5.965225279485572685, -0.08597719988137648983 ) ) ;
#14548=CIRCLE ( 'NONE', #71273, 2.040000000000000036 ) ;
#14556=DIRECTION ( 'NONE',  ( 0.000000000000000000, 0.000000000000000000, -1.000000000000000000 ) ) ;
#14563=VECTOR ( 'NONE', #6207, 1000.000000000000000 ) ;
#14565=CARTESIAN_POINT ( 'NONE',  ( 3.251543564379332008, -6.376774720514424288, 21.68810402963413964 ) ) ;
#14570=VERTEX_POINT ( 'NONE', #99929 ) ;
#14573=DIRECTION ( 'NONE',  ( -0.000000000000000000, 1.000000000000000000, -0.000000000000000000 ) ) ;
#14575=DIRECTION ( 'NONE',  ( 0.000000000000000000, 0.000000000000000000, 1.000000000000000000 ) ) ;
#14577=ADVANCED_FACE ( 'NONE', ( #15712 ), #63415, .T. ) ;
#14593=B_SPLINE_CURVE_WITH_KNOTS ( 'NONE', 3,
 ( #73291, #42361, #10380, #96127, #19486, #9879 ),
 .UNSPECIFIED., .F., .F.,
 ( 4, 2, 4 ),
 ( -8.871155308958663375E-06, 0.0009003829173646808823, 0.001809636990038320306 ),
 .UNSPECIFIED. ) ;
#14596=ORIENTED_EDGE ( 'NONE', *, *, #43436, .F. ) ;
#14620=CARTESIAN_POINT ( 'NONE',  ( 31.93426202889373400, 5.965225279485572685, 6.907000118922836940 ) ) ;
#14624=CARTESIAN_POINT ( 'NONE',  ( 4.966983519792414370, -6.376774720514415407, 19.83633487160803099 ) ) ;
#14626=DIRECTION ( 'NONE',  ( 0.000000000000000000, 0.000000000000000000, -1.000000000000000000 ) ) ;
#14628=LINE ( 'NONE', #85142, #49600 ) ;
#14640=VECTOR ( 'NONE', #45134, 1000.000000000000114 ) ;
#14647=CARTESIAN_POINT ( 'NONE',  ( 11.69063526134919684, -3.622774720514426949, -29.65990201929480108 ) ) ;
#14649=CARTESIAN_POINT ( 'NONE',  ( -1.122631020312409245, -5.876774720514411854, 19.41635569784906679 ) ) ;
#14672=PLANE ( 'NONE',  #57081 ) ;
#14673=ORIENTED_EDGE ( 'NONE', *, *, #74314, .T. ) ;
#14675=CARTESIAN_POINT ( 'NONE',  ( -5.903826827417286260, -5.876774720514418071, 20.39230070883895252 ) ) ;
#14686=AXIS2_PLACEMENT_3D ( 'NONE', #90633, #60700, #21110 ) ;
#14688=CARTESIAN_POINT ( 'NONE',  ( 33.63447098073278596, -3.363532777116247541, -11.63841935007238426 ) ) ;
#14720=ORIENTED_EDGE ( 'NONE', *, *, #48598, .F. ) ;
#14721=EDGE_CURVE ( 'NONE', #69556, #37181, #28323, .T. ) ;
#14727=ORIENTED_EDGE ( 'NONE', *, *, #34101, .T. ) ;
#14733=CARTESIAN_POINT ( 'NONE',  ( 30.56736729430419430, 3.651218969664528302, 25.10220481361090705 ) ) ;
#14744=CARTESIAN_POINT ( 'NONE',  ( -65.05438548721848235, -5.356774720514425603, 27.45402280011862572 ) ) ;
#14755=FACE_OUTER_BOUND ( 'NONE', #58885, .T. ) ;
#14759=DIRECTION ( 'NONE',  ( -0.7071067811865442421, 0.000000000000000000, -0.7071067811865507924 ) ) ;
#14763=CIRCLE ( 'NONE', #30998, 1.699999999999994849 ) ;
#14774=EDGE_CURVE ( 'NONE', #41750, #77030, #43558, .T. ) ;
#14777=EDGE_LOOP ( 'NONE', ( #79395, #20224, #27756, #37916 ) ) ;
#14778=DIRECTION ( 'NONE',  ( -0.000000000000000000, 1.000000000000000000, -0.000000000000000000 ) ) ;
#14781=DIRECTION ( 'NONE',  ( 0.000000000000000000, 1.000000000000000000, 0.000000000000000000 ) ) ;
#14794=ORIENTED_EDGE ( 'NONE', *, *, #71716, .T. ) ;
#14799=CARTESIAN_POINT ( 'NONE',  ( 5.864177746775673050, -6.376774720514426065, 21.69926562011473337 ) ) ;
#14800=CARTESIAN_POINT ( 'NONE',  ( 10.54059822343757880, -5.876774720514426953, 22.82308057603841078 ) ) ;
#14807=EDGE_CURVE ( 'NONE', #24461, #96004, #39346, .T. ) ;
#14815=CARTESIAN_POINT ( 'NONE',  ( -1.363607173041644582, -5.876774720514419847, 20.50445910983877340 ) ) ;
#14818=EDGE_LOOP ( 'NONE', ( #32329, #80215, #81795, #94245 ) ) ;
#14833=EDGE_CURVE ( 'NONE', #52438, #28254, #21690, .T. ) ;
#14841=CARTESIAN_POINT ( 'NONE',  ( -5.923037968371668072, -6.376774720514413630, 19.62288733224861303 ) ) ;
#14868=AXIS2_PLACEMENT_3D ( 'NONE', #88537, #79913, #1302 ) ;
#14872=DIRECTION ( 'NONE',  ( -0.000000000000000000, 1.000000000000000000, -0.000000000000000000 ) ) ;
#14878=LINE ( 'NONE', #38218, #85443 ) ;
#14883=DIRECTION ( 'NONE',  ( 1.000000000000000000, 0.000000000000000000, 0.000000000000000000 ) ) ;
#14885=ORIENTED_EDGE ( 'NONE', *, *, #3697, .F. ) ;
#14887=ADVANCED_FACE ( 'NONE', ( #15585 ), #96084, .T. ) ;
#14894=B_SPLINE_CURVE_WITH_KNOTS ( 'NONE', 3,
 ( #55083, #8895, #1789, #32728 ),
 .UNSPECIFIED., .F., .F.,
 ( 4, 4 ),
 ( 0.007591229774494646920, 0.009012827652035957510 ),
 .UNSPECIFIED. ) ;
#14898=VERTEX_POINT ( 'NONE', #46550 ) ;
#14900=PLANE ( 'NONE',  #30928 ) ;
#14904=FACE_OUTER_BOUND ( 'NONE', #91911, .T. ) ;
#14905=VECTOR ( 'NONE', #77948, 1000.000000000000000 ) ;
#14910=ORIENTED_EDGE ( 'NONE', *, *, #21399, .T. ) ;
#14918=DIRECTION ( 'NONE',  ( 0.000000000000000000, 0.000000000000000000, -1.000000000000000000 ) ) ;
#14932=ADVANCED_FACE ( 'NONE', ( #24202 ), #78481, .F. ) ;
#14941=CIRCLE ( 'NONE', #99178, 0.8160000000000008358 ) ;
#14953=CARTESIAN_POINT ( 'NONE',  ( 0.2885822020289898759, -5.876774720514415407, 19.94806476610988710 ) ) ;
#14959=AXIS2_PLACEMENT_3D ( 'NONE', #37537, #44653, #75579 ) ;
#14963=AXIS2_PLACEMENT_3D ( 'NONE', #87720, #26318, #26814 ) ;
#14969=CARTESIAN_POINT ( 'NONE',  ( -28.98875734969026396, 5.965225279485572685, -0.08597719988137648983 ) ) ;
#14977=CARTESIAN_POINT ( 'NONE',  ( -4.141025641025641413, -6.376774720514420736, 20.67377804487180271 ) ) ;
#14981=ORIENTED_EDGE ( 'NONE', *, *, #67253, .F. ) ;
#14984=DIRECTION ( 'NONE',  ( 0.7640209514960704107, 0.000000000000000000, -0.6451914333552789538 ) ) ;
#15001=ORIENTED_EDGE ( 'NONE', *, *, #31783, .T. ) ;
#15004=CARTESIAN_POINT ( 'NONE',  ( 5.659515148182856947, -5.356774720517040400, -27.47062408582486270 ) ) ;
#15005=AXIS2_PLACEMENT_3D ( 'NONE', #82770, #67073, #78019 ) ;
#15010=EDGE_LOOP ( 'NONE', ( #78188, #19633, #55982, #29639 ) ) ;
#15011=DIRECTION ( 'NONE',  ( -0.000000000000000000, -1.000000000000000000, -0.000000000000000000 ) ) ;
#15021=DIRECTION ( 'NONE',  ( -1.000000000000000000, 0.000000000000000000, 0.000000000000000000 ) ) ;
#15026=AXIS2_PLACEMENT_3D ( 'NONE', #80879, #58059, #19466 ) ;
#15034=CARTESIAN_POINT ( 'NONE',  ( -5.837039262820512775, -5.876774720514413630, 19.76512419871795245 ) ) ;
#15036=FACE_OUTER_BOUND ( 'NONE', #31704, .T. ) ;
#15037=CARTESIAN_POINT ( 'NONE',  ( 27.53860345374808105, -1.682774720514426114, -8.321925749325325583 ) ) ;
#15038=FACE_BOUND ( 'NONE', #37865, .T. ) ;
#15048=DIRECTION ( 'NONE',  ( -0.000000000000000000, 1.000000000000000000, -0.000000000000000000 ) ) ;
#15057=EDGE_CURVE ( 'NONE', #93291, #94842, #32278, .T. ) ;
#15060=VECTOR ( 'NONE', #13550, 1000.000000000000000 ) ;
#15064=LINE ( 'NONE', #46032, #22428 ) ;
#15065=CARTESIAN_POINT ( 'NONE',  ( 2.832419239133125544, -6.376774720514422512, 21.23415460623727213 ) ) ;
#15076=AXIS2_PLACEMENT_3D ( 'NONE', #12652, #43118, #76039 ) ;
#15077=EDGE_CURVE ( 'NONE', #96155, #47456, #95063, .T. ) ;
#15083=CARTESIAN_POINT ( 'NONE',  ( 4.451706829556401956, -5.876774720514407413, 18.91922570401084513 ) ) ;
#15085=CARTESIAN_POINT ( 'NONE',  ( -5.053929855541893446, -6.376774720514408301, 19.14848118821636547 ) ) ;
#15086=LINE ( 'NONE', #61284, #79226 ) ;
#15092=CARTESIAN_POINT ( 'NONE',  ( -5.115065434581078208, -6.376774720514410077, 19.15054976246387497 ) ) ;
#15122=ORIENTED_EDGE ( 'NONE', *, *, #76000, .T. ) ;
#15124=ORIENTED_EDGE ( 'NONE', *, *, #64696, .F. ) ;
#15125=DIRECTION ( 'NONE',  ( -2.501730345825856179E-15, 6.879758451021104590E-15, -1.000000000000000000 ) ) ;
#15127=VERTEX_POINT ( 'NONE', #41401 ) ;
#15128=CARTESIAN_POINT ( 'NONE',  ( 4.740341618695937065, -5.876774720514402972, 18.75174579344860248 ) ) ;
#15140=CARTESIAN_POINT ( 'NONE',  ( 31.55236408230781819, -6.376774720514426953, 19.84760796525321780 ) ) ;
#15169=EDGE_CURVE ( 'NONE', #22949, #32255, #55955, .T. ) ;
#15175=EDGE_CURVE ( 'NONE', #24103, #16838, #46235, .T. ) ;
#15176=CARTESIAN_POINT ( 'NONE',  ( 10.24059822343757808, -5.876774720514426953, 17.17691942396160698 ) ) ;
#15190=CARTESIAN_POINT ( 'NONE',  ( 33.37790122608239329, -4.268345726061002487, -11.54778842029335806 ) ) ;
#15191=ORIENTED_EDGE ( 'NONE', *, *, #9557, .F. ) ;
#15196=CARTESIAN_POINT ( 'NONE',  ( -0.5315124411682757843, -5.876774720514411854, 19.46509473978807847 ) ) ;
#15199=VECTOR ( 'NONE', #50550, 1000.000000000000000 ) ;
#15203=ADVANCED_FACE ( 'NONE', ( #25667 ), #72856, .F. ) ;
#15206=ORIENTED_EDGE ( 'NONE', *, *, #29838, .T. ) ;
#15212=LINE ( 'NONE', #16712, #64083 ) ;
#15215=ORIENTED_EDGE ( 'NONE', *, *, #96965, .F. ) ;
#15217=AXIS2_PLACEMENT_3D ( 'NONE', #38509, #30895, #61862 ) ;
#15232=EDGE_LOOP ( 'NONE', ( #35832, #16717, #8866, #44029 ) ) ;
#15235=CARTESIAN_POINT ( 'NONE',  ( 2.649863049427662709, -5.876774720514419847, 20.71861240329949538 ) ) ;
#15238=VERTEX_POINT ( 'NONE', #63760 ) ;
#15239=CARTESIAN_POINT ( 'NONE',  ( 30.57287095715020087, 6.475225279485571583, 25.41160796525326404 ) ) ;
#15248=EDGE_LOOP ( 'NONE', ( #9964, #73663, #60686, #30349 ) ) ;
#15267=DIRECTION ( 'NONE',  ( -0.000000000000000000, 1.000000000000000000, -0.000000000000000000 ) ) ;
#15268=CARTESIAN_POINT ( 'NONE',  ( 31.64388307978972747, -6.098167052574009261, 27.71102684943996053 ) ) ;
#15269=DIRECTION ( 'NONE',  ( 0.000000000000000000, -1.000000000000000000, 0.000000000000000000 ) ) ;
#15278=VERTEX_POINT ( 'NONE', #40894 ) ;
#15289=ORIENTED_EDGE ( 'NONE', *, *, #70162, .F. ) ;
#15315=CARTESIAN_POINT ( 'NONE',  ( 31.48454476783385658, -4.132774720514426292, -1.134026763942596494 ) ) ;
#15318=CARTESIAN_POINT ( 'NONE',  ( 5.328346181807287252, -5.876774720514418071, 20.81670806933143680 ) ) ;
#15322=CARTESIAN_POINT ( 'NONE',  ( 27.53860345374808105, -3.356774720514427823, 1.647607965253212292 ) ) ;
#15325=DIRECTION ( 'NONE',  ( 0.000000000000000000, -1.000000000000000000, 0.000000000000000000 ) ) ;
#15332=EDGE_CURVE ( 'NONE', #33363, #67215, #39774, .T. ) ;
#15339=CARTESIAN_POINT ( 'NONE',  ( 9.150000000000000355, -6.376774720514426953, -15.70000000000000284 ) ) ;
#15344=B_SPLINE_CURVE_WITH_KNOTS ( 'NONE', 3,
 ( #57075, #64704, #49462, #73287, #88011, #43340, #18490, #11379 ),
 .UNSPECIFIED., .F., .F.,
 ( 4, 2, 2, 4 ),
 ( 1.199502015590836694E-17, 0.001846270405096679841, 0.003692540810193348840, 0.007385081620386685537 ),
 .UNSPECIFIED. ) ;
#15353=CARTESIAN_POINT ( 'NONE',  ( 3.398951772795901771, -5.876774720514403860, 18.23562605320997676 ) ) ;
#15357=VERTEX_POINT ( 'NONE', #20540 ) ;
#15362=ORIENTED_EDGE ( 'NONE', *, *, #42796, .T. ) ;
#15366=ORIENTED_EDGE ( 'NONE', *, *, #3849, .T. ) ;
#15369=VERTEX_POINT ( 'NONE', #35293 ) ;
#15371=CARTESIAN_POINT ( 'NONE',  ( 31.14267748017797999, -4.481735162546526041, -3.047060235321866539 ) ) ;
#15381=CARTESIAN_POINT ( 'NONE',  ( 32.15269211224249091, -6.376774720514427841, 3.401810532325274750 ) ) ;
#15383=AXIS2_PLACEMENT_3D ( 'NONE', #49960, #27102, #97112 ) ;
#15384=ADVANCED_FACE ( 'NONE', ( #21040 ), #13428, .F. ) ;
#15393=DIRECTION ( 'NONE',  ( 0.000000000000000000, 0.000000000000000000, 1.000000000000000000 ) ) ;
#15405=CYLINDRICAL_SURFACE ( 'NONE', #90171, 3.570000000000003837 ) ;
#15414=DIRECTION ( 'NONE',  ( 0.000000000000000000, -1.000000000000000000, 0.000000000000000000 ) ) ;
#15422=CARTESIAN_POINT ( 'NONE',  ( 4.453188626415028217, -6.376774720514422512, 21.07953283331298167 ) ) ;
#15425=CARTESIAN_POINT ( 'NONE',  ( 5.641653616409716854, -5.876774720514419847, 20.81030773351227481 ) ) ;
#15436=CARTESIAN_POINT ( 'NONE',  ( -23.31187512739357715, -0.3587747205144061202, -17.31005501743528541 ) ) ;
#15451=AXIS2_PLACEMENT_3D ( 'NONE', #41957, #43452, #20093 ) ;
#15453=CARTESIAN_POINT ( 'NONE',  ( 0.1739078616027790736, -5.876774720514415407, 19.75705121608222115 ) ) ;
#15457=CARTESIAN_POINT ( 'NONE',  ( 14.76093561896379214, -3.316774720514426456, -27.37148769130089931 ) ) ;
#15460=VERTEX_POINT ( 'NONE', #62619 ) ;
#15469=ORIENTED_EDGE ( 'NONE', *, *, #80758, .F. ) ;
#15470=CARTESIAN_POINT ( 'NONE',  ( -65.05438548721848235, -5.356774720514425603, 0.7300228001186309656 ) ) ;
#15471=ORIENTED_EDGE ( 'NONE', *, *, #74122, .T. ) ;
#15475=CARTESIAN_POINT ( 'NONE',  ( -4.152941208099351300, -5.876774720514415407, 20.35309744218305639 ) ) ;
#15480=CARTESIAN_POINT ( 'NONE',  ( -19.77875734969026311, -3.316774720514426456, 29.49402280011862487 ) ) ;
#15482=CARTESIAN_POINT ( 'NONE',  ( -4.141166922167975883, -6.376774720514420736, 20.63520656483649063 ) ) ;
#15491=EDGE_CURVE ( 'NONE', #75557, #1512, #17415, .T. ) ;
#15496=CARTESIAN_POINT ( 'NONE',  ( 8.720390671778812219, -3.316774720514306996, -27.07197491306147086 ) ) ;
#15498=CARTESIAN_POINT ( 'NONE',  ( 29.73860345376319003, -4.772774720514425972, -8.849814207987163783 ) ) ;
#15508=DIRECTION ( 'NONE',  ( -0.000000000000000000, 0.000000000000000000, 1.000000000000000000 ) ) ;
#15509=ORIENTED_EDGE ( 'NONE', *, *, #43023, .T. ) ;
#15512=CYLINDRICAL_SURFACE ( 'NONE', #62888, 1.836000000000000743 ) ;
#15516=EDGE_LOOP ( 'NONE', ( #66128, #10753, #95256, #28647, #57943, #83759, #23966, #81877, #84498, #18633, #17921, #98855 ) ) ;
#15523=ORIENTED_EDGE ( 'NONE', *, *, #17717, .F. ) ;
#15536=CARTESIAN_POINT ( 'NONE',  ( 32.54628039735602130, -5.044004387208919304, -11.78547710168594165 ) ) ;
#15538=EDGE_CURVE ( 'NONE', #63330, #81513, #34666, .T. ) ;
#15564=CARTESIAN_POINT ( 'NONE',  ( 22.81105451610979173, -2.682774720540237468, -16.21691820600746681 ) ) ;
#15582=DIRECTION ( 'NONE',  ( 0.7512896232465892110, 0.000000000000000000, 0.6599726524652350657 ) ) ;
#15585=FACE_OUTER_BOUND ( 'NONE', #10654, .T. ) ;
#15586=CIRCLE ( 'NONE', #26904, 253.2618649670780826 ) ;
#15595=VECTOR ( 'NONE', #35490, 1000.000000000000000 ) ;
#15598=EDGE_LOOP ( 'NONE', ( #28215, #97985, #581, #4779 ) ) ;
#15617=VERTEX_POINT ( 'NONE', #66137 ) ;
#15619=CARTESIAN_POINT ( 'NONE',  ( -53.01255352321339842, -4.772774720514425972, 35.59556822165056644 ) ) ;
#15621=ORIENTED_EDGE ( 'NONE', *, *, #99072, .F. ) ;
#15624=CARTESIAN_POINT ( 'NONE',  ( 3.825381322105384285, -5.876774720514399419, 18.16071977647550995 ) ) ;
#15632=VECTOR ( 'NONE', #27423, 1000.000000000000000 ) ;
#15633=EDGE_CURVE ( 'NONE', #58927, #25949, #59075, .T. ) ;
#15645=DIRECTION ( 'NONE',  ( -0.000000000000000000, 1.000000000000000000, -0.000000000000000000 ) ) ;
#15651=DIRECTION ( 'NONE',  ( -1.000000000000000000, 0.000000000000000000, 2.501730345825856573E-15 ) ) ;
#15653=ORIENTED_EDGE ( 'NONE', *, *, #53162, .F. ) ;
#15654=CARTESIAN_POINT ( 'NONE',  ( -20.27875734969026311, 7.743225279485574042, 24.00402280011862288 ) ) ;
#15658=DIRECTION ( 'NONE',  ( 0.000000000000000000, 0.000000000000000000, -1.000000000000000000 ) ) ;
#15659=DIRECTION ( 'NONE',  ( 0.000000000000000000, 0.000000000000000000, 1.000000000000000000 ) ) ;
#15668=EDGE_CURVE ( 'NONE', #99093, #83403, #46536, .T. ) ;
#15670=AXIS2_PLACEMENT_3D ( 'NONE', #51448, #38198, #53448 ) ;
#15675=AXIS2_PLACEMENT_3D ( 'NONE', #5406, #99236, #99724 ) ;
#15677=EDGE_LOOP ( 'NONE', ( #45867, #2898, #2902, #72185 ) ) ;
#15679=CARTESIAN_POINT ( 'NONE',  ( -24.90875734969025501, 5.965225279485572685, 30.51402280011862089 ) ) ;
#15682=LINE ( 'NONE', #92799, #18840 ) ;
#15688=ORIENTED_EDGE ( 'NONE', *, *, #62159, .F. ) ;
#15694=LINE ( 'NONE', #8085, #81568 ) ;
#15698=CARTESIAN_POINT ( 'NONE',  ( -0.9540731552372990754, -5.876774720514411854, 19.74568812963596542 ) ) ;
#15700=EDGE_CURVE ( 'NONE', #89719, #67804, #38643, .T. ) ;
#15702=EDGE_LOOP ( 'NONE', ( #18519, #39014, #47204, #35876 ) ) ;
#15707=ORIENTED_EDGE ( 'NONE', *, *, #31783, .F. ) ;
#15710=CARTESIAN_POINT ( 'NONE',  ( -0.02075734969026423599, 5.965225279485572685, -28.54397719988136828 ) ) ;
#15712=FACE_OUTER_BOUND ( 'NONE', #90195, .T. ) ;
#15731=ORIENTED_EDGE ( 'NONE', *, *, #12205, .F. ) ;
#15733=CARTESIAN_POINT ( 'NONE',  ( -4.977357939505175466, -6.376774720514410077, 19.14913681718893557 ) ) ;
#15736=AXIS2_PLACEMENT_3D ( 'NONE', #48976, #79908, #10398 ) ;
#15737=ADVANCED_FACE ( 'NONE', ( #8710 ), #68604, .F. ) ;
#15752=CARTESIAN_POINT ( 'NONE',  ( 4.959846025536391423, -5.876774720514417183, 20.32314756232572250 ) ) ;
#15758=ORIENTED_EDGE ( 'NONE', *, *, #74789, .F. ) ;
#15761=CARTESIAN_POINT ( 'NONE',  ( 15.29947331669757737, -3.406413700670902323, -27.16854001216721670 ) ) ;
#15763=CARTESIAN_POINT ( 'NONE',  ( 3.036358173076929123, -5.876774720514419847, 20.87990785256409865 ) ) ;
#15766=EDGE_LOOP ( 'NONE', ( #35964, #47017, #92619, #48338 ) ) ;
#15771=CARTESIAN_POINT ( 'NONE',  ( 31.65781406150966149, -5.771867554241929987, 28.25297929084395321 ) ) ;
#15776=CARTESIAN_POINT ( 'NONE',  ( -19.77875734969026311, 6.143225279485574397, 27.31649921512899937 ) ) ;
#15779=CARTESIAN_POINT ( 'NONE',  ( -4.968349358974361252, -5.876774720514412742, 19.46153846153847056 ) ) ;
#15793=CARTESIAN_POINT ( 'NONE',  ( -24.90875734969025501, -3.316774720514426456, 26.43402280011862615 ) ) ;
#15795=VERTEX_POINT ( 'NONE', #92428 ) ;
#15806=CARTESIAN_POINT ( 'NONE',  ( -2.104002878010082789, -5.876774720514410077, 19.15289935703627222 ) ) ;
#15815=CARTESIAN_POINT ( 'NONE',  ( 10.50543233995236037, -4.482436650883735219, -26.67361961461832109 ) ) ;
#15821=DIRECTION ( 'NONE',  ( -0.9921023176230513441, 0.000000000000000000, 0.1254312216594016538 ) ) ;
#15822=CARTESIAN_POINT ( 'NONE',  ( 0.3910256410256394144, -5.876774720514412742, 19.63681891025641235 ) ) ;
#15829=EDGE_CURVE ( 'NONE', #25204, #89557, #55388, .T. ) ;
#15836=ORIENTED_EDGE ( 'NONE', *, *, #4774, .T. ) ;
#15839=CARTESIAN_POINT ( 'NONE',  ( -6.072964844751159497, -6.376774720514410077, 19.44316438561912008 ) ) ;
#15845=ORIENTED_EDGE ( 'NONE', *, *, #987, .F. ) ;
#15854=CARTESIAN_POINT ( 'NONE',  ( 3.325015365150250535, -5.876774720514402972, 18.26971317031913955 ) ) ;
#15859=CARTESIAN_POINT ( 'NONE',  ( -53.01255352321339842, -4.772774720514425972, 35.59556822165056644 ) ) ;
#15867=B_SPLINE_CURVE_WITH_KNOTS ( 'NONE', 3,
 ( #78627, #69546, #30969, #85253, #55832, #7640, #9640, #63451, #22837, #38586, #86262, #47209, #77132, #26, #61936, #16742, #86758, #71047, #1536, #92866, #92366, #23343 ),
 .UNSPECIFIED., .F., .F.,
 ( 4, 2, 2, 2, 2, 2, 2, 2, 2, 2, 4 ),
 ( 0.0003089662623631434001, 0.001025905326923032615, 0.001742844391482921938, 0.002459783456042811262, 0.002818252988322752887, 0.003176722520602694947, 0.003535192052882637007, 0.003893661585162578632, 0.004610600649722459282, 0.005327539714282339932, 0.006044478778842219714 ),
 .UNSPECIFIED. ) ;
#15874=CARTESIAN_POINT ( 'NONE',  ( 29.73860345376319003, -1.682774720514426114, -8.849814207987163783 ) ) ;
#15881=CARTESIAN_POINT ( 'NONE',  ( 6.429811694900724461, -6.376774720514426065, 21.48000018967326596 ) ) ;
#15884=CARTESIAN_POINT ( 'NONE',  ( 7.141559373243376641, -5.876774720514415407, 19.83742167145384983 ) ) ;
#15885=CARTESIAN_POINT ( 'NONE',  ( 30.93860345374796594, 6.475225279485573360, 19.84760796525321780 ) ) ;
#15887=ORIENTED_EDGE ( 'NONE', *, *, #926, .F. ) ;
#15891=DIRECTION ( 'NONE',  ( -0.000000000000000000, 1.000000000000000000, -0.000000000000000000 ) ) ;
#15896=CARTESIAN_POINT ( 'NONE',  ( 30.09341516180546350, 1.477225279485574028, -11.39311774897855933 ) ) ;
#15899=VERTEX_POINT ( 'NONE', #86823 ) ;
#15904=CARTESIAN_POINT ( 'NONE',  ( 2.993128331772667572, -5.876774720514403860, 18.53171057923899312 ) ) ;
#15910=B_SPLINE_SURFACE_WITH_KNOTS ( 'NONE', 3, 1, ( 
 ( #71713, #71210 ),
 ( #33649, #33140 ),
 ( #39745, #1201 ),
 ( #63108, #64628 ),
 ( #47876, #25532 ),
 ( #94035, #87934 ),
 ( #24520, #1705 ),
 ( #77792, #78795 ),
 ( #9294, #32638 ),
 ( #63614, #64122 ),
 ( #688, #48377 ),
 ( #55999, #95040 ),
 ( #86924, #26027 ),
 ( #56502, #95542 ),
 ( #16402, #78301 ),
 ( #87425, #17922 ),
 ( #48881, #79808 ),
 ( #10306, #36142 ),
 ( #42772, #51369 ),
 ( #58495, #66620 ),
 ( #43265, #3215 ),
 ( #97534, #89431 ),
 ( #88436, #19903 ),
 ( #49388, #50877 ),
 ( #28032, #82310 ),
 ( #81816, #27032 ),
 ( #58991, #20394 ) ),
 .UNSPECIFIED., .F., .F., .F.,
 ( 4, 1, 1, 1, 1, 1, 1, 1, 1, 1, 1, 1, 1, 1, 1, 1, 1, 1, 1, 1, 1, 1, 1, 1, 4 ),
 ( 2, 2 ),
 ( 0.000000000000000000, 0.06811324674912544452, 0.1325644684346005686, 0.1934266930244679106, 0.2502184821984413388, 0.3035685554824333332, 0.3535758444159123881, 0.4002351701272690576, 0.4435864585068350907, 0.4846193083749509301, 0.5242924705629079529, 0.5623796179232622983, 0.5990492626598917791, 0.6349401741080455963, 0.6697821542752002699, 0.7040087777416839110, 0.7378419440949924857, 0.7710977456761829441, 0.8038960730129318666, 0.8364148124046564270, 0.8686388349573493928, 0.9007151219040273604, 0.9333783422757061521, 0.9662128536530091294, 1.000000000000000000 ),
 ( 0.000000000000000000, 1.000000000000000000 ),
 .UNSPECIFIED. ) ;
#15920=CARTESIAN_POINT ( 'NONE',  ( 4.653494883475234545, -6.376774720514415407, 20.13747874360300116 ) ) ;
#15933=PLANE ( 'NONE',  #60476 ) ;
#15935=CARTESIAN_POINT ( 'NONE',  ( -7.640838998533831194, -5.876774720514417183, 20.32624910079993086 ) ) ;
#15942=ORIENTED_EDGE ( 'NONE', *, *, #40295, .F. ) ;
#15953=AXIS2_PLACEMENT_3D ( 'NONE', #14187, #96943, #13688 ) ;
#15961=VERTEX_POINT ( 'NONE', #64529 ) ;
#15962=DIRECTION ( 'NONE',  ( 0.000000000000000000, 0.000000000000000000, 1.000000000000000000 ) ) ;
#15986=ORIENTED_EDGE ( 'NONE', *, *, #79267, .T. ) ;
#15995=VECTOR ( 'NONE', #50789, 1000.000000000000000 ) ;
#15997=CARTESIAN_POINT ( 'NONE',  ( 7.732492003039795669, -3.316774720515257791, -27.16032169665734486 ) ) ;
#16003=ORIENTED_EDGE ( 'NONE', *, *, #59308, .F. ) ;
#16005=DIRECTION ( 'NONE',  ( 0.000000000000000000, 0.000000000000000000, -1.000000000000000000 ) ) ;
#16013=VECTOR ( 'NONE', #46405, 1000.000000000000114 ) ;
#16018=CARTESIAN_POINT ( 'NONE',  ( -3.826923076923078426, -5.876774720514409189, 19.19230769230769695 ) ) ;
#16027=DIRECTION ( 'NONE',  ( -0.000000000000000000, 1.000000000000000000, -0.000000000000000000 ) ) ;
#16041=CARTESIAN_POINT ( 'NONE',  ( -2.762050907158362989, -5.876774720514416295, 19.89644244529369033 ) ) ;
#16044=DIRECTION ( 'NONE',  ( 0.000000000000000000, 0.000000000000000000, -1.000000000000000000 ) ) ;
#16045=CARTESIAN_POINT ( 'NONE',  ( 4.856316114246853388, -5.876774720514408301, 19.03119074624055074 ) ) ;
#16066=VECTOR ( 'NONE', #14458, 1000.000000000000000 ) ;
#16069=ADVANCED_FACE ( 'NONE', ( #81720 ), #30987, .T. ) ;
#16078=CARTESIAN_POINT ( 'NONE',  ( 4.017909867803298063, -5.876774720514403860, 18.55402206357357286 ) ) ;
#16079=VECTOR ( 'NONE', #75603, 1000.000000000000000 ) ;
#16084=VECTOR ( 'NONE', #40064, 1000.000000000000000 ) ;
#16094=DIRECTION ( 'NONE',  ( -1.000000000000000000, 0.000000000000000000, 5.238131417152343399E-15 ) ) ;
#16098=ORIENTED_EDGE ( 'NONE', *, *, #46286, .T. ) ;
#16109=CARTESIAN_POINT ( 'NONE',  ( 4.451706829556401956, -5.876774720514407413, 18.91922570401084513 ) ) ;
#16111=ORIENTED_EDGE ( 'NONE', *, *, #27341, .F. ) ;
#16134=PLANE ( 'NONE',  #89718 ) ;
#16139=AXIS2_PLACEMENT_3D ( 'NONE', #81567, #35401, #96786 ) ;
#16140=CARTESIAN_POINT ( 'NONE',  ( 22.02124265030973760, 7.743225279485574042, 16.20402280011862217 ) ) ;
#16143=DIRECTION ( 'NONE',  ( 0.000000000000000000, 0.000000000000000000, -1.000000000000000000 ) ) ;
#16150=CARTESIAN_POINT ( 'NONE',  ( 30.93860345374796594, 5.965225279485573573, 28.83647319851474933 ) ) ;
#16151=ORIENTED_EDGE ( 'NONE', *, *, #73822, .T. ) ;
#16156=CARTESIAN_POINT ( 'NONE',  ( 24.71017632900190719, -3.356774720514427379, 1.647607965253211848 ) ) ;
#16175=FACE_OUTER_BOUND ( 'NONE', #67552, .T. ) ;
#16183=DIRECTION ( 'NONE',  ( 0.000000000000000000, 0.000000000000000000, -1.000000000000000000 ) ) ;
#16198=EDGE_CURVE ( 'NONE', #41593, #46359, #3957, .T. ) ;
#16208=DIRECTION ( 'NONE',  ( 0.000000000000000000, 0.000000000000000000, -1.000000000000000000 ) ) ;
#16213=DIRECTION ( 'NONE',  ( 0.000000000000000000, 0.000000000000000000, 1.000000000000000000 ) ) ;
#16214=ORIENTED_EDGE ( 'NONE', *, *, #63541, .F. ) ;
#16217=ORIENTED_EDGE ( 'NONE', *, *, #24621, .F. ) ;
#16218=ADVANCED_FACE ( 'NONE', ( #37037 ), #61390, .F. ) ;
#16220=CARTESIAN_POINT ( 'NONE',  ( -7.324001883147635894, -5.876774720514414518, 20.17732409774492197 ) ) ;
#16221=CARTESIAN_POINT ( 'NONE',  ( 31.04236049493789906, 5.965225279485572685, 19.84760796525321780 ) ) ;
#16223=AXIS2_PLACEMENT_3D ( 'NONE', #28580, #66679, #67660 ) ;
#16230=AXIS2_PLACEMENT_3D ( 'NONE', #68636, #93846, #99554 ) ;
#16237=CARTESIAN_POINT ( 'NONE',  ( -4.752075056065355518, -6.376774720514406525, 19.17724329193115551 ) ) ;
#16240=CIRCLE ( 'NONE', #19499, 28.45799999999999486 ) ;
#16263=EDGE_LOOP ( 'NONE', ( #57348, #78136, #58324, #60204 ) ) ;
#16273=DIRECTION ( 'NONE',  ( 0.000000000000000000, 0.000000000000000000, 1.000000000000000000 ) ) ;
#16275=CARTESIAN_POINT ( 'NONE',  ( 31.61913385939691423, -4.417689821282788643, 26.66246549260776177 ) ) ;
#16291=CARTESIAN_POINT ( 'NONE',  ( 14.53567905697413565, -3.934666312338137129, -28.27917189340610804 ) ) ;
#16294=DIRECTION ( 'NONE',  ( -0.000000000000000000, 1.000000000000000000, -0.000000000000000000 ) ) ;
#16300=AXIS2_PLACEMENT_3D ( 'NONE', #46820, #85875, #16352 ) ;
#16309=CARTESIAN_POINT ( 'NONE',  ( -1.304987980769231948, -6.376774720514413630, 19.76512419871795245 ) ) ;
#16312=EDGE_CURVE ( 'NONE', #5889, #97460, #78577, .T. ) ;
#16317=CARTESIAN_POINT ( 'NONE',  ( 31.27206728860909024, -4.132774720514318822, -3.930752063305056332 ) ) ;
#16328=CARTESIAN_POINT ( 'NONE',  ( 5.635247460261607166, -5.876774720514423400, 21.53093896358932469 ) ) ;
#16331=DIRECTION ( 'NONE',  ( 0.000000000000000000, 0.000000000000000000, 1.000000000000000000 ) ) ;
#16343=DIRECTION ( 'NONE',  ( -0.8264557562326033668, -0.000000000000000000, -0.5630016722799281448 ) ) ;
#16344=ORIENTED_EDGE ( 'NONE', *, *, #54722, .T. ) ;
#16350=CARTESIAN_POINT ( 'NONE',  ( -28.47875734969025885, 6.475225279485573360, -0.08597719988137300651 ) ) ;
#16351=CARTESIAN_POINT ( 'NONE',  ( 7.164391295225654765, -5.876774720514419847, 20.71606273170883838 ) ) ;
#16352=DIRECTION ( 'NONE',  ( 0.000000000000000000, 0.000000000000000000, 1.000000000000000000 ) ) ;
#16370=ORIENTED_EDGE ( 'NONE', *, *, #85679, .T. ) ;
#16380=CARTESIAN_POINT ( 'NONE',  ( -1.267404104715736279, -6.376774720514411854, 19.66076420632889921 ) ) ;
#16386=ORIENTED_EDGE ( 'NONE', *, *, #68246, .T. ) ;
#16388=DIRECTION ( 'NONE',  ( 0.000000000000000000, 0.000000000000000000, -1.000000000000000000 ) ) ;
#16393=CARTESIAN_POINT ( 'NONE',  ( 22.11522345091601949, -4.214729766064097660, -16.31575456565007443 ) ) ;
#16397=ORIENTED_EDGE ( 'NONE', *, *, #78411, .T. ) ;
#16402=CARTESIAN_POINT ( 'NONE',  ( 4.585161930874343206, -6.376774720514427841, 21.47592444013076118 ) ) ;
#16411=CARTESIAN_POINT ( 'NONE',  ( -23.29179552176162105, -0.3587747205144061202, -17.29637630388739211 ) ) ;
#16413=B_SPLINE_CURVE_WITH_KNOTS ( 'NONE', 3,
 ( #42296, #35658, #12297, #51883, #13294, #88446, #43768, #44269, #65629, #28042 ),
 .UNSPECIFIED., .F., .F.,
 ( 4, 2, 2, 2, 4 ),
 ( 0.000000000000000000, 0.0004833345490728424001, 0.0009666690981456848002, 0.001450003647218527092, 0.001933338196291368299 ),
 .UNSPECIFIED. ) ;
#16417=CARTESIAN_POINT ( 'NONE',  ( 6.666194146093591399, -6.376774720514413630, 19.75460921626947908 ) ) ;
#16418=CYLINDRICAL_SURFACE ( 'NONE', #82315, 12.23252173913042995 ) ;
#16424=EDGE_CURVE ( 'NONE', #95862, #3328, #57775, .T. ) ;
#16442=ORIENTED_EDGE ( 'NONE', *, *, #66654, .F. ) ;
#16447=ORIENTED_EDGE ( 'NONE', *, *, #98152, .F. ) ;
#16452=DIRECTION ( 'NONE',  ( 0.000000000000000000, -1.000000000000000000, 0.000000000000000000 ) ) ;
#16460=AXIS2_PLACEMENT_3D ( 'NONE', #61216, #15011, #86026 ) ;
#16467=CARTESIAN_POINT ( 'NONE',  ( 13.99288689683290166, 5.965225279485572685, -28.28242551218217926 ) ) ;
#16479=CARTESIAN_POINT ( 'NONE',  ( -2.188401442307694289, -5.876774720514411854, 19.46153846153846700 ) ) ;
#16486=DIRECTION ( 'NONE',  ( -0.7512896232465892110, -0.000000000000000000, -0.6599726524652350657 ) ) ;
#16491=ADVANCED_FACE ( 'NONE', ( #11578 ), #89714, .F. ) ;
#16493=DIRECTION ( 'NONE',  ( 0.000000000000000000, 1.000000000000000000, 0.000000000000000000 ) ) ;
#16495=DIRECTION ( 'NONE',  ( -1.000000000000000000, -0.000000000000000000, 0.000000000000000000 ) ) ;
#16496=DIRECTION ( 'NONE',  ( 0.000000000000000000, 0.000000000000000000, -1.000000000000000000 ) ) ;
#16497=CARTESIAN_POINT ( 'NONE',  ( 9.315600972258334167, -0.3587747205144265483, 28.35070303307545458 ) ) ;
#16509=EDGE_LOOP ( 'NONE', ( #48101, #55495, #7399, #3906, #32467, #15191, #79872, #97834, #53198, #57957, #57351, #37604, #68034, #82986, #56677, #86503, #40613, #55430, #92483, #55242, #18206, #12870, #43580, #25197, #8842 ) ) ;
#16518=ORIENTED_EDGE ( 'NONE', *, *, #91847, .T. ) ;
#16521=DIRECTION ( 'NONE',  ( 0.000000000000000000, -1.000000000000000000, 0.000000000000000000 ) ) ;
#16534=CIRCLE ( 'NONE', #18220, 12.65241003308275758 ) ;
#16537=CARTESIAN_POINT ( 'NONE',  ( -2.220741593810419801, -5.876774720514411854, 19.46247113826587238 ) ) ;
#16541=CARTESIAN_POINT ( 'NONE',  ( 3.960454120839856706, -5.876774720514403860, 18.17119035270509997 ) ) ;
#16545=DIRECTION ( 'NONE',  ( 0.000000000000000000, -1.000000000000000000, 0.000000000000000000 ) ) ;
#16552=VECTOR ( 'NONE', #28174, 1000.000000000000000 ) ;
#16555=CARTESIAN_POINT ( 'NONE',  ( 10.24059822343757808, -6.376774720514426953, 17.91871304725684766 ) ) ;
#16576=DIRECTION ( 'NONE',  ( 0.000000000000000000, 0.000000000000000000, 1.000000000000000000 ) ) ;
#16583=CARTESIAN_POINT ( 'NONE',  ( -5.837039262820512775, -6.376774720514415407, 19.76512419871795245 ) ) ;
#16591=ORIENTED_EDGE ( 'NONE', *, *, #32363, .F. ) ;
#16599=ORIENTED_EDGE ( 'NONE', *, *, #7550, .T. ) ;
#16600=LINE ( 'NONE', #86624, #29881 ) ;
#16604=CARTESIAN_POINT ( 'NONE',  ( 4.214857194124448370, -5.876774720514403860, 18.65898740197609840 ) ) ;
#16608=DIRECTION ( 'NONE',  ( 0.000000000000000000, 0.000000000000000000, 1.000000000000000000 ) ) ;
#16621=VERTEX_POINT ( 'NONE', #84084 ) ;
#16622=CARTESIAN_POINT ( 'NONE',  ( -6.072964844751159497, -5.876774720514410077, 19.44316438561912008 ) ) ;
#16632=DIRECTION ( 'NONE',  ( 0.000000000000000000, -1.000000000000000000, 0.000000000000000000 ) ) ;
#16635=CIRCLE ( 'NONE', #52280, 0.3000000000000016542 ) ;
#16637=CARTESIAN_POINT ( 'NONE',  ( 5.717289507243529023, -5.356774720514425603, -25.39219853617311173 ) ) ;
#16638=EDGE_CURVE ( 'NONE', #66356, #74013, #60741, .T. ) ;
#16639=CARTESIAN_POINT ( 'NONE',  ( 4.967948717948723392, -6.376774720514415407, 20.00140224358974095 ) ) ;
#16640=VERTEX_POINT ( 'NONE', #76962 ) ;
#16651=CARTESIAN_POINT ( 'NONE',  ( -23.71328795744024021, 5.965225279485594001, -17.58350715675015152 ) ) ;
#16653=FACE_OUTER_BOUND ( 'NONE', #78271, .T. ) ;
#16657=VECTOR ( 'NONE', #14024, 1000.000000000000000 ) ;
#16659=EDGE_CURVE ( 'NONE', #30745, #77700, #75963, .T. ) ;
#16662=LINE ( 'NONE', #57258, #70952 ) ;
#16676=ORIENTED_EDGE ( 'NONE', *, *, #44419, .F. ) ;
#16684=ORIENTED_EDGE ( 'NONE', *, *, #48997, .T. ) ;
#16695=CARTESIAN_POINT ( 'NONE',  ( -0.4362980769230789257, -5.876774720514411854, 19.46153846153846345 ) ) ;
#16700=ORIENTED_EDGE ( 'NONE', *, *, #92289, .F. ) ;
#16712=CARTESIAN_POINT ( 'NONE',  ( 32.45853543194704116, -0.3587747205144265483, 9.169203677920338080 ) ) ;
#16717=ORIENTED_EDGE ( 'NONE', *, *, #1100, .T. ) ;
#16719=CARTESIAN_POINT ( 'NONE',  ( -1.304987980769231948, -6.376774720514413630, 19.76512419871795245 ) ) ;
#16721=PLANE ( 'NONE',  #37997 ) ;
#16722=CIRCLE ( 'NONE', #94447, 1.836000000000000743 ) ;
#16724=FACE_OUTER_BOUND ( 'NONE', #11469, .T. ) ;
#16727=VERTEX_POINT ( 'NONE', #63276 ) ;
#16732=ADVANCED_FACE ( 'NONE', ( #17576 ), #54651, .F. ) ;
#16733=CARTESIAN_POINT ( 'NONE',  ( -4.620655831143558601, -6.376774720514410077, 19.21747685089457036 ) ) ;
#16736=CARTESIAN_POINT ( 'NONE',  ( 0.000000000000000000, -4.056774720514426669, 4.299999999999999822 ) ) ;
#16738=AXIS2_PLACEMENT_3D ( 'NONE', #47867, #86416, #77782 ) ;
#16742=CARTESIAN_POINT ( 'NONE',  ( 25.30723783573411012, -5.176466091202484243, -8.329609793420479136 ) ) ;
#16743=CARTESIAN_POINT ( 'NONE',  ( 5.088854283150510582, -3.311779300275201177, -27.56292346345011524 ) ) ;
#16747=DIRECTION ( 'NONE',  ( -0.000000000000000000, 1.000000000000000000, -0.000000000000000000 ) ) ;
#16749=B_SPLINE_SURFACE_WITH_KNOTS ( 'NONE', 3, 1, ( 
 ( #80940, #43387 ),
 ( #50006, #97654 ),
 ( #44382, #34274 ),
 ( #96658, #11426 ),
 ( #42401, #89551 ),
 ( #74325, #19529 ),
 ( #65246, #20035 ),
 ( #4816, #66739 ),
 ( #90050, #51491 ),
 ( #60614, #21513 ),
 ( #68212, #31132 ),
 ( #30637, #92035 ),
 ( #22008, #53499 ),
 ( #77298, #84424 ),
 ( #23503, #15904 ),
 ( #83926, #45874 ),
 ( #37754, #91536 ),
 ( #76792, #60115 ),
 ( #76300, #30133 ),
 ( #69711, #85420 ),
 ( #52491, #83419 ),
 ( #7293, #190 ),
 ( #54482, #75308 ),
 ( #62105, #98642 ),
 ( #36762, #93026 ),
 ( #14406, #52995 ),
 ( #5805, #6796 ) ),
 .UNSPECIFIED., .F., .F., .F.,
 ( 4, 1, 1, 1, 1, 1, 1, 1, 1, 1, 1, 1, 1, 1, 1, 1, 1, 1, 1, 1, 1, 1, 1, 1, 4 ),
 ( 2, 2 ),
 ( 0.000000000000000000, 0.06527777045992599891, 0.1272054409606112602, 0.1861682170588502272, 0.2416754997382695169, 0.2941145050635431968, 0.3436091886235829174, 0.3903870759341810937, 0.4344634103958515681, 0.4766455533866958971, 0.5170022931272251210, 0.5559361803014920556, 0.5937164392999396689, 0.6300571764906928163, 0.6656014334950210998, 0.7007446912418848761, 0.7349167217326266766, 0.7686809964330385547, 0.8020868126442075585, 0.8348488267452134348, 0.8674333878737416903, 0.9001375891431748766, 0.9328060676261197282, 0.9662118838372896201, 1.000000000000000000 ),
 ( 0.000000000000000000, 1.000000000000000000 ),
 .UNSPECIFIED. ) ;
#16753=ADVANCED_FACE ( 'NONE', ( #8963 ), #70367, .F. ) ;
#16763=CARTESIAN_POINT ( 'NONE',  ( 2.911360383046243783, -5.876774720514417183, 20.24673073119071276 ) ) ;
#16789=LINE ( 'NONE', #63495, #24916 ) ;
#16796=CARTESIAN_POINT ( 'NONE',  ( 30.43908124610669930, -1.684774720514424784, -13.86910542224429044 ) ) ;
#16797=CARTESIAN_POINT ( 'NONE',  ( -19.69812919673063689, 5.965225279485592225, -22.00173861453435720 ) ) ;
#16799=DIRECTION ( 'NONE',  ( 0.000000000000000000, 1.000000000000000000, 0.000000000000000000 ) ) ;
#16808=ORIENTED_EDGE ( 'NONE', *, *, #37515, .F. ) ;
#16814=AXIS2_PLACEMENT_3D ( 'NONE', #47133, #63374, #78050 ) ;
#16819=DIRECTION ( 'NONE',  ( 4.218136541796977197E-15, 1.000000000000000000, 1.324960360541890271E-16 ) ) ;
#16827=CARTESIAN_POINT ( 'NONE',  ( 22.65031661608483660, -500000.0000000000582, -20.71116937900383093 ) ) ;
#16829=DIRECTION ( 'NONE',  ( 0.000000000000000000, -1.000000000000000000, 0.000000000000000000 ) ) ;
#16838=VERTEX_POINT ( 'NONE', #83835 ) ;
#16847=CARTESIAN_POINT ( 'NONE',  ( 6.996935307331598075, -5.876774720514423400, 21.22729008382901128 ) ) ;
#16848=ORIENTED_EDGE ( 'NONE', *, *, #57124, .F. ) ;
#16852=FACE_OUTER_BOUND ( 'NONE', #62831, .T. ) ;
#16853=ORIENTED_EDGE ( 'NONE', *, *, #67457, .F. ) ;
#16857=CARTESIAN_POINT ( 'NONE',  ( 6.509931258083027750, -6.376774720514417183, 20.09204137875607188 ) ) ;
#16891=EDGE_CURVE ( 'NONE', #5613, #58474, #21421, .T. ) ;
#16895=EDGE_CURVE ( 'NONE', #57446, #32453, #44788, .T. ) ;
#16896=ORIENTED_EDGE ( 'NONE', *, *, #60770, .T. ) ;
#16898=DIRECTION ( 'NONE',  ( 0.000000000000000000, 0.000000000000000000, -1.000000000000000000 ) ) ;
#16930=CARTESIAN_POINT ( 'NONE',  ( 6.044119082205957838, -5.876774720514423400, 21.40268112089023589 ) ) ;
#16934=B_SPLINE_CURVE_WITH_KNOTS ( 'NONE', 3,
 ( #14309, #20927, #13309, #45282, #12314, #82828, #89950, #20420, #12813, #44289, #74713, #75218 ),
 .UNSPECIFIED., .F., .F.,
 ( 4, 2, 2, 2, 2, 4 ),
 ( -0.003357017750235514672, -0.001150730439442379169, 0.001055556871350756334, 0.002158700526747327555, 0.003261844182143899644, 0.005468131492937042953 ),
 .UNSPECIFIED. ) ;
#16941=VECTOR ( 'NONE', #12057, 1000.000000000000000 ) ;
#16954=LINE ( 'NONE', #38790, #82449 ) ;
#16966=AXIS2_PLACEMENT_3D ( 'NONE', #19812, #12702, #81229 ) ;
#16968=ORIENTED_EDGE ( 'NONE', *, *, #60948, .F. ) ;
#16970=PLANE ( 'NONE',  #81890 ) ;
#16971=ORIENTED_EDGE ( 'NONE', *, *, #42606, .T. ) ;
#16972=CARTESIAN_POINT ( 'NONE',  ( 3.325015365150250535, -6.376774720514402972, 18.26971317031913955 ) ) ;
#16979=VECTOR ( 'NONE', #87653, 1000.000000000000000 ) ;
#16986=CARTESIAN_POINT ( 'NONE',  ( -1.501937386944296460, -5.876774720514415407, 19.86422795159478483 ) ) ;
#16999=DIRECTION ( 'NONE',  ( 0.000000000000000000, 0.000000000000000000, 1.000000000000000000 ) ) ;
#17000=CARTESIAN_POINT ( 'NONE',  ( 30.09341516180546350, -1.682774720514426114, -11.39311774897855933 ) ) ;
#17020=CIRCLE ( 'NONE', #80249, 2.249999999999998668 ) ;
#17022=FACE_OUTER_BOUND ( 'NONE', #6194, .T. ) ;
#17037=DIRECTION ( 'NONE',  ( 0.000000000000000000, 0.000000000000000000, 1.000000000000000000 ) ) ;
#17042=DIRECTION ( 'NONE',  ( 0.000000000000000000, 0.000000000000000000, 1.000000000000000000 ) ) ;
#17045=VECTOR ( 'NONE', #45061, 1000.000000000000000 ) ;
#17059=AXIS2_PLACEMENT_3D ( 'NONE', #19467, #87490, #3273 ) ;
#17066=CARTESIAN_POINT ( 'NONE',  ( 4.016587897052070311, -5.876774720514425177, 21.44459449800855921 ) ) ;
#17070=EDGE_LOOP ( 'NONE', ( #13224, #38560, #81632 ) ) ;
#17073=DIRECTION ( 'NONE',  ( -0.000000000000000000, 0.000000000000000000, -1.000000000000000000 ) ) ;
#17080=ORIENTED_EDGE ( 'NONE', *, *, #82640, .T. ) ;
#17112=CARTESIAN_POINT ( 'NONE',  ( 4.627238781264984446, -6.376774720514408301, 19.49219360614394247 ) ) ;
#17116=CARTESIAN_POINT ( 'NONE',  ( 3.421177667410916001, 5.965225279485572685, 28.69411518427638441 ) ) ;
#17117=ORIENTED_EDGE ( 'NONE', *, *, #22981, .F. ) ;
#17121=ORIENTED_EDGE ( 'NONE', *, *, #14833, .T. ) ;
#17122=VECTOR ( 'NONE', #13968, 1000.000000000000000 ) ;
#17127=DIRECTION ( 'NONE',  ( -0.000000000000000000, 1.000000000000000000, -0.000000000000000000 ) ) ;
#17144=LINE ( 'NONE', #40491, #35275 ) ;
#17148=CARTESIAN_POINT ( 'NONE',  ( 26.73860345374794178, -1.682774720514426114, -1.272392034746785860 ) ) ;
#17152=DIRECTION ( 'NONE',  ( -1.000000000000000000, -0.000000000000000000, -7.994117400814786717E-16 ) ) ;
#17157=CARTESIAN_POINT ( 'NONE',  ( -5.576843645946834016, -6.376774720514418959, 20.41272575174755133 ) ) ;
#17161=CARTESIAN_POINT ( 'NONE',  ( -53.01255352321339842, -1.682774720514426114, 35.59556822165056644 ) ) ;
#17165=CARTESIAN_POINT ( 'NONE',  ( -12.64432969575900323, 5.965225279485592225, -26.13179214487284696 ) ) ;
#17170=DIRECTION ( 'NONE',  ( 0.000000000000000000, 0.000000000000000000, -1.000000000000000000 ) ) ;
#17173=CARTESIAN_POINT ( 'NONE',  ( 5.705253819860196529, -6.376774720514415407, 19.95963554344900714 ) ) ;
#17178=CARTESIAN_POINT ( 'NONE',  ( -6.181720432442950219, -6.376774720514410077, 19.67464842890028720 ) ) ;
#17179=CARTESIAN_POINT ( 'NONE',  ( -29.49875734969025842, -0.3587747205144265483, 17.86602280011862476 ) ) ;
#17183=AXIS2_PLACEMENT_3D ( 'NONE', #3536, #27857, #34478 ) ;
#17186=VERTEX_POINT ( 'NONE', #75593 ) ;
#17188=CARTESIAN_POINT ( 'NONE',  ( 22.81105451610979173, 8.475225279485572472, -19.61691820600746539 ) ) ;
#17209=DIRECTION ( 'NONE',  ( 0.000000000000000000, 1.000000000000000000, -0.000000000000000000 ) ) ;
#17222=CARTESIAN_POINT ( 'NONE',  ( -1.488488975859286523, -6.376774720514411854, 19.49847411603315095 ) ) ;
#17225=VECTOR ( 'NONE', #75901, 1000.000000000000000 ) ;
#17239=ORIENTED_EDGE ( 'NONE', *, *, #58997, .F. ) ;
#17248=CARTESIAN_POINT ( 'NONE',  ( 5.087148743171193033, -3.314277014504871222, -27.56324057082087364 ) ) ;
#17257=EDGE_LOOP ( 'NONE', ( #56075, #15688, #58228, #74786, #9752, #81278, #30573 ) ) ;
#17258=EDGE_CURVE ( 'NONE', #47463, #54335, #85053, .T. ) ;
#17279=AXIS2_PLACEMENT_3D ( 'NONE', #26188, #4361, #19066 ) ;
#17280=CARTESIAN_POINT ( 'NONE',  ( 31.62961302973990030, -4.065030569019225659, 27.09489828165477476 ) ) ;
#17304=VERTEX_POINT ( 'NONE', #97452 ) ;
#17315=PLANE ( 'NONE',  #5192 ) ;
#17320=CARTESIAN_POINT ( 'NONE',  ( 31.48454476783385658, -4.132774720514426292, -1.134026763942596494 ) ) ;
#17321=VERTEX_POINT ( 'NONE', #66035 ) ;
#17323=CARTESIAN_POINT ( 'NONE',  ( 9.747210413488877734, -4.783584857593751849, -26.42012502324587686 ) ) ;
#17330=CARTESIAN_POINT ( 'NONE',  ( -3.108974358974359475, -5.876774720514418071, 20.36458333333334281 ) ) ;
#17360=CARTESIAN_POINT ( 'NONE',  ( 6.586338672804227024, -6.376774720514415407, 20.10086663068103618 ) ) ;
#17361=CARTESIAN_POINT ( 'NONE',  ( 5.786755829966409692, -5.876774720514413630, 19.89762986309224857 ) ) ;
#17367=VECTOR ( 'NONE', #42239, 1000.000000000000000 ) ;
#17376=ORIENTED_EDGE ( 'NONE', *, *, #2578, .T. ) ;
#17380=CARTESIAN_POINT ( 'NONE',  ( 26.73860345374794178, -5.356774720496559894, 19.84760796525321425 ) ) ;
#17392=CARTESIAN_POINT ( 'NONE',  ( 22.81105451610979173, -500000.0000000000582, -16.21691820600746681 ) ) ;
#17395=VERTEX_POINT ( 'NONE', #93327 ) ;
#17406=LINE ( 'NONE', #72707, #17840 ) ;
#17413=CARTESIAN_POINT ( 'NONE',  ( -5.576923076923076650, -5.876774720514417183, 20.44941907051282470 ) ) ;
#17415=B_SPLINE_CURVE_WITH_KNOTS ( 'NONE', 3,
 ( #63125, #16417, #1216, #30659, #55008 ),
 .UNSPECIFIED., .F., .F.,
 ( 4, 1, 4 ),
 ( 0.000000000000000000, 0.5126593363417801807, 0.9999999999999998890 ),
 .UNSPECIFIED. ) ;
#17427=CARTESIAN_POINT ( 'NONE',  ( 3.296548071537245495, -5.876774720514425177, 21.29143507544719682 ) ) ;
#17434=CARTESIAN_POINT ( 'NONE',  ( -0.02075734969026423599, -0.3587747205144213303, -0.08597719988137648983 ) ) ;
#17438=ORIENTED_EDGE ( 'NONE', *, *, #97352, .T. ) ;
#17451=ORIENTED_EDGE ( 'NONE', *, *, #48666, .T. ) ;
#17475=ORIENTED_EDGE ( 'NONE', *, *, #24533, .T. ) ;
#17478=AXIS2_PLACEMENT_3D ( 'NONE', #62354, #68956, #30387 ) ;
#17487=CARTESIAN_POINT ( 'NONE',  ( 7.010993867624484288, -5.876774720514418071, 20.34381700913260715 ) ) ;
#17488=CARTESIAN_POINT ( 'NONE',  ( 30.09341516180546350, -1.682774720514426114, -11.39311774897855933 ) ) ;
#17496=VECTOR ( 'NONE', #48898, 1000.000000000000000 ) ;
#17499=CARTESIAN_POINT ( 'NONE',  ( 0.000000000000000000, -4.056774720514426669, 0.000000000000000000 ) ) ;
#17508=CARTESIAN_POINT ( 'NONE',  ( 5.105333984060716368, -3.311071866383498374, -27.56005651598365347 ) ) ;
#17513=CARTESIAN_POINT ( 'NONE',  ( 13.91401389203221406, 5.965225279485572685, 158.0376437107427137 ) ) ;
#17524=ORIENTED_EDGE ( 'NONE', *, *, #97679, .F. ) ;
#17533=VERTEX_POINT ( 'NONE', #76594 ) ;
#17535=CARTESIAN_POINT ( 'NONE',  ( -4.465079497292244959, -6.376774720514410077, 19.29815762497054976 ) ) ;
#17539=CARTESIAN_POINT ( 'NONE',  ( 13.10664265030973930, 5.965225279485574461, -28.64597719988137570 ) ) ;
#17542=ORIENTED_EDGE ( 'NONE', *, *, #86548, .T. ) ;
#17548=DIRECTION ( 'NONE',  ( -0.000000000000000000, 1.000000000000000000, -0.000000000000000000 ) ) ;
#17550=AXIS2_PLACEMENT_3D ( 'NONE', #38082, #69036, #84757 ) ;
#17553=CARTESIAN_POINT ( 'NONE',  ( -4.141025641025640525, -6.376774720514418959, 20.67377804487179915 ) ) ;
#17564=CARTESIAN_POINT ( 'NONE',  ( 4.878909776184770742E-15, -6.376774720514426953, 22.50000000000000355 ) ) ;
#17566=CARTESIAN_POINT ( 'NONE',  ( 16.09828331921171696, -3.622774695106080411, -27.82448843548682405 ) ) ;
#17569=CARTESIAN_POINT ( 'NONE',  ( 2.611202098145462891, -5.876774720514420736, 20.45574432200782766 ) ) ;
#17571=CARTESIAN_POINT ( 'NONE',  ( 4.595037417369686850, -6.376774720514420736, 20.70846556543617467 ) ) ;
#17576=FACE_OUTER_BOUND ( 'NONE', #47350, .T. ) ;
#17609=VERTEX_POINT ( 'NONE', #33939 ) ;
#17619=CARTESIAN_POINT ( 'NONE',  ( 4.572862496014544753, -5.876774720514409189, 19.20224321281611068 ) ) ;
#17626=ORIENTED_EDGE ( 'NONE', *, *, #82644, .F. ) ;
#17633=CARTESIAN_POINT ( 'NONE',  ( -6.728471858368818559, -5.876774720514409189, 19.14926908420045137 ) ) ;
#17638=ORIENTED_EDGE ( 'NONE', *, *, #23752, .T. ) ;
#17649=CARTESIAN_POINT ( 'NONE',  ( 31.63608488009067443, -0.6647747205144267646, 27.34773273846992225 ) ) ;
#17689=PLANE ( 'NONE',  #92786 ) ;
#17691=ORIENTED_EDGE ( 'NONE', *, *, #89017, .F. ) ;
#17695=LINE ( 'NONE', #92808, #18867 ) ;
#17704=CARTESIAN_POINT ( 'NONE',  ( -1.041963229364719634, -6.376774720514417183, 20.24089781925592746 ) ) ;
#17706=ADVANCED_FACE ( 'NONE', ( #2496 ), #9099, .T. ) ;
#17717=EDGE_CURVE ( 'NONE', #50837, #32014, #33434, .T. ) ;
#17721=VECTOR ( 'NONE', #46264, 1000.000000000000000 ) ;
#17723=DIRECTION ( 'NONE',  ( 0.000000000000000000, -1.000000000000000000, 0.000000000000000000 ) ) ;
#17725=ORIENTED_EDGE ( 'NONE', *, *, #80833, .F. ) ;
#17728=ORIENTED_EDGE ( 'NONE', *, *, #61187, .F. ) ;
#17729=EDGE_CURVE ( 'NONE', #12603, #26207, #56797, .T. ) ;
#17736=DIRECTION ( 'NONE',  ( 0.000000000000000000, 0.000000000000000000, 1.000000000000000000 ) ) ;
#17748=ORIENTED_EDGE ( 'NONE', *, *, #18035, .T. ) ;
#17762=CARTESIAN_POINT ( 'NONE',  ( 4.638796026491669444, -5.876774720514423400, 21.40644651702305268 ) ) ;
#17764=CIRCLE ( 'NONE', #87431, 80.18232118519037499 ) ;
#17783=CARTESIAN_POINT ( 'NONE',  ( 28.20688450243589784, -4.772774720514425972, -7.073367244511575613 ) ) ;
#17784=ADVANCED_FACE ( 'NONE', ( #65913 ), #66411, .F. ) ;
#17806=ORIENTED_EDGE ( 'NONE', *, *, #89298, .T. ) ;
#17812=LINE ( 'NONE', #34039, #82085 ) ;
#17817=CIRCLE ( 'NONE', #89162, 130.7884398600581335 ) ;
#17818=ORIENTED_EDGE ( 'NONE', *, *, #6931, .F. ) ;
#17825=DIRECTION ( 'NONE',  ( -0.000000000000000000, 1.000000000000000000, -0.000000000000000000 ) ) ;
#17840=VECTOR ( 'NONE', #47866, 999.9999999999998863 ) ;
#17847=LINE ( 'NONE', #112, #14491 ) ;
#17856=ORIENTED_EDGE ( 'NONE', *, *, #93861, .F. ) ;
#17860=DIRECTION ( 'NONE',  ( -0.000000000000000000, 1.000000000000000000, -0.000000000000000000 ) ) ;
#17865=CARTESIAN_POINT ( 'NONE',  ( 7.116579217368891541, -5.876774720514415407, 20.51774267661129869 ) ) ;
#17866=CARTESIAN_POINT ( 'NONE',  ( 5.557675543255346184, -5.876774720514415407, 20.10561748372801461 ) ) ;
#17870=DIRECTION ( 'NONE',  ( 1.000000000000000000, 0.000000000000000000, -2.168404344971008868E-16 ) ) ;
#17876=EDGE_LOOP ( 'NONE', ( #33811, #5854, #62803, #9255 ) ) ;
#17888=ORIENTED_EDGE ( 'NONE', *, *, #90952, .F. ) ;
#17908=LINE ( 'NONE', #72204, #25592 ) ;
#17910=EDGE_CURVE ( 'NONE', #82409, #17980, #12590, .T. ) ;
#17914=CIRCLE ( 'NONE', #82722, 12.23252173913042995 ) ;
#17916=DIRECTION ( 'NONE',  ( 0.000000000000000000, -1.000000000000000000, 0.000000000000000000 ) ) ;
#17919=CARTESIAN_POINT ( 'NONE',  ( -5.314757719055156038, -5.876774720514410077, 19.55912026249540858 ) ) ;
#17921=ORIENTED_EDGE ( 'NONE', *, *, #28818, .T. ) ;
#17922=CARTESIAN_POINT ( 'NONE',  ( 4.527536911777373163, -5.876774720514421624, 21.53954785142818196 ) ) ;
#17929=VERTEX_POINT ( 'NONE', #98314 ) ;
#17933=CARTESIAN_POINT ( 'NONE',  ( 3.787259615384621192, -5.876774720514425177, 21.48076923076922640 ) ) ;
#17938=CARTESIAN_POINT ( 'NONE',  ( 6.179707021866671646, -5.876774720514425177, 21.45334750074374242 ) ) ;
#17950=CARTESIAN_POINT ( 'NONE',  ( -7.617563585130437076, -5.876774720514411854, 19.95084900476494383 ) ) ;
#17959=ORIENTED_EDGE ( 'NONE', *, *, #25901, .T. ) ;
#17961=CARTESIAN_POINT ( 'NONE',  ( 6.955725288069978696, -6.376774720514426065, 21.70430095680336890 ) ) ;
#17964=EDGE_CURVE ( 'NONE', #23326, #50923, #86041, .T. ) ;
#17965=DIRECTION ( 'NONE',  ( 0.9496245541219264785, 0.000000000000000000, 0.3133898629642195011 ) ) ;
#17969=VECTOR ( 'NONE', #78296, 1000.000000000000114 ) ;
#17976=ORIENTED_EDGE ( 'NONE', *, *, #93305, .T. ) ;
#17977=DIRECTION ( 'NONE',  ( -0.000000000000000000, -1.000000000000000000, -0.000000000000000000 ) ) ;
#17980=VERTEX_POINT ( 'NONE', #99317 ) ;
#17981=CARTESIAN_POINT ( 'NONE',  ( 2.590388488674697953, -6.376774720514415407, 19.94764386045124027 ) ) ;
#17990=PLANE ( 'NONE',  #2941 ) ;
#17995=EDGE_CURVE ( 'NONE', #96649, #15961, #53666, .T. ) ;
#17998=CARTESIAN_POINT ( 'NONE',  ( -6.741682653110981249, -0.3587747205144265483, 30.62569541381301619 ) ) ;
#18015=VERTEX_POINT ( 'NONE', #29311 ) ;
#18019=ORIENTED_EDGE ( 'NONE', *, *, #45555, .T. ) ;
#18022=VERTEX_POINT ( 'NONE', #46052 ) ;
#18027=ORIENTED_EDGE ( 'NONE', *, *, #88515, .F. ) ;
#18034=CARTESIAN_POINT ( 'NONE',  ( -24.90875734969025501, 5.965225279485572685, 30.00402280011862288 ) ) ;
#18035=EDGE_CURVE ( 'NONE', #90358, #5613, #22183, .T. ) ;
#18043=ORIENTED_EDGE ( 'NONE', *, *, #80633, .T. ) ;
#18044=EDGE_CURVE ( 'NONE', #62667, #71923, #56170, .T. ) ;
#18061=EDGE_CURVE ( 'NONE', #98531, #20076, #15586, .T. ) ;
#18062=DIRECTION ( 'NONE',  ( 1.000000000000000000, 0.000000000000000000, -2.168404344971008868E-16 ) ) ;
#18069=CARTESIAN_POINT ( 'NONE',  ( 2.598243466966731585, -6.376774720514413630, 20.31174627870924709 ) ) ;
#18071=CARTESIAN_POINT ( 'NONE',  ( 4.415069475862049231, -6.376774720514424288, 21.13806644168711557 ) ) ;
#18086=VERTEX_POINT ( 'NONE', #71891 ) ;
#18111=ORIENTED_EDGE ( 'NONE', *, *, #17729, .F. ) ;
#18116=EDGE_LOOP ( 'NONE', ( #34364, #77960, #68670, #16344 ) ) ;
#18119=CARTESIAN_POINT ( 'NONE',  ( 31.64143112576189765, -0.3587747205144265483, 14.03360796525321774 ) ) ;
#18121=ORIENTED_EDGE ( 'NONE', *, *, #26642, .F. ) ;
#18127=ORIENTED_EDGE ( 'NONE', *, *, #67198, .T. ) ;
#18130=CYLINDRICAL_SURFACE ( 'NONE', #42248, 3.060000000000000053 ) ;
#18133=VERTEX_POINT ( 'NONE', #64800 ) ;
#18145=AXIS2_PLACEMENT_3D ( 'NONE', #49120, #88671, #19142 ) ;
#18151=CARTESIAN_POINT ( 'NONE',  ( 29.71615239255367413, -4.563867803339911156, 27.78418661847934246 ) ) ;
#18160=CARTESIAN_POINT ( 'NONE',  ( -4.286263797015736595E-16, -4.056774720514426669, -3.500000000000000000 ) ) ;
#18163=EDGE_CURVE ( 'NONE', #80744, #64204, #13922, .T. ) ;
#18191=EDGE_CURVE ( 'NONE', #13725, #33057, #90596, .T. ) ;
#18196=LINE ( 'NONE', #17188, #34349 ) ;
#18197=DIRECTION ( 'NONE',  ( 5.238131417152343399E-15, 0.000000000000000000, -1.000000000000000000 ) ) ;
#18198=EDGE_LOOP ( 'NONE', ( #60927, #87393, #28449, #65498, #47694, #21931 ) ) ;
#18206=ORIENTED_EDGE ( 'NONE', *, *, #15175, .T. ) ;
#18213=CARTESIAN_POINT ( 'NONE',  ( -11.64875734969026233, -0.3587747205144265483, 31.02402280011862246 ) ) ;
#18220=AXIS2_PLACEMENT_3D ( 'NONE', #34380, #11041, #33877 ) ;
#18227=ORIENTED_EDGE ( 'NONE', *, *, #98310, .F. ) ;
#18243=CARTESIAN_POINT ( 'NONE',  ( -6.072964844751159497, -5.876774720514410077, 19.44316438561912008 ) ) ;
#18244=CARTESIAN_POINT ( 'NONE',  ( 3.672440828437461224, -5.876774720514403860, 18.52532110411518573 ) ) ;
#18258=VECTOR ( 'NONE', #29641, 1000.000000000000000 ) ;
#18270=FACE_OUTER_BOUND ( 'NONE', #19266, .T. ) ;
#18274=CARTESIAN_POINT ( 'NONE',  ( 3.050049012211247579, -6.376774720514426065, 21.53019692557248632 ) ) ;
#18282=CARTESIAN_POINT ( 'NONE',  ( -27.96875734969026084, -3.316774720514426456, 24.50402280011861933 ) ) ;
#18289=DIRECTION ( 'NONE',  ( 0.000000000000000000, 0.000000000000000000, 1.000000000000000000 ) ) ;
#18302=CARTESIAN_POINT ( 'NONE',  ( -0.02075734969026423599, -0.3587747205144213303, -0.08597719988137648983 ) ) ;
#18307=AXIS2_PLACEMENT_3D ( 'NONE', #13365, #66700, #97120 ) ;
#18317=CARTESIAN_POINT ( 'NONE',  ( 6.127395130496778641, -5.876774720514417183, 20.13872869980892943 ) ) ;
#18318=EDGE_LOOP ( 'NONE', ( #77533, #77212, #23385, #97434 ) ) ;
#18328=CIRCLE ( 'NONE', #96122, 0.8160000000000007248 ) ;
#18335=DIRECTION ( 'NONE',  ( 0.000000000000000000, -1.000000000000000000, 0.000000000000000000 ) ) ;
#18336=VECTOR ( 'NONE', #16521, 1000.000000000000000 ) ;
#18337=EDGE_CURVE ( 'NONE', #534, #99971, #84477, .T. ) ;
#18346=ORIENTED_EDGE ( 'NONE', *, *, #47666, .F. ) ;
#18354=VERTEX_POINT ( 'NONE', #99680 ) ;
#18359=VERTEX_POINT ( 'NONE', #46417 ) ;
#18363=CARTESIAN_POINT ( 'NONE',  ( 7.116579217368891541, -6.376774720514415407, 20.51774267661129869 ) ) ;
#18374=EDGE_LOOP ( 'NONE', ( #30323, #71689, #96482, #99079 ) ) ;
#18377=CIRCLE ( 'NONE', #21543, 129.7684398600581233 ) ;
#18380=FACE_OUTER_BOUND ( 'NONE', #14211, .T. ) ;
#18390=CARTESIAN_POINT ( 'NONE',  ( 5.329826657887789310, -5.876774720514418071, 20.66144943787464783 ) ) ;
#18393=ORIENTED_EDGE ( 'NONE', *, *, #66406, .T. ) ;
#18394=DIRECTION ( 'NONE',  ( -0.000000000000000000, 1.000000000000000000, -0.000000000000000000 ) ) ;
#18395=DIRECTION ( 'NONE',  ( 1.000000000000000000, 0.000000000000000000, 0.000000000000000000 ) ) ;
#18397=VECTOR ( 'NONE', #50363, 1000.000000000000000 ) ;
#18409=AXIS2_PLACEMENT_3D ( 'NONE', #38512, #22267, #29397 ) ;
#18414=CARTESIAN_POINT ( 'NONE',  ( -5.238752036864926964, -5.876774720514408301, 19.51517878119694061 ) ) ;
#18429=ORIENTED_EDGE ( 'NONE', *, *, #42383, .T. ) ;
#18449=ADVANCED_FACE ( 'NONE', ( #39799 ), #7473, .T. ) ;
#18455=ORIENTED_EDGE ( 'NONE', *, *, #19976, .F. ) ;
#18471=VERTEX_POINT ( 'NONE', #39298 ) ;
#18476=CARTESIAN_POINT ( 'NONE',  ( 2.710830299132254595, -6.376774720514410077, 19.05039662921485544 ) ) ;
#18479=ORIENTED_EDGE ( 'NONE', *, *, #3465, .F. ) ;
#18481=CARTESIAN_POINT ( 'NONE',  ( 24.71017632900190719, -5.356774720514427379, 1.647607965253213624 ) ) ;
#18487=CARTESIAN_POINT ( 'NONE',  ( 7.166666666666668739, -5.876774720514419847, 20.78665865384614975 ) ) ;
#18490=CARTESIAN_POINT ( 'NONE',  ( 32.23865423223558935, -4.540774720514431095, 2.161924922174277341 ) ) ;
#18494=LINE ( 'NONE', #17998, #52347 ) ;
#18497=CARTESIAN_POINT ( 'NONE',  ( 14.73162737928355170, -2.682774720514426559, -27.37940951657878941 ) ) ;
#18504=LINE ( 'NONE', #79900, #38520 ) ;
#18509=CARTESIAN_POINT ( 'NONE',  ( 5.184553252003285984, 5.965225279485572685, -28.06387035751381731 ) ) ;
#18512=VERTEX_POINT ( 'NONE', #56550 ) ;
#18517=VECTOR ( 'NONE', #67039, 1000.000000000000000 ) ;
#18518=CARTESIAN_POINT ( 'NONE',  ( -5.941268476065055815, -6.376774720514417183, 20.11414146978959749 ) ) ;
#18519=ORIENTED_EDGE ( 'NONE', *, *, #50598, .F. ) ;
#18522=CARTESIAN_POINT ( 'NONE',  ( 30.46555845599590029, -5.356774720514427379, 2.040766579062852415 ) ) ;
#18523=ADVANCED_FACE ( 'NONE', ( #24567 ), #40309, .F. ) ;
#18530=ORIENTED_EDGE ( 'NONE', *, *, #10647, .T. ) ;
#18547=DIRECTION ( 'NONE',  ( 0.000000000000000000, -1.000000000000000000, 0.000000000000000000 ) ) ;
#18554=DIRECTION ( 'NONE',  ( -0.000000000000000000, 1.000000000000000000, -0.000000000000000000 ) ) ;
#18561=CARTESIAN_POINT ( 'NONE',  ( 30.93860345374796594, -0.6647747205144267646, 23.11160796525322070 ) ) ;
#18567=DIRECTION ( 'NONE',  ( -0.000000000000000000, 1.000000000000000000, -0.000000000000000000 ) ) ;
#18570=ORIENTED_EDGE ( 'NONE', *, *, #24774, .T. ) ;
#18583=CARTESIAN_POINT ( 'NONE',  ( 30.09341516180546350, -4.772774720514425972, -11.39311774897855933 ) ) ;
#18604=FACE_OUTER_BOUND ( 'NONE', #35058, .T. ) ;
#18607=EDGE_CURVE ( 'NONE', #42749, #14525, #21888, .T. ) ;
#18613=ADVANCED_FACE ( 'NONE', ( #61984 ), #23387, .F. ) ;
#18619=ORIENTED_EDGE ( 'NONE', *, *, #85580, .T. ) ;
#18622=ORIENTED_EDGE ( 'NONE', *, *, #50945, .F. ) ;
#18629=VERTEX_POINT ( 'NONE', #85814 ) ;
#18633=ORIENTED_EDGE ( 'NONE', *, *, #45769, .F. ) ;
#18643=CARTESIAN_POINT ( 'NONE',  ( -7.326845193947049140, -5.876774720514417183, 20.33046051580616265 ) ) ;
#18650=CARTESIAN_POINT ( 'NONE',  ( 5.271800844830267785, -3.316774720514427344, -28.56638892017480913 ) ) ;
#18659=CARTESIAN_POINT ( 'NONE',  ( -1.174900045708346497, -6.376774720514413630, 19.48569229636960998 ) ) ;
#18673=CARTESIAN_POINT ( 'NONE',  ( 15.58962545129235799, 6.475225279485573360, -26.91365498785467025 ) ) ;
#18679=VERTEX_POINT ( 'NONE', #16797 ) ;
#18684=CARTESIAN_POINT ( 'NONE',  ( -9.278253834636473130, -5.876774720514426953, 21.78128695274316229 ) ) ;
#18692=DIRECTION ( 'NONE',  ( 1.000000000000000000, 0.000000000000000000, 0.000000000000000000 ) ) ;
#18695=CARTESIAN_POINT ( 'NONE',  ( 3.797776442307698286, -6.376774720514427841, 21.83974358974358410 ) ) ;
#18700=AXIS2_PLACEMENT_3D ( 'NONE', #30440, #76597, #998 ) ;
#18704=EDGE_CURVE ( 'NONE', #4364, #16838, #55885, .T. ) ;
#18714=B_SPLINE_CURVE_WITH_KNOTS ( 'NONE', 3,
 ( #53429, #85355, #84357, #14841, #38177, #69137, #15839, #100059, #62535, #39183, #70139, #30574, #77229, #31067, #93463 ),
 .UNSPECIFIED., .F., .F.,
 ( 4, 1, 1, 1, 1, 1, 1, 1, 1, 1, 1, 1, 4 ),
 ( 0.000000000000000000, 0.07176606415833990116, 0.1412255357663689537, 0.2091158524974625343, 0.2748396534685271231, 0.3394829303752209260, 0.4024762667353996570, 0.4649418891713271162, 0.5268326406463837985, 0.6474148160608227398, 0.7655615117859490004, 0.8816150870393316685, 1.000000000000000000 ),
 .UNSPECIFIED. ) ;
#18716=CARTESIAN_POINT ( 'NONE',  ( 14.83405752585509596, -4.881907540129173384, -27.54622755360215791 ) ) ;
#18718=ADVANCED_FACE ( 'NONE', ( #25914 ), #94422, .T. ) ;
#18730=ORIENTED_EDGE ( 'NONE', *, *, #20439, .F. ) ;
#18735=CARTESIAN_POINT ( 'NONE',  ( 3.450324536843889067, -5.876774720514404748, 18.60429515659643229 ) ) ;
#18739=CARTESIAN_POINT ( 'NONE',  ( 7.805843057017202824, 6.475225279485576024, -27.15467198446602026 ) ) ;
#18749=EDGE_CURVE ( 'NONE', #37181, #45653, #36752, .T. ) ;
#18751=VECTOR ( 'NONE', #60529, 1000.000000000000000 ) ;
#18752=ORIENTED_EDGE ( 'NONE', *, *, #45221, .T. ) ;
#18756=EDGE_CURVE ( 'NONE', #91151, #58098, #38337, .T. ) ;
#18758=ORIENTED_EDGE ( 'NONE', *, *, #25024, .F. ) ;
#18759=CARTESIAN_POINT ( 'NONE',  ( 0.3627416911114360598, -5.876774720514411854, 19.59793130852656873 ) ) ;
#18765=CARTESIAN_POINT ( 'NONE',  ( -19.80875734969026425, 5.965225279485572685, 31.02402280011862246 ) ) ;
#18785=VECTOR ( 'NONE', #83775, 1000.000000000000000 ) ;
#18794=VECTOR ( 'NONE', #97333, 1000.000000000000000 ) ;
#18795=DIRECTION ( 'NONE',  ( 1.252131230780251742E-15, -6.886721769291384876E-15, 1.000000000000000000 ) ) ;
#18800=AXIS2_PLACEMENT_3D ( 'NONE', #43921, #74852, #36309 ) ;
#18803=CARTESIAN_POINT ( 'NONE',  ( 30.53060340732035982, -0.6647747205144264315, 20.86760796525322093 ) ) ;
#18807=CARTESIAN_POINT ( 'NONE',  ( -7.640476926272304681, -5.876774720514415407, 20.25188360057253689 ) ) ;
#18818=AXIS2_PLACEMENT_3D ( 'NONE', #95041, #25533, #56503 ) ;
#18820=PLANE ( 'NONE',  #87515 ) ;
#18826=EDGE_CURVE ( 'NONE', #51471, #34388, #62615, .T. ) ;
#18831=VERTEX_POINT ( 'NONE', #3591 ) ;
#18840=VECTOR ( 'NONE', #23280, 1000.000000000000227 ) ;
#18849=EDGE_LOOP ( 'NONE', ( #27123, #60728, #96602, #56395, #68823 ) ) ;
#18850=CARTESIAN_POINT ( 'NONE',  ( 6.996935307331598075, -6.376774720514424288, 21.22729008382901128 ) ) ;
#18853=AXIS2_PLACEMENT_3D ( 'NONE', #53802, #62418, #60919 ) ;
#18863=ORIENTED_EDGE ( 'NONE', *, *, #9000, .F. ) ;
#18865=CARTESIAN_POINT ( 'NONE',  ( 2.677564053859940341, -5.876774720514407413, 19.16116138973293559 ) ) ;
#18867=VECTOR ( 'NONE', #41042, 1000.000000000000000 ) ;
#18868=FACE_OUTER_BOUND ( 'NONE', #54527, .T. ) ;
#18869=LINE ( 'NONE', #33099, #77211 ) ;
#18873=ORIENTED_EDGE ( 'NONE', *, *, #61831, .F. ) ;
#18874=ORIENTED_EDGE ( 'NONE', *, *, #34686, .T. ) ;
#18875=DIRECTION ( 'NONE',  ( 0.000000000000000000, 0.000000000000000000, 1.000000000000000000 ) ) ;
#18885=CARTESIAN_POINT ( 'NONE',  ( 6.763596848542221984, -5.876774720514425177, 21.40271460634751577 ) ) ;
#18886=VERTEX_POINT ( 'NONE', #73102 ) ;
#18893=CARTESIAN_POINT ( 'NONE',  ( 11.84174468958795323, 6.475225279485574248, -27.06880646454217043 ) ) ;
#18897=CARTESIAN_POINT ( 'NONE',  ( 30.93860345374796594, 6.475225279485573360, 19.84760796525321780 ) ) ;
#18903=LINE ( 'NONE', #3698, #26333 ) ;
#18904=ORIENTED_EDGE ( 'NONE', *, *, #54831, .F. ) ;
#18906=CARTESIAN_POINT ( 'NONE',  ( -5.576690828732316696, -5.876774720514415407, 20.34213149456667935 ) ) ;
#18911=AXIS2_PLACEMENT_3D ( 'NONE', #9932, #93658, #31773 ) ;
#18916=ORIENTED_EDGE ( 'NONE', *, *, #46341, .T. ) ;
#18919=VECTOR ( 'NONE', #59907, 1000.000000000000000 ) ;
#18922=CARTESIAN_POINT ( 'NONE',  ( 3.748501943728875574, -6.376774720514426065, 21.47917144995767558 ) ) ;
#18926=CARTESIAN_POINT ( 'NONE',  ( 30.77564450787169648, -1.682774720514426114, -9.689394075852828081 ) ) ;
#18927=VECTOR ( 'NONE', #83374, 1000.000000000000000 ) ;
#18929=FACE_OUTER_BOUND ( 'NONE', #96958, .T. ) ;
#18937=EDGE_CURVE ( 'NONE', #38118, #37689, #29051, .T. ) ;
#18940=CARTESIAN_POINT ( 'NONE',  ( 13.64113475014448618, -3.316774720514425567, -28.24100986136700442 ) ) ;
#18942=CARTESIAN_POINT ( 'NONE',  ( -7.536766146225033047, -6.376774720514411854, 19.63296556618507438 ) ) ;
#18945=ORIENTED_EDGE ( 'NONE', *, *, #96745, .F. ) ;
#18953=CARTESIAN_POINT ( 'NONE',  ( 6.830155907162054341, -6.376774720514427841, 21.76451523534627341 ) ) ;
#18964=VECTOR ( 'NONE', #66108, 1000.000000000000000 ) ;
#18966=PLANE ( 'NONE',  #31901 ) ;
#18972=DIRECTION ( 'NONE',  ( 0.000000000000000000, -1.000000000000000000, 0.000000000000000000 ) ) ;
#18974=ORIENTED_EDGE ( 'NONE', *, *, #44352, .T. ) ;
#18977=CARTESIAN_POINT ( 'NONE',  ( -4.854568188115255367, -5.876774720514410077, 19.46611907402017394 ) ) ;
#18982=CARTESIAN_POINT ( 'NONE',  ( 6.727829057902616761, -5.876774720514417183, 20.13865202822440281 ) ) ;
#18987=DIRECTION ( 'NONE',  ( -0.000000000000000000, 1.000000000000000000, -0.000000000000000000 ) ) ;
#18990=CARTESIAN_POINT ( 'NONE',  ( 3.165726958143470160, -5.876774720514421624, 21.14296526391294506 ) ) ;
#18993=VERTEX_POINT ( 'NONE', #15315 ) ;
#19000=LINE ( 'NONE', #3798, #67339 ) ;
#19011=DIRECTION ( 'NONE',  ( 0.000000000000000000, 0.000000000000000000, 1.000000000000000000 ) ) ;
#19012=EDGE_CURVE ( 'NONE', #56601, #63059, #92440, .T. ) ;
#19037=PLANE ( 'NONE',  #96082 ) ;
#19041=FACE_OUTER_BOUND ( 'NONE', #27552, .T. ) ;
#19048=DIRECTION ( 'NONE',  ( -0.5473879298857849962, 5.908253122965993883E-15, -0.8368789961609472972 ) ) ;
#19052=LINE ( 'NONE', #25668, #29009 ) ;
#19059=AXIS2_PLACEMENT_3D ( 'NONE', #24635, #55614, #56621 ) ;
#19063=CARTESIAN_POINT ( 'NONE',  ( 2.949406532984364393, -6.376774720514410077, 19.42899254576129664 ) ) ;
#19065=VECTOR ( 'NONE', #50328, 1000.000000000000114 ) ;
#19066=DIRECTION ( 'NONE',  ( 0.000000000000000000, 0.000000000000000000, 1.000000000000000000 ) ) ;
#19074=CYLINDRICAL_SURFACE ( 'NONE', #19211, 252.4458649670781085 ) ;
#19084=ORIENTED_EDGE ( 'NONE', *, *, #93827, .T. ) ;
#19099=CARTESIAN_POINT ( 'NONE',  ( 2.935461252226840401, -6.376774720514420736, 20.47627681611744777 ) ) ;
#19106=CARTESIAN_POINT ( 'NONE',  ( -1.041963229364719634, -5.876774720514417183, 20.24089781925592746 ) ) ;
#19111=VERTEX_POINT ( 'NONE', #79221 ) ;
#19116=ORIENTED_EDGE ( 'NONE', *, *, #49854, .T. ) ;
#19120=FACE_OUTER_BOUND ( 'NONE', #73882, .T. ) ;
#19122=ORIENTED_EDGE ( 'NONE', *, *, #91704, .F. ) ;
#19129=ORIENTED_EDGE ( 'NONE', *, *, #21906, .F. ) ;
#19141=B_SPLINE_CURVE_WITH_KNOTS ( 'NONE', 3,
 ( #81673, #27880, #4559, #74064, #65977, #11157, #73073, #64979, #96896, #95893, #12146, #42133, #66481, #11649, #26388, #18274, #34003, #58838, #49743, #49245, #26885, #20255, #57359, #88291, #42626, #73564, #51223 ),
 .UNSPECIFIED., .F., .F.,
 ( 4, 1, 1, 1, 1, 1, 1, 1, 1, 1, 1, 1, 1, 1, 1, 1, 1, 1, 1, 1, 1, 1, 1, 1, 4 ),
 ( 0.000000000000000000, 0.06506328961727787796, 0.1267731664665228408, 0.1855157632260783507, 0.2407646791677146292, 0.2929797960235977494, 0.3422503727797667206, 0.3889192861856601846, 0.4327756640583091396, 0.4746284326311175361, 0.5147746906379525589, 0.5536058934984424695, 0.5914264064311723912, 0.6280281199460664432, 0.6638036341103201732, 0.6989843361316636638, 0.7335914893067054798, 0.7676284691511399139, 0.8012083477865917791, 0.8342638397266231021, 0.8669806947287760357, 0.8997197415181603652, 0.9327019124985379550, 0.9661758834327495160, 1.000000000000000000 ),
 .UNSPECIFIED. ) ;
#19142=DIRECTION ( 'NONE',  ( 0.000000000000000000, 0.000000000000000000, 1.000000000000000000 ) ) ;
#19146=CARTESIAN_POINT ( 'NONE',  ( -6.815415664272417295, -6.376774720514410077, 19.46427715384223234 ) ) ;
#19151=CARTESIAN_POINT ( 'NONE',  ( 8.462785143989153269, -3.316774720514427344, -28.02084008811334215 ) ) ;
#19154=CARTESIAN_POINT ( 'NONE',  ( -1.358974358974357921, -6.376774720514420736, 20.75510817307693046 ) ) ;
#19164=CARTESIAN_POINT ( 'NONE',  ( -65.05438548721848235, -3.316774720514426456, 29.49402280011861777 ) ) ;
#19171=DIRECTION ( 'NONE',  ( 0.000000000000000000, -1.000000000000000000, 0.000000000000000000 ) ) ;
#19174=EDGE_CURVE ( 'NONE', #32707, #93325, #2621, .T. ) ;
#19182=CARTESIAN_POINT ( 'NONE',  ( -25.92875734969025814, -3.316774720514426456, 0.7300228001186309656 ) ) ;
#19190=FACE_OUTER_BOUND ( 'NONE', #36760, .T. ) ;
#19192=CARTESIAN_POINT ( 'NONE',  ( 282.9764569301858046, -1.682774720514426114, 20.79159422840526616 ) ) ;
#19193=ORIENTED_EDGE ( 'NONE', *, *, #81113, .T. ) ;
#19194=CARTESIAN_POINT ( 'NONE',  ( 6.127395130496778641, -6.376774720514417183, 20.13872869980892943 ) ) ;
#19198=CARTESIAN_POINT ( 'NONE',  ( 4.967622410992271753, -6.376774720514415407, 20.05703257908297843 ) ) ;
#19202=CARTESIAN_POINT ( 'NONE',  ( 0.000000000000000000, 1.477225279485574028, 19.84760796525321425 ) ) ;
#19206=EDGE_CURVE ( 'NONE', #49156, #98244, #74121, .T. ) ;
#19208=LINE ( 'NONE', #66419, #9590 ) ;
#19209=LINE ( 'NONE', #66910, #63118 ) ;
#19210=ORIENTED_EDGE ( 'NONE', *, *, #61754, .T. ) ;
#19211=AXIS2_PLACEMENT_3D ( 'NONE', #56664, #19573, #41937 ) ;
#19213=ORIENTED_EDGE ( 'NONE', *, *, #75882, .F. ) ;
#19218=CARTESIAN_POINT ( 'NONE',  ( -6.752792875861700850, -5.876774720514411854, 19.46247113826586528 ) ) ;
#19230=ORIENTED_EDGE ( 'NONE', *, *, #36492, .F. ) ;
#19236=CARTESIAN_POINT ( 'NONE',  ( 3.085011456917871264, -5.876774720514409189, 19.00082519311127172 ) ) ;
#19238=DIRECTION ( 'NONE',  ( -0.000000000000000000, -1.000000000000000000, -0.000000000000000000 ) ) ;
#19247=CARTESIAN_POINT ( 'NONE',  ( 5.730633878096764278, -5.876774720514418071, 20.45679216967608838 ) ) ;
#19249=CYLINDRICAL_SURFACE ( 'NONE', #60535, 91.74549126261076992 ) ;
#19254=VERTEX_POINT ( 'NONE', #11221 ) ;
#19257=DIRECTION ( 'NONE',  ( 0.000000000000000000, 1.000000000000000000, 0.000000000000000000 ) ) ;
#19266=EDGE_LOOP ( 'NONE', ( #58596, #42952, #28453, #50935 ) ) ;
#19270=AXIS2_PLACEMENT_3D ( 'NONE', #39327, #93111, #268 ) ;
#19283=CARTESIAN_POINT ( 'NONE',  ( 4.487249349319938574, -5.876774720514420736, 21.01618089687719504 ) ) ;
#19303=ADVANCED_FACE ( 'NONE', ( #50790 ), #42688, .T. ) ;
#19305=CARTESIAN_POINT ( 'NONE',  ( 5.641575934020636396, -5.876774720514419847, 20.76276410292889096 ) ) ;
#19314=EDGE_CURVE ( 'NONE', #18354, #88212, #19815, .T. ) ;
#19327=DIRECTION ( 'NONE',  ( 0.000000000000000000, 0.000000000000000000, -1.000000000000000000 ) ) ;
#19328=ORIENTED_EDGE ( 'NONE', *, *, #63219, .T. ) ;
#19329=VECTOR ( 'NONE', #15325, 1000.000000000000000 ) ;
#19350=ORIENTED_EDGE ( 'NONE', *, *, #83136, .F. ) ;
#19357=CARTESIAN_POINT ( 'NONE',  ( 0.3910256410256441884, -6.376774720514427841, 21.75000000000000000 ) ) ;
#19362=ORIENTED_EDGE ( 'NONE', *, *, #59115, .T. ) ;
#19366=DIRECTION ( 'NONE',  ( 0.000000000000000000, 1.000000000000000000, 0.000000000000000000 ) ) ;
#19369=DIRECTION ( 'NONE',  ( -0.09721092304694051167, 0.000000000000000000, 0.9952638024365005887 ) ) ;
#19373=ORIENTED_EDGE ( 'NONE', *, *, #98934, .F. ) ;
#19382=CARTESIAN_POINT ( 'NONE',  ( 7.480769230769231726, -6.376774720514420736, 20.77403846153845635 ) ) ;
#19385=CARTESIAN_POINT ( 'NONE',  ( 6.996935307331598075, -6.376774720514424288, 21.22729008382901128 ) ) ;
#19397=AXIS2_PLACEMENT_3D ( 'NONE', #32896, #33383, #31893 ) ;
#19409=EDGE_CURVE ( 'NONE', #78997, #81513, #46170, .T. ) ;
#19417=VECTOR ( 'NONE', #88880, 1000.000000000000000 ) ;
#19422=DIRECTION ( 'NONE',  ( 0.6599726524652352877, 0.000000000000000000, -0.7512896232465891000 ) ) ;
#19423=VECTOR ( 'NONE', #43378, 1000.000000000000000 ) ;
#19440=CARTESIAN_POINT ( 'NONE',  ( 8.422997646657599091, -6.376774720514429617, -25.04887774224060237 ) ) ;
#19444=VERTEX_POINT ( 'NONE', #84214 ) ;
#19445=DIRECTION ( 'NONE',  ( -0.000000000000000000, 1.000000000000000000, -0.000000000000000000 ) ) ;
#19447=ORIENTED_EDGE ( 'NONE', *, *, #78705, .F. ) ;
#19462=CIRCLE ( 'NONE', #32441, 129.7684398600581517 ) ;
#19466=DIRECTION ( 'NONE',  ( 0.000000000000000000, 0.000000000000000000, -1.000000000000000000 ) ) ;
#19467=CARTESIAN_POINT ( 'NONE',  ( 0.000000000000000000, 1.477225279485574028, 0.000000000000000000 ) ) ;
#19468=DIRECTION ( 'NONE',  ( 0.000000000000000000, 0.000000000000000000, 1.000000000000000000 ) ) ;
#19469=VERTEX_POINT ( 'NONE', #82721 ) ;
#19479=DIRECTION ( 'NONE',  ( -0.000000000000000000, 1.000000000000000000, -0.000000000000000000 ) ) ;
#19480=CARTESIAN_POINT ( 'NONE',  ( 6.431189903846153300, -5.876774720514424288, 20.08974358974358765 ) ) ;
#19484=LINE ( 'NONE', #57576, #20515 ) ;
#19486=CARTESIAN_POINT ( 'NONE',  ( 33.08751910920749140, -4.671536413567966228, -11.65282283138775377 ) ) ;
#19488=LINE ( 'NONE', #51949, #2161 ) ;
#19490=B_SPLINE_CURVE_WITH_KNOTS ( 'NONE', 3,
 ( #67866, #5947, #37412, #19671, #68358, #21168, #4473 ),
 .UNSPECIFIED., .F., .F.,
 ( 4, 1, 1, 1, 4 ),
 ( 0.000000000000000000, 0.2537340756906634187, 0.5030351201318574716, 0.7500135973308806880, 1.000000000000000000 ),
 .UNSPECIFIED. ) ;
#19493=CARTESIAN_POINT ( 'NONE',  ( 15.22325621495362391, -2.682774720514426559, -27.23549315679322547 ) ) ;
#19499=AXIS2_PLACEMENT_3D ( 'NONE', #54672, #1881, #9485 ) ;
#19507=DIRECTION ( 'NONE',  ( 0.000000000000000000, 0.000000000000000000, 1.000000000000000000 ) ) ;
#19515=EDGE_LOOP ( 'NONE', ( #67492, #81650, #70828, #97348 ) ) ;
#19519=CARTESIAN_POINT ( 'NONE',  ( -10.24059822343757808, -5.876774720514426953, 17.17691942396160698 ) ) ;
#19522=EDGE_CURVE ( 'NONE', #53541, #24982, #8208, .T. ) ;
#19529=CARTESIAN_POINT ( 'NONE',  ( 2.628295812946869425, -5.876774720514412742, 19.40849182188139110 ) ) ;
#19536=ORIENTED_EDGE ( 'NONE', *, *, #5596, .T. ) ;
#19550=CARTESIAN_POINT ( 'NONE',  ( 10.24059822343757808, -6.376774720514426953, 0.000000000000000000 ) ) ;
#19558=CARTESIAN_POINT ( 'NONE',  ( 14.92699176545193573, -5.063793094955947538, -27.26229911407732942 ) ) ;
#19559=VECTOR ( 'NONE', #15021, 1000.000000000000000 ) ;
#19562=VECTOR ( 'NONE', #24087, 1000.000000000000000 ) ;
#19564=CARTESIAN_POINT ( 'NONE',  ( 2.903846153846159517, -6.376774720514415407, 19.99999999999999289 ) ) ;
#19571=PLANE ( 'NONE',  #56530 ) ;
#19573=DIRECTION ( 'NONE',  ( -0.000000000000000000, 1.000000000000000000, -0.000000000000000000 ) ) ;
#19592=CARTESIAN_POINT ( 'NONE',  ( 13.91401389203221406, 5.965225279485572685, 158.0376437107427137 ) ) ;
#19602=EDGE_CURVE ( 'NONE', #96476, #58114, #39554, .T. ) ;
#19606=B_SPLINE_CURVE_WITH_KNOTS ( 'NONE', 3,
 ( #8889, #40342, #26114, #64711, #10386, #32722, #62693 ),
 .UNSPECIFIED., .F., .F.,
 ( 4, 1, 1, 1, 4 ),
 ( 0.000000000000000000, 0.2537340756906609762, 0.5030351201318566945, 0.7500135973308793558, 1.000000000000000000 ),
 .UNSPECIFIED. ) ;
#19613=ORIENTED_EDGE ( 'NONE', *, *, #62876, .T. ) ;
#19616=ORIENTED_EDGE ( 'NONE', *, *, #47821, .T. ) ;
#19626=LINE ( 'NONE', #12515, #69627 ) ;
#19633=ORIENTED_EDGE ( 'NONE', *, *, #39155, .F. ) ;
#19642=DIRECTION ( 'NONE',  ( 0.000000000000000000, -1.000000000000000000, 0.000000000000000000 ) ) ;
#19650=CARTESIAN_POINT ( 'NONE',  ( 3.036358173076929123, -5.876774720514420736, 20.87990785256409865 ) ) ;
#19654=CARTESIAN_POINT ( 'NONE',  ( -0.9257915630711897048, -5.876774720514408301, 19.25892998154168012 ) ) ;
#19661=DIRECTION ( 'NONE',  ( 0.000000000000000000, 1.000000000000000000, 0.000000000000000000 ) ) ;
#19665=CARTESIAN_POINT ( 'NONE',  ( 11.62916340711181284, 5.965225279485572685, 28.75961759920349792 ) ) ;
#19668=CARTESIAN_POINT ( 'NONE',  ( 9.278253834636469577, -6.376774720514426953, 18.51871304725684553 ) ) ;
#19671=CARTESIAN_POINT ( 'NONE',  ( -4.752075056065355518, -6.376774720514406525, 19.17724329193115551 ) ) ;
#19675=FACE_OUTER_BOUND ( 'NONE', #64059, .T. ) ;
#19686=CARTESIAN_POINT ( 'NONE',  ( 5.642655980204820843, -6.376774720514418959, 20.71586687040766961 ) ) ;
#19695=CARTESIAN_POINT ( 'NONE',  ( -27.13414387080440093, -0.3587747205144061202, -10.21530720150730609 ) ) ;
#19702=DIRECTION ( 'NONE',  ( -3.639962309748244178E-15, -1.000000000000000000, 2.135627652102599075E-15 ) ) ;
#19706=EDGE_LOOP ( 'NONE', ( #34948, #21789, #25513, #10580, #75410, #44750, #37957, #55344, #81008, #77486, #61949, #35473, #9203, #88512, #95234, #42085 ) ) ;
#19714=DIRECTION ( 'NONE',  ( 0.000000000000000000, -1.000000000000000000, 0.000000000000000000 ) ) ;
#19720=ORIENTED_EDGE ( 'NONE', *, *, #97720, .T. ) ;
#19725=CIRCLE ( 'NONE', #1935, 253.2618649670780826 ) ;
#19730=CARTESIAN_POINT ( 'NONE',  ( 11.41483471809167405, 6.475225279485574248, -27.05170832580397189 ) ) ;
#19738=CARTESIAN_POINT ( 'NONE',  ( 5.641575934020636396, -6.376774720514420736, 20.76276410292889096 ) ) ;
#19741=ORIENTED_EDGE ( 'NONE', *, *, #32528, .F. ) ;
#19751=CARTESIAN_POINT ( 'NONE',  ( -0.02075734969026423599, 5.965225279485572685, -0.08597719988137648983 ) ) ;
#19757=ORIENTED_EDGE ( 'NONE', *, *, #54052, .T. ) ;
#19769=DIRECTION ( 'NONE',  ( -0.1254312216594016538, 0.000000000000000000, -0.9921023176230513441 ) ) ;
#19770=CARTESIAN_POINT ( 'NONE',  ( -11.64875734969026233, -0.3587747205144265483, 31.02402280011862246 ) ) ;
#19771=EDGE_CURVE ( 'NONE', #99974, #81663, #72515, .T. ) ;
#19776=DIRECTION ( 'NONE',  ( 1.000000000000000000, 0.000000000000000000, 0.000000000000000000 ) ) ;
#19778=CARTESIAN_POINT ( 'NONE',  ( 4.453188626415028217, -5.876774720514422512, 21.07953283331298167 ) ) ;
#19789=LINE ( 'NONE', #56390, #90697 ) ;
#19794=DIRECTION ( 'NONE',  ( 0.000000000000000000, -1.000000000000000000, 0.000000000000000000 ) ) ;
#19796=ORIENTED_EDGE ( 'NONE', *, *, #61018, .T. ) ;
#19812=CARTESIAN_POINT ( 'NONE',  ( 10.54059822343757880, -6.376774720514426953, 22.82308057603841078 ) ) ;
#19815=LINE ( 'NONE', #81731, #98295 ) ;
#19837=LINE ( 'NONE', #5625, #62486 ) ;
#19857=DIRECTION ( 'NONE',  ( 0.3133898629642195011, 5.365801633547218220E-16, -0.9496245541219264785 ) ) ;
#19861=B_SPLINE_SURFACE_WITH_KNOTS ( 'NONE', 3, 1, ( 
 ( #14032, #91661 ),
 ( #21639, #99756 ),
 ( #30261, #61240 ),
 ( #52119, #14536 ),
 ( #21149, #43997 ),
 ( #53125, #69330 ),
 ( #67350, #61739 ),
 ( #22141, #28775 ),
 ( #6437, #83043 ),
 ( #45512, #92656 ),
 ( #82555, #68341 ),
 ( #37393, #60737 ),
 ( #13038, #74930 ),
 ( #5435, #59738 ),
 ( #13533, #75430 ),
 ( #5931, #36884 ),
 ( #67851, #39382 ),
 ( #32266, #819 ),
 ( #94160, #47504 ) ),
 .UNSPECIFIED., .F., .F., .F.,
 ( 4, 1, 1, 1, 1, 1, 1, 1, 1, 1, 1, 1, 1, 1, 1, 1, 4 ),
 ( 2, 2 ),
 ( 0.000000000000000000, 0.07735147826526167503, 0.1497817737883350153, 0.2198699552839552540, 0.2879755066202374092, 0.3546781060271980701, 0.4187834319376945169, 0.4827347082469889417, 0.5473072519464179386, 0.5826981022599692084, 0.6240955651677930760, 0.6712929496345362290, 0.7243202075485730695, 0.7838489433400213091, 0.8494366971205804528, 0.9216570148063001344, 1.000000000000000000 ),
 ( 0.000000000000000000, 1.000000000000000000 ),
 .UNSPECIFIED. ) ;
#19877=CARTESIAN_POINT ( 'NONE',  ( 6.826756808399247589, -6.376774720514424288, 21.36722843294932161 ) ) ;
#19881=EDGE_CURVE ( 'NONE', #67682, #13448, #53670, .T. ) ;
#19882=EDGE_CURVE ( 'NONE', #87855, #44756, #93208, .T. ) ;
#19883=ORIENTED_EDGE ( 'NONE', *, *, #78299, .F. ) ;
#19897=ORIENTED_EDGE ( 'NONE', *, *, #69369, .F. ) ;
#19903=CARTESIAN_POINT ( 'NONE',  ( 4.038745349937860496, -5.876774720514428729, 21.81354843764681206 ) ) ;
#19912=ORIENTED_EDGE ( 'NONE', *, *, #72035, .F. ) ;
#19920=CARTESIAN_POINT ( 'NONE',  ( -28.49194798280535323, 5.965225279485572685, 28.38521343323375490 ) ) ;
#19924=CYLINDRICAL_SURFACE ( 'NONE', #66347, 11.85241003308275864 ) ;
#19925=FACE_OUTER_BOUND ( 'NONE', #8685, .T. ) ;
#19929=CARTESIAN_POINT ( 'NONE',  ( 7.166666666666668739, -6.376774720514420736, 20.78665865384614975 ) ) ;
#19931=ORIENTED_EDGE ( 'NONE', *, *, #55536, .F. ) ;
#19933=CARTESIAN_POINT ( 'NONE',  ( 3.787259615384621192, -6.376774720514426065, 21.48076923076922640 ) ) ;
#19935=CARTESIAN_POINT ( 'NONE',  ( 8.655157120174900243, -3.316774720514428232, -28.10018424651253000 ) ) ;
#19950=CARTESIAN_POINT ( 'NONE',  ( 13.10664265030973930, -0.3587747205144256601, -28.64597719988137570 ) ) ;
#19953=LINE ( 'NONE', #89974, #71368 ) ;
#19955=AXIS2_PLACEMENT_3D ( 'NONE', #63265, #9457, #54643 ) ;
#19973=LINE ( 'NONE', #82374, #66519 ) ;
#19976=EDGE_CURVE ( 'NONE', #32255, #33057, #40010, .T. ) ;
#19989=CARTESIAN_POINT ( 'NONE',  ( -1.044871794871793602, -5.876774720514418071, 20.44941907051282115 ) ) ;
#19996=ORIENTED_EDGE ( 'NONE', *, *, #52888, .T. ) ;
#19997=VECTOR ( 'NONE', #83543, 1000.000000000000000 ) ;
#20000=ORIENTED_EDGE ( 'NONE', *, *, #84718, .F. ) ;
#20002=FACE_OUTER_BOUND ( 'NONE', #61341, .T. ) ;
#20010=EDGE_LOOP ( 'NONE', ( #81405, #16896, #16853, #6779 ) ) ;
#20013=ADVANCED_FACE ( 'NONE', ( #34325 ), #89113, .F. ) ;
#20015=ORIENTED_EDGE ( 'NONE', *, *, #80046, .F. ) ;
#20016=DIRECTION ( 'NONE',  ( 0.000000000000000000, 0.000000000000000000, 1.000000000000000000 ) ) ;
#20033=AXIS2_PLACEMENT_3D ( 'NONE', #67208, #28627, #65720 ) ;
#20035=CARTESIAN_POINT ( 'NONE',  ( 2.650685085285006348, -5.876774720514410966, 19.28073557658628445 ) ) ;
#20036=CARTESIAN_POINT ( 'NONE',  ( -28.32169924589829080, -0.3587747205143964613, -8.244178532169451401 ) ) ;
#20040=AXIS2_PLACEMENT_3D ( 'NONE', #36495, #84164, #53236 ) ;
#20046=CARTESIAN_POINT ( 'NONE',  ( 30.93860345374796594, -0.6647747205144264315, 19.84760796525321780 ) ) ;
#20055=CARTESIAN_POINT ( 'NONE',  ( -25.92875734969026169, -5.356774720514426491, 23.50402280011861933 ) ) ;
#20056=CARTESIAN_POINT ( 'NONE',  ( -4.177535645411178500, -5.876774720514415407, 20.17598923696320767 ) ) ;
#20075=CARTESIAN_POINT ( 'NONE',  ( -2.599001758237162285, -6.376774720514413630, 19.60308799987317485 ) ) ;
#20076=VERTEX_POINT ( 'NONE', #82484 ) ;
#20082=DIRECTION ( 'NONE',  ( -0.000000000000000000, -1.000000000000000000, -0.000000000000000000 ) ) ;
#20089=LINE ( 'NONE', #58173, #58416 ) ;
#20092=CARTESIAN_POINT ( 'NONE',  ( 19.75748517575715368, -0.3587747205144265483, 28.87153971905864580 ) ) ;
#20093=DIRECTION ( 'NONE',  ( 0.000000000000000000, 0.000000000000000000, 1.000000000000000000 ) ) ;
#20099=ORIENTED_EDGE ( 'NONE', *, *, #96521, .F. ) ;
#20104=AXIS2_PLACEMENT_3D ( 'NONE', #23190, #72764, #47054 ) ;
#20117=ORIENTED_EDGE ( 'NONE', *, *, #5693, .F. ) ;
#20122=VERTEX_POINT ( 'NONE', #66794 ) ;
#20126=ORIENTED_EDGE ( 'NONE', *, *, #6284, .T. ) ;
#20140=B_SPLINE_SURFACE_WITH_KNOTS ( 'NONE', 3, 1, ( 
 ( #72546, #25858 ),
 ( #95371, #49220 ),
 ( #56833, #3038 ),
 ( #57337, #74039 ),
 ( #42604, #19730 ),
 ( #35482, #57829 ),
 ( #43096, #65950 ),
 ( #89262, #80651 ),
 ( #26364, #42105 ),
 ( #87766, #66454 ),
 ( #41600, #18739 ),
 ( #58325, #4535 ),
 ( #4032, #34976 ),
 ( #11136, #50207 ) ),
 .UNSPECIFIED., .F., .F., .F.,
 ( 4, 2, 2, 2, 2, 2, 4 ),
 ( 2, 2 ),
 ( 0.000000000000000000, 0.2500000000000001110, 0.3750000000000001110, 0.5000000000000002220, 0.6250000000000003331, 0.7500000000000004441, 1.000000000000000000 ),
 ( 0.000000000000000000, 1.000000000000000000 ),
 .UNSPECIFIED. ) ;
#20142=ORIENTED_EDGE ( 'NONE', *, *, #80614, .F. ) ;
#20146=CARTESIAN_POINT ( 'NONE',  ( 14.61581670307174008, -6.376774720514426953, -27.35847990810646024 ) ) ;
#20170=LINE ( 'NONE', #51132, #15060 ) ;
#20171=AXIS2_PLACEMENT_3D ( 'NONE', #71410, #64322, #24221 ) ;
#20182=DIRECTION ( 'NONE',  ( 0.000000000000000000, 0.000000000000000000, 1.000000000000000000 ) ) ;
#20184=CARTESIAN_POINT ( 'NONE',  ( -4.926336369345162502, -0.3587747205143967943, -28.61095484066305161 ) ) ;
#20189=CARTESIAN_POINT ( 'NONE',  ( 6.059061188053544988, -6.376774720514417183, 20.16803580207560742 ) ) ;
#20202=FACE_OUTER_BOUND ( 'NONE', #14818, .T. ) ;
#20208=ORIENTED_EDGE ( 'NONE', *, *, #36592, .T. ) ;
#20215=LINE ( 'NONE', #75001, #57429 ) ;
#20222=CARTESIAN_POINT ( 'NONE',  ( 7.041152093163508319, -5.876774720514424288, 21.17127001373575368 ) ) ;
#20224=ORIENTED_EDGE ( 'NONE', *, *, #2700, .F. ) ;
#20228=VECTOR ( 'NONE', #21920, 1000.000000000000000 ) ;
#20231=ORIENTED_EDGE ( 'NONE', *, *, #98722, .T. ) ;
#20235=ADVANCED_FACE ( 'NONE', ( #63670 ), #18966, .F. ) ;
#20244=DIRECTION ( 'NONE',  ( 0.000000000000000000, 0.000000000000000000, 1.000000000000000000 ) ) ;
#20255=CARTESIAN_POINT ( 'NONE',  ( 3.474198977381013798, -6.376774720514426065, 21.79108561604954986 ) ) ;
#20261=CARTESIAN_POINT ( 'NONE',  ( -3.054691362729579751, -6.376774720514413630, 19.78730719034165375 ) ) ;
#20270=CARTESIAN_POINT ( 'NONE',  ( 30.53060340732035982, -1.682774720514426114, -1.272392034746785860 ) ) ;
#20274=CARTESIAN_POINT ( 'NONE',  ( 3.902919446070569176, -5.876774720514426953, 21.47497695444087284 ) ) ;
#20293=VECTOR ( 'NONE', #83595, 1000.000000000000114 ) ;
#20295=CARTESIAN_POINT ( 'NONE',  ( 5.981014360695730225, -6.376774720514426065, 21.36744920115099333 ) ) ;
#20298=CARTESIAN_POINT ( 'NONE',  ( 13.86067930708168738, -5.152774720514425866, -28.23766061416633022 ) ) ;
#20299=FACE_OUTER_BOUND ( 'NONE', #84220, .T. ) ;
#20307=VECTOR ( 'NONE', #85107, 1000.000000000000000 ) ;
#20310=LINE ( 'NONE', #51281, #42188 ) ;
#20313=DIRECTION ( 'NONE',  ( 0.000000000000000000, 1.000000000000000000, 0.000000000000000000 ) ) ;
#20326=ORIENTED_EDGE ( 'NONE', *, *, #84590, .T. ) ;
#20329=ORIENTED_EDGE ( 'NONE', *, *, #84161, .F. ) ;
#20334=ORIENTED_EDGE ( 'NONE', *, *, #6926, .F. ) ;
#20342=DIRECTION ( 'NONE',  ( -0.000000000000000000, -1.000000000000000000, -0.000000000000000000 ) ) ;
#20375=CARTESIAN_POINT ( 'NONE',  ( 0.7051282051282027341, -5.876774720514409189, 19.19230769230768985 ) ) ;
#20393=EDGE_LOOP ( 'NONE', ( #35947, #8112, #59579, #35551 ) ) ;
#20394=CARTESIAN_POINT ( 'NONE',  ( 3.797776442307698286, -5.876774720514426953, 21.83974358974358410 ) ) ;
#20401=CARTESIAN_POINT ( 'NONE',  ( 2.922108196329484375, -5.876774720514417183, 20.36383711510645256 ) ) ;
#20404=EDGE_LOOP ( 'NONE', ( #9918, #85419, #61647, #72781 ) ) ;
#20406=CARTESIAN_POINT ( 'NONE',  ( 6.044871794871792048, -6.376774720514401196, 18.16025641025640880 ) ) ;
#20409=CARTESIAN_POINT ( 'NONE',  ( -7.131053040288445999, -6.376774720514413630, 19.60308799987318196 ) ) ;
#20413=CARTESIAN_POINT ( 'NONE',  ( 5.802984775641024662, -5.876774720514403860, 18.35026041666666430 ) ) ;
#20417=ORIENTED_EDGE ( 'NONE', *, *, #80491, .T. ) ;
#20420=CARTESIAN_POINT ( 'NONE',  ( 11.29837800214456855, -4.960377205085137575, -27.59811486027058436 ) ) ;
#20424=ADVANCED_FACE ( 'NONE', ( #4252 ), #68142, .T. ) ;
#20430=CARTESIAN_POINT ( 'NONE',  ( -1.409217194013772101, -5.876774720514417183, 20.11414146978959749 ) ) ;
#20435=VECTOR ( 'NONE', #27843, 1000.000000000000000 ) ;
#20437=VECTOR ( 'NONE', #55440, 1000.000000000000000 ) ;
#20439=EDGE_CURVE ( 'NONE', #36659, #21242, #93580, .T. ) ;
#20446=VERTEX_POINT ( 'NONE', #50427 ) ;
#20448=DIRECTION ( 'NONE',  ( -1.000000000000000000, 0.000000000000000000, 0.000000000000000000 ) ) ;
#20465=CARTESIAN_POINT ( 'NONE',  ( 6.044871794871792048, -6.376774720514401196, 18.16025641025640880 ) ) ;
#20470=ORIENTED_EDGE ( 'NONE', *, *, #71999, .F. ) ;
#20474=DIRECTION ( 'NONE',  ( 0.000000000000000000, -1.000000000000000000, 0.000000000000000000 ) ) ;
#20482=CARTESIAN_POINT ( 'NONE',  ( 3.296548071537245495, -5.876774720514426065, 21.29143507544719682 ) ) ;
#20487=VERTEX_POINT ( 'NONE', #41077 ) ;
#20492=CARTESIAN_POINT ( 'NONE',  ( -22.05275734969026047, 5.965225279485572685, 31.02402280011862246 ) ) ;
#20501=CARTESIAN_POINT ( 'NONE',  ( 7.166666666666668739, -6.376774720514414518, 20.78665865384614975 ) ) ;
#20506=ORIENTED_EDGE ( 'NONE', *, *, #56400, .F. ) ;
#20509=CARTESIAN_POINT ( 'NONE',  ( 30.61138385796263606, -5.156104205939422869, 27.19700247792284031 ) ) ;
#20515=VECTOR ( 'NONE', #18987, 1000.000000000000000 ) ;
#20518=VECTOR ( 'NONE', #5775, 1000.000000000000000 ) ;
#20540=CARTESIAN_POINT ( 'NONE',  ( 19.75748517575715368, -0.3587747205144265483, 28.87153971905864580 ) ) ;
#20541=LINE ( 'NONE', #35788, #92243 ) ;
#20543=CARTESIAN_POINT ( 'NONE',  ( 8.000000000000003553, -6.376774720514426953, 22.50000000000000355 ) ) ;
#20544=DIRECTION ( 'NONE',  ( -0.000000000000000000, -1.000000000000000000, -0.000000000000000000 ) ) ;
#20556=CARTESIAN_POINT ( 'NONE',  ( -0.5315124411682757843, -6.376774720514411854, 19.46509473978807847 ) ) ;
#20557=CARTESIAN_POINT ( 'NONE',  ( 22.81105451610979173, -500000.0000000000582, -18.46691820600746681 ) ) ;
#20564=CARTESIAN_POINT ( 'NONE',  ( -1.044792363895550302, -5.876774720514417183, 20.41272575174754422 ) ) ;
#20568=CARTESIAN_POINT ( 'NONE',  ( -10.54059822343757880, -5.876774720514426953, 22.82308057603841078 ) ) ;
#20570=AXIS2_PLACEMENT_3D ( 'NONE', #23876, #55859, #86785 ) ;
#20588=DIRECTION ( 'NONE',  ( 0.000000000000000000, 0.000000000000000000, 1.000000000000000000 ) ) ;
#20591=VECTOR ( 'NONE', #89524, 1000.000000000000000 ) ;
#20592=CARTESIAN_POINT ( 'NONE',  ( 10.86264265030973952, 5.965225279485574461, -28.64597719988137570 ) ) ;
#20602=CARTESIAN_POINT ( 'NONE',  ( -2.806649551956928335, -5.876774720514410966, 19.35116211686183618 ) ) ;
#20609=CARTESIAN_POINT ( 'NONE',  ( 6.431189903846153300, -6.376774720514415407, 20.08974358974358765 ) ) ;
#20612=EDGE_CURVE ( 'NONE', #9578, #36415, #53917, .T. ) ;
#20618=ORIENTED_EDGE ( 'NONE', *, *, #13552, .T. ) ;
#20633=ORIENTED_EDGE ( 'NONE', *, *, #53140, .T. ) ;
#20640=FACE_OUTER_BOUND ( 'NONE', #26721, .T. ) ;
#20643=FACE_OUTER_BOUND ( 'NONE', #90300, .T. ) ;
#20666=FACE_OUTER_BOUND ( 'NONE', #91022, .T. ) ;
#20667=LINE ( 'NONE', #21165, #68519 ) ;
#20683=LINE ( 'NONE', #52644, #96201 ) ;
#20688=FACE_OUTER_BOUND ( 'NONE', #48339, .T. ) ;
#20692=CARTESIAN_POINT ( 'NONE',  ( 3.045412351277957175, -6.376774720514422512, 20.90433128744512814 ) ) ;
#20706=EDGE_LOOP ( 'NONE', ( #47417, #30361, #25350, #87386, #41958, #30611, #1531 ) ) ;
#20716=AXIS2_PLACEMENT_3D ( 'NONE', #30148, #61122, #8317 ) ;
#20728=AXIS2_PLACEMENT_3D ( 'NONE', #14234, #31979, #93872 ) ;
#20732=DIRECTION ( 'NONE',  ( 0.000000000000000000, -1.000000000000000000, 0.000000000000000000 ) ) ;
#20734=ORIENTED_EDGE ( 'NONE', *, *, #61964, .F. ) ;
#20740=CARTESIAN_POINT ( 'NONE',  ( 6.199338013146583393, -6.376774720514415407, 20.11757922567734980 ) ) ;
#20743=EDGE_LOOP ( 'NONE', ( #93308, #44060, #10746, #67534 ) ) ;
#20747=LINE ( 'NONE', #14132, #70911 ) ;
#20759=CARTESIAN_POINT ( 'NONE',  ( -3.103301570662693187, -6.376774720514418959, 20.14409848895067512 ) ) ;
#20760=CARTESIAN_POINT ( 'NONE',  ( 10.46399479596398052, -2.894108053847758377, -27.03001098546561209 ) ) ;
#20764=CARTESIAN_POINT ( 'NONE',  ( 9.402885806365684829, -0.3587747205144265483, 29.04108526060719342 ) ) ;
#20783=DIRECTION ( 'NONE',  ( 0.6451914333552730696, 0.000000000000000000, 0.7640209514960754067 ) ) ;
#20799=DIRECTION ( 'NONE',  ( 1.000000000000000000, 0.000000000000000000, 0.000000000000000000 ) ) ;
#20805=EDGE_CURVE ( 'NONE', #98963, #66356, #58797, .T. ) ;
#20807=VERTEX_POINT ( 'NONE', #64937 ) ;
#20808=CIRCLE ( 'NONE', #92085, 1.399999999999999911 ) ;
#20823=LINE ( 'NONE', #29943, #16079 ) ;
#20827=EDGE_CURVE ( 'NONE', #51970, #68195, #51456, .T. ) ;
#20838=LINE ( 'NONE', #77122, #95548 ) ;
#20839=ORIENTED_EDGE ( 'NONE', *, *, #62859, .F. ) ;
#20840=ORIENTED_EDGE ( 'NONE', *, *, #48438, .F. ) ;
#20854=AXIS2_PLACEMENT_3D ( 'NONE', #74890, #98225, #6884 ) ;
#20863=VERTEX_POINT ( 'NONE', #7002 ) ;
#20869=CARTESIAN_POINT ( 'NONE',  ( -6.487934372591614540, -5.876774720514411854, 19.49432735726520605 ) ) ;
#20873=VECTOR ( 'NONE', #53538, 999.9999999999998863 ) ;
#20877=CARTESIAN_POINT ( 'NONE',  ( -24.97666371003640506, -0.3587747205143964613, -15.72894043976419454 ) ) ;
#20881=CARTESIAN_POINT ( 'NONE',  ( 9.278253834636473130, -6.376774720514426953, 21.78128695274316229 ) ) ;
#20889=AXIS2_PLACEMENT_3D ( 'NONE', #28784, #5444, #76936 ) ;
#20901=CARTESIAN_POINT ( 'NONE',  ( -0.02075734969026423599, -0.3587747205144213303, -0.08597719988137648983 ) ) ;
#20905=EDGE_CURVE ( 'NONE', #69249, #77603, #75002, .T. ) ;
#20915=CARTESIAN_POINT ( 'NONE',  ( -7.318926569091948942, -6.376774720514417183, 20.09505574050193033 ) ) ;
#20918=DIRECTION ( 'NONE',  ( 0.000000000000000000, 0.000000000000000000, 1.000000000000000000 ) ) ;
#20926=DIRECTION ( 'NONE',  ( 0.7071067811865442421, 0.000000000000000000, 0.7071067811865507924 ) ) ;
#20927=CARTESIAN_POINT ( 'NONE',  ( 6.875727764383598561, -6.376774720514435835, -25.57138887952572404 ) ) ;
#20930=DIRECTION ( 'NONE',  ( 0.000000000000000000, 1.000000000000000000, 8.393823270855534040E-16 ) ) ;
#20935=CARTESIAN_POINT ( 'NONE',  ( -1.358974358974357921, -5.876774720514419847, 20.75510817307693046 ) ) ;
#20944=VERTEX_POINT ( 'NONE', #37948 ) ;
#20947=DIRECTION ( 'NONE',  ( 0.000000000000000000, -1.000000000000000000, 0.000000000000000000 ) ) ;
#20955=EDGE_CURVE ( 'NONE', #36399, #77096, #61306, .T. ) ;
#20959=DIRECTION ( 'NONE',  ( -0.1311553622875919756, 6.845827386180409975E-16, -0.9913618264504692190 ) ) ;
#20966=CARTESIAN_POINT ( 'NONE',  ( -29.49875734969026198, 5.965225279485572685, 0.1180228001186258285 ) ) ;
#20975=VERTEX_POINT ( 'NONE', #44570 ) ;
#20989=FACE_OUTER_BOUND ( 'NONE', #42173, .T. ) ;
#20992=CARTESIAN_POINT ( 'NONE',  ( -28.98875734969026396, -0.3587747205144265483, 10.11402280011862587 ) ) ;
#21009=FACE_OUTER_BOUND ( 'NONE', #88564, .T. ) ;
#21040=FACE_OUTER_BOUND ( 'NONE', #96218, .T. ) ;
#21043=CYLINDRICAL_SURFACE ( 'NONE', #48888, 1.399999999999999911 ) ;
#21051=CARTESIAN_POINT ( 'NONE',  ( -0.9827876235267493099, -6.376774720514415407, 19.81240905262004404 ) ) ;
#21064=AXIS2_PLACEMENT_3D ( 'NONE', #2620, #64541, #95451 ) ;
#21075=CARTESIAN_POINT ( 'NONE',  ( 30.09341516180546350, 1.477225279485574028, -13.09311774897855862 ) ) ;
#21082=CIRCLE ( 'NONE', #37255, 0.8160000000000007248 ) ;
#21098=CARTESIAN_POINT ( 'NONE',  ( -3.035630128403670192, -5.876774720514412742, 19.71630089903357685 ) ) ;
#21103=DIRECTION ( 'NONE',  ( 1.226388327005079762E-16, 0.000000000000000000, -1.000000000000000000 ) ) ;
#21107=DIRECTION ( 'NONE',  ( 0.000000000000000000, 1.000000000000000000, 0.000000000000000000 ) ) ;
#21110=DIRECTION ( 'NONE',  ( 0.000000000000000000, 0.000000000000000000, 1.000000000000000000 ) ) ;
#21113=ORIENTED_EDGE ( 'NONE', *, *, #74314, .F. ) ;
#21116=DIRECTION ( 'NONE',  ( 0.000000000000000000, -1.000000000000000000, 0.000000000000000000 ) ) ;
#21128=EDGE_CURVE ( 'NONE', #2790, #32607, #58679, .T. ) ;
#21133=CYLINDRICAL_SURFACE ( 'NONE', #31096, 1.699999999999994849 ) ;
#21149=CARTESIAN_POINT ( 'NONE',  ( -2.457093156980370452, -6.376774720514411854, 19.51167604195716976 ) ) ;
#21151=DIRECTION ( 'NONE',  ( 0.000000000000000000, -1.000000000000000000, 0.000000000000000000 ) ) ;
#21165=CARTESIAN_POINT ( 'NONE',  ( 30.00738719773715601, -4.772774720514425972, -9.049252915307084422 ) ) ;
#21168=CARTESIAN_POINT ( 'NONE',  ( -4.977357939505175466, -6.376774720514410077, 19.14913681718893557 ) ) ;
#21177=CARTESIAN_POINT ( 'NONE',  ( 2.677468215678941110, -5.876774720514418959, 20.83735685176740304 ) ) ;
#21179=DIRECTION ( 'NONE',  ( 0.000000000000000000, -1.000000000000000000, 0.000000000000000000 ) ) ;
#21185=DIRECTION ( 'NONE',  ( -0.000000000000000000, 1.000000000000000000, -0.000000000000000000 ) ) ;
#21187=LINE ( 'NONE', #36920, #31766 ) ;
#21197=CARTESIAN_POINT ( 'NONE',  ( 6.698292889820671725, -5.876774720514424288, 21.80822233811499444 ) ) ;
#21208=ORIENTED_EDGE ( 'NONE', *, *, #35484, .T. ) ;
#21226=ORIENTED_EDGE ( 'NONE', *, *, #79158, .F. ) ;
#21238=CARTESIAN_POINT ( 'NONE',  ( 5.642655980204820843, -5.876774720514418071, 20.71586687040766961 ) ) ;
#21242=VERTEX_POINT ( 'NONE', #82013 ) ;
#21248=ORIENTED_EDGE ( 'NONE', *, *, #85743, .F. ) ;
#21250=DIRECTION ( 'NONE',  ( 0.000000000000000000, 0.000000000000000000, -1.000000000000000000 ) ) ;
#21268=DIRECTION ( 'NONE',  ( 0.000000000000000000, -1.000000000000000000, 0.000000000000000000 ) ) ;
#21273=LINE ( 'NONE', #13660, #39489 ) ;
#21280=CARTESIAN_POINT ( 'NONE',  ( -5.895658455092926076, -6.376774720514418959, 20.50445910983877340 ) ) ;
#21291=ORIENTED_EDGE ( 'NONE', *, *, #30050, .T. ) ;
#21294=CARTESIAN_POINT ( 'NONE',  ( 22.02124265030973760, 7.743225279485574042, 16.20402280011862217 ) ) ;
#21296=CARTESIAN_POINT ( 'NONE',  ( 33.00535138976576377, -3.570691370340801640, -12.97242311383999791 ) ) ;
#21297=ORIENTED_EDGE ( 'NONE', *, *, #93861, .T. ) ;
#21321=ORIENTED_EDGE ( 'NONE', *, *, #97312, .T. ) ;
#21322=LINE ( 'NONE', #30451, #25020 ) ;
#21324=FACE_OUTER_BOUND ( 'NONE', #19706, .T. ) ;
#21329=VECTOR ( 'NONE', #70855, 1000.000000000000000 ) ;
#21333=DIRECTION ( 'NONE',  ( -0.000000000000000000, 1.000000000000000000, -0.000000000000000000 ) ) ;
#21335=ORIENTED_EDGE ( 'NONE', *, *, #96959, .T. ) ;
#21350=VERTEX_POINT ( 'NONE', #61684 ) ;
#21352=AXIS2_PLACEMENT_3D ( 'NONE', #41783, #79318, #73711 ) ;
#21365=LINE ( 'NONE', #89400, #31907 ) ;
#21368=CARTESIAN_POINT ( 'NONE',  ( 5.399550031317772891, 1.324225279485572893, -28.54570968858208246 ) ) ;
#21372=CARTESIAN_POINT ( 'NONE',  ( 29.60442047479375205, -4.849628492681046232, 28.81422082199668466 ) ) ;
#21381=VECTOR ( 'NONE', #39366, 1000.000000000000227 ) ;
#21383=ORIENTED_EDGE ( 'NONE', *, *, #33756, .F. ) ;
#21391=DIRECTION ( 'NONE',  ( -2.910297583984928910E-15, -1.000000000000000000, 3.056206645085457922E-15 ) ) ;
#21394=ORIENTED_EDGE ( 'NONE', *, *, #88072, .T. ) ;
#21399=EDGE_CURVE ( 'NONE', #66223, #30337, #100195, .T. ) ;
#21405=CARTESIAN_POINT ( 'NONE',  ( -1.456683411003494966, -6.376774720514415407, 19.95737465391042775 ) ) ;
#21408=CARTESIAN_POINT ( 'NONE',  ( -7.326695514711824231, -6.376774720514417183, 20.26757654895259719 ) ) ;
#21415=DIRECTION ( 'NONE',  ( 4.472869286569333237E-16, -1.000000000000000000, -7.102795889480452575E-16 ) ) ;
#21416=CARTESIAN_POINT ( 'NONE',  ( 4.639188450898540594, -6.376774720514418959, 20.39229233339611014 ) ) ;
#21421=LINE ( 'NONE', #82831, #62401 ) ;
#21425=CARTESIAN_POINT ( 'NONE',  ( -1.380763273332680896, -5.876774720514418071, 20.28973052848695602 ) ) ;
#21426=LINE ( 'NONE', #90459, #18751 ) ;
#21445=CARTESIAN_POINT ( 'NONE',  ( -4.141025641025642301, -6.376774720514411854, 19.63681891025641235 ) ) ;
#21447=ORIENTED_EDGE ( 'NONE', *, *, #93486, .T. ) ;
#21448=CARTESIAN_POINT ( 'NONE',  ( 4.712727796232543120, -5.356774720514425603, -25.55789472434992859 ) ) ;
#21455=PLANE ( 'NONE',  #42176 ) ;
#21461=CARTESIAN_POINT ( 'NONE',  ( 13.91401389203221406, -3.316774720514426456, 158.0376437107427137 ) ) ;
#21469=EDGE_CURVE ( 'NONE', #14570, #18015, #90433, .T. ) ;
#21475=EDGE_LOOP ( 'NONE', ( #78469, #60073, #85366, #23629 ) ) ;
#21483=DIRECTION ( 'NONE',  ( 0.000000000000000000, 0.000000000000000000, -1.000000000000000000 ) ) ;
#21488=ORIENTED_EDGE ( 'NONE', *, *, #66648, .F. ) ;
#21489=ADVANCED_FACE ( 'NONE', ( #73284, #34224 ), #33719, .T. ) ;
#21495=VECTOR ( 'NONE', #76561, 1000.000000000000000 ) ;
#21498=CYLINDRICAL_SURFACE ( 'NONE', #38377, 28.45799999999999486 ) ;
#21501=CARTESIAN_POINT ( 'NONE',  ( 29.70220533163293908, -3.584876737299458771, 28.20564067568759015 ) ) ;
#21503=CARTESIAN_POINT ( 'NONE',  ( -0.02075734969026423599, -3.316774720514426456, -0.08597719988137648983 ) ) ;
#21504=VECTOR ( 'NONE', #12568, 1000.000000000000227 ) ;
#21513=CARTESIAN_POINT ( 'NONE',  ( 2.747717285871495108, -5.876774720514405637, 18.94713297040818034 ) ) ;
#21514=CYLINDRICAL_SURFACE ( 'NONE', #25490, 0.2999999999999981570 ) ;
#21523=DIRECTION ( 'NONE',  ( -1.000000000000000000, 0.000000000000000000, -0.000000000000000000 ) ) ;
#21527=ADVANCED_FACE ( 'NONE', ( #87504 ), #17990, .F. ) ;
#21532=DIRECTION ( 'NONE',  ( 0.000000000000000000, -1.000000000000000000, 0.000000000000000000 ) ) ;
#21534=CARTESIAN_POINT ( 'NONE',  ( -4.743266218460161276, -5.876774720514413630, 19.49357334786887108 ) ) ;
#21538=AXIS2_PLACEMENT_3D ( 'NONE', #50217, #11636, #2545 ) ;
#21543=AXIS2_PLACEMENT_3D ( 'NONE', #62257, #56150, #40414 ) ;
#21546=CARTESIAN_POINT ( 'NONE',  ( -1.540913562699879114, -6.376774720514410077, 19.44316438561912008 ) ) ;
#21553=VERTEX_POINT ( 'NONE', #79880 ) ;
#21555=CARTESIAN_POINT ( 'NONE',  ( 25.05730599792489599, -2.682774720540237468, -18.59674224247002172 ) ) ;
#21560=ORIENTED_EDGE ( 'NONE', *, *, #65875, .T. ) ;
#21573=LINE ( 'NONE', #53556, #17122 ) ;
#21577=CARTESIAN_POINT ( 'NONE',  ( 4.190829928318763109, -6.376774720514401196, 18.23548058298382557 ) ) ;
#21590=CARTESIAN_POINT ( 'NONE',  ( -0.7827064370038755436, -5.876774720514410966, 19.55912026249540148 ) ) ;
#21601=CARTESIAN_POINT ( 'NONE',  ( 4.017909867803298063, -6.376774720514402972, 18.55402206357357286 ) ) ;
#21613=ORIENTED_EDGE ( 'NONE', *, *, #61338, .F. ) ;
#21623=CARTESIAN_POINT ( 'NONE',  ( -10.15655021453082263, -4.851073166933324465, 30.10912256999369774 ) ) ;
#21625=DIRECTION ( 'NONE',  ( -0.000000000000000000, 1.000000000000000000, -0.000000000000000000 ) ) ;
#21634=LINE ( 'NONE', #95908, #67654 ) ;
#21637=FACE_OUTER_BOUND ( 'NONE', #40453, .T. ) ;
#21639=CARTESIAN_POINT ( 'NONE',  ( -2.220741593810419801, -6.376774720514411854, 19.46247113826587238 ) ) ;
#21650=VECTOR ( 'NONE', #13419, 1000.000000000000000 ) ;
#21654=CARTESIAN_POINT ( 'NONE',  ( -4.141025641025638748, -5.876774720514426953, 21.75000000000000355 ) ) ;
#21665=CARTESIAN_POINT ( 'NONE',  ( 28.30015606816038698, 1.477225279485574028, -13.13501953239208930 ) ) ;
#21668=VERTEX_POINT ( 'NONE', #74275 ) ;
#21670=DIRECTION ( 'NONE',  ( 0.000000000000000000, 0.000000000000000000, 1.000000000000000000 ) ) ;
#21690=LINE ( 'NONE', #52661, #20293 ) ;
#21695=CARTESIAN_POINT ( 'NONE',  ( -4.465079497292244959, -5.876774720514410077, 19.29815762497054976 ) ) ;
#21712=ORIENTED_EDGE ( 'NONE', *, *, #29854, .F. ) ;
#21719=ORIENTED_EDGE ( 'NONE', *, *, #33179, .F. ) ;
#21723=CARTESIAN_POINT ( 'NONE',  ( 4.856316114246853388, -6.376774720514408301, 19.03119074624055074 ) ) ;
#21733=FACE_OUTER_BOUND ( 'NONE', #12511, .T. ) ;
#21734=DIRECTION ( 'NONE',  ( -0.000000000000000000, 1.000000000000000000, -0.000000000000000000 ) ) ;
#21754=ORIENTED_EDGE ( 'NONE', *, *, #84391, .F. ) ;
#21762=CYLINDRICAL_SURFACE ( 'NONE', #44728, 4.299999999999999822 ) ;
#21763=CARTESIAN_POINT ( 'NONE',  ( 0.000000000000000000, -4.056774720514426669, 0.000000000000000000 ) ) ;
#21768=CARTESIAN_POINT ( 'NONE',  ( -10.21384395349166496, 6.475225279485573360, 29.49402280011861777 ) ) ;
#21777=LINE ( 'NONE', #90313, #1031 ) ;
#21787=CARTESIAN_POINT ( 'NONE',  ( 33.63416148851499088, -3.931067265920685561, -11.97433369283768734 ) ) ;
#21789=ORIENTED_EDGE ( 'NONE', *, *, #40097, .T. ) ;
#21799=CARTESIAN_POINT ( 'NONE',  ( -1.140932434931746582E-13, -6.376774720514426953, 21.78128695274321203 ) ) ;
#21800=ORIENTED_EDGE ( 'NONE', *, *, #88846, .T. ) ;
#21809=CARTESIAN_POINT ( 'NONE',  ( 5.654014271574485662, -5.876774720514419847, 20.92503208403226722 ) ) ;
#21811=CARTESIAN_POINT ( 'NONE',  ( 33.74124265030975067, -3.622774720514426949, -12.32597719988138252 ) ) ;
#21827=ORIENTED_EDGE ( 'NONE', *, *, #59642, .T. ) ;
#21833=CARTESIAN_POINT ( 'NONE',  ( 6.697025426467099862, -6.376774720514424288, 21.43052570396496037 ) ) ;
#21834=CARTESIAN_POINT ( 'NONE',  ( 2.787364042957740651, -5.876774720514424288, 21.14548745790758488 ) ) ;
#21836=ORIENTED_EDGE ( 'NONE', *, *, #52356, .T. ) ;
#21858=VERTEX_POINT ( 'NONE', #54434 ) ;
#21859=CARTESIAN_POINT ( 'NONE',  ( -6.181720432442950219, -5.876774720514410966, 19.67464842890028720 ) ) ;
#21875=AXIS2_PLACEMENT_3D ( 'NONE', #8980, #39932, #33821 ) ;
#21876=PLANE ( 'NONE',  #24350 ) ;
#21884=PLANE ( 'NONE',  #59364 ) ;
#21888=LINE ( 'NONE', #52868, #88546 ) ;
#21890=AXIS2_PLACEMENT_3D ( 'NONE', #73890, #66296, #27718 ) ;
#21902=DIRECTION ( 'NONE',  ( -1.000000000000000000, -0.000000000000000000, 0.000000000000000000 ) ) ;
#21906=EDGE_CURVE ( 'NONE', #1896, #45069, #91997, .T. ) ;
#21915=CARTESIAN_POINT ( 'NONE',  ( -3.108974358974355923, -6.376774720514427841, 21.75000000000001066 ) ) ;
#21916=ADVANCED_FACE ( 'NONE', ( #39194 ), #70152, .T. ) ;
#21920=DIRECTION ( 'NONE',  ( 1.000000000000000000, 0.000000000000000000, -5.238131417152343399E-15 ) ) ;
#21923=CARTESIAN_POINT ( 'NONE',  ( -2.188401442307694289, -6.376774720514411854, 19.46153846153846700 ) ) ;
#21931=ORIENTED_EDGE ( 'NONE', *, *, #92161, .T. ) ;
#21944=ORIENTED_EDGE ( 'NONE', *, *, #85445, .F. ) ;
#21945=CARTESIAN_POINT ( 'NONE',  ( 30.93860345374796239, 5.965225279485572685, 26.43402280011862615 ) ) ;
#21962=AXIS2_PLACEMENT_3D ( 'NONE', #23810, #47167, #83713 ) ;
#21964=LINE ( 'NONE', #68165, #18927 ) ;
#21982=CARTESIAN_POINT ( 'NONE',  ( 5.399550031316281640, -0.3587747205144061202, -28.54570968857217395 ) ) ;
#21999=CARTESIAN_POINT ( 'NONE',  ( 20.59900142331985151, -4.215361659006737760, -17.99865718129769832 ) ) ;
#22000=CARTESIAN_POINT ( 'NONE',  ( 6.371704462700114924, -5.876774720514427841, 21.83798798526824214 ) ) ;
#22005=DIRECTION ( 'NONE',  ( -0.000000000000000000, 1.000000000000000000, -0.000000000000000000 ) ) ;
#22008=CARTESIAN_POINT ( 'NONE',  ( 2.884397429187188333, -6.376774720514406525, 18.67943752795919110 ) ) ;
#22031=VECTOR ( 'NONE', #44894, 1000.000000000000000 ) ;
#22034=LINE ( 'NONE', #68235, #75316 ) ;
#22036=CIRCLE ( 'NONE', #69060, 1.325999999999990298 ) ;
#22042=EDGE_CURVE ( 'NONE', #90366, #50837, #26491, .T. ) ;
#22043=EDGE_CURVE ( 'NONE', #87115, #33316, #26981, .T. ) ;
#22044=CARTESIAN_POINT ( 'NONE',  ( -1.030996059302438761, -6.376774720514415407, 20.06599527532949878 ) ) ;
#22049=CARTESIAN_POINT ( 'NONE',  ( -24.90875734969025501, -6.376774720514426953, 27.45402280011862572 ) ) ;
#22050=CARTESIAN_POINT ( 'NONE',  ( 0.000000000000000000, -5.876774720514426953, 15.00000000000000178 ) ) ;
#22053=DIRECTION ( 'NONE',  ( 1.000000000000000000, 0.000000000000000000, 0.000000000000000000 ) ) ;
#22059=VECTOR ( 'NONE', #49277, 1000.000000000000000 ) ;
#22060=ORIENTED_EDGE ( 'NONE', *, *, #75096, .T. ) ;
#22062=CARTESIAN_POINT ( 'NONE',  ( -10.54059822343757880, -5.876774720514426953, 22.82308057603841078 ) ) ;
#22072=CARTESIAN_POINT ( 'NONE',  ( 0.000000000000000000, -4.056774720514426669, 0.000000000000000000 ) ) ;
#22078=DIRECTION ( 'NONE',  ( 0.000000000000000000, 0.000000000000000000, 1.000000000000000000 ) ) ;
#22100=ORIENTED_EDGE ( 'NONE', *, *, #62191, .F. ) ;
#22101=VECTOR ( 'NONE', #66037, 1000.000000000000000 ) ;
#22102=DIRECTION ( 'NONE',  ( 0.000000000000000000, 1.478457507934778393E-16, -1.000000000000000000 ) ) ;
#22104=ORIENTED_EDGE ( 'NONE', *, *, #59460, .F. ) ;
#22105=ORIENTED_EDGE ( 'NONE', *, *, #807, .T. ) ;
#22106=VECTOR ( 'NONE', #65554, 1000.000000000000114 ) ;
#22125=LINE ( 'NONE', #53108, #57058 ) ;
#22130=ORIENTED_EDGE ( 'NONE', *, *, #29838, .F. ) ;
#22135=FACE_OUTER_BOUND ( 'NONE', #71568, .T. ) ;
#22141=CARTESIAN_POINT ( 'NONE',  ( -2.656471864501908975, -6.376774720514411854, 19.66116880005639800 ) ) ;
#22150=DIRECTION ( 'NONE',  ( -1.000000000000000000, 0.000000000000000000, 0.000000000000000000 ) ) ;
#22163=EDGE_CURVE ( 'NONE', #60537, #47938, #67759, .T. ) ;
#22171=VERTEX_POINT ( 'NONE', #28470 ) ;
#22178=CARTESIAN_POINT ( 'NONE',  ( 14.76093561896379214, 5.965225279485572685, -27.88148769130088667 ) ) ;
#22183=LINE ( 'NONE', #76970, #82026 ) ;
#22205=VECTOR ( 'NONE', #91011, 1000.000000000000000 ) ;
#22219=LINE ( 'NONE', #53202, #50733 ) ;
#22225=CARTESIAN_POINT ( 'NONE',  ( 4.967948717948723392, -5.876774720514413630, 20.00140224358974095 ) ) ;
#22230=LINE ( 'NONE', #7523, #83684 ) ;
#22231=DIRECTION ( 'NONE',  ( -0.6755245625654127117, 0.4376337494475115442, -0.5934166046845339437 ) ) ;
#22239=DIRECTION ( 'NONE',  ( 2.216313064514630211E-15, -7.253388211138789781E-15, 1.000000000000000000 ) ) ;
#22242=CARTESIAN_POINT ( 'NONE',  ( 12.66784028006542151, -2.682774720514427003, -27.12025593822526304 ) ) ;
#22251=ORIENTED_EDGE ( 'NONE', *, *, #72583, .T. ) ;
#22257=DIRECTION ( 'NONE',  ( -0.000000000000000000, 1.000000000000000000, -0.000000000000000000 ) ) ;
#22262=CARTESIAN_POINT ( 'NONE',  ( 11.62916340711181284, -0.3587747205144265483, 28.75961759920349792 ) ) ;
#22265=ORIENTED_EDGE ( 'NONE', *, *, #80751, .F. ) ;
#22266=DIRECTION ( 'NONE',  ( 0.000000000000000000, 1.000000000000000000, -8.673617379884035472E-16 ) ) ;
#22267=DIRECTION ( 'NONE',  ( -0.000000000000000000, -1.000000000000000000, -0.000000000000000000 ) ) ;
#22272=CARTESIAN_POINT ( 'NONE',  ( -5.891837592278976743, -5.876774720514418071, 20.62654306927474934 ) ) ;
#22293=CARTESIAN_POINT ( 'NONE',  ( -0.7067007548136460260, -5.876774720514410077, 19.51517878119693350 ) ) ;
#22300=VECTOR ( 'NONE', #71833, 1000.000000000000000 ) ;
#22312=ORIENTED_EDGE ( 'NONE', *, *, #94920, .T. ) ;
#22320=CYLINDRICAL_SURFACE ( 'NONE', #79304, 1.399999999999998579 ) ;
#22321=ADVANCED_FACE ( 'NONE', ( #92867 ), #77635, .F. ) ;
#22322=CYLINDRICAL_SURFACE ( 'NONE', #18853, 1.399999999999998579 ) ;
#22329=EDGE_LOOP ( 'NONE', ( #2668, #59752, #85789, #74626 ) ) ;
#22342=PLANE ( 'NONE',  #59528 ) ;
#22353=ORIENTED_EDGE ( 'NONE', *, *, #66242, .T. ) ;
#22356=CARTESIAN_POINT ( 'NONE',  ( 15.29947330337541445, -3.316774720514426456, -27.16854002387010780 ) ) ;
#22360=ORIENTED_EDGE ( 'NONE', *, *, #42902, .F. ) ;
#22363=EDGE_CURVE ( 'NONE', #78994, #25204, #36963, .T. ) ;
#22364=AXIS2_PLACEMENT_3D ( 'NONE', #14422, #68726, #14918 ) ;
#22374=LINE ( 'NONE', #83290, #98943 ) ;
#22398=ADVANCED_FACE ( 'NONE', ( #71048 ), #33980, .F. ) ;
#22405=CARTESIAN_POINT ( 'NONE',  ( 22.02124265030973760, 6.143225279485574397, 12.85402280011862430 ) ) ;
#22412=ORIENTED_EDGE ( 'NONE', *, *, #28014, .F. ) ;
#22418=CARTESIAN_POINT ( 'NONE',  ( -13.89275734969026388, 5.965225279485572685, 31.02402280011862246 ) ) ;
#22426=CARTESIAN_POINT ( 'NONE',  ( -29.49875734969025842, 5.965225279485572685, 15.62202280011862321 ) ) ;
#22427=DIRECTION ( 'NONE',  ( 0.000000000000000000, 0.000000000000000000, -1.000000000000000000 ) ) ;
#22428=VECTOR ( 'NONE', #62767, 1000.000000000000114 ) ;
#22432=CARTESIAN_POINT ( 'NONE',  ( 17.47419131657910185, -0.3587747205144265483, 28.31804950686278843 ) ) ;
#22441=ORIENTED_EDGE ( 'NONE', *, *, #47666, .T. ) ;
#22452=CARTESIAN_POINT ( 'NONE',  ( 0.3906119451836247425, -6.376774720514418959, 20.56083401959467594 ) ) ;
#22455=EDGE_LOOP ( 'NONE', ( #54896, #4708, #50803, #90998 ) ) ;
#22462=CARTESIAN_POINT ( 'NONE',  ( 32.01683625711453374, -5.152774720514459617, -11.91548796314834036 ) ) ;
#22467=ORIENTED_EDGE ( 'NONE', *, *, #72017, .T. ) ;
#22471=ORIENTED_EDGE ( 'NONE', *, *, #69482, .F. ) ;
#22477=EDGE_CURVE ( 'NONE', #20863, #71424, #34547, .T. ) ;
#22478=CARTESIAN_POINT ( 'NONE',  ( 5.271800844963591359, -0.3587747205143965168, -28.56638892015329745 ) ) ;
#22490=ORIENTED_EDGE ( 'NONE', *, *, #83931, .T. ) ;
#22491=EDGE_CURVE ( 'NONE', #83112, #18471, #66022, .T. ) ;
#22505=VECTOR ( 'NONE', #49752, 1000.000000000000000 ) ;
#22509=CIRCLE ( 'NONE', #30639, 252.4458649670781085 ) ;
#22512=ADVANCED_FACE ( 'NONE', ( #62268 ), #55161, .F. ) ;
#22543=VERTEX_POINT ( 'NONE', #32303 ) ;
#22545=CARTESIAN_POINT ( 'NONE',  ( -3.826923076923074429, -6.376774720514427841, 21.75000000000000355 ) ) ;
#22551=CARTESIAN_POINT ( 'NONE',  ( -0.3225169060639742624, -5.876774720514411854, 19.46611907402017749 ) ) ;
#22568=ORIENTED_EDGE ( 'NONE', *, *, #34194, .T. ) ;
#22570=ORIENTED_EDGE ( 'NONE', *, *, #79308, .F. ) ;
#22576=CARTESIAN_POINT ( 'NONE',  ( -0.4362980769230789257, -5.876774720514411854, 19.46153846153846345 ) ) ;
#22582=FACE_OUTER_BOUND ( 'NONE', #28570, .T. ) ;
#22590=ORIENTED_EDGE ( 'NONE', *, *, #60458, .T. ) ;
#22591=CARTESIAN_POINT ( 'NONE',  ( 4.647383884978952828, -6.376774720514411854, 19.72975307774251164 ) ) ;
#22621=CARTESIAN_POINT ( 'NONE',  ( 15.89146238746079831, -3.595713655330296188, -28.00617091144486182 ) ) ;
#22637=DIRECTION ( 'NONE',  ( -0.000000000000000000, 1.000000000000000000, -0.000000000000000000 ) ) ;
#22638=VECTOR ( 'NONE', #50615, 1000.000000000000000 ) ;
#22646=DIRECTION ( 'NONE',  ( 1.000000000000000000, 0.000000000000000000, 0.000000000000000000 ) ) ;
#22649=CARTESIAN_POINT ( 'NONE',  ( 14.61581670307174008, 6.475225279485573360, -27.35847990810646024 ) ) ;
#22653=CARTESIAN_POINT ( 'NONE',  ( -27.96875734969026084, -3.316774720514426456, -0.08597719988137648983 ) ) ;
#22662=CARTESIAN_POINT ( 'NONE',  ( 3.769931535195356620, -5.876774720514429617, 21.83933825178638699 ) ) ;
#22667=AXIS2_PLACEMENT_3D ( 'NONE', #27391, #66965, #41626 ) ;
#22680=DIRECTION ( 'NONE',  ( 2.439088438507244272E-15, -7.805083003223181985E-15, 1.000000000000000000 ) ) ;
#22687=CARTESIAN_POINT ( 'NONE',  ( -5.799455386767018439, -5.876774720514413630, 19.66076420632890276 ) ) ;
#22691=FACE_BOUND ( 'NONE', #7406, .T. ) ;
#22692=ORIENTED_EDGE ( 'NONE', *, *, #4975, .F. ) ;
#22701=ORIENTED_EDGE ( 'NONE', *, *, #83896, .T. ) ;
#22711=VERTEX_POINT ( 'NONE', #26194 ) ;
#22719=ORIENTED_EDGE ( 'NONE', *, *, #51229, .T. ) ;
#22720=CARTESIAN_POINT ( 'NONE',  ( 4.692776824272364422, -5.876774720514404748, 18.67160386110882442 ) ) ;
#22722=CARTESIAN_POINT ( 'NONE',  ( 27.86270917940689174, -0.3587747205144265483, 29.49402280011862487 ) ) ;
#22728=CARTESIAN_POINT ( 'NONE',  ( 6.377880655330028681, -6.376774720514424288, 21.48000012937543346 ) ) ;
#22730=VECTOR ( 'NONE', #24756, 1000.000000000000000 ) ;
#22733=CIRCLE ( 'NONE', #51881, 132.8284398600581824 ) ;
#22734=VERTEX_POINT ( 'NONE', #5222 ) ;
#22737=AXIS2_PLACEMENT_3D ( 'NONE', #21763, #21268, #92783 ) ;
#22739=VECTOR ( 'NONE', #84607, 1000.000000000000000 ) ;
#22756=LINE ( 'NONE', #16156, #5831 ) ;
#22760=FACE_OUTER_BOUND ( 'NONE', #56937, .T. ) ;
#22763=PLANE ( 'NONE',  #15217 ) ;
#22770=CARTESIAN_POINT ( 'NONE',  ( 14.61581670307174008, -2.682774720514426559, -27.35847990810646024 ) ) ;
#22778=EDGE_CURVE ( 'NONE', #10925, #43589, #53200, .T. ) ;
#22784=CARTESIAN_POINT ( 'NONE',  ( 33.60604063885286052, -3.409250796720436405, -11.91850954671862617 ) ) ;
#22785=ORIENTED_EDGE ( 'NONE', *, *, #69335, .T. ) ;
#22793=ORIENTED_EDGE ( 'NONE', *, *, #12644, .T. ) ;
#22817=CARTESIAN_POINT ( 'NONE',  ( 6.431189903846153300, -6.376774720514415407, 20.08974358974358765 ) ) ;
#22824=ORIENTED_EDGE ( 'NONE', *, *, #52103, .T. ) ;
#22828=ORIENTED_EDGE ( 'NONE', *, *, #80633, .F. ) ;
#22837=CARTESIAN_POINT ( 'NONE',  ( 25.04758448870090604, -5.021277251288436716, -9.725080715181634972 ) ) ;
#22845=ORIENTED_EDGE ( 'NONE', *, *, #77524, .T. ) ;
#22855=CARTESIAN_POINT ( 'NONE',  ( 15.03452642382691629, -3.688048319827653021, -27.40128341529669598 ) ) ;
#22861=ADVANCED_FACE ( 'NONE', ( #83598 ), #28826, .F. ) ;
#22863=EDGE_CURVE ( 'NONE', #43985, #42816, #67903, .T. ) ;
#22890=ADVANCED_FACE ( 'NONE', ( #92706 ), #7475, .T. ) ;
#22895=CARTESIAN_POINT ( 'NONE',  ( 32.65434780274890159, -3.991214330829748747, -3.988850826987774489 ) ) ;
#22896=CARTESIAN_POINT ( 'NONE',  ( -1.438454482798693146, -5.876774720514410077, 19.55848054040323092 ) ) ;
#22898=DIRECTION ( 'NONE',  ( -0.000000000000000000, 1.000000000000000000, -0.000000000000000000 ) ) ;
#22909=DIRECTION ( 'NONE',  ( -1.000000000000000000, 0.000000000000000000, 0.000000000000000000 ) ) ;
#22912=CARTESIAN_POINT ( 'NONE',  ( 5.742690948595683409, -5.876774720514426953, 21.62260900090680593 ) ) ;
#22936=ORIENTED_EDGE ( 'NONE', *, *, #79331, .T. ) ;
#22937=CARTESIAN_POINT ( 'NONE',  ( 0.3910256410256383042, -5.876774720514409189, 19.19230769230768985 ) ) ;
#22941=ORIENTED_EDGE ( 'NONE', *, *, #12707, .T. ) ;
#22942=CARTESIAN_POINT ( 'NONE',  ( 32.88562546571908740, -0.3587747205144265483, -5.083907541707153754 ) ) ;
#22943=CARTESIAN_POINT ( 'NONE',  ( 30.00738719773716667, -1.682774720514426114, -9.049252915307089751 ) ) ;
#22946=ADVANCED_FACE ( 'NONE', ( #57673 ), #88616, .T. ) ;
#22949=VERTEX_POINT ( 'NONE', #3394 ) ;
#22980=CARTESIAN_POINT ( 'NONE',  ( 30.79432203307449711, -6.272817126675294119, 0.6151397435758989563 ) ) ;
#22981=EDGE_CURVE ( 'NONE', #34332, #66516, #44652, .T. ) ;
#22984=ORIENTED_EDGE ( 'NONE', *, *, #71207, .F. ) ;
#22990=AXIS2_PLACEMENT_3D ( 'NONE', #95561, #25549, #65638 ) ;
#22993=DIRECTION ( 'NONE',  ( -0.000000000000000000, -1.000000000000000000, -0.000000000000000000 ) ) ;
#22996=ADVANCED_FACE ( 'NONE', ( #60174, #52547 ), #76359, .F. ) ;
#23001=DIRECTION ( 'NONE',  ( -0.8264557562326033668, 6.845827386180409975E-16, -0.5630016722799281448 ) ) ;
#23002=ORIENTED_EDGE ( 'NONE', *, *, #64627, .F. ) ;
#23006=AXIS2_PLACEMENT_3D ( 'NONE', #63482, #9165, #24389 ) ;
#23019=CARTESIAN_POINT ( 'NONE',  ( 4.415069475862049231, -6.376774720514424288, 21.13806644168711557 ) ) ;
#23029=CARTESIAN_POINT ( 'NONE',  ( 0.3791100739519297491, -5.876774720514418959, 20.35309744218306349 ) ) ;
#23030=CARTESIAN_POINT ( 'NONE',  ( 14.76093561896379214, 5.965225279485572685, -26.55548769130089681 ) ) ;
#23033=CARTESIAN_POINT ( 'NONE',  ( -7.641025641025641413, -5.876774720514418071, 20.36458333333334636 ) ) ;
#23037=VECTOR ( 'NONE', #25128, 1000.000000000000000 ) ;
#23040=B_SPLINE_SURFACE_WITH_KNOTS ( 'NONE', 3, 1, ( 
 ( #8781, #85391 ),
 ( #15881, #46846 ),
 ( #77765, #661 ),
 ( #62575, #87910 ),
 ( #65099, #89405 ),
 ( #41749, #49866 ),
 ( #4175, #18885 ),
 ( #19877, #65597 ),
 ( #43243, #50852 ),
 ( #72192, #41237 ),
 ( #19385, #11775 ),
 ( #58470, #97511 ),
 ( #35125, #81291 ),
 ( #96018, #42259 ),
 ( #81791, #11278 ),
 ( #12264, #2681 ),
 ( #79783, #34628 ),
 ( #72690, #89903 ),
 ( #33620, #88914 ) ),
 .UNSPECIFIED., .F., .F., .F.,
 ( 4, 1, 1, 1, 1, 1, 1, 1, 1, 1, 1, 1, 1, 1, 1, 1, 4 ),
 ( 2, 2 ),
 ( 0.000000000000000000, 0.06795034759975315808, 0.1332598223836991558, 0.1978002967596463879, 0.2608458295516827841, 0.3233192927503678593, 0.3862817224595723742, 0.4500615162333133634, 0.5152075844858158282, 0.5796407692199310180, 0.6418172023841524076, 0.7016924412115357335, 0.7607690981778945094, 0.8192540511346849685, 0.8787376269055532374, 0.9381582970160912138, 1.000000000000000000 ),
 ( 0.000000000000000000, 1.000000000000000000 ),
 .UNSPECIFIED. ) ;
#23043=EDGE_CURVE ( 'NONE', #78121, #68153, #21573, .T. ) ;
#23052=CARTESIAN_POINT ( 'NONE',  ( -0.3225169060639742624, -6.376774720514411854, 19.46611907402017749 ) ) ;
#23066=ORIENTED_EDGE ( 'NONE', *, *, #3044, .F. ) ;
#23067=CARTESIAN_POINT ( 'NONE',  ( 4.821763668436347849, -6.376774720514406525, 18.93074869776452829 ) ) ;
#23075=CARTESIAN_POINT ( 'NONE',  ( -4.165021623707020559, -5.876774720514417183, 20.26087634804756377 ) ) ;
#23081=LINE ( 'NONE', #54072, #62920 ) ;
#23085=CARTESIAN_POINT ( 'NONE',  ( -4.358143420448500116, -6.376774720514413630, 19.75705121608222115 ) ) ;
#23086=DIRECTION ( 'NONE',  ( -0.5473879298857849962, 5.908253122965993883E-15, -0.8368789961609472972 ) ) ;
#23087=EDGE_CURVE ( 'NONE', #89282, #70995, #7857, .T. ) ;
#23094=LINE ( 'NONE', #100207, #63324 ) ;
#23095=ORIENTED_EDGE ( 'NONE', *, *, #71968, .T. ) ;
#23097=DIRECTION ( 'NONE',  ( -0.1254312216594016538, 0.000000000000000000, -0.9921023176230513441 ) ) ;
#23102=CARTESIAN_POINT ( 'NONE',  ( 5.109298100551870725, -3.316774720514426456, -27.55941679637892250 ) ) ;
#23104=CARTESIAN_POINT ( 'NONE',  ( 30.93860345374796594, 6.475225279485573360, 29.23160796525321814 ) ) ;
#23112=EDGE_CURVE ( 'NONE', #62167, #96134, #56556, .T. ) ;
#23133=AXIS2_PLACEMENT_3D ( 'NONE', #42420, #81950, #66755 ) ;
#23145=CARTESIAN_POINT ( 'NONE',  ( -2.188401442307694289, -6.376774720514411854, 19.46153846153846700 ) ) ;
#23153=CARTESIAN_POINT ( 'NONE',  ( -24.90875734969025501, -6.376774720514426953, 26.43402280011862615 ) ) ;
#23155=CARTESIAN_POINT ( 'NONE',  ( 30.56047832681635867, 2.297196155479663826, 24.67598410064777070 ) ) ;
#23161=CARTESIAN_POINT ( 'NONE',  ( 3.552327343495968570, -5.876774720514427841, 21.81288606793570395 ) ) ;
#23171=EDGE_CURVE ( 'NONE', #14525, #22171, #245, .T. ) ;
#23179=EDGE_CURVE ( 'NONE', #32453, #2424, #93243, .T. ) ;
#23186=CARTESIAN_POINT ( 'NONE',  ( -5.654682302363691626, -6.376774720514410077, 19.41635569784906323 ) ) ;
#23190=CARTESIAN_POINT ( 'NONE',  ( 3.509873074917118085, 5.965225279485572685, 29.15869884040363758 ) ) ;
#23192=DIRECTION ( 'NONE',  ( 0.000000000000000000, -1.000000000000000000, 0.000000000000000000 ) ) ;
#23198=FACE_OUTER_BOUND ( 'NONE', #42599, .T. ) ;
#23209=VERTEX_POINT ( 'NONE', #40807 ) ;
#23219=ORIENTED_EDGE ( 'NONE', *, *, #62509, .F. ) ;
#23224=CARTESIAN_POINT ( 'NONE',  ( 27.86270917940689174, -0.3587747205144265483, 29.49402280011862487 ) ) ;
#23227=CARTESIAN_POINT ( 'NONE',  ( 4.115763745420833786, -6.376774720514402972, 18.20859014712428348 ) ) ;
#23237=VERTEX_POINT ( 'NONE', #54538 ) ;
#23246=ORIENTED_EDGE ( 'NONE', *, *, #68061, .T. ) ;
#23255=CARTESIAN_POINT ( 'NONE',  ( -7.999999999999996447, -5.876774720514426953, 22.50000000000000355 ) ) ;
#23273=( BOUNDED_SURFACE ( )  B_SPLINE_SURFACE ( 3, 2, ( 
 ( #43703, #52318, #44704 ),
 ( #75629, #75140, #50821 ),
 ( #11743, #74640, #12233 ),
 ( #42720, #43214, #82751 ),
 ( #67056, #66067, #4645 ),
 ( #73653, #4146, #58442 ),
 ( #59941, #97965, #35098 ),
 ( #96987, #66571, #89376 ) ),
 .UNSPECIFIED., .F., .F., .T. ) 
 B_SPLINE_SURFACE_WITH_KNOTS ( ( 4, 2, 2, 4 ),
 ( 3, 3 ),
 ( -2.579859069429257801E-16, 0.0001012599413938862529, 0.0002025198827880304918, 0.0004050397655763189695 ),
 ( 0.000000000000000000, 1.000000000000000000 ),
 .UNSPECIFIED. ) 
 GEOMETRIC_REPRESENTATION_ITEM ( )  RATIONAL_B_SPLINE_SURFACE ( (
 ( 1.000000000000000000, 0.8117984224358114620, 1.000000000000000000),
 ( 1.000000000000000000, 0.8431000163380804047, 1.000000000000000000),
 ( 1.000000000000000000, 0.8706302742274283357, 1.000000000000000000),
 ( 1.000000000000000000, 0.9180857590576141369, 1.000000000000000000),
 ( 1.000000000000000000, 0.9379650217683797031, 1.000000000000000000),
 ( 1.000000000000000000, 0.9847826944377771063, 1.000000000000000000),
 ( 1.000000000000000000, 1.000057331644988556, 1.000000000000000000),
 ( 1.000000000000000000, 1.000000000000000000, 1.000000000000000000) ) ) 
 REPRESENTATION_ITEM ( '' )  SURFACE ( )  );
#23280=DIRECTION ( 'NONE',  ( -0.7863974287229266169, -5.639749025771352497E-15, 0.6177208787939496570 ) ) ;
#23282=DIRECTION ( 'NONE',  ( 0.000000000000000000, -1.000000000000000000, 0.000000000000000000 ) ) ;
#23285=ORIENTED_EDGE ( 'NONE', *, *, #18163, .T. ) ;
#23296=CARTESIAN_POINT ( 'NONE',  ( -0.4362980769230789257, -6.376774720514411854, 19.46153846153846345 ) ) ;
#23302=CARTESIAN_POINT ( 'NONE',  ( 27.53860345374808105, -5.356774720496559894, 0.000000000000000000 ) ) ;
#23326=VERTEX_POINT ( 'NONE', #65179 ) ;
#23335=ORIENTED_EDGE ( 'NONE', *, *, #78969, .T. ) ;
#23343=CARTESIAN_POINT ( 'NONE',  ( 26.73860345374794534, -5.058662225110310828, -7.113848178280766099 ) ) ;
#23350=CARTESIAN_POINT ( 'NONE',  ( 4.527536911777373163, -5.876774720514422512, 21.53954785142818196 ) ) ;
#23351=AXIS2_PLACEMENT_3D ( 'NONE', #79367, #77855, #85987 ) ;
#23361=CARTESIAN_POINT ( 'NONE',  ( 2.976770017179964700, -5.876774720514419847, 20.68690469677381927 ) ) ;
#23385=ORIENTED_EDGE ( 'NONE', *, *, #37188, .F. ) ;
#23387=PLANE ( 'NONE',  #10816 ) ;
#23399=CARTESIAN_POINT ( 'NONE',  ( 32.40823333110732563, -4.442403080972329832, -4.096588619916003537 ) ) ;
#23400=CARTESIAN_POINT ( 'NONE',  ( -2.243088942307695177, -5.876774720514409189, 19.14743589743590491 ) ) ;
#23414=EDGE_CURVE ( 'NONE', #21242, #58098, #89982, .T. ) ;
#23418=CARTESIAN_POINT ( 'NONE',  ( 11.62916340711181284, -0.3587747205144265483, 28.75961759920349792 ) ) ;
#23455=CARTESIAN_POINT ( 'NONE',  ( 26.74698519091204574, 1.477225279485574028, -10.98683230472874151 ) ) ;
#23478=CARTESIAN_POINT ( 'NONE',  ( 7.460332110455646593, -5.876774720514418959, 20.55293369838740247 ) ) ;
#23482=AXIS2_PLACEMENT_3D ( 'NONE', #1759, #63167, #63678 ) ;
#23483=ORIENTED_EDGE ( 'NONE', *, *, #81654, .T. ) ;
#23486=CARTESIAN_POINT ( 'NONE',  ( -17.97250661212648026, 5.965225279485594001, -23.43622901028613015 ) ) ;
#23497=ORIENTED_EDGE ( 'NONE', *, *, #17910, .F. ) ;
#23499=DIRECTION ( 'NONE',  ( -0.1489078231574191280, 0.000000000000000000, 0.9888510809027406534 ) ) ;
#23503=CARTESIAN_POINT ( 'NONE',  ( 2.993128331772667572, -6.376774720514402972, 18.53171057923899312 ) ) ;
#23513=VECTOR ( 'NONE', #64029, 1000.000000000000000 ) ;
#23529=EDGE_CURVE ( 'NONE', #77894, #77030, #43061, .T. ) ;
#23535=DIRECTION ( 'NONE',  ( 1.000000000000000000, 0.000000000000000000, 0.000000000000000000 ) ) ;
#23545=EDGE_CURVE ( 'NONE', #35163, #53312, #83532, .T. ) ;
#23548=CIRCLE ( 'NONE', #78672, 28.96799999999999287 ) ;
#23556=EDGE_CURVE ( 'NONE', #24603, #45647, #25341, .T. ) ;
#23573=PLANE ( 'NONE',  #17059 ) ;
#23591=DIRECTION ( 'NONE',  ( -0.000000000000000000, 1.000000000000000000, -0.000000000000000000 ) ) ;
#23598=CARTESIAN_POINT ( 'NONE',  ( 9.402885806365684829, 5.965225279485572685, 29.04108526060719342 ) ) ;
#23600=ORIENTED_EDGE ( 'NONE', *, *, #14221, .F. ) ;
#23604=CARTESIAN_POINT ( 'NONE',  ( 8.476323908354110870, -5.356774720513951316, -27.09030197689322961 ) ) ;
#23610=CARTESIAN_POINT ( 'NONE',  ( 0.000000000000000000, -2.056774720514426669, 0.000000000000000000 ) ) ;
#23619=EDGE_CURVE ( 'NONE', #24603, #49218, #41586, .T. ) ;
#23629=ORIENTED_EDGE ( 'NONE', *, *, #85983, .T. ) ;
#23650=CARTESIAN_POINT ( 'NONE',  ( -53.01255352321339842, -14.82721238576461609, 35.59556822165056644 ) ) ;
#23660=CARTESIAN_POINT ( 'NONE',  ( 22.02124265030973760, 7.743225279485574042, 14.80402280011862359 ) ) ;
#23678=CARTESIAN_POINT ( 'NONE',  ( 14.88911825943084111, -3.458829258258214523, -27.36295217134173541 ) ) ;
#23687=CARTESIAN_POINT ( 'NONE',  ( 4.627238781264984446, -5.876774720514409189, 19.49219360614394247 ) ) ;
#23702=DIRECTION ( 'NONE',  ( 0.000000000000000000, 0.000000000000000000, -1.000000000000000000 ) ) ;
#23710=ORIENTED_EDGE ( 'NONE', *, *, #81807, .F. ) ;
#23716=CARTESIAN_POINT ( 'NONE',  ( -65.05438548721848235, -3.316774720514426456, 29.49402280011861777 ) ) ;
#23718=AXIS2_PLACEMENT_3D ( 'NONE', #77950, #54156, #85080 ) ;
#23720=CARTESIAN_POINT ( 'NONE',  ( 4.451706829556401956, -6.376774720514406525, 18.91922570401084513 ) ) ;
#23725=ORIENTED_EDGE ( 'NONE', *, *, #56789, .T. ) ;
#23727=ORIENTED_EDGE ( 'NONE', *, *, #68355, .T. ) ;
#23730=ORIENTED_EDGE ( 'NONE', *, *, #31345, .T. ) ;
#23742=VECTOR ( 'NONE', #77994, 1000.000000000000000 ) ;
#23746=ORIENTED_EDGE ( 'NONE', *, *, #5089, .T. ) ;
#23749=VERTEX_POINT ( 'NONE', #73525 ) ;
#23752=EDGE_CURVE ( 'NONE', #37372, #73685, #28338, .T. ) ;
#23767=CARTESIAN_POINT ( 'NONE',  ( -28.47875734969026240, 6.475225279485573360, 26.43402280011862615 ) ) ;
#23778=EDGE_CURVE ( 'NONE', #50658, #30492, #4519, .T. ) ;
#23781=CARTESIAN_POINT ( 'NONE',  ( 0.000000000000000000, -2.682774720514426559, 0.000000000000000000 ) ) ;
#23788=CARTESIAN_POINT ( 'NONE',  ( -12.84880425037202656, -0.3587747205143964613, -26.59900746623529244 ) ) ;
#23793=VECTOR ( 'NONE', #97195, 1000.000000000000000 ) ;
#23800=VERTEX_POINT ( 'NONE', #27842 ) ;
#23810=CARTESIAN_POINT ( 'NONE',  ( 22.81105451610979173, -2.682774720514426559, -18.46691820600746681 ) ) ;
#23826=EDGE_LOOP ( 'NONE', ( #26120, #18752, #52037, #86109, #74201, #25641, #80256, #23746 ) ) ;
#23832=CARTESIAN_POINT ( 'NONE',  ( 2.904244945035652670, -6.376774720514415407, 20.04207437776001299 ) ) ;
#23835=EDGE_LOOP ( 'NONE', ( #10989, #51765, #28092, #50101, #19447, #15509, #63594, #28517, #84114, #15206, #15122 ) ) ;
#23858=PLANE ( 'NONE',  #44241 ) ;
#23863=ORIENTED_EDGE ( 'NONE', *, *, #79905, .F. ) ;
#23870=DIRECTION ( 'NONE',  ( 0.000000000000000000, -1.000000000000000000, 0.000000000000000000 ) ) ;
#23876=CARTESIAN_POINT ( 'NONE',  ( -20.27875734969026311, -6.376774720514428729, 24.00402280011862288 ) ) ;
#23880=CARTESIAN_POINT ( 'NONE',  ( 31.60706529141451426, -6.376774720514427841, 26.12024523944107557 ) ) ;
#23883=CIRCLE ( 'NONE', #64422, 251.4258649670780699 ) ;
#23897=DIRECTION ( 'NONE',  ( -0.000000000000000000, 1.000000000000000000, -0.000000000000000000 ) ) ;
#23905=DIRECTION ( 'NONE',  ( -1.000000000000000000, 0.000000000000000000, 0.000000000000000000 ) ) ;
#23935=DIRECTION ( 'NONE',  ( 0.000000000000000000, 0.000000000000000000, 1.000000000000000000 ) ) ;
#23938=CARTESIAN_POINT ( 'NONE',  ( 5.359050311451609261, -5.876774720514419847, 21.05346524168807676 ) ) ;
#23939=ORIENTED_EDGE ( 'NONE', *, *, #49844, .F. ) ;
#23945=ORIENTED_EDGE ( 'NONE', *, *, #28575, .T. ) ;
#23955=ORIENTED_EDGE ( 'NONE', *, *, #37643, .T. ) ;
#23962=CARTESIAN_POINT ( 'NONE',  ( 6.431189903846153300, -6.376774720514415407, 20.08974358974358765 ) ) ;
#23966=ORIENTED_EDGE ( 'NONE', *, *, #64606, .F. ) ;
#23970=CIRCLE ( 'NONE', #20716, 91.74549126261076992 ) ;
#23986=CARTESIAN_POINT ( 'NONE',  ( -7.138063944469604571, -6.376774720514408301, 19.21974929698718881 ) ) ;
#24003=FACE_OUTER_BOUND ( 'NONE', #84013, .T. ) ;
#24006=LINE ( 'NONE', #1689, #82228 ) ;
#24015=DIRECTION ( 'NONE',  ( 0.000000000000000000, 0.000000000000000000, -1.000000000000000000 ) ) ;
#24020=DIRECTION ( 'NONE',  ( 0.000000000000000000, 0.000000000000000000, -1.000000000000000000 ) ) ;
#24030=DIRECTION ( 'NONE',  ( 0.000000000000000000, 0.000000000000000000, 1.000000000000000000 ) ) ;
#24034=CARTESIAN_POINT ( 'NONE',  ( 4.573489327750471567, -6.376774720514420736, 20.79634280254998657 ) ) ;
#24041=FACE_OUTER_BOUND ( 'NONE', #58921, .T. ) ;
#24047=CARTESIAN_POINT ( 'NONE',  ( -29.49875734969025842, -0.3587747205144262708, 15.62202280011862321 ) ) ;
#24053=EDGE_CURVE ( 'NONE', #86736, #22711, #39457, .T. ) ;
#24058=VECTOR ( 'NONE', #92321, 1000.000000000000000 ) ;
#24073=CARTESIAN_POINT ( 'NONE',  ( 0.000000000000000000, -5.876774720514426953, 0.000000000000000000 ) ) ;
#24082=CARTESIAN_POINT ( 'NONE',  ( 3.714584954927674154, -6.376774720514402972, 18.16171433633635246 ) ) ;
#24084=EDGE_LOOP ( 'NONE', ( #27608, #48413, #46908, #95725 ) ) ;
#24086=DIRECTION ( 'NONE',  ( -0.4009304992412300317, 6.845827386180410961E-16, -0.9161084732596779245 ) ) ;
#24087=DIRECTION ( 'NONE',  ( 0.000000000000000000, 0.000000000000000000, 1.000000000000000000 ) ) ;
#24089=ORIENTED_EDGE ( 'NONE', *, *, #88838, .T. ) ;
#24103=VERTEX_POINT ( 'NONE', #18119 ) ;
#24104=CARTESIAN_POINT ( 'NONE',  ( 1.140932434931746582E-13, -5.876774720514426953, 21.78128695274321203 ) ) ;
#24111=AXIS2_PLACEMENT_3D ( 'NONE', #77099, #84720, #16208 ) ;
#24113=CARTESIAN_POINT ( 'NONE',  ( 5.865642684142210683, -5.356774720514426491, -25.36740469599890702 ) ) ;
#24114=AXIS2_PLACEMENT_3D ( 'NONE', #82544, #66355, #97280 ) ;
#24123=ORIENTED_EDGE ( 'NONE', *, *, #83611, .T. ) ;
#24126=CARTESIAN_POINT ( 'NONE',  ( -5.891303133519534718, -6.376774720514420736, 20.71116975788854475 ) ) ;
#24134=ORIENTED_EDGE ( 'NONE', *, *, #70162, .T. ) ;
#24142=CARTESIAN_POINT ( 'NONE',  ( -4.141025641025642301, -6.376774720514411854, 19.63681891025641235 ) ) ;
#24159=CARTESIAN_POINT ( 'NONE',  ( -2.656471864501908975, -5.876774720514412742, 19.66116880005639800 ) ) ;
#24162=CYLINDRICAL_SURFACE ( 'NONE', #71176, 1.700000000000000178 ) ;
#24166=CARTESIAN_POINT ( 'NONE',  ( 30.93860345374796594, -6.376774720514426953, 28.83647319851474933 ) ) ;
#24175=PLANE ( 'NONE',  #19955 ) ;
#24177=CARTESIAN_POINT ( 'NONE',  ( 3.825768195983636044, -5.876774720514423400, 21.47884071039599618 ) ) ;
#24193=CARTESIAN_POINT ( 'NONE',  ( 4.653515142448186204, -5.876774720514414518, 19.86181745814487343 ) ) ;
#24198=ORIENTED_EDGE ( 'NONE', *, *, #40617, .T. ) ;
#24200=CARTESIAN_POINT ( 'NONE',  ( -3.108974358974355923, -5.876774720514426953, 21.75000000000001066 ) ) ;
#24202=FACE_OUTER_BOUND ( 'NONE', #10914, .T. ) ;
#24212=ORIENTED_EDGE ( 'NONE', *, *, #9373, .T. ) ;
#24215=ORIENTED_EDGE ( 'NONE', *, *, #2950, .T. ) ;
#24221=DIRECTION ( 'NONE',  ( 0.9980236263794188822, 0.000000000000000000, -0.06283980576413537855 ) ) ;
#24222=EDGE_CURVE ( 'NONE', #9746, #15899, #67299, .T. ) ;
#24236=VERTEX_POINT ( 'NONE', #82015 ) ;
#24238=CARTESIAN_POINT ( 'NONE',  ( -6.775140224358976226, -6.376774720514408301, 19.14743589743590846 ) ) ;
#24240=ORIENTED_EDGE ( 'NONE', *, *, #36745, .T. ) ;
#24254=CARTESIAN_POINT ( 'NONE',  ( 6.184520403203631389, -5.356774720514425603, -25.32021290018218451 ) ) ;
#24255=AXIS2_PLACEMENT_3D ( 'NONE', #17161, #1453, #15659 ) ;
#24256=ADVANCED_FACE ( 'NONE', ( #22582 ), #6881, .F. ) ;
#24279=AXIS2_PLACEMENT_3D ( 'NONE', #47092, #94749, #93245 ) ;
#24288=CIRCLE ( 'NONE', #22667, 1.835999999999983423 ) ;
#24290=CARTESIAN_POINT ( 'NONE',  ( -0.02075734969026423599, 6.475225279485573360, -0.08597719988137648983 ) ) ;
#24292=CARTESIAN_POINT ( 'NONE',  ( 5.495499487697820484, -6.376774720514418959, 20.18701882043406926 ) ) ;
#24293=DIRECTION ( 'NONE',  ( -1.000000000000000000, 0.000000000000000000, 1.526034937513432889E-15 ) ) ;
#24324=AXIS2_PLACEMENT_3D ( 'NONE', #59055, #29083, #89991 ) ;
#24326=EDGE_CURVE ( 'NONE', #20122, #91108, #61687, .T. ) ;
#24330=EDGE_CURVE ( 'NONE', #86922, #17186, #72357, .T. ) ;
#24350=AXIS2_PLACEMENT_3D ( 'NONE', #64499, #64997, #71588 ) ;
#24360=EDGE_CURVE ( 'NONE', #54291, #21668, #47953, .T. ) ;
#24365=DIRECTION ( 'NONE',  ( 1.000000000000000000, 0.000000000000000000, 5.238131417152343399E-15 ) ) ;
#24388=CARTESIAN_POINT ( 'NONE',  ( 31.69157588030328299, -3.540801019308528197, 29.47507166493026176 ) ) ;
#24389=DIRECTION ( 'NONE',  ( -0.9888510809027408754, -0.000000000000000000, -0.1489078231574183231 ) ) ;
#24397=CARTESIAN_POINT ( 'NONE',  ( -5.238752036864926964, -5.876774720514410966, 19.51517878119694061 ) ) ;
#24402=CARTESIAN_POINT ( 'NONE',  ( -4.686006777320708139, 5.965225279485572685, 29.60911411231905888 ) ) ;
#24414=EDGE_LOOP ( 'NONE', ( #12998, #32548, #22441, #32194 ) ) ;
#24415=CIRCLE ( 'NONE', #16300, 2.040000000000000036 ) ;
#24421=DIRECTION ( 'NONE',  ( 0.000000000000000000, -1.000000000000000000, 0.000000000000000000 ) ) ;
#24422=DIRECTION ( 'NONE',  ( -1.000000000000000000, -0.000000000000000000, 0.000000000000000000 ) ) ;
#24424=CARTESIAN_POINT ( 'NONE',  ( 5.742690948595683409, -6.376774720514427841, 21.62260900090680593 ) ) ;
#24425=CARTESIAN_POINT ( 'NONE',  ( 22.65031661608460922, -2.682774720514426559, -20.71116937900381672 ) ) ;
#24429=CARTESIAN_POINT ( 'NONE',  ( 31.37501302269236092, -4.132774720514428068, -3.717120176012354449 ) ) ;
#24437=LINE ( 'NONE', #86347, #39831 ) ;
#24461=VERTEX_POINT ( 'NONE', #74764 ) ;
#24463=CARTESIAN_POINT ( 'NONE',  ( -29.49875734969026198, -0.3587747205144265483, 10.11402280011862587 ) ) ;
#24465=ORIENTED_EDGE ( 'NONE', *, *, #44517, .T. ) ;
#24468=CARTESIAN_POINT ( 'NONE',  ( 6.853365600657045142, -5.876774720514415407, 20.20310688689519196 ) ) ;
#24469=CARTESIAN_POINT ( 'NONE',  ( 0.3791100739519297491, -6.376774720514418959, 20.35309744218306349 ) ) ;
#24474=LINE ( 'NONE', #32085, #20437 ) ;
#24479=CARTESIAN_POINT ( 'NONE',  ( 33.41145047975764726, -4.538943570064878585, -12.61568413423376889 ) ) ;
#24486=CARTESIAN_POINT ( 'NONE',  ( 32.16024265030974050, -0.3587747205144265483, 16.27760796525321751 ) ) ;
#24488=VERTEX_POINT ( 'NONE', #33722 ) ;
#24493=PLANE ( 'NONE',  #66010 ) ;
#24500=B_SPLINE_CURVE_WITH_KNOTS ( 'NONE', 3,
 ( #67609, #97046, #6190, #83812, #27547, #90431 ),
 .UNSPECIFIED., .F., .F.,
 ( 4, 2, 4 ),
 ( -8.872634692045293004E-06, 0.0009000329399760627434, 0.001808938514644170764 ),
 .UNSPECIFIED. ) ;
#24509=ADVANCED_FACE ( 'NONE', ( #26611 ), #66195, .F. ) ;
#24513=EDGE_CURVE ( 'NONE', #99093, #92445, #15344, .T. ) ;
#24520=CARTESIAN_POINT ( 'NONE',  ( 4.910384361841649614, -6.376774720514420736, 20.73924463800384643 ) ) ;
#24525=ORIENTED_EDGE ( 'NONE', *, *, #64631, .T. ) ;
#24533=EDGE_CURVE ( 'NONE', #65803, #54238, #58076, .T. ) ;
#24535=CARTESIAN_POINT ( 'NONE',  ( 3.249631081431332280, -5.876774720514423400, 21.24682042713427776 ) ) ;
#24546=CARTESIAN_POINT ( 'NONE',  ( -0.3225169060639742624, -5.876774720514411854, 19.46611907402017749 ) ) ;
#24550=DIRECTION ( 'NONE',  ( 1.000000000000000000, 0.000000000000000000, -1.252131230780251939E-15 ) ) ;
#24555=ORIENTED_EDGE ( 'NONE', *, *, #4107, .T. ) ;
#24562=ORIENTED_EDGE ( 'NONE', *, *, #42113, .T. ) ;
#24565=CARTESIAN_POINT ( 'NONE',  ( -29.49875734969025842, 5.965225279485572685, 23.37402280011862743 ) ) ;
#24567=FACE_OUTER_BOUND ( 'NONE', #16509, .T. ) ;
#24568=EDGE_CURVE ( 'NONE', #39794, #43715, #83102, .T. ) ;
#24578=CARTESIAN_POINT ( 'NONE',  ( -53.01255352321339842, -4.132774720514426292, 35.59556822165056644 ) ) ;
#24584=CARTESIAN_POINT ( 'NONE',  ( 4.653846153846159517, -6.376774720514415407, 19.99999999999999289 ) ) ;
#24586=CARTESIAN_POINT ( 'NONE',  ( -4.141166922167975883, -5.876774720514419847, 20.63520656483649063 ) ) ;
#24601=CARTESIAN_POINT ( 'NONE',  ( 32.66876533700882845, 5.965225279485572685, -12.58926540598385557 ) ) ;
#24603=VERTEX_POINT ( 'NONE', #96609 ) ;
#24606=VERTEX_POINT ( 'NONE', #4769 ) ;
#24607=DIRECTION ( 'NONE',  ( -8.659560562354873694E-17, -0.7071067811865525687, -0.7071067811865425767 ) ) ;
#24608=CARTESIAN_POINT ( 'NONE',  ( -10.24059822343757808, -5.876774720514426953, 0.000000000000000000 ) ) ;
#24609=CARTESIAN_POINT ( 'NONE',  ( 9.131215498121711960, -5.356774720514425603, -25.00673578072587588 ) ) ;
#24615=LINE ( 'NONE', #40359, #37243 ) ;
#24619=CARTESIAN_POINT ( 'NONE',  ( -6.033988668995577065, -6.376774720514413630, 19.86422795159478483 ) ) ;
#24621=EDGE_CURVE ( 'NONE', #45070, #31086, #85368, .T. ) ;
#24635=CARTESIAN_POINT ( 'NONE',  ( 32.16024265030974050, 5.965225279485572685, 16.27760796525321751 ) ) ;
#24636=CARTESIAN_POINT ( 'NONE',  ( -4.312370003044874167, -6.376774720514408301, 19.42522865122897358 ) ) ;
#24641=CARTESIAN_POINT ( 'NONE',  ( -5.799455386767018439, -5.876774720514413630, 19.66076420632890276 ) ) ;
#24647=CARTESIAN_POINT ( 'NONE',  ( 32.19706240494739546, -5.152774720514445406, -11.87117847608345933 ) ) ;
#24668=DIRECTION ( 'NONE',  ( 0.000000000000000000, 0.000000000000000000, 1.000000000000000000 ) ) ;
#24669=DIRECTION ( 'NONE',  ( -0.000000000000000000, -1.000000000000000000, -0.000000000000000000 ) ) ;
#24687=CARTESIAN_POINT ( 'NONE',  ( 4.372949846226492632, -5.876774720514405637, 18.80635842184136308 ) ) ;
#24719=CARTESIAN_POINT ( 'NONE',  ( 4.653846153846159517, -6.376774720514415407, 19.99999999999999289 ) ) ;
#24729=VECTOR ( 'NONE', #63100, 1000.000000000000000 ) ;
#24731=DIRECTION ( 'NONE',  ( 0.000000000000000000, 0.000000000000000000, 1.000000000000000000 ) ) ;
#24735=ORIENTED_EDGE ( 'NONE', *, *, #71968, .F. ) ;
#24736=CARTESIAN_POINT ( 'NONE',  ( -6.128026245051341192, -5.876774720514410966, 19.39236848396478763 ) ) ;
#24737=CARTESIAN_POINT ( 'NONE',  ( 22.02124265030973760, -6.376774720514428729, 19.20402280011862217 ) ) ;
#24744=ORIENTED_EDGE ( 'NONE', *, *, #48984, .F. ) ;
#24745=VECTOR ( 'NONE', #29278, 1000.000000000000000 ) ;
#24749=DIRECTION ( 'NONE',  ( 0.000000000000000000, 0.000000000000000000, -1.000000000000000000 ) ) ;
#24752=DIRECTION ( 'NONE',  ( -0.000000000000000000, 1.000000000000000000, -0.000000000000000000 ) ) ;
#24756=DIRECTION ( 'NONE',  ( 1.000000000000000000, 0.000000000000000000, 0.000000000000000000 ) ) ;
#24774=EDGE_CURVE ( 'NONE', #27638, #35495, #57809, .T. ) ;
#24780=EDGE_CURVE ( 'NONE', #82889, #18993, #28598, .T. ) ;
#24783=LINE ( 'NONE', #25793, #44024 ) ;
#24786=CARTESIAN_POINT ( 'NONE',  ( -6.487934372591614540, -6.376774720514411854, 19.49432735726520605 ) ) ;
#24810=CARTESIAN_POINT ( 'NONE',  ( 32.53135143123563466, -0.3587747205144265483, 6.926385399448451885 ) ) ;
#24815=VECTOR ( 'NONE', #23535, 1000.000000000000000 ) ;
#24831=CARTESIAN_POINT ( 'NONE',  ( -7.064692883725313344, -5.876774720514411854, 19.55266968305501862 ) ) ;
#24834=CARTESIAN_POINT ( 'NONE',  ( -12.84880425037202656, -0.3587747205143964613, -26.59900746623529244 ) ) ;
#24847=CARTESIAN_POINT ( 'NONE',  ( 0.2196812790064107401, -6.376774720514408301, 19.42522865122897002 ) ) ;
#24854=DIRECTION ( 'NONE',  ( 1.000000000000000000, 0.000000000000000000, 0.000000000000000000 ) ) ;
#24862=DIRECTION ( 'NONE',  ( -0.7512896232465891000, 0.000000000000000000, -0.6599726524652352877 ) ) ;
#24870=VERTEX_POINT ( 'NONE', #34606 ) ;
#24871=CARTESIAN_POINT ( 'NONE',  ( 32.76524810979199742, -3.299944812882172229, -3.892744026461423701 ) ) ;
#24876=CARTESIAN_POINT ( 'NONE',  ( 3.036358173076929123, -6.376774720514420736, 20.87990785256409865 ) ) ;
#24879=ORIENTED_EDGE ( 'NONE', *, *, #76220, .F. ) ;
#24881=CIRCLE ( 'NONE', #78323, 129.7684398600581517 ) ;
#24892=LINE ( 'NONE', #94909, #55663 ) ;
#24901=DIRECTION ( 'NONE',  ( -4.089440751051245812E-15, -1.000000000000000000, 1.042451643221144600E-15 ) ) ;
#24905=DIRECTION ( 'NONE',  ( 0.000000000000000000, 0.000000000000000000, 1.000000000000000000 ) ) ;
#24912=ORIENTED_EDGE ( 'NONE', *, *, #67671, .T. ) ;
#24915=CARTESIAN_POINT ( 'NONE',  ( 6.431189903846153300, -5.876774720514424288, 20.08974358974358765 ) ) ;
#24916=VECTOR ( 'NONE', #39627, 1000.000000000000000 ) ;
#24917=ORIENTED_EDGE ( 'NONE', *, *, #39092, .T. ) ;
#24921=CARTESIAN_POINT ( 'NONE',  ( 10.86264264036872440, -0.3587747205144257157, -28.05717073575603138 ) ) ;
#24924=CARTESIAN_POINT ( 'NONE',  ( 19.72776355195876263, 5.965225279485572685, 28.39950002376592764 ) ) ;
#24929=ORIENTED_EDGE ( 'NONE', *, *, #60458, .F. ) ;
#24930=EDGE_CURVE ( 'NONE', #10530, #23209, #77244, .T. ) ;
#24936=CARTESIAN_POINT ( 'NONE',  ( 0.7051282051282027341, -6.376774720514408301, 19.19230769230768985 ) ) ;
#24946=EDGE_CURVE ( 'NONE', #67290, #18359, #27985, .T. ) ;
#24947=ORIENTED_EDGE ( 'NONE', *, *, #72984, .T. ) ;
#24950=B_SPLINE_CURVE_WITH_KNOTS ( 'NONE', 3,
 ( #26480, #87873, #80258, #49831, #42222, #83744, #15235, #60436, #36571, #67541, #21834, #75621, #98461, #29961, #44202, #82744, #91359, #14225, #6626, #53814, #69535, #60930, #76128, #13228, #68531, #84747, #46192 ),
 .UNSPECIFIED., .F., .F.,
 ( 4, 1, 1, 1, 1, 1, 1, 1, 1, 1, 1, 1, 1, 1, 1, 1, 1, 1, 1, 1, 1, 1, 1, 1, 4 ),
 ( 0.000000000000000000, 0.06506328961727787796, 0.1267731664665228408, 0.1855157632260783507, 0.2407646791677146292, 0.2929797960235977494, 0.3422503727797667206, 0.3889192861856601846, 0.4327756640583091396, 0.4746284326311175361, 0.5147746906379525589, 0.5536058934984424695, 0.5914264064311723912, 0.6280281199460664432, 0.6638036341103201732, 0.6989843361316636638, 0.7335914893067054798, 0.7676284691511399139, 0.8012083477865917791, 0.8342638397266231021, 0.8669806947287760357, 0.8997197415181603652, 0.9327019124985379550, 0.9661758834327495160, 1.000000000000000000 ),
 .UNSPECIFIED. ) ;
#24954=ADVANCED_FACE ( 'NONE', ( #18868 ), #49341, .F. ) ;
#24956=LINE ( 'NONE', #55930, #41973 ) ;
#24962=ORIENTED_EDGE ( 'NONE', *, *, #3422, .F. ) ;
#24967=CARTESIAN_POINT ( 'NONE',  ( -12.84880425037203011, 5.965225279485592225, -26.59900746623528534 ) ) ;
#24972=LINE ( 'NONE', #48835, #61022 ) ;
#24982=VERTEX_POINT ( 'NONE', #73660 ) ;
#24990=CARTESIAN_POINT ( 'NONE',  ( 7.176111537430461595, -6.376774720514424288, 21.53668079471899333 ) ) ;
#24991=CARTESIAN_POINT ( 'NONE',  ( 6.156881756163101294, -5.876774720514414518, 19.74809127057764968 ) ) ;
#25014=EDGE_CURVE ( 'NONE', #59202, #1020, #27494, .T. ) ;
#25016=CARTESIAN_POINT ( 'NONE',  ( -5.554587162835583847, -6.376774720514417183, 19.99258394656885329 ) ) ;
#25020=VECTOR ( 'NONE', #53297, 1000.000000000000000 ) ;
#25024=EDGE_CURVE ( 'NONE', #45617, #71712, #96530, .T. ) ;
#25025=DIRECTION ( 'NONE',  ( 0.000000000000000000, 1.000000000000000000, 0.000000000000000000 ) ) ;
#25039=CARTESIAN_POINT ( 'NONE',  ( 5.671135738765417322, -5.876774720514421624, 20.99074880795119924 ) ) ;
#25041=DIRECTION ( 'NONE',  ( -4.218136541796977197E-15, -1.000000000000000000, -1.324960360541890271E-16 ) ) ;
#25049=AXIS2_PLACEMENT_3D ( 'NONE', #19668, #19171, #51131 ) ;
#25050=CARTESIAN_POINT ( 'NONE',  ( 4.784292611721462585, -6.376774720514426953, -25.54547254883130947 ) ) ;
#25052=CARTESIAN_POINT ( 'NONE',  ( -7.640838998533831194, -6.376774720514417183, 20.32624910079993086 ) ) ;
#25061=CARTESIAN_POINT ( 'NONE',  ( 6.467769777575680834, -6.376774720514427841, 21.83821538399986650 ) ) ;
#25063=EDGE_CURVE ( 'NONE', #47722, #67682, #84256, .T. ) ;
#25070=DIRECTION ( 'NONE',  ( -0.000000000000000000, 1.000000000000000000, -0.000000000000000000 ) ) ;
#25073=EDGE_CURVE ( 'NONE', #70350, #88394, #5144, .T. ) ;
#25082=ORIENTED_EDGE ( 'NONE', *, *, #28380, .F. ) ;
#25084=CARTESIAN_POINT ( 'NONE',  ( 32.33217928425140997, -6.376774720514426953, -12.20610769812822483 ) ) ;
#25099=B_SPLINE_CURVE_WITH_KNOTS ( 'NONE', 3,
 ( #49365, #80294, #41751, #72692, #67087, #5167, #21372, #29488, #66601, #13760, #89905, #4679, #59969, #51348, #90404, #37613, #75170, #97513 ),
 .UNSPECIFIED., .F., .F.,
 ( 4, 2, 2, 2, 2, 2, 2, 2, 4 ),
 ( 0.000000000000000000, 0.0005980878512858794297, 0.001196175702571757558, 0.001794263553857635470, 0.002392351405143513382, 0.002990439256429391728, 0.003588527107715270073, 0.004186614959001148419, 0.004784702810287026764 ),
 .UNSPECIFIED. ) ;
#25101=VERTEX_POINT ( 'NONE', #67558 ) ;
#25107=ORIENTED_EDGE ( 'NONE', *, *, #48666, .F. ) ;
#25109=CARTESIAN_POINT ( 'NONE',  ( 5.109298100548420152, -3.316774720514426456, -27.55941679637948383 ) ) ;
#25121=EDGE_CURVE ( 'NONE', #97326, #19469, #6137, .T. ) ;
#25125=AXIS2_PLACEMENT_3D ( 'NONE', #97553, #13303, #6698 ) ;
#25128=DIRECTION ( 'NONE',  ( 0.000000000000000000, -1.000000000000000000, 0.000000000000000000 ) ) ;
#25134=ORIENTED_EDGE ( 'NONE', *, *, #6389, .F. ) ;
#25136=CARTESIAN_POINT ( 'NONE',  ( -4.495793269230770939, -6.376774720514410077, 19.27714342948718595 ) ) ;
#25137=ADVANCED_FACE ( 'NONE', ( #91871 ), #22342, .F. ) ;
#25157=CARTESIAN_POINT ( 'NONE',  ( -2.532641601674031850, -5.876774720514410077, 19.55266968305501507 ) ) ;
#25166=VECTOR ( 'NONE', #78262, 1000.000000000000000 ) ;
#25170=CIRCLE ( 'NONE', #2519, 2.249999999999998668 ) ;
#25175=CARTESIAN_POINT ( 'NONE',  ( 2.627412086454235851, -6.376774720514420736, 20.59155478446653831 ) ) ;
#25189=ORIENTED_EDGE ( 'NONE', *, *, #4122, .T. ) ;
#25195=VECTOR ( 'NONE', #19445, 1000.000000000000000 ) ;
#25197=ORIENTED_EDGE ( 'NONE', *, *, #26970, .F. ) ;
#25204=VERTEX_POINT ( 'NONE', #30974 ) ;
#25206=ADVANCED_FACE ( 'NONE', ( #77137 ), #93876, .T. ) ;
#25211=ORIENTED_EDGE ( 'NONE', *, *, #3465, .T. ) ;
#25214=ORIENTED_EDGE ( 'NONE', *, *, #78157, .T. ) ;
#25225=ORIENTED_EDGE ( 'NONE', *, *, #32363, .T. ) ;
#25240=CARTESIAN_POINT ( 'NONE',  ( -6.185411026474866958, -5.876774720514411854, 19.34586827028016742 ) ) ;
#25249=TOROIDAL_SURFACE ( 'NONE', #12269, 3.060000000000000053, 3.060000000000000053 ) ;
#25253=ORIENTED_EDGE ( 'NONE', *, *, #12585, .T. ) ;
#25255=CYLINDRICAL_SURFACE ( 'NONE', #18145, 3.979149600822063704 ) ;
#25261=CARTESIAN_POINT ( 'NONE',  ( -7.188523146553190912, -6.376774720514413630, 19.66116880005639800 ) ) ;
#25262=LINE ( 'NONE', #56241, #66536 ) ;
#25290=CARTESIAN_POINT ( 'NONE',  ( 10.86264265030973952, -0.3587747205144257157, -28.64597719988137570 ) ) ;
#25291=DIRECTION ( 'NONE',  ( -1.000000000000000000, 0.000000000000000000, -0.000000000000000000 ) ) ;
#25302=VECTOR ( 'NONE', #72511, 1000.000000000000000 ) ;
#25311=DIRECTION ( 'NONE',  ( -0.7071067811865507924, 0.000000000000000000, 0.7071067811865442421 ) ) ;
#25317=EDGE_CURVE ( 'NONE', #33670, #47722, #73058, .T. ) ;
#25320=ORIENTED_EDGE ( 'NONE', *, *, #76347, .T. ) ;
#25321=CARTESIAN_POINT ( 'NONE',  ( 4.400426145423703694, -6.376774720514426065, 21.64763382324305852 ) ) ;
#25322=CARTESIAN_POINT ( 'NONE',  ( 0.000000000000000000, 1.477225279485574028, 0.000000000000000000 ) ) ;
#25336=CARTESIAN_POINT ( 'NONE',  ( -1.540913562699879114, -6.376774720514410077, 19.44316438561912008 ) ) ;
#25341=LINE ( 'NONE', #95356, #54415 ) ;
#25349=EDGE_CURVE ( 'NONE', #69866, #88394, #30330, .T. ) ;
#25350=ORIENTED_EDGE ( 'NONE', *, *, #741, .T. ) ;
#25351=FACE_OUTER_BOUND ( 'NONE', #33627, .T. ) ;
#25363=EDGE_CURVE ( 'NONE', #12265, #10530, #58822, .T. ) ;
#25364=AXIS2_PLACEMENT_3D ( 'NONE', #49778, #16799, #65015 ) ;
#25367=CARTESIAN_POINT ( 'NONE',  ( 4.038745349937860496, -5.876774720514428729, 21.81354843764681206 ) ) ;
#25401=CARTESIAN_POINT ( 'NONE',  ( -5.563047341353722253, -5.876774720514414518, 20.06599527532950589 ) ) ;
#25405=VERTEX_POINT ( 'NONE', #16497 ) ;
#25424=CARTESIAN_POINT ( 'NONE',  ( 5.642655980204820843, -5.876774720514418959, 20.71586687040766961 ) ) ;
#25425=ORIENTED_EDGE ( 'NONE', *, *, #40383, .F. ) ;
#25429=CARTESIAN_POINT ( 'NONE',  ( 11.78947449592735275, -0.3587747205144256601, -28.08498176919931666 ) ) ;
#25434=CARTESIAN_POINT ( 'NONE',  ( 10.86264265030973952, -0.3587747205144257157, -27.62597719988137612 ) ) ;
#25436=AXIS2_PLACEMENT_3D ( 'NONE', #7546, #78542, #93779 ) ;
#25440=CARTESIAN_POINT ( 'NONE',  ( 10.24059822343757808, -6.376774720514426953, 22.08128695274315945 ) ) ;
#25443=AXIS2_PLACEMENT_3D ( 'NONE', #18583, #56679, #48567 ) ;
#25447=ORIENTED_EDGE ( 'NONE', *, *, #81530, .F. ) ;
#25470=CARTESIAN_POINT ( 'NONE',  ( 5.367993895751241418, -6.376774720514418959, 20.45854982692612722 ) ) ;
#25485=CARTESIAN_POINT ( 'NONE',  ( 12.40597316965629560, -5.152774720514427642, -26.28458722401733993 ) ) ;
#25490=AXIS2_PLACEMENT_3D ( 'NONE', #11925, #51000, #36763 ) ;
#25494=CARTESIAN_POINT ( 'NONE',  ( 30.53060340732037048, -2.682774720514426559, -2.322449884495168870 ) ) ;
#25502=CARTESIAN_POINT ( 'NONE',  ( 6.058092820189922456, -5.876774720514413630, 19.77091638250125882 ) ) ;
#25513=ORIENTED_EDGE ( 'NONE', *, *, #35312, .T. ) ;
#25515=DIRECTION ( 'NONE',  ( -0.000000000000000000, 1.000000000000000000, -0.000000000000000000 ) ) ;
#25521=AXIS2_PLACEMENT_3D ( 'NONE', #29566, #36689, #74254 ) ;
#25525=EDGE_LOOP ( 'NONE', ( #45035, #85581, #79159, #71025 ) ) ;
#25527=CARTESIAN_POINT ( 'NONE',  ( -5.533628790199073499, -5.876774720514415407, 19.87297243748313491 ) ) ;
#25531=EDGE_CURVE ( 'NONE', #84743, #31713, #75659, .T. ) ;
#25532=CARTESIAN_POINT ( 'NONE',  ( 4.948291700218025113, -5.876774720514418071, 20.47145334051262111 ) ) ;
#25533=DIRECTION ( 'NONE',  ( -0.000000000000000000, 1.000000000000000000, -0.000000000000000000 ) ) ;
#25544=DIRECTION ( 'NONE',  ( -0.7512896232465892110, -0.000000000000000000, -0.6599726524652350657 ) ) ;
#25549=DIRECTION ( 'NONE',  ( 0.000000000000000000, -1.000000000000000000, 0.000000000000000000 ) ) ;
#25550=CARTESIAN_POINT ( 'NONE',  ( -27.25988310792305214, 5.965225279485572685, 30.32664379231667695 ) ) ;
#25569=CARTESIAN_POINT ( 'NONE',  ( 7.448826589983275959, -6.376774720514420736, 21.05250386848070221 ) ) ;
#25574=LINE ( 'NONE', #55035, #37152 ) ;
#25582=VECTOR ( 'NONE', #17870, 1000.000000000000000 ) ;
#25589=CARTESIAN_POINT ( 'NONE',  ( 2.589743589743596086, -6.376774720514415407, 20.00140224358974095 ) ) ;
#25590=ADVANCED_FACE ( 'NONE', ( #66715 ), #87139, .T. ) ;
#25591=VERTEX_POINT ( 'NONE', #76764 ) ;
#25592=VECTOR ( 'NONE', #2692, 1000.000000000000000 ) ;
#25595=CARTESIAN_POINT ( 'NONE',  ( 22.02124265030973760, -4.776774720514394446, 17.60402280011861009 ) ) ;
#25608=CARTESIAN_POINT ( 'NONE',  ( -1.359251851468251449, -5.876774720514419847, 20.71116975788854120 ) ) ;
#25610=LINE ( 'NONE', #48460, #43623 ) ;
#25614=ORIENTED_EDGE ( 'NONE', *, *, #89398, .T. ) ;
#25622=DIRECTION ( 'NONE',  ( 0.000000000000000000, 0.000000000000000000, -1.000000000000000000 ) ) ;
#25638=CARTESIAN_POINT ( 'NONE',  ( 31.71875899258513698, -3.424184405370887863, -3.672337713816452354 ) ) ;
#25641=ORIENTED_EDGE ( 'NONE', *, *, #14807, .T. ) ;
#25646=CARTESIAN_POINT ( 'NONE',  ( -20.27875734969026311, -7.835183881457444599, 22.60402280011862430 ) ) ;
#25647=DIRECTION ( 'NONE',  ( -0.1875268396392987258, 0.000000000000000000, -0.9822594791677485837 ) ) ;
#25660=EDGE_CURVE ( 'NONE', #38725, #54291, #30106, .T. ) ;
#25664=LINE ( 'NONE', #1839, #4592 ) ;
#25667=FACE_OUTER_BOUND ( 'NONE', #90487, .T. ) ;
#25668=CARTESIAN_POINT ( 'NONE',  ( -4.141025641025641413, -6.376774720514420736, 20.67377804487180271 ) ) ;
#25676=CARTESIAN_POINT ( 'NONE',  ( 15.03220655128773942, -5.152774720514418760, -26.94699118253608816 ) ) ;
#25694=VERTEX_POINT ( 'NONE', #13880 ) ;
#25701=ORIENTED_EDGE ( 'NONE', *, *, #16424, .T. ) ;
#25710=EDGE_LOOP ( 'NONE', ( #12143, #52718, #42003, #34369 ) ) ;
#25715=VECTOR ( 'NONE', #95781, 1000.000000000000000 ) ;
#25719=CARTESIAN_POINT ( 'NONE',  ( 3.025806405283164136, -6.376774720514420736, 20.84867811309776542 ) ) ;
#25723=EDGE_CURVE ( 'NONE', #49812, #32014, #14878, .T. ) ;
#25725=DIRECTION ( 'NONE',  ( -1.000000000000000000, 0.000000000000000000, 0.000000000000000000 ) ) ;
#25728=ADVANCED_FACE ( 'NONE', ( #86896 ), #24493, .F. ) ;
#25730=CARTESIAN_POINT ( 'NONE',  ( 3.787259615384621192, -6.376774720514404748, 18.51923076923076295 ) ) ;
#25732=ORIENTED_EDGE ( 'NONE', *, *, #97424, .F. ) ;
#25737=ORIENTED_EDGE ( 'NONE', *, *, #89703, .F. ) ;
#25738=VECTOR ( 'NONE', #46907, 1000.000000000000227 ) ;
#25748=CARTESIAN_POINT ( 'NONE',  ( -5.837039262820512775, -5.876774720514413630, 19.76512419871795245 ) ) ;
#25749=AXIS2_PLACEMENT_3D ( 'NONE', #19192, #66401, #82101 ) ;
#25750=CARTESIAN_POINT ( 'NONE',  ( 13.91401389203221406, 5.965225279485572685, 158.0376437107427137 ) ) ;
#25763=ORIENTED_EDGE ( 'NONE', *, *, #11711, .T. ) ;
#25766=FACE_OUTER_BOUND ( 'NONE', #26621, .T. ) ;
#25767=CARTESIAN_POINT ( 'NONE',  ( -7.294102189209645815, -5.876774720514413630, 19.89644244529368677 ) ) ;
#25772=CARTESIAN_POINT ( 'NONE',  ( 8.462785143989153269, 5.965225279485592225, -28.02084008811334215 ) ) ;
#25790=VECTOR ( 'NONE', #13962, 1000.000000000000000 ) ;
#25793=CARTESIAN_POINT ( 'NONE',  ( -17.64648606763744354, 5.965225279485594001, -23.04404205923972526 ) ) ;
#25794=ORIENTED_EDGE ( 'NONE', *, *, #36586, .F. ) ;
#25808=DIRECTION ( 'NONE',  ( -0.000000000000000000, 1.000000000000000000, -0.000000000000000000 ) ) ;
#25817=DIRECTION ( 'NONE',  ( 0.000000000000000000, -1.000000000000000000, 0.000000000000000000 ) ) ;
#25819=ORIENTED_EDGE ( 'NONE', *, *, #84923, .T. ) ;
#25823=CARTESIAN_POINT ( 'NONE',  ( 4.948291700218025113, -6.376774720514418959, 20.47145334051262111 ) ) ;
#25824=CARTESIAN_POINT ( 'NONE',  ( 8.000000000000003553, -5.876774720514426953, 22.50000000000000355 ) ) ;
#25837=CARTESIAN_POINT ( 'NONE',  ( 32.76111974776238611, -3.316774720514426900, -3.850861272813261849 ) ) ;
#25853=CARTESIAN_POINT ( 'NONE',  ( 3.160575456146155204, -5.876774720514408301, 18.86877352677795372 ) ) ;
#25858=CARTESIAN_POINT ( 'NONE',  ( 14.61581676225068449, 6.475225279485576912, -27.35847991880143226 ) ) ;
#25872=ORIENTED_EDGE ( 'NONE', *, *, #99520, .T. ) ;
#25873=VECTOR ( 'NONE', #49070, 1000.000000000000000 ) ;
#25875=VECTOR ( 'NONE', #91828, 1000.000000000000000 ) ;
#25879=VECTOR ( 'NONE', #92626, 999.9999999999998863 ) ;
#25883=CARTESIAN_POINT ( 'NONE',  ( 0.3627416911114360598, -6.376774720514411854, 19.59793130852656873 ) ) ;
#25896=DIRECTION ( 'NONE',  ( -0.000000000000000000, -1.000000000000000000, -0.000000000000000000 ) ) ;
#25901=EDGE_CURVE ( 'NONE', #39794, #46605, #80539, .T. ) ;
#25907=CARTESIAN_POINT ( 'NONE',  ( 4.653846153846159517, -5.876774720514419847, 19.99999999999999289 ) ) ;
#25908=CARTESIAN_POINT ( 'NONE',  ( 2.903846153846159517, -6.376774720514415407, 19.99999999999999289 ) ) ;
#25914=FACE_OUTER_BOUND ( 'NONE', #82738, .T. ) ;
#25923=CARTESIAN_POINT ( 'NONE',  ( 5.641025641025643189, -5.876774720514419847, 20.78665865384615330 ) ) ;
#25925=EDGE_CURVE ( 'NONE', #95782, #59162, #8105, .T. ) ;
#25926=ORIENTED_EDGE ( 'NONE', *, *, #6222, .F. ) ;
#25930=DIRECTION ( 'NONE',  ( 0.02119372647573786531, -9.594337693711052596E-15, 0.9997753877537052247 ) ) ;
#25938=CIRCLE ( 'NONE', #71282, 0.8160000000000000586 ) ;
#25944=DIRECTION ( 'NONE',  ( -0.000000000000000000, 1.000000000000000000, -0.000000000000000000 ) ) ;
#25946=AXIS2_PLACEMENT_3D ( 'NONE', #45374, #76291, #15393 ) ;
#25949=VERTEX_POINT ( 'NONE', #73188 ) ;
#25966=ADVANCED_FACE ( 'NONE', ( #10783 ), #42257, .F. ) ;
#25969=ORIENTED_EDGE ( 'NONE', *, *, #33415, .T. ) ;
#25973=CARTESIAN_POINT ( 'NONE',  ( 7.052174998393318184, -6.376774720514418959, 20.39928653130861136 ) ) ;
#25974=CARTESIAN_POINT ( 'NONE',  ( 5.400898774349120579, -6.376774720514417183, 20.36357656736558042 ) ) ;
#25983=DIRECTION ( 'NONE',  ( 0.000000000000000000, 1.478457507934778393E-16, -1.000000000000000000 ) ) ;
#25988=EDGE_LOOP ( 'NONE', ( #72082, #29524, #24562, #8615 ) ) ;
#25993=FACE_OUTER_BOUND ( 'NONE', #70420, .T. ) ;
#25995=ORIENTED_EDGE ( 'NONE', *, *, #98934, .T. ) ;
#26000=CARTESIAN_POINT ( 'NONE',  ( 5.344006250707635353, -5.876774720514418959, 20.55781796641452885 ) ) ;
#26002=LINE ( 'NONE', #96513, #83604 ) ;
#26007=CARTESIAN_POINT ( 'NONE',  ( 27.86270917940689174, -6.376774720514426953, 29.02104833056109001 ) ) ;
#26008=VECTOR ( 'NONE', #93268, 1000.000000000000000 ) ;
#26016=FACE_OUTER_BOUND ( 'NONE', #29825, .T. ) ;
#26018=VECTOR ( 'NONE', #66496, 1000.000000000000000 ) ;
#26024=DIRECTION ( 'NONE',  ( 0.000000000000000000, 0.000000000000000000, -1.000000000000000000 ) ) ;
#26027=CARTESIAN_POINT ( 'NONE',  ( 4.689770114687411784, -5.876774720514423400, 21.33175327469028915 ) ) ;
#26032=VERTEX_POINT ( 'NONE', #50850 ) ;
#26037=ORIENTED_EDGE ( 'NONE', *, *, #89908, .T. ) ;
#26043=EDGE_CURVE ( 'NONE', #76027, #12135, #74178, .T. ) ;
#26053=EDGE_CURVE ( 'NONE', #30745, #92987, #99986, .T. ) ;
#26059=CARTESIAN_POINT ( 'NONE',  ( -7.421417143192116761, -5.876774720514411854, 19.43823095447975291 ) ) ;
#26060=CIRCLE ( 'NONE', #34183, 3.060000000000001830 ) ;
#26062=B_SPLINE_CURVE_WITH_KNOTS ( 'NONE', 3,
 ( #59965, #37107, #60959, #91884, #82779, #7149, #61458, #90400 ),
 .UNSPECIFIED., .F., .F.,
 ( 4, 2, 2, 4 ),
 ( 0.06220205793350375156, 0.06492579111525004221, 0.06628765770612317365, 0.06764952429699631897 ),
 .UNSPECIFIED. ) ;
#26067=VERTEX_POINT ( 'NONE', #6154 ) ;
#26069=ADVANCED_FACE ( 'NONE', ( #67083 ), #97993, .T. ) ;
#26070=CARTESIAN_POINT ( 'NONE',  ( 7.176111537430461595, -5.876774720514424288, 21.53668079471899333 ) ) ;
#26071=CARTESIAN_POINT ( 'NONE',  ( 5.949073730962466833, 5.965225279485572685, -27.94053387008862188 ) ) ;
#26072=DIRECTION ( 'NONE',  ( -0.3133898629642195011, -5.365801633547207373E-16, 0.9496245541219264785 ) ) ;
#26076=CIRCLE ( 'NONE', #60069, 3.349999999999998757 ) ;
#26088=EDGE_CURVE ( 'NONE', #58916, #31553, #26062, .T. ) ;
#26091=CARTESIAN_POINT ( 'NONE',  ( 3.116263380642223968, -6.376774720514401196, 18.40799819116699609 ) ) ;
#26099=EDGE_CURVE ( 'NONE', #63660, #37998, #84774, .T. ) ;
#26105=EDGE_CURVE ( 'NONE', #65645, #93691, #51846, .T. ) ;
#26113=ORIENTED_EDGE ( 'NONE', *, *, #50598, .T. ) ;
#26114=CARTESIAN_POINT ( 'NONE',  ( -0.08860454909227881426, -6.376774720514410077, 19.21747685089457036 ) ) ;
#26115=ORIENTED_EDGE ( 'NONE', *, *, #93991, .F. ) ;
#26120=ORIENTED_EDGE ( 'NONE', *, *, #94255, .T. ) ;
#26127=CARTESIAN_POINT ( 'NONE',  ( 0.000000000000000000, -5.876774720514426953, 0.000000000000000000 ) ) ;
#26134=CARTESIAN_POINT ( 'NONE',  ( -65.05438548721848235, 6.475225279485573360, 29.49402280011861777 ) ) ;
#26152=VECTOR ( 'NONE', #31147, 1000.000000000000000 ) ;
#26158=LINE ( 'NONE', #97172, #85208 ) ;
#26163=EDGE_CURVE ( 'NONE', #96476, #41375, #53843, .T. ) ;
#26168=DIRECTION ( 'NONE',  ( -1.000000000000000000, 0.000000000000000000, 0.000000000000000000 ) ) ;
#26173=PLANE ( 'NONE',  #65650 ) ;
#26181=FACE_OUTER_BOUND ( 'NONE', #67843, .T. ) ;
#26183=ADVANCED_FACE ( 'NONE', ( #14755 ), #82344, .T. ) ;
#26188=CARTESIAN_POINT ( 'NONE',  ( -9.940598223437577374, -5.876774720514426953, 17.91871304725684766 ) ) ;
#26194=CARTESIAN_POINT ( 'NONE',  ( 9.940598223437573822, -5.876774720514426953, 21.78128695274315874 ) ) ;
#26195=EDGE_CURVE ( 'NONE', #86736, #57446, #55853, .T. ) ;
#26203=CARTESIAN_POINT ( 'NONE',  ( -9.149999999999996803, -5.876774720514426953, 11.88602120139452012 ) ) ;
#26207=VERTEX_POINT ( 'NONE', #40114 ) ;
#26217=CARTESIAN_POINT ( 'NONE',  ( -0.005606649364735081555, -6.376774720514410077, 19.25713806424188235 ) ) ;
#26244=EDGE_LOOP ( 'NONE', ( #8782, #4081, #61586, #20326 ) ) ;
#26246=DIRECTION ( 'NONE',  ( -0.000000000000000000, -1.000000000000000000, -0.000000000000000000 ) ) ;
#26249=ORIENTED_EDGE ( 'NONE', *, *, #18749, .T. ) ;
#26258=CARTESIAN_POINT ( 'NONE',  ( -28.98875734969026041, -0.3587747205144265483, 17.86602280011862476 ) ) ;
#26274=DIRECTION ( 'NONE',  ( 0.000000000000000000, 0.000000000000000000, -1.000000000000000000 ) ) ;
#26275=DIRECTION ( 'NONE',  ( 0.000000000000000000, 0.000000000000000000, -1.000000000000000000 ) ) ;
#26281=CARTESIAN_POINT ( 'NONE',  ( -1.222978892338334012, -6.376774720514413630, 19.56655654527324373 ) ) ;
#26283=AXIS2_PLACEMENT_3D ( 'NONE', #6087, #50781, #82213 ) ;
#26293=EDGE_CURVE ( 'NONE', #58916, #20863, #80524, .T. ) ;
#26297=ORIENTED_EDGE ( 'NONE', *, *, #26868, .T. ) ;
#26298=CARTESIAN_POINT ( 'NONE',  ( 32.16024265030974050, -0.3587747205144265483, 16.27760796525321751 ) ) ;
#26312=CARTESIAN_POINT ( 'NONE',  ( -29.49875734969025842, 5.965225279485572685, 15.62202280011862321 ) ) ;
#26314=ORIENTED_EDGE ( 'NONE', *, *, #23414, .F. ) ;
#26318=DIRECTION ( 'NONE',  ( -0.000000000000000000, 1.000000000000000000, -0.000000000000000000 ) ) ;
#26325=CARTESIAN_POINT ( 'NONE',  ( 4.967948717948723392, -6.376774720514415407, 20.00140224358974095 ) ) ;
#26329=DIRECTION ( 'NONE',  ( 0.000000000000000000, -1.000000000000000000, 0.000000000000000000 ) ) ;
#26333=VECTOR ( 'NONE', #17916, 1000.000000000000000 ) ;
#26345=CARTESIAN_POINT ( 'NONE',  ( 8.000000000000003553, -5.876774720514426953, 22.50000000000000355 ) ) ;
#26347=DIRECTION ( 'NONE',  ( -1.000000000000000000, 1.232047923278981953E-16, 0.000000000000000000 ) ) ;
#26350=ORIENTED_EDGE ( 'NONE', *, *, #27938, .F. ) ;
#26351=CIRCLE ( 'NONE', #23133, 1.529999999999999805 ) ;
#26355=EDGE_CURVE ( 'NONE', #34238, #26990, #18504, .T. ) ;
#26363=VERTEX_POINT ( 'NONE', #87528 ) ;
#26364=CARTESIAN_POINT ( 'NONE',  ( 9.016989526679575206, -3.316774720514426900, -27.05137190084761301 ) ) ;
#26373=VECTOR ( 'NONE', #9804, 1000.000000000000000 ) ;
#26374=FACE_OUTER_BOUND ( 'NONE', #90348, .T. ) ;
#26375=ORIENTED_EDGE ( 'NONE', *, *, #44528, .F. ) ;
#26378=EDGE_LOOP ( 'NONE', ( #57828, #71937, #71193, #3613 ) ) ;
#26388=CARTESIAN_POINT ( 'NONE',  ( 2.989331223418256744, -6.376774720514424288, 21.46569930292093886 ) ) ;
#26390=CARTESIAN_POINT ( 'NONE',  ( -24.55517127435777525, -0.3587747205143967943, -15.44180958690143157 ) ) ;
#26416=ADVANCED_FACE ( 'NONE', ( #56084 ), #10901, .T. ) ;
#26421=VECTOR ( 'NONE', #62689, 1000.000000000000000 ) ;
#26428=ADVANCED_FACE ( 'NONE', ( #72305 ), #64210, .T. ) ;
#26435=EDGE_CURVE ( 'NONE', #79539, #9124, #54686, .T. ) ;
#26438=EDGE_CURVE ( 'NONE', #27719, #34332, #34243, .T. ) ;
#26440=CARTESIAN_POINT ( 'NONE',  ( 33.69795529655567634, 6.475225279485573360, 20.86760796525322093 ) ) ;
#26444=CARTESIAN_POINT ( 'NONE',  ( 32.25249349869195470, -1.684774720514423674, -12.65342752644894553 ) ) ;
#26474=ADVANCED_FACE ( 'NONE', ( #20002 ), #97130, .F. ) ;
#26479=CARTESIAN_POINT ( 'NONE',  ( 7.081057417352553784, -6.376774720514424288, 21.11453472826393352 ) ) ;
#26480=CARTESIAN_POINT ( 'NONE',  ( 2.589743589743596086, -5.876774720514419847, 20.00140224358974095 ) ) ;
#26484=PLANE ( 'NONE',  #94003 ) ;
#26489=ORIENTED_EDGE ( 'NONE', *, *, #55776, .T. ) ;
#26490=VECTOR ( 'NONE', #14883, 1000.000000000000000 ) ;
#26491=LINE ( 'NONE', #96489, #25582 ) ;
#26494=DIRECTION ( 'NONE',  ( -1.000000000000000000, 0.000000000000000000, 0.000000000000000000 ) ) ;
#26497=CARTESIAN_POINT ( 'NONE',  ( 33.74607884027702909, -0.3587747205144265483, -4.999864028243830916 ) ) ;
#26499=VECTOR ( 'NONE', #20930, 1000.000000000000000 ) ;
#26511=CARTESIAN_POINT ( 'NONE',  ( 5.367993895751241418, -5.876774720514418071, 20.45854982692612722 ) ) ;
#26521=CARTESIAN_POINT ( 'NONE',  ( 9.051621769697627329, 6.475225279485570695, -27.04979394446680274 ) ) ;
#26526=DIRECTION ( 'NONE',  ( 0.000000000000000000, 0.000000000000000000, -1.000000000000000000 ) ) ;
#26528=CIRCLE ( 'NONE', #83222, 129.7684398600581517 ) ;
#26531=VERTEX_POINT ( 'NONE', #67696 ) ;
#26533=CARTESIAN_POINT ( 'NONE',  ( -5.576923076923076650, -6.376774720514418959, 20.44941907051282470 ) ) ;
#26547=CARTESIAN_POINT ( 'NONE',  ( 2.905029696106983916, -5.876774720514416295, 20.12486936895525957 ) ) ;
#26548=ADVANCED_FACE ( 'NONE', ( #20989 ), #50970, .F. ) ;
#26559=DIRECTION ( 'NONE',  ( 0.000000000000000000, 0.000000000000000000, 1.000000000000000000 ) ) ;
#26567=VECTOR ( 'NONE', #94720, 1000.000000000000000 ) ;
#26570=CARTESIAN_POINT ( 'NONE',  ( 6.055070916906798217, -3.316774720512750019, -28.43998667593618990 ) ) ;
#26572=CARTESIAN_POINT ( 'NONE',  ( -6.901944873432418248, -6.376774720514410077, 19.15221817653406688 ) ) ;
#26583=FACE_OUTER_BOUND ( 'NONE', #33086, .T. ) ;
#26584=ORIENTED_EDGE ( 'NONE', *, *, #36567, .F. ) ;
#26586=EDGE_CURVE ( 'NONE', #86771, #95782, #57535, .T. ) ;
#26590=LINE ( 'NONE', #11359, #85841 ) ;
#26596=CARTESIAN_POINT ( 'NONE',  ( 33.10875634548599322, 5.965225279485572685, -11.42349945801155719 ) ) ;
#26601=CYLINDRICAL_SURFACE ( 'NONE', #1672, 3.060000000000000053 ) ;
#26611=FACE_OUTER_BOUND ( 'NONE', #57325, .T. ) ;
#26613=VERTEX_POINT ( 'NONE', #42372 ) ;
#26614=FACE_OUTER_BOUND ( 'NONE', #76279, .T. ) ;
#26616=B_SPLINE_CURVE_WITH_KNOTS ( 'NONE', 3,
 ( #861, #56666, #62783, #49050, #72384, #2879, #70372, #93698, #55164, #10974, #4368, #81487, #20075, #89098, #97699, #88601, #34315, #12463, #27701 ),
 .UNSPECIFIED., .F., .F.,
 ( 4, 1, 1, 1, 1, 1, 1, 1, 1, 1, 1, 1, 1, 1, 1, 1, 4 ),
 ( 0.000000000000000000, 0.07834298519369982394, 0.1505633028794195749, 0.2161510566599787464, 0.2756797924514269305, 0.3287070503654637710, 0.3759044348322068685, 0.4173018977400307916, 0.4526927480535820614, 0.5172652917530110583, 0.5812165680623054831, 0.6453218939728019299, 0.7120244933797625908, 0.7801300447160447460, 0.8502182262116649847, 0.9226485217347383250, 1.000000000000000000 ),
 .UNSPECIFIED. ) ;
#26621=EDGE_LOOP ( 'NONE', ( #17959, #49485, #57227, #46850 ) ) ;
#26638=DIRECTION ( 'NONE',  ( 0.6451914333552788428, 0.000000000000000000, 0.7640209514960702997 ) ) ;
#26641=VECTOR ( 'NONE', #63311, 1000.000000000000000 ) ;
#26642=EDGE_CURVE ( 'NONE', #15369, #70394, #96340, .T. ) ;
#26644=CARTESIAN_POINT ( 'NONE',  ( 30.09341516180546350, -1.682774720514426114, -11.39311774897855933 ) ) ;
#26646=ORIENTED_EDGE ( 'NONE', *, *, #89398, .F. ) ;
#26647=CARTESIAN_POINT ( 'NONE',  ( 31.51256023177338861, -4.716437395117331732, -1.484035900832843868 ) ) ;
#26650=ORIENTED_EDGE ( 'NONE', *, *, #85046, .T. ) ;
#26665=DIRECTION ( 'NONE',  ( -0.000000000000000000, 1.000000000000000000, -0.000000000000000000 ) ) ;
#26678=FACE_OUTER_BOUND ( 'NONE', #63653, .T. ) ;
#26690=CARTESIAN_POINT ( 'NONE',  ( 3.248328688408994580, -6.376774720514406525, 18.75910638930973917 ) ) ;
#26699=CIRCLE ( 'NONE', #28355, 6.000000000000000888 ) ;
#26701=B_SPLINE_CURVE_WITH_KNOTS ( 'NONE', 3,
 ( #32263, #1829, #63234, #61736, #8430, #39878, #39380, #86051, #55623, #70334, #85045, #78428, #24641, #48004, #15034 ),
 .UNSPECIFIED., .F., .F.,
 ( 4, 1, 1, 1, 1, 1, 1, 1, 1, 1, 1, 1, 4 ),
 ( 0.000000000000000000, 0.08415201884431650070, 0.1665323202984589912, 0.2488363311465309202, 0.3312461454872611122, 0.4129571090216161422, 0.4904942776695665474, 0.5661557919819242279, 0.6399873346864671797, 0.7167654882718511589, 0.8021439047100994424, 0.8958332007101933447, 1.000000000000000000 ),
 .UNSPECIFIED. ) ;
#26715=PLANE ( 'NONE',  #52416 ) ;
#26717=B_SPLINE_CURVE_WITH_KNOTS ( 'NONE', 3,
 ( #32280, #55637, #61251, #85563, #94173, #78945, #70854, #38390, #16045, #40402, #76937, #48019, #71355, #69344, #61750, #39892, #84562, #55134, #63250, #31276, #62245, #7939, #38889, #16541, #30272, #69850, #7435 ),
 .UNSPECIFIED., .F., .F.,
 ( 4, 1, 1, 1, 1, 1, 1, 1, 1, 1, 1, 1, 1, 1, 1, 1, 1, 1, 1, 1, 1, 1, 1, 1, 4 ),
 ( 0.000000000000000000, 0.06859462225874299324, 0.1332460424433017654, 0.1943125864682570259, 0.2512792231169669877, 0.3045134392563472181, 0.3542349066533249102, 0.4004805887739895653, 0.4434107549384915803, 0.4840148686163446845, 0.5232523007732032827, 0.5610423727283604389, 0.5979002393643996216, 0.6335184888561951055, 0.6683143511696515437, 0.7024956712863811292, 0.7366853535134582076, 0.7702931693607886210, 0.8034372550192486750, 0.8359129516660284143, 0.8684602457892908189, 0.9008465382431825041, 0.9334665246307077835, 0.9662575752981232835, 1.000000000000000000 ),
 .UNSPECIFIED. ) ;
#26721=EDGE_LOOP ( 'NONE', ( #37694, #24465, #99700, #7996 ) ) ;
#26730=CARTESIAN_POINT ( 'NONE',  ( -0.02075734969026423599, -0.3587747205144213303, -0.08597719988137648983 ) ) ;
#26736=CARTESIAN_POINT ( 'NONE',  ( -8.978253834636468866, -6.376774720514426953, 21.48128695274316158 ) ) ;
#26743=EDGE_CURVE ( 'NONE', #37899, #69965, #11643, .T. ) ;
#26762=CARTESIAN_POINT ( 'NONE',  ( 33.13288845015618023, -0.3587747205144265483, -0.1650522222209214185 ) ) ;
#26767=FACE_OUTER_BOUND ( 'NONE', #68148, .T. ) ;
#26772=CIRCLE ( 'NONE', #44664, 251.4258649670780699 ) ;
#26775=DIRECTION ( 'NONE',  ( 1.000000000000000000, 0.000000000000000000, 0.000000000000000000 ) ) ;
#26778=CARTESIAN_POINT ( 'NONE',  ( 25.61870917940689196, -6.376774720514426953, 28.79814474876424768 ) ) ;
#26788=CARTESIAN_POINT ( 'NONE',  ( -25.92875734969026524, -3.316774720514426456, -0.08597719988137648983 ) ) ;
#26810=CARTESIAN_POINT ( 'NONE',  ( -22.05275734969026047, -0.3587747205144262708, 30.51402280011862089 ) ) ;
#26814=DIRECTION ( 'NONE',  ( 0.000000000000000000, 0.000000000000000000, 1.000000000000000000 ) ) ;
#26823=DIRECTION ( 'NONE',  ( 1.000000000000000000, 0.000000000000000000, 0.000000000000000000 ) ) ;
#26828=AXIS2_PLACEMENT_3D ( 'NONE', #52424, #61037, #45801 ) ;
#26838=ORIENTED_EDGE ( 'NONE', *, *, #46477, .F. ) ;
#26839=ORIENTED_EDGE ( 'NONE', *, *, #26163, .F. ) ;
#26845=CARTESIAN_POINT ( 'NONE',  ( 0.000000000000000000, -4.056774720514426669, 0.000000000000000000 ) ) ;
#26856=CARTESIAN_POINT ( 'NONE',  ( 2.903846153846159517, -5.876774720514415407, 19.99999999999999289 ) ) ;
#26861=CARTESIAN_POINT ( 'NONE',  ( 8.720681858489903959, -3.316774720514428232, -28.09278397295777197 ) ) ;
#26868=EDGE_CURVE ( 'NONE', #36206, #65103, #20747, .T. ) ;
#26882=CARTESIAN_POINT ( 'NONE',  ( 0.06697178475903577122, -5.876774720514410077, 19.29815762497054976 ) ) ;
#26885=CARTESIAN_POINT ( 'NONE',  ( 3.398286024651508530, -6.376774720514429617, 21.76255057507181334 ) ) ;
#26893=CARTESIAN_POINT ( 'NONE',  ( 25.83488407601164383, -2.682774720514426559, -11.31196583263649735 ) ) ;
#26895=B_SPLINE_CURVE_WITH_KNOTS ( 'NONE', 3,
 ( #49999, #47987, #72832, #11419, #80429 ),
 .UNSPECIFIED., .F., .F.,
 ( 4, 1, 4 ),
 ( 0.005748367439507872691, 0.007020066368101311738, 0.008291765296694749918 ),
 .UNSPECIFIED. ) ;
#26904=AXIS2_PLACEMENT_3D ( 'NONE', #94203, #86098, #16576 ) ;
#26908=CARTESIAN_POINT ( 'NONE',  ( 4.595037417369686850, -5.876774720514419847, 20.70846556543617467 ) ) ;
#26909=CARTESIAN_POINT ( 'NONE',  ( -3.826923076923078426, -6.376774720514408301, 19.19230769230769695 ) ) ;
#26911=CARTESIAN_POINT ( 'NONE',  ( 27.53860345374771867, -4.772774720514425972, -9.482392034746242260 ) ) ;
#26912=VECTOR ( 'NONE', #19422, 1000.000000000000114 ) ;
#26916=CARTESIAN_POINT ( 'NONE',  ( -5.891025641025639636, -6.376774720514420736, 20.75510817307693046 ) ) ;
#26923=SHAPE_REPRESENTATION ( 'Plastic Part 2', ( #37391 ), #61811 ) ;
#26924=CARTESIAN_POINT ( 'NONE',  ( -10.40290173325841216, -5.356774720514425603, 27.45402280011861862 ) ) ;
#26941=CIRCLE ( 'NONE', #12364, 0.2999999999999981570 ) ;
#26948=CARTESIAN_POINT ( 'NONE',  ( 22.81105451610979173, -500000.0000000000582, -20.71691820600746681 ) ) ;
#26949=VERTEX_POINT ( 'NONE', #32370 ) ;
#26954=ORIENTED_EDGE ( 'NONE', *, *, #32989, .F. ) ;
#26956=AXIS2_PLACEMENT_3D ( 'NONE', #83566, #35422, #29288 ) ;
#26958=LINE ( 'NONE', #57932, #65903 ) ;
#26962=VECTOR ( 'NONE', #91439, 1000.000000000000000 ) ;
#26965=VERTEX_POINT ( 'NONE', #70944 ) ;
#26970=EDGE_CURVE ( 'NONE', #25591, #22543, #31368, .T. ) ;
#26972=CIRCLE ( 'NONE', #96653, 2.499999999999993339 ) ;
#26976=CARTESIAN_POINT ( 'NONE',  ( 5.557675543255346184, -6.376774720514415407, 20.10561748372801461 ) ) ;
#26980=ADVANCED_FACE ( 'NONE', ( #418 ), #39488, .T. ) ;
#26981=LINE ( 'NONE', #56950, #19065 ) ;
#26990=VERTEX_POINT ( 'NONE', #86155 ) ;
#26992=CARTESIAN_POINT ( 'NONE',  ( 12.17747153392518733, -4.565036639100802596, -27.62487831441275787 ) ) ;
#26994=ORIENTED_EDGE ( 'NONE', *, *, #77524, .F. ) ;
#27000=EDGE_LOOP ( 'NONE', ( #58706, #69823, #86141, #89642 ) ) ;
#27014=EDGE_LOOP ( 'NONE', ( #15758, #45682, #59802, #56323 ) ) ;
#27017=CARTESIAN_POINT ( 'NONE',  ( 30.53060340732036337, -5.329285123471891872, 3.289350009555732868 ) ) ;
#27021=CARTESIAN_POINT ( 'NONE',  ( -7.641025641025641413, -5.876774720514418071, 20.36458333333334636 ) ) ;
#27028=CARTESIAN_POINT ( 'NONE',  ( -5.382328594919684406, -6.376774720514413630, 19.61227901093090864 ) ) ;
#27030=EDGE_CURVE ( 'NONE', #17929, #67306, #48892, .T. ) ;
#27032=CARTESIAN_POINT ( 'NONE',  ( 3.825380556292953482, -5.876774720514426953, 21.83927723428477208 ) ) ;
#27039=EDGE_LOOP ( 'NONE', ( #28585, #19912, #65806, #20231 ) ) ;
#27048=DIRECTION ( 'NONE',  ( 0.6599726524652350657, 0.000000000000000000, -0.7512896232465892110 ) ) ;
#27062=CARTESIAN_POINT ( 'NONE',  ( 20.13489193910630703, -2.682774720514426559, -22.92085183005112370 ) ) ;
#27064=CARTESIAN_POINT ( 'NONE',  ( 10.86431179149619908, -3.316774720514763075, -28.05678185015766246 ) ) ;
#27066=CARTESIAN_POINT ( 'NONE',  ( -7.617563585130437076, -6.376774720514411854, 19.95084900476494383 ) ) ;
#27071=ORIENTED_EDGE ( 'NONE', *, *, #66812, .T. ) ;
#27077=CARTESIAN_POINT ( 'NONE',  ( 3.176458874063926352, 5.965225279485592225, -28.85257003503889095 ) ) ;
#27079=FACE_OUTER_BOUND ( 'NONE', #90034, .T. ) ;
#27091=DIRECTION ( 'NONE',  ( -0.000000000000000000, 1.000000000000000000, -0.000000000000000000 ) ) ;
#27095=VERTEX_POINT ( 'NONE', #26762 ) ;
#27102=DIRECTION ( 'NONE',  ( -0.000000000000000000, 1.000000000000000000, -0.000000000000000000 ) ) ;
#27103=DIRECTION ( 'NONE',  ( 0.000000000000000000, -1.000000000000000000, 0.000000000000000000 ) ) ;
#27107=DIRECTION ( 'NONE',  ( -0.000000000000000000, -1.000000000000000000, -0.000000000000000000 ) ) ;
#27114=EDGE_CURVE ( 'NONE', #46643, #31571, #17144, .T. ) ;
#27116=CARTESIAN_POINT ( 'NONE',  ( 14.61581676223891613, -3.582999323269832725, -27.35847991879931485 ) ) ;
#27118=VECTOR ( 'NONE', #84851, 1000.000000000000000 ) ;
#27123=ORIENTED_EDGE ( 'NONE', *, *, #91036, .T. ) ;
#27146=CARTESIAN_POINT ( 'NONE',  ( -28.98875734969026041, 5.965225279485572685, 15.62202280011862321 ) ) ;
#27156=VECTOR ( 'NONE', #63346, 1000.000000000000000 ) ;
#27177=LINE ( 'NONE', #41915, #76013 ) ;
#27181=DIRECTION ( 'NONE',  ( -0.000000000000000000, -1.000000000000000000, -0.000000000000000000 ) ) ;
#27187=CARTESIAN_POINT ( 'NONE',  ( 15.94332860179735256, -4.994534053089958014, -27.96060887785571580 ) ) ;
#27200=VECTOR ( 'NONE', #74080, 1000.000000000000227 ) ;
#27204=ORIENTED_EDGE ( 'NONE', *, *, #56098, .F. ) ;
#27206=DIRECTION ( 'NONE',  ( -0.9496245541219264785, 6.845827386180410961E-16, -0.3133898629642195011 ) ) ;
#27211=DIRECTION ( 'NONE',  ( 0.000000000000000000, 1.000000000000000000, 0.000000000000000000 ) ) ;
#27213=ORIENTED_EDGE ( 'NONE', *, *, #34931, .F. ) ;
#27221=CARTESIAN_POINT ( 'NONE',  ( -0.4909855769230799249, -5.876774720514410077, 19.14743589743590491 ) ) ;
#27223=DIRECTION ( 'NONE',  ( 0.000000000000000000, 1.000000000000000000, 0.000000000000000000 ) ) ;
#27233=ORIENTED_EDGE ( 'NONE', *, *, #89908, .F. ) ;
#27234=VECTOR ( 'NONE', #52593, 1000.000000000000227 ) ;
#27235=CARTESIAN_POINT ( 'NONE',  ( -1.001577508147789342, -5.876774720514412742, 19.87297243748311004 ) ) ;
#27244=EDGE_CURVE ( 'NONE', #94756, #94339, #86654, .T. ) ;
#27255=LINE ( 'NONE', #95260, #41627 ) ;
#27256=LINE ( 'NONE', #97257, #37172 ) ;
#27259=ORIENTED_EDGE ( 'NONE', *, *, #26043, .T. ) ;
#27274=CARTESIAN_POINT ( 'NONE',  ( -7.326845193947049140, -6.376774720514417183, 20.33046051580616265 ) ) ;
#27279=CARTESIAN_POINT ( 'NONE',  ( -5.063563723219555612, -6.376774720514408301, 19.46509473978807847 ) ) ;
#27283=EDGE_CURVE ( 'NONE', #17533, #93024, #43496, .T. ) ;
#27298=LINE ( 'NONE', #57273, #96335 ) ;
#27309=EDGE_CURVE ( 'NONE', #50554, #93259, #89161, .T. ) ;
#27310=ORIENTED_EDGE ( 'NONE', *, *, #33415, .F. ) ;
#27313=CARTESIAN_POINT ( 'NONE',  ( 31.33322533232960083, -4.132774720514427180, -3.827970713771306155 ) ) ;
#27314=DIRECTION ( 'NONE',  ( -0.000000000000000000, 1.000000000000000000, -0.000000000000000000 ) ) ;
#27315=VERTEX_POINT ( 'NONE', #74431 ) ;
#27318=ADVANCED_FACE ( 'NONE', ( #29246 ), #5915, .F. ) ;
#27323=CARTESIAN_POINT ( 'NONE',  ( 4.115044103975469270, -6.376774720514427841, 21.79213183355573946 ) ) ;
#27341=EDGE_CURVE ( 'NONE', #93999, #49156, #87713, .T. ) ;
#27346=EDGE_LOOP ( 'NONE', ( #10523, #36151, #47606, #28857 ) ) ;
#27360=ORIENTED_EDGE ( 'NONE', *, *, #14388, .F. ) ;
#27371=ADVANCED_FACE ( 'NONE', ( #61717 ), #15512, .T. ) ;
#27373=CARTESIAN_POINT ( 'NONE',  ( 6.404294203292168142, -5.876774720514415407, 20.09052689972686423 ) ) ;
#27382=VERTEX_POINT ( 'NONE', #92141 ) ;
#27385=CARTESIAN_POINT ( 'NONE',  ( 0.3085469314987323020, -6.376774720514413630, 19.52341893546493523 ) ) ;
#27391=CARTESIAN_POINT ( 'NONE',  ( 29.80070917940689412, 5.965225279485572685, 27.39560796525321607 ) ) ;
#27407=CARTESIAN_POINT ( 'NONE',  ( 32.84232313084847732, -4.840274619473232676, -11.71291885348859196 ) ) ;
#27410=CARTESIAN_POINT ( 'NONE',  ( 3.176458874063931681, -0.3587747205143967943, -28.85257003503889806 ) ) ;
#27420=VERTEX_POINT ( 'NONE', #86033 ) ;
#27423=DIRECTION ( 'NONE',  ( 1.000000000000000000, 0.000000000000000000, 0.000000000000000000 ) ) ;
#27426=CARTESIAN_POINT ( 'NONE',  ( -22.05275734969026047, 5.965225279485572685, 31.02402280011862246 ) ) ;
#27434=CARTESIAN_POINT ( 'NONE',  ( 6.403846153846157740, -5.876774720514425177, 21.48076923076922995 ) ) ;
#27436=ORIENTED_EDGE ( 'NONE', *, *, #97720, .F. ) ;
#27441=EDGE_CURVE ( 'NONE', #10045, #80664, #85026, .T. ) ;
#27444=CARTESIAN_POINT ( 'NONE',  ( -24.90875734969025501, 5.965225279485572685, 30.00402280011862288 ) ) ;
#27450=EDGE_CURVE ( 'NONE', #54238, #23749, #8911, .T. ) ;
#27453=DIRECTION ( 'NONE',  ( -0.000000000000000000, 1.000000000000000000, -0.000000000000000000 ) ) ;
#27459=AXIS2_PLACEMENT_3D ( 'NONE', #5545, #75545, #82174 ) ;
#27465=EDGE_LOOP ( 'NONE', ( #18863, #46943, #43932, #47062, #24929 ) ) ;
#27471=LINE ( 'NONE', #43685, #22106 ) ;
#27475=VECTOR ( 'NONE', #75165, 1000.000000000000000 ) ;
#27479=CARTESIAN_POINT ( 'NONE',  ( 6.627987042499408510, -6.376774720514424288, 21.45334999081212146 ) ) ;
#27493=EDGE_CURVE ( 'NONE', #8750, #56847, #59466, .T. ) ;
#27494=LINE ( 'NONE', #34107, #17367 ) ;
#27505=B_SPLINE_CURVE_WITH_KNOTS ( 'NONE', 3,
 ( #18695, #96332, #43054, #10096, #65912, #27323, #33433, #89223, #3497, #25321, #64418, #34438, #33938, #42065, #64917, #12081, #10594, #56795, #73496, #95335, #56297, #58284, #25823, #88729, #95830, #19198, #26325 ),
 .UNSPECIFIED., .F., .F.,
 ( 4, 1, 1, 1, 1, 1, 1, 1, 1, 1, 1, 1, 1, 1, 1, 1, 1, 1, 1, 1, 1, 1, 1, 1, 4 ),
 ( 0.000000000000000000, 0.03378714634699089836, 0.06662165772429383404, 0.09928487809597265346, 0.1313611650426506072, 0.1635851875953436008, 0.1961039269870681889, 0.2289022543238170004, 0.2621580559050075143, 0.2959912222583161445, 0.3302178457247997301, 0.3650598258919544037, 0.4009507373401082209, 0.4376203820767376462, 0.4757075294370921026, 0.5153806916250490699, 0.5564135414931649093, 0.5997648298727309424, 0.6464241555840876119, 0.6964314445175666668, 0.7497815178015586612, 0.8065733069755320894, 0.8674355315653994314, 0.9318867532508745555, 1.000000000000000000 ),
 .UNSPECIFIED. ) ;
#27516=ORIENTED_EDGE ( 'NONE', *, *, #52740, .F. ) ;
#27536=B_SPLINE_CURVE_WITH_KNOTS ( 'NONE', 3,
 ( #44520, #35902, #52627, #66871, #43527, #45525, #83564, #14047 ),
 .UNSPECIFIED., .F., .F.,
 ( 4, 2, 2, 4 ),
 ( 0.000000000000000000, 0.0004967474533590028650, 0.0007451211800385037012, 0.0009934949067180044290 ),
 .UNSPECIFIED. ) ;
#27547=CARTESIAN_POINT ( 'NONE',  ( 33.23241444531825550, -3.542570809989110447, -12.77295888271925328 ) ) ;
#27549=AXIS2_PLACEMENT_3D ( 'NONE', #55237, #47615, #48116 ) ;
#27552=EDGE_LOOP ( 'NONE', ( #30075, #21226, #32384, #2733 ) ) ;
#27557=CARTESIAN_POINT ( 'NONE',  ( -28.98875734969026041, -6.376774720514426953, 26.43402280011862615 ) ) ;
#27559=PLANE ( 'NONE',  #40833 ) ;
#27560=DIRECTION ( 'NONE',  ( 2.338552693767719605E-15, 0.000000000000000000, 1.000000000000000000 ) ) ;
#27565=ORIENTED_EDGE ( 'NONE', *, *, #82644, .T. ) ;
#27567=CARTESIAN_POINT ( 'NONE',  ( 3.825768195983636044, -6.376774720514424288, 21.47884071039599618 ) ) ;
#27570=CARTESIAN_POINT ( 'NONE',  ( 10.16119454606818984, -3.316774720514931829, -28.04611093432389524 ) ) ;
#27572=CARTESIAN_POINT ( 'NONE',  ( -7.536766146225033047, -5.876774720514411854, 19.63296556618507438 ) ) ;
#27575=ORIENTED_EDGE ( 'NONE', *, *, #993, .F. ) ;
#27576=CARTESIAN_POINT ( 'NONE',  ( 30.53060340732036337, -5.266063118920828678, 0.9746665865322270417 ) ) ;
#27578=EDGE_LOOP ( 'NONE', ( #98089, #8917, #48221, #2647 ) ) ;
#27580=CARTESIAN_POINT ( 'NONE',  ( -23.59123376470063960, 6.143225279485574397, 23.50402280011862288 ) ) ;
#27581=CARTESIAN_POINT ( 'NONE',  ( 13.74975846015576586, 5.965225279485572685, -27.72022515045486557 ) ) ;
#27586=CARTESIAN_POINT ( 'NONE',  ( -1.733151984336291695, -5.876774720514407413, 19.29154511076646017 ) ) ;
#27589=DIRECTION ( 'NONE',  ( 0.000000000000000000, 0.000000000000000000, 1.000000000000000000 ) ) ;
#27592=AXIS2_PLACEMENT_3D ( 'NONE', #29217, #97234, #43946 ) ;
#27594=CARTESIAN_POINT ( 'NONE',  ( -9.150000000000000355, -5.876774720514426953, -15.69999999999999929 ) ) ;
#27596=ORIENTED_EDGE ( 'NONE', *, *, #47543, .T. ) ;
#27601=B_SPLINE_CURVE_WITH_KNOTS ( 'NONE', 3,
 ( #52709, #22728, #14128, #98867, #28362, #99854, #29360, #6529, #53718, #30359, #45599, #59323, #45105, #68430, #76519, #90268, #98365, #37480, #76026 ),
 .UNSPECIFIED., .F., .F.,
 ( 4, 1, 1, 1, 1, 1, 1, 1, 1, 1, 1, 1, 1, 1, 1, 1, 4 ),
 ( 0.000000000000000000, 0.06796237149445635839, 0.1332834028675231042, 0.1978352977570558280, 0.2608919865309880515, 0.3233765044831760083, 0.3863500754690888384, 0.4496377310517142845, 0.5147953269783583918, 0.5792399132410295248, 0.6418141777582890839, 0.7013585647860598460, 0.7607267659857199771, 0.8192220679243895631, 0.8787161693846299304, 0.9381473540533086242, 1.000000000000000000 ),
 .UNSPECIFIED. ) ;
#27602=VERTEX_POINT ( 'NONE', #94647 ) ;
#27608=ORIENTED_EDGE ( 'NONE', *, *, #8179, .T. ) ;
#27621=EDGE_CURVE ( 'NONE', #99954, #2424, #32246, .T. ) ;
#27631=DIRECTION ( 'NONE',  ( -0.2488812114211666759, -0.000000000000000000, -0.9685340172660599212 ) ) ;
#27633=CARTESIAN_POINT ( 'NONE',  ( 10.86264265030973952, 5.965225279485574461, -28.05717073599341305 ) ) ;
#27638=VERTEX_POINT ( 'NONE', #63729 ) ;
#27643=DIRECTION ( 'NONE',  ( 0.000000000000000000, 1.000000000000000000, 0.000000000000000000 ) ) ;
#27645=ORIENTED_EDGE ( 'NONE', *, *, #91243, .F. ) ;
#27678=CARTESIAN_POINT ( 'NONE',  ( -4.440151687742864617, -5.876774720514411854, 19.67013632031035897 ) ) ;
#27686=ADVANCED_FACE ( 'NONE', ( #17022 ), #10245, .F. ) ;
#27690=FACE_OUTER_BOUND ( 'NONE', #88412, .T. ) ;
#27691=CARTESIAN_POINT ( 'NONE',  ( 2.909586618535765723, -6.376774720514411854, 19.75512108203924200 ) ) ;
#27699=ADVANCED_FACE ( 'NONE', ( #1309 ), #63216, .T. ) ;
#27701=CARTESIAN_POINT ( 'NONE',  ( -2.188401442307694289, -6.376774720514411854, 19.46153846153846700 ) ) ;
#27718=DIRECTION ( 'NONE',  ( 1.156482317317878549E-14, 0.000000000000000000, 1.000000000000000000 ) ) ;
#27719=VERTEX_POINT ( 'NONE', #13394 ) ;
#27722=ORIENTED_EDGE ( 'NONE', *, *, #69596, .F. ) ;
#27729=CARTESIAN_POINT ( 'NONE',  ( -1.030996059302438761, -5.876774720514415407, 20.06599527532949878 ) ) ;
#27733=DIRECTION ( 'NONE',  ( -1.000000000000000000, 1.232047923278981953E-16, 0.000000000000000000 ) ) ;
#27743=LINE ( 'NONE', #36354, #60044 ) ;
#27748=CARTESIAN_POINT ( 'NONE',  ( 5.802984775641024662, -6.376774720514402972, 18.35026041666666430 ) ) ;
#27749=DIRECTION ( 'NONE',  ( 0.000000000000000000, -1.000000000000000000, 0.000000000000000000 ) ) ;
#27752=VERTEX_POINT ( 'NONE', #44370 ) ;
#27756=ORIENTED_EDGE ( 'NONE', *, *, #44863, .T. ) ;
#27765=DIRECTION ( 'NONE',  ( 0.000000000000000000, 0.000000000000000000, -1.000000000000000000 ) ) ;
#27779=LINE ( 'NONE', #43999, #46018 ) ;
#27791=DIRECTION ( 'NONE',  ( -0.000000000000000000, 1.000000000000000000, -0.000000000000000000 ) ) ;
#27794=CARTESIAN_POINT ( 'NONE',  ( -11.64875734969026233, 5.965225279485572685, 31.02402280011862246 ) ) ;
#27797=VERTEX_POINT ( 'NONE', #96642 ) ;
#27814=CARTESIAN_POINT ( 'NONE',  ( 6.351517594976544778, -6.376774720514417183, 20.09206396488320578 ) ) ;
#27818=CARTESIAN_POINT ( 'NONE',  ( 3.671066620544169101, -6.376774720514424288, 21.47597918715562670 ) ) ;
#27832=ORIENTED_EDGE ( 'NONE', *, *, #39212, .T. ) ;
#27834=EDGE_LOOP ( 'NONE', ( #45339, #1885, #60305, #27204 ) ) ;
#27835=EDGE_LOOP ( 'NONE', ( #63983, #70759 ) ) ;
#27837=CARTESIAN_POINT ( 'NONE',  ( 15.03086228770605004, -5.128928118853483653, -26.95277610321158690 ) ) ;
#27842=CARTESIAN_POINT ( 'NONE',  ( 22.02124265030973760, 7.743225279485574042, 18.45402280011862217 ) ) ;
#27843=DIRECTION ( 'NONE',  ( 0.000000000000000000, -1.000000000000000000, 0.000000000000000000 ) ) ;
#27851=ADVANCED_FACE ( 'NONE', ( #21009 ), #51478, .F. ) ;
#27853=CARTESIAN_POINT ( 'NONE',  ( 3.051095722660301934, -5.876774720514410077, 19.07493897947323092 ) ) ;
#27857=DIRECTION ( 'NONE',  ( -0.000000000000000000, 1.000000000000000000, -0.000000000000000000 ) ) ;
#27865=CARTESIAN_POINT ( 'NONE',  ( 6.351517594976544778, -5.876774720514417183, 20.09206396488320578 ) ) ;
#27868=ORIENTED_EDGE ( 'NONE', *, *, #66252, .T. ) ;
#27871=EDGE_LOOP ( 'NONE', ( #99688, #68976, #16098, #65823 ) ) ;
#27872=VECTOR ( 'NONE', #52885, 1000.000000000000227 ) ;
#27876=CARTESIAN_POINT ( 'NONE',  ( 0.03625801282051022839, -5.876774720514410077, 19.27714342948718240 ) ) ;
#27880=CARTESIAN_POINT ( 'NONE',  ( 2.590395174287518643, -6.376774720514415407, 20.05492615153064762 ) ) ;
#27881=ADVANCED_FACE ( 'NONE', ( #91025 ), #21498, .T. ) ;
#27884=CARTESIAN_POINT ( 'NONE',  ( 33.00535138976592719, -3.570691370340881576, -12.97242311383975988 ) ) ;
#27888=CARTESIAN_POINT ( 'NONE',  ( 3.509873074917118085, 5.965225279485572685, 29.15869884040363758 ) ) ;
#27892=AXIS2_PLACEMENT_3D ( 'NONE', #21915, #29539, #90945 ) ;
#27909=ADVANCED_FACE ( 'NONE', ( #61599 ), #84904, .T. ) ;
#27930=CARTESIAN_POINT ( 'NONE',  ( 12.88745205064172694, -3.316774720517230435, -28.14312002837575477 ) ) ;
#27932=PLANE ( 'NONE',  #26283 ) ;
#27938=EDGE_CURVE ( 'NONE', #70560, #78258, #99926, .T. ) ;
#27985=LINE ( 'NONE', #88388, #14101 ) ;
#27999=CARTESIAN_POINT ( 'NONE',  ( -5.891025641025639636, -5.876774720514419847, 20.75510817307693046 ) ) ;
#28014=EDGE_CURVE ( 'NONE', #23237, #11869, #44868, .T. ) ;
#28017=DIRECTION ( 'NONE',  ( -0.000000000000000000, 1.000000000000000000, -0.000000000000000000 ) ) ;
#28032=CARTESIAN_POINT ( 'NONE',  ( 3.879810481058463711, -6.376774720514427841, 21.83835767234735670 ) ) ;
#28042=CARTESIAN_POINT ( 'NONE',  ( 30.61643171304413613, -3.316774720514426456, 27.37433008668288181 ) ) ;
#28048=DIRECTION ( 'NONE',  ( -0.09721092304694055330, 0.000000000000000000, 0.9952638024365006997 ) ) ;
#28062=EDGE_CURVE ( 'NONE', #40153, #26363, #72201, .T. ) ;
#28064=CARTESIAN_POINT ( 'NONE',  ( 12.98941176919429097, -3.316774720517114972, -28.15829778459866262 ) ) ;
#28067=EDGE_CURVE ( 'NONE', #66329, #34477, #9189, .T. ) ;
#28070=EDGE_LOOP ( 'NONE', ( #9097, #29251, #96618, #46957 ) ) ;
#28078=CIRCLE ( 'NONE', #55615, 0.3000000000000016542 ) ;
#28086=FACE_OUTER_BOUND ( 'NONE', #54950, .T. ) ;
#28091=CARTESIAN_POINT ( 'NONE',  ( 30.61643171304413613, -3.316774720514426456, 27.37433008668288181 ) ) ;
#28092=ORIENTED_EDGE ( 'NONE', *, *, #68009, .T. ) ;
#28107=VECTOR ( 'NONE', #71878, 1000.000000000000000 ) ;
#28108=CARTESIAN_POINT ( 'NONE',  ( 29.71896661235086157, -4.666145129001815661, 27.69970538640514235 ) ) ;
#28114=EDGE_LOOP ( 'NONE', ( #31372, #90011, #28140, #46556 ) ) ;
#28129=CARTESIAN_POINT ( 'NONE',  ( 7.311104923646705167, -6.376774720514415407, 20.13320233724603980 ) ) ;
#28133=ORIENTED_EDGE ( 'NONE', *, *, #70652, .F. ) ;
#28140=ORIENTED_EDGE ( 'NONE', *, *, #66541, .F. ) ;
#28142=DIRECTION ( 'NONE',  ( 0.000000000000000000, 0.000000000000000000, 1.000000000000000000 ) ) ;
#28144=CARTESIAN_POINT ( 'NONE',  ( 29.73620800866979863, -5.101103159685075106, 27.18593991345460381 ) ) ;
#28153=VECTOR ( 'NONE', #89772, 1000.000000000000000 ) ;
#28154=CARTESIAN_POINT ( 'NONE',  ( 3.248328688408994580, -6.376774720514406525, 18.75910638930973917 ) ) ;
#28172=DIRECTION ( 'NONE',  ( -0.000000000000000000, 1.000000000000000000, -0.000000000000000000 ) ) ;
#28174=DIRECTION ( 'NONE',  ( 0.7071067811865476838, 0.000000000000000000, -0.7071067811865474617 ) ) ;
#28186=CARTESIAN_POINT ( 'NONE',  ( 7.107139210497321002, -6.376774720514413630, 19.78447747620696617 ) ) ;
#28187=EDGE_CURVE ( 'NONE', #26613, #32255, #88923, .T. ) ;
#28198=CARTESIAN_POINT ( 'NONE',  ( 0.3906119451836247425, -6.376774720514418959, 20.56083401959467594 ) ) ;
#28205=EDGE_LOOP ( 'NONE', ( #39870, #47853, #66145, #100356, #22104, #10704, #18570, #78026, #93220, #66179 ) ) ;
#28215=ORIENTED_EDGE ( 'NONE', *, *, #15668, .F. ) ;
#28231=VECTOR ( 'NONE', #46300, 1000.000000000000000 ) ;
#28244=LINE ( 'NONE', #59205, #8059 ) ;
#28254=VERTEX_POINT ( 'NONE', #44742 ) ;
#28260=DIRECTION ( 'NONE',  ( -0.000000000000000000, 1.000000000000000000, -0.000000000000000000 ) ) ;
#28266=EDGE_LOOP ( 'NONE', ( #25872, #66319, #31969, #58648 ) ) ;
#28273=CARTESIAN_POINT ( 'NONE',  ( -1.292025413547811308, -5.876774720514411854, 19.72913074730690752 ) ) ;
#28289=TOROIDAL_SURFACE ( 'NONE', #76863, 1.020000000000000018, 3.060000000000000053 ) ;
#28305=CARTESIAN_POINT ( 'NONE',  ( 31.42094490286590514, -4.276934461241891583, -0.4045216949806126339 ) ) ;
#28323=LINE ( 'NONE', #74982, #17045 ) ;
#28338=LINE ( 'NONE', #96358, #28483 ) ;
#28341=EDGE_LOOP ( 'NONE', ( #90506, #90499, #35944, #99370 ) ) ;
#28350=DIRECTION ( 'NONE',  ( 0.000000000000000000, 0.000000000000000000, -1.000000000000000000 ) ) ;
#28353=EDGE_CURVE ( 'NONE', #17395, #44756, #74030, .T. ) ;
#28355=AXIS2_PLACEMENT_3D ( 'NONE', #32356, #17127, #56718 ) ;
#28360=CARTESIAN_POINT ( 'NONE',  ( 6.351517594976544778, -6.376774720514417183, 20.09206396488320578 ) ) ;
#28362=CARTESIAN_POINT ( 'NONE',  ( 6.179707021866671646, -6.376774720514426065, 21.45334750074374242 ) ) ;
#28380=EDGE_CURVE ( 'NONE', #59937, #75883, #23883, .T. ) ;
#28392=ORIENTED_EDGE ( 'NONE', *, *, #84923, .F. ) ;
#28396=LINE ( 'NONE', #51247, #8328 ) ;
#28397=DIRECTION ( 'NONE',  ( 0.1875268396392986980, 0.000000000000000000, 0.9822594791677485837 ) ) ;
#28435=VERTEX_POINT ( 'NONE', #47238 ) ;
#28445=CARTESIAN_POINT ( 'NONE',  ( 13.91401389203221406, -6.376774720514426953, 158.0376437107427137 ) ) ;
#28447=ORIENTED_EDGE ( 'NONE', *, *, #58422, .T. ) ;
#28449=ORIENTED_EDGE ( 'NONE', *, *, #88090, .F. ) ;
#28453=ORIENTED_EDGE ( 'NONE', *, *, #67647, .T. ) ;
#28454=DIRECTION ( 'NONE',  ( 0.000000000000000000, 1.000000000000000000, 0.000000000000000000 ) ) ;
#28470=CARTESIAN_POINT ( 'NONE',  ( -4.141025641025642301, -5.876774720514409189, 19.19230769230769695 ) ) ;
#28480=DIRECTION ( 'NONE',  ( 0.000000000000000000, -1.000000000000000000, 0.000000000000000000 ) ) ;
#28482=ORIENTED_EDGE ( 'NONE', *, *, #6718, .T. ) ;
#28483=VECTOR ( 'NONE', #96857, 1000.000000000000000 ) ;
#28488=VECTOR ( 'NONE', #48611, 1000.000000000000000 ) ;
#28490=CARTESIAN_POINT ( 'NONE',  ( 10.86264264036872440, -0.3587747205144257157, -28.05717073575603138 ) ) ;
#28494=DIRECTION ( 'NONE',  ( -0.6401411605457395515, 0.000000000000000000, -0.7682573101345366862 ) ) ;
#28499=ADVANCED_FACE ( 'NONE', ( #22135 ), #34015, .F. ) ;
#28501=VECTOR ( 'NONE', #30429, 1000.000000000000000 ) ;
#28516=DIRECTION ( 'NONE',  ( 0.000000000000000000, -1.000000000000000000, 0.000000000000000000 ) ) ;
#28517=ORIENTED_EDGE ( 'NONE', *, *, #99415, .T. ) ;
#28531=DIRECTION ( 'NONE',  ( 0.000000000000000000, -1.000000000000000000, 0.000000000000000000 ) ) ;
#28534=CARTESIAN_POINT ( 'NONE',  ( -6.905879715866854340, -6.376774720514411854, 19.48240003225459560 ) ) ;
#28542=CARTESIAN_POINT ( 'NONE',  ( 4.653726706778644306, -5.876774720514415407, 20.04674869880385302 ) ) ;
#28543=VECTOR ( 'NONE', #60142, 999.9999999999998863 ) ;
#28544=B_SPLINE_CURVE_WITH_KNOTS ( 'NONE', 3,
 ( #26856, #89758, #51198, #65945, #50202, #56829, #87762, #96868, #72541, #82141, #27853, #19236, #3034, #25853, #88767, #95366, #11622, #73535, #18735, #58320, #18244, #4028, #58810 ),
 .UNSPECIFIED., .F., .F.,
 ( 4, 1, 1, 1, 1, 1, 1, 1, 1, 1, 1, 1, 1, 1, 1, 1, 1, 1, 1, 1, 4 ),
 ( 0.000000000000000000, 0.06568119799063895647, 0.1284864641740642022, 0.1881751303280073950, 0.2451061306699852116, 0.2994484245294744551, 0.3508229360093824134, 0.3999416805337764336, 0.4466717436323716650, 0.4912545333734980035, 0.5333763442704358981, 0.5738527549682231887, 0.6125263117194529316, 0.6495971364453292374, 0.6855320415538496137, 0.7201057860682000822, 0.7538376629736500689, 0.8189254160467134280, 0.8804934616501639555, 0.9403113338460573623, 1.000000000000000000 ),
 .UNSPECIFIED. ) ;
#28550=CARTESIAN_POINT ( 'NONE',  ( -1.501937386944296460, -5.876774720514415407, 19.86422795159478483 ) ) ;
#28556=CARTESIAN_POINT ( 'NONE',  ( 5.742690948595683409, -6.376774720514427841, 21.62260900090680593 ) ) ;
#28570=EDGE_LOOP ( 'NONE', ( #21248, #65194, #23955, #40149 ) ) ;
#28575=EDGE_CURVE ( 'NONE', #45069, #45070, #21634, .T. ) ;
#28580=CARTESIAN_POINT ( 'NONE',  ( 9.278253834636469577, -5.876774720514426953, 18.51871304725684553 ) ) ;
#28582=ORIENTED_EDGE ( 'NONE', *, *, #45028, .T. ) ;
#28585=ORIENTED_EDGE ( 'NONE', *, *, #45555, .F. ) ;
#28593=EDGE_CURVE ( 'NONE', #20863, #35820, #83545, .T. ) ;
#28598=CIRCLE ( 'NONE', #64348, 252.4458649670781085 ) ;
#28599=DIRECTION ( 'NONE',  ( 0.000000000000000000, 0.000000000000000000, 1.000000000000000000 ) ) ;
#28602=FACE_OUTER_BOUND ( 'NONE', #18849, .T. ) ;
#28609=EDGE_LOOP ( 'NONE', ( #67296, #90429, #4093, #85818 ) ) ;
#28610=CARTESIAN_POINT ( 'NONE',  ( 14.61581676223891613, -2.682774720514426559, -27.35847991879931485 ) ) ;
#28613=ORIENTED_EDGE ( 'NONE', *, *, #2595, .F. ) ;
#28627=DIRECTION ( 'NONE',  ( 0.7071067811865474617, 0.000000000000000000, 0.7071067811865476838 ) ) ;
#28628=FACE_OUTER_BOUND ( 'NONE', #60608, .T. ) ;
#28636=CARTESIAN_POINT ( 'NONE',  ( -27.25988310792305214, -0.3587747205144265483, 30.32664379231667695 ) ) ;
#28638=CARTESIAN_POINT ( 'NONE',  ( 30.60862754225505000, -4.127879075750807480, 27.06827100787837992 ) ) ;
#28639=DIRECTION ( 'NONE',  ( -0.000000000000000000, 1.000000000000000000, -0.000000000000000000 ) ) ;
#28645=LINE ( 'NONE', #81930, #69832 ) ;
#28647=ORIENTED_EDGE ( 'NONE', *, *, #4539, .F. ) ;
#28651=CIRCLE ( 'NONE', #4326, 2.500000000000189626 ) ;
#28655=EDGE_LOOP ( 'NONE', ( #97767, #13845, #4119, #94119 ) ) ;
#28658=DIRECTION ( 'NONE',  ( -0.000000000000000000, 1.000000000000000000, -0.000000000000000000 ) ) ;
#28659=LINE ( 'NONE', #44394, #78364 ) ;
#28663=DIRECTION ( 'NONE',  ( 0.000000000000000000, -1.000000000000000000, 0.000000000000000000 ) ) ;
#28669=CARTESIAN_POINT ( 'NONE',  ( -4.289200894924355190, -5.876774720514414518, 19.85590024959437017 ) ) ;
#28677=FACE_OUTER_BOUND ( 'NONE', #34058, .T. ) ;
#28678=DIRECTION ( 'NONE',  ( 0.9913618264504693300, 5.365801633547217234E-16, -0.1311553622875920033 ) ) ;
#28679=CARTESIAN_POINT ( 'NONE',  ( -1.304987980769231948, -6.376774720514413630, 19.76512419871795245 ) ) ;
#28697=VECTOR ( 'NONE', #38368, 1000.000000000000000 ) ;
#28706=DIRECTION ( 'NONE',  ( 1.000000000000000000, 0.000000000000000000, 0.000000000000000000 ) ) ;
#28711=VECTOR ( 'NONE', #1875, 1000.000000000000000 ) ;
#28714=ORIENTED_EDGE ( 'NONE', *, *, #47939, .T. ) ;
#28728=FACE_OUTER_BOUND ( 'NONE', #62862, .T. ) ;
#28733=EDGE_LOOP ( 'NONE', ( #8839, #84296, #61987 ) ) ;
#28734=FACE_OUTER_BOUND ( 'NONE', #83776, .T. ) ;
#28738=LINE ( 'NONE', #59699, #73405 ) ;
#28749=ORIENTED_EDGE ( 'NONE', *, *, #97337, .T. ) ;
#28757=VECTOR ( 'NONE', #45505, 1000.000000000000000 ) ;
#28761=CARTESIAN_POINT ( 'NONE',  ( 27.53860345374771867, -500000.0000000000582, -9.482392034746242260 ) ) ;
#28762=ORIENTED_EDGE ( 'NONE', *, *, #91146, .F. ) ;
#28770=AXIS2_PLACEMENT_3D ( 'NONE', #94290, #86186, #17170 ) ;
#28775=CARTESIAN_POINT ( 'NONE',  ( -2.656471864501908975, -5.876774720514410077, 19.66116880005639800 ) ) ;
#28784=CARTESIAN_POINT ( 'NONE',  ( -24.55517127435777525, -0.3587747205143967943, -15.44180958690143157 ) ) ;
#28798=DIRECTION ( 'NONE',  ( -0.000000000000000000, -1.000000000000000000, -0.000000000000000000 ) ) ;
#28801=PLANE ( 'NONE',  #72418 ) ;
#28803=CARTESIAN_POINT ( 'NONE',  ( 31.35973677934181936, -4.378374783736292741, 0.3342810658314839256 ) ) ;
#28807=CARTESIAN_POINT ( 'NONE',  ( 22.02124265030973760, -6.376774720514428729, 16.20402280011862217 ) ) ;
#28810=PLANE ( 'NONE',  #67418 ) ;
#28818=EDGE_CURVE ( 'NONE', #56886, #13066, #48504, .T. ) ;
#28825=CARTESIAN_POINT ( 'NONE',  ( 7.072045900997899537, -5.876774720514426953, 21.62824307385093192 ) ) ;
#28826=PLANE ( 'NONE',  #46297 ) ;
#28836=ORIENTED_EDGE ( 'NONE', *, *, #37859, .F. ) ;
#28856=LINE ( 'NONE', #91741, #12959 ) ;
#28857=ORIENTED_EDGE ( 'NONE', *, *, #42201, .F. ) ;
#28867=CARTESIAN_POINT ( 'NONE',  ( 5.697397333356354565, -5.876774720514418071, 20.51730809691671809 ) ) ;
#28883=CARTESIAN_POINT ( 'NONE',  ( -0.5830141525297981575, -5.876774720514410077, 19.15054976246387497 ) ) ;
#28895=LINE ( 'NONE', #45628, #9794 ) ;
#28901=CARTESIAN_POINT ( 'NONE',  ( -4.141025641025640525, -6.376774720514418959, 20.67377804487179915 ) ) ;
#28907=CARTESIAN_POINT ( 'NONE',  ( 15.32643653063177958, -2.682774720514426559, -27.14485409495429380 ) ) ;
#28912=VECTOR ( 'NONE', #24668, 1000.000000000000000 ) ;
#28925=CIRCLE ( 'NONE', #25749, 252.4458649670781085 ) ;
#28930=ORIENTED_EDGE ( 'NONE', *, *, #43090, .F. ) ;
#28939=EDGE_CURVE ( 'NONE', #95847, #90525, #9417, .T. ) ;
#28943=VERTEX_POINT ( 'NONE', #88558 ) ;
#28952=CARTESIAN_POINT ( 'NONE',  ( 32.16024265030974050, -0.3587747205144265483, 16.27760796525321751 ) ) ;
#28958=VERTEX_POINT ( 'NONE', #50007 ) ;
#28987=ORIENTED_EDGE ( 'NONE', *, *, #3147, .F. ) ;
#28988=CARTESIAN_POINT ( 'NONE',  ( -5.903826827417286260, -5.876774720514418071, 20.39230070883895252 ) ) ;
#28990=DIRECTION ( 'NONE',  ( 1.000000000000000000, 0.000000000000000000, 0.000000000000000000 ) ) ;
#28993=CARTESIAN_POINT ( 'NONE',  ( 15.30881860688521989, -3.493868136757170451, -27.16033061360459300 ) ) ;
#29001=CARTESIAN_POINT ( 'NONE',  ( 31.31283134548411340, 1.477225279485574028, -10.20862453625735533 ) ) ;
#29007=LINE ( 'NONE', #29501, #97791 ) ;
#29009=VECTOR ( 'NONE', #18554, 1000.000000000000000 ) ;
#29015=CARTESIAN_POINT ( 'NONE',  ( -7.326923076923076650, -6.376774720514417183, 20.36318108974359831 ) ) ;
#29018=EDGE_CURVE ( 'NONE', #12619, #5267, #41895, .T. ) ;
#29042=LINE ( 'NONE', #59510, #63779 ) ;
#29043=CARTESIAN_POINT ( 'NONE',  ( 4.639188450898540594, -5.876774720514418071, 20.39229233339611014 ) ) ;
#29046=LINE ( 'NONE', #36664, #26499 ) ;
#29051=LINE ( 'NONE', #22418, #26962 ) ;
#29053=ORIENTED_EDGE ( 'NONE', *, *, #63883, .F. ) ;
#29065=LINE ( 'NONE', #58048, #37323 ) ;
#29083=DIRECTION ( 'NONE',  ( -0.000000000000000000, 1.000000000000000000, -0.000000000000000000 ) ) ;
#29095=CARTESIAN_POINT ( 'NONE',  ( 6.666194146093591399, -5.876774720514413630, 19.75460921626947908 ) ) ;
#29097=VERTEX_POINT ( 'NONE', #36267 ) ;
#29109=CARTESIAN_POINT ( 'NONE',  ( -6.775140224358976226, -6.376774720514408301, 19.14743589743590846 ) ) ;
#29110=VECTOR ( 'NONE', #79736, 1000.000000000000000 ) ;
#29111=DIRECTION ( 'NONE',  ( 1.000000000000000000, 0.000000000000000000, -1.257682986112628908E-16 ) ) ;
#29118=CARTESIAN_POINT ( 'NONE',  ( 0.000000000000000000, -2.056774720514426669, 0.000000000000000000 ) ) ;
#29128=CARTESIAN_POINT ( 'NONE',  ( 30.62555539057593634, -4.734697315945937568, 27.74929510164747981 ) ) ;
#29134=ORIENTED_EDGE ( 'NONE', *, *, #50945, .T. ) ;
#29139=CARTESIAN_POINT ( 'NONE',  ( 3.749014282529493869, -6.376774720514404748, 18.52125941707705792 ) ) ;
#29141=ADVANCED_FACE ( 'NONE', ( #74811 ), #21514, .F. ) ;
#29148=EDGE_CURVE ( 'NONE', #78994, #404, #42889, .T. ) ;
#29161=CARTESIAN_POINT ( 'NONE',  ( 13.91401389203221406, 5.965225279485572685, 158.0376437107427137 ) ) ;
#29167=CARTESIAN_POINT ( 'NONE',  ( -65.05438548721848235, -5.356774720514425603, 0.7300228001186309656 ) ) ;
#29175=AXIS2_PLACEMENT_3D ( 'NONE', #74755, #81880, #73765 ) ;
#29176=ADVANCED_FACE ( 'NONE', ( #89552 ), #44383, .T. ) ;
#29187=CYLINDRICAL_SURFACE ( 'NONE', #9094, 0.3000000000000016542 ) ;
#29188=VECTOR ( 'NONE', #50430, 1000.000000000000000 ) ;
#29192=DIRECTION ( 'NONE',  ( -0.4009304992412300317, 6.845827386180410961E-16, -0.9161084732596779245 ) ) ;
#29200=FACE_OUTER_BOUND ( 'NONE', #34241, .T. ) ;
#29209=ORIENTED_EDGE ( 'NONE', *, *, #15700, .F. ) ;
#29217=CARTESIAN_POINT ( 'NONE',  ( 32.45853543194704116, -0.3587747205144265483, 9.169203677920338080 ) ) ;
#29221=CARTESIAN_POINT ( 'NONE',  ( -3.035630128403670192, -6.376774720514413630, 19.71630089903357685 ) ) ;
#29223=CARTESIAN_POINT ( 'NONE',  ( -4.635780534842457001, -6.376774720514410077, 19.53657742262743113 ) ) ;
#29226=CARTESIAN_POINT ( 'NONE',  ( 10.24059822343757808, -5.876774720514426953, 17.91871304725684766 ) ) ;
#29233=ORIENTED_EDGE ( 'NONE', *, *, #43319, .F. ) ;
#29245=ORIENTED_EDGE ( 'NONE', *, *, #99760, .F. ) ;
#29246=FACE_OUTER_BOUND ( 'NONE', #7395, .T. ) ;
#29247=AXIS2_PLACEMENT_3D ( 'NONE', #2925, #26246, #40474 ) ;
#29250=CARTESIAN_POINT ( 'NONE',  ( -27.15721599100127648, -6.376774720514425177, -10.22292133548837256 ) ) ;
#29251=ORIENTED_EDGE ( 'NONE', *, *, #29018, .F. ) ;
#29255=EDGE_CURVE ( 'NONE', #3834, #49731, #85421, .T. ) ;
#29258=CARTESIAN_POINT ( 'NONE',  ( 0.000000000000000000, -5.876774720514426953, 15.00000000000000178 ) ) ;
#29259=CARTESIAN_POINT ( 'NONE',  ( -5.837039262820512775, -5.876774720514413630, 19.76512419871795245 ) ) ;
#29278=DIRECTION ( 'NONE',  ( -0.1875268396392987258, 0.000000000000000000, -0.9822594791677485837 ) ) ;
#29285=ADVANCED_FACE ( 'NONE', ( #84425 ), #15405, .T. ) ;
#29288=DIRECTION ( 'NONE',  ( 0.000000000000000000, 0.000000000000000000, -1.000000000000000000 ) ) ;
#29291=ADVANCED_FACE ( 'NONE', ( #69712 ), #99630, .F. ) ;
#29299=ORIENTED_EDGE ( 'NONE', *, *, #46001, .F. ) ;
#29303=CARTESIAN_POINT ( 'NONE',  ( -4.141025641025638748, -6.376774720514427841, 21.75000000000000355 ) ) ;
#29306=B_SPLINE_CURVE_WITH_KNOTS ( 'NONE', 3,
 ( #31221, #62190, #93115, #21601, #85505, #76388, #44469, #5890, #54083, #68797, #67815, #75894, #61201, #98738, #91127, #92614, #53084, #45964, #69291, #22591, #52574, #84511, #83509 ),
 .UNSPECIFIED., .F., .F.,
 ( 4, 1, 1, 1, 1, 1, 1, 1, 1, 1, 1, 1, 1, 1, 1, 1, 1, 1, 1, 1, 4 ),
 ( 0.000000000000000000, 0.06038661931106227565, 0.1208832485859964029, 0.1827546186251403082, 0.2478110297583512034, 0.2812991000432494282, 0.3150876241506579412, 0.3497023955502757131, 0.3848565811185565289, 0.4209661972261032892, 0.4585111882611391243, 0.4971747221273126183, 0.5376020478662695279, 0.5805030184200120624, 0.6274675400267057945, 0.6783882095592440598, 0.7339832205925608255, 0.7937467045508355135, 0.8577136721607333536, 0.9266978643613864586, 1.000000000000000000 ),
 .UNSPECIFIED. ) ;
#29307=EDGE_CURVE ( 'NONE', #78121, #37899, #77299, .T. ) ;
#29311=CARTESIAN_POINT ( 'NONE',  ( 7.166666666666668739, -5.876774720514419847, 20.78665865384614975 ) ) ;
#29315=AXIS2_PLACEMENT_3D ( 'NONE', #1707, #25025, #63112 ) ;
#29319=DIRECTION ( 'NONE',  ( 0.6599726524652352877, 0.000000000000000000, -0.7512896232465891000 ) ) ;
#29323=CARTESIAN_POINT ( 'NONE',  ( -4.401146115524053215, -5.876774720514411854, 19.34190049657481936 ) ) ;
#29344=VERTEX_POINT ( 'NONE', #87935 ) ;
#29346=CYLINDRICAL_SURFACE ( 'NONE', #34508, 8.452410033082760066 ) ;
#29350=ORIENTED_EDGE ( 'NONE', *, *, #34030, .T. ) ;
#29351=CARTESIAN_POINT ( 'NONE',  ( 4.588387839717440464, -5.876774720514399419, 18.52756237589653665 ) ) ;
#29352=ORIENTED_EDGE ( 'NONE', *, *, #5711, .T. ) ;
#29360=CARTESIAN_POINT ( 'NONE',  ( 6.044119082205957838, -6.376774720514424288, 21.40268112089023589 ) ) ;
#29368=DIRECTION ( 'NONE',  ( -1.000000000000000000, 1.232047923278981953E-16, 0.000000000000000000 ) ) ;
#29379=DIRECTION ( 'NONE',  ( -0.000000000000000000, -1.000000000000000000, -0.000000000000000000 ) ) ;
#29389=CARTESIAN_POINT ( 'NONE',  ( 2.589743589743596086, -6.376774720514415407, 20.00140224358974095 ) ) ;
#29395=ORIENTED_EDGE ( 'NONE', *, *, #1936, .T. ) ;
#29397=DIRECTION ( 'NONE',  ( 0.000000000000000000, 0.000000000000000000, -1.000000000000000000 ) ) ;
#29400=ORIENTED_EDGE ( 'NONE', *, *, #92519, .F. ) ;
#29410=ORIENTED_EDGE ( 'NONE', *, *, #1162, .F. ) ;
#29414=CARTESIAN_POINT ( 'NONE',  ( 33.61752870511802627, -3.456547803086310378, -11.38123630260490948 ) ) ;
#29428=CARTESIAN_POINT ( 'NONE',  ( 2.903846153846159517, -6.376774720514415407, 19.99999999999999289 ) ) ;
#29434=ADVANCED_FACE ( 'NONE', ( #56000 ), #64123, .F. ) ;
#29449=CIRCLE ( 'NONE', #53808, 84.48086791635431325 ) ;
#29470=AXIS2_PLACEMENT_3D ( 'NONE', #60519, #43786, #51398 ) ;
#29479=DIRECTION ( 'NONE',  ( 0.000000000000000000, 0.000000000000000000, -1.000000000000000000 ) ) ;
#29483=CARTESIAN_POINT ( 'NONE',  ( 14.64534568429317218, -3.754078354150065522, -27.31564152833324499 ) ) ;
#29488=CARTESIAN_POINT ( 'NONE',  ( 29.61836285113398048, -5.182350003425200136, 28.59212231372686119 ) ) ;
#29489=EDGE_CURVE ( 'NONE', #49712, #90366, #74209, .T. ) ;
#29490=EDGE_CURVE ( 'NONE', #35863, #54059, #44759, .T. ) ;
#29501=CARTESIAN_POINT ( 'NONE',  ( -27.25988310792305214, -0.3587747205144265483, 30.32664379231667695 ) ) ;
#29519=VECTOR ( 'NONE', #45402, 1000.000000000000000 ) ;
#29520=AXIS2_PLACEMENT_3D ( 'NONE', #41550, #94821, #57777 ) ;
#29524=ORIENTED_EDGE ( 'NONE', *, *, #95888, .T. ) ;
#29531=DIRECTION ( 'NONE',  ( 0.000000000000000000, 1.000000000000000000, 0.000000000000000000 ) ) ;
#29539=DIRECTION ( 'NONE',  ( -0.000000000000000000, 0.000000000000000000, -1.000000000000000000 ) ) ;
#29541=AXIS2_PLACEMENT_3D ( 'NONE', #45006, #75925, #38869 ) ;
#29547=ADVANCED_FACE ( 'NONE', ( #54875 ), #7521, .T. ) ;
#29549=CARTESIAN_POINT ( 'NONE',  ( -1.456683411003494966, -6.376774720514415407, 19.95737465391042775 ) ) ;
#29552=CARTESIAN_POINT ( 'NONE',  ( 5.328346181807287252, -6.376774720514418959, 20.81670806933143680 ) ) ;
#29558=CYLINDRICAL_SURFACE ( 'NONE', #73572, 251.9358649670780892 ) ;
#29566=CARTESIAN_POINT ( 'NONE',  ( -0.02075734969026423599, 6.475225279485573360, -0.08597719988137648983 ) ) ;
#29570=DIRECTION ( 'NONE',  ( -0.000000000000000000, -1.000000000000000000, -0.000000000000000000 ) ) ;
#29581=FACE_OUTER_BOUND ( 'NONE', #49974, .T. ) ;
#29585=ORIENTED_EDGE ( 'NONE', *, *, #13711, .T. ) ;
#29590=CARTESIAN_POINT ( 'NONE',  ( 0.3910256410256394144, -6.376774720514411854, 19.63681891025641235 ) ) ;
#29594=AXIS2_PLACEMENT_3D ( 'NONE', #2721, #33661, #95557 ) ;
#29602=ORIENTED_EDGE ( 'NONE', *, *, #62396, .F. ) ;
#29608=CARTESIAN_POINT ( 'NONE',  ( 7.433267315672343223, -6.376774720514418959, 20.43888261666079842 ) ) ;
#29611=EDGE_CURVE ( 'NONE', #46585, #34762, #64515, .T. ) ;
#29616=CARTESIAN_POINT ( 'NONE',  ( 31.16918082143019220, -5.911085521256299380, -1.357342440710215481 ) ) ;
#29620=B_SPLINE_CURVE_WITH_KNOTS ( 'NONE', 3,
 ( #68943, #74558, #28883, #6547, #68446, #84158, #59847, #66967, #97879, #14649, #37993, #82665, #44115, #75043, #5539 ),
 .UNSPECIFIED., .F., .F.,
 ( 4, 1, 1, 1, 1, 1, 1, 1, 1, 1, 1, 1, 4 ),
 ( 0.000000000000000000, 0.08415201884431637580, 0.1665323202984579920, 0.2488363311465297822, 0.3312461454872601685, 0.4129571090216147544, 0.4904942776695643825, 0.5661557919819225626, 0.6399873346864677348, 0.7167654882718510478, 0.8021439047100968889, 0.8958332007101900141, 1.000000000000000000 ),
 .UNSPECIFIED. ) ;
#29621=ORIENTED_EDGE ( 'NONE', *, *, #18044, .F. ) ;
#29630=CARTESIAN_POINT ( 'NONE',  ( 5.864177746775673050, -5.876774720514425177, 21.69926562011473337 ) ) ;
#29631=AXIS2_PLACEMENT_3D ( 'NONE', #90816, #75574, #5576 ) ;
#29639=ORIENTED_EDGE ( 'NONE', *, *, #66242, .F. ) ;
#29640=CARTESIAN_POINT ( 'NONE',  ( 2.949406532984364393, -6.376774720514410077, 19.42899254576129664 ) ) ;
#29641=DIRECTION ( 'NONE',  ( 0.000000000000000000, -1.000000000000000000, 0.000000000000000000 ) ) ;
#29665=AXIS2_PLACEMENT_3D ( 'NONE', #49232, #3049, #64470 ) ;
#29673=CARTESIAN_POINT ( 'NONE',  ( -1.967852706420949005, -6.376774720514408301, 19.18381548539530357 ) ) ;
#29690=CARTESIAN_POINT ( 'NONE',  ( 0.3180806761505774460, -6.376774720514415407, 20.02963804100705403 ) ) ;
#29700=EDGE_CURVE ( 'NONE', #14119, #6499, #95019, .T. ) ;
#29704=VERTEX_POINT ( 'NONE', #90811 ) ;
#29718=FACE_OUTER_BOUND ( 'NONE', #3641, .T. ) ;
#29722=CARTESIAN_POINT ( 'NONE',  ( -4.243469080022288509, -6.376774720514411854, 19.94806476610987644 ) ) ;
#29724=ORIENTED_EDGE ( 'NONE', *, *, #64631, .F. ) ;
#29733=VERTEX_POINT ( 'NONE', #73103 ) ;
#29741=LINE ( 'NONE', #62202, #5963 ) ;
#29744=ORIENTED_EDGE ( 'NONE', *, *, #98722, .F. ) ;
#29752=DIRECTION ( 'NONE',  ( 0.000000000000000000, 0.000000000000000000, 1.000000000000000000 ) ) ;
#29758=CARTESIAN_POINT ( 'NONE',  ( -24.90875734969025501, -6.376774720514426953, 26.43402280011862615 ) ) ;
#29763=LINE ( 'NONE', #68829, #28697 ) ;
#29776=AXIS2_PLACEMENT_3D ( 'NONE', #41025, #32405, #63880 ) ;
#29778=CARTESIAN_POINT ( 'NONE',  ( 3.509873074917118085, -0.3587747205144265483, 29.15869884040363758 ) ) ;
#29792=ORIENTED_EDGE ( 'NONE', *, *, #58936, .T. ) ;
#29797=CARTESIAN_POINT ( 'NONE',  ( -23.31187512739357359, 5.965225279485572685, -17.31005501743528185 ) ) ;
#29799=ORIENTED_EDGE ( 'NONE', *, *, #3044, .T. ) ;
#29800=LINE ( 'NONE', #99308, #83213 ) ;
#29809=VECTOR ( 'NONE', #27091, 1000.000000000000000 ) ;
#29810=CARTESIAN_POINT ( 'NONE',  ( 26.73860345374794178, -1.682774720514426114, -1.272392034746785860 ) ) ;
#29816=EDGE_CURVE ( 'NONE', #94137, #76027, #11679, .T. ) ;
#29817=B_SPLINE_CURVE_WITH_KNOTS ( 'NONE', 3,
 ( #66430, #51181, #27837, #88247, #87745, #18716 ),
 .UNSPECIFIED., .F., .F.,
 ( 4, 2, 4 ),
 ( 0.000000000000000000, 0.0005107898210030667376, 0.001021579642006133475 ),
 .UNSPECIFIED. ) ;
#29825=EDGE_LOOP ( 'NONE', ( #24879, #42857, #22105, #87753 ) ) ;
#29828=B_SPLINE_CURVE_WITH_KNOTS ( 'NONE', 3,
 ( #50412, #27576, #74239, #10342, #35186, #65657, #4734, #58526 ),
 .UNSPECIFIED., .F., .F.,
 ( 4, 2, 2, 4 ),
 ( 0.09426293957327776252, 0.09592851477271921445, 0.09759408997216065251, 0.1009252403710435564 ),
 .UNSPECIFIED. ) ;
#29836=EDGE_CURVE ( 'NONE', #48360, #28254, #38518, .T. ) ;
#29838=EDGE_CURVE ( 'NONE', #62214, #65103, #52256, .T. ) ;
#29842=ORIENTED_EDGE ( 'NONE', *, *, #84391, .T. ) ;
#29852=CARTESIAN_POINT ( 'NONE',  ( 4.740341618695937065, -6.376774720514404748, 18.75174579344860248 ) ) ;
#29854=EDGE_CURVE ( 'NONE', #22734, #35967, #29903, .T. ) ;
#29881=VECTOR ( 'NONE', #9999, 1000.000000000000000 ) ;
#29902=CARTESIAN_POINT ( 'NONE',  ( -5.891303133519534718, -5.876774720514419847, 20.71116975788854475 ) ) ;
#29903=LINE ( 'NONE', #15176, #51277 ) ;
#29915=CARTESIAN_POINT ( 'NONE',  ( 33.41145047975789595, -4.538943570064395416, -12.61568413423384172 ) ) ;
#29924=CARTESIAN_POINT ( 'NONE',  ( -1.001577508147789342, -5.876774720514411854, 19.87297243748311004 ) ) ;
#29932=LINE ( 'NONE', #83217, #3061 ) ;
#29933=CARTESIAN_POINT ( 'NONE',  ( 5.727631217150810805, -5.876774720514421624, 21.11407618546790133 ) ) ;
#29934=AXIS2_PLACEMENT_3D ( 'NONE', #34427, #43046, #97322 ) ;
#29943=CARTESIAN_POINT ( 'NONE',  ( -22.05275734969026047, 5.965225279485572685, 30.51402280011862089 ) ) ;
#29960=CARTESIAN_POINT ( 'NONE',  ( -4.495793269230770939, -5.876774720514410077, 19.27714342948718595 ) ) ;
#29961=CARTESIAN_POINT ( 'NONE',  ( 2.933277810221831761, -5.876774720514424288, 21.39432064584807947 ) ) ;
#29983=CARTESIAN_POINT ( 'NONE',  ( -5.895658455092926076, -5.876774720514418071, 20.50445910983877340 ) ) ;
#29990=VERTEX_POINT ( 'NONE', #76563 ) ;
#30009=DIRECTION ( 'NONE',  ( 0.000000000000000000, 0.000000000000000000, 1.000000000000000000 ) ) ;
#30016=DIRECTION ( 'NONE',  ( 0.000000000000000000, 0.000000000000000000, 1.000000000000000000 ) ) ;
#30020=DIRECTION ( 'NONE',  ( -0.7071067811865474617, 0.000000000000000000, -0.7071067811865476838 ) ) ;
#30024=CARTESIAN_POINT ( 'NONE',  ( -1.358974358974357921, -6.376774720514420736, 20.75510817307693046 ) ) ;
#30034=LINE ( 'NONE', #83331, #14563 ) ;
#30035=VECTOR ( 'NONE', #17825, 1000.000000000000000 ) ;
#30041=CARTESIAN_POINT ( 'NONE',  ( -1.743696941008423984, -5.876774720514413630, 19.59984006504825160 ) ) ;
#30044=CARTESIAN_POINT ( 'NONE',  ( 5.331146515430939203, -6.376774720514420736, 20.91308853528358469 ) ) ;
#30045=VERTEX_POINT ( 'NONE', #17179 ) ;
#30050=EDGE_CURVE ( 'NONE', #12135, #5267, #2469, .T. ) ;
#30056=CARTESIAN_POINT ( 'NONE',  ( -1.488488975859286523, -5.876774720514410966, 19.49847411603315095 ) ) ;
#30072=ORIENTED_EDGE ( 'NONE', *, *, #57570, .T. ) ;
#30074=AXIS2_PLACEMENT_3D ( 'NONE', #8289, #39235, #60603 ) ;
#30075=ORIENTED_EDGE ( 'NONE', *, *, #45836, .F. ) ;
#30091=CARTESIAN_POINT ( 'NONE',  ( 32.87794144969610244, -3.622774687813811845, -13.08434676285136256 ) ) ;
#30092=CARTESIAN_POINT ( 'NONE',  ( 27.53860345374808105, -5.356774720514425603, -6.982392034745776854 ) ) ;
#30104=CARTESIAN_POINT ( 'NONE',  ( -7.627782137226129855, -6.376774720514413630, 20.04377961306771994 ) ) ;
#30106=LINE ( 'NONE', #83899, #22205 ) ;
#30108=CARTESIAN_POINT ( 'NONE',  ( -0.7614568544629641833, -6.376774720514408301, 19.18727597066020962 ) ) ;
#30122=CARTESIAN_POINT ( 'NONE',  ( 21.29879217689888904, -4.383176333286276538, -16.78405200760721527 ) ) ;
#30123=LINE ( 'NONE', #97277, #88105 ) ;
#30133=CARTESIAN_POINT ( 'NONE',  ( 3.252808283508203058, -5.876774720514403860, 18.30939203766361345 ) ) ;
#30148=CARTESIAN_POINT ( 'NONE',  ( -53.01255352321339842, -2.682774720514426559, 35.59556822165056644 ) ) ;
#30153=VECTOR ( 'NONE', #55971, 1000.000000000000114 ) ;
#30159=VECTOR ( 'NONE', #98015, 1000.000000000000000 ) ;
#30163=LINE ( 'NONE', #47400, #60503 ) ;
#30185=EDGE_CURVE ( 'NONE', #67539, #41980, #45478, .T. ) ;
#30194=CARTESIAN_POINT ( 'NONE',  ( 4.966983519792414370, -6.376774720514415407, 19.83633487160803099 ) ) ;
#30196=ORIENTED_EDGE ( 'NONE', *, *, #98220, .F. ) ;
#30206=CARTESIAN_POINT ( 'NONE',  ( -2.606012662418322634, -6.376774720514410077, 19.21974929698718881 ) ) ;
#30210=CIRCLE ( 'NONE', #88603, 3.060000000000000053 ) ;
#30211=CARTESIAN_POINT ( 'NONE',  ( -4.194375271223358403, -6.376774720514417183, 20.09898898868106087 ) ) ;
#30213=ORIENTED_EDGE ( 'NONE', *, *, #98736, .T. ) ;
#30217=ORIENTED_EDGE ( 'NONE', *, *, #25121, .F. ) ;
#30219=ORIENTED_EDGE ( 'NONE', *, *, #76107, .T. ) ;
#30222=ORIENTED_EDGE ( 'NONE', *, *, #39212, .F. ) ;
#30239=EDGE_CURVE ( 'NONE', #90630, #86027, #93618, .T. ) ;
#30260=AXIS2_PLACEMENT_3D ( 'NONE', #176, #62584, #100105 ) ;
#30261=CARTESIAN_POINT ( 'NONE',  ( -2.283364382221138467, -6.376774720514411854, 19.46427715384223944 ) ) ;
#30269=CARTESIAN_POINT ( 'NONE',  ( 9.940598223437577374, -5.876774720514426953, 17.91871304725684766 ) ) ;
#30272=CARTESIAN_POINT ( 'NONE',  ( 3.879812756903532556, -5.876774720514401196, 18.16163344421570969 ) ) ;
#30286=CARTESIAN_POINT ( 'NONE',  ( 3.251543564379332008, -5.876774720514424288, 21.68810402963413964 ) ) ;
#30288=LINE ( 'NONE', #60763, #60280 ) ;
#30290=DIRECTION ( 'NONE',  ( 0.000000000000000000, 1.000000000000000000, 0.000000000000000000 ) ) ;
#30294=VECTOR ( 'NONE', #60709, 1000.000000000000000 ) ;
#30311=EDGE_CURVE ( 'NONE', #58343, #73040, #26941, .T. ) ;
#30312=CARTESIAN_POINT ( 'NONE',  ( -5.654682302363691626, -5.876774720514410077, 19.41635569784906323 ) ) ;
#30323=ORIENTED_EDGE ( 'NONE', *, *, #71144, .F. ) ;
#30330=CIRCLE ( 'NONE', #56293, 2.999999999999999112 ) ;
#30337=VERTEX_POINT ( 'NONE', #68336 ) ;
#30341=AXIS2_PLACEMENT_3D ( 'NONE', #20036, #81935, #12417 ) ;
#30347=B_SPLINE_SURFACE_WITH_KNOTS ( 'NONE', 3, 1, ( 
 ( #54516, #23033 ),
 ( #25052, #15935 ),
 ( #46901, #77824 ),
 ( #8333, #39277 ),
 ( #54028, #93556 ),
 ( #27066, #17950 ),
 ( #97070, #4229 ),
 ( #3248, #73245 ),
 ( #72750, #57532 ),
 ( #18942, #27572 ),
 ( #58030, #80853 ),
 ( #80346, #26059 ),
 ( #48913, #34680 ),
 ( #50906, #57031 ),
 ( #79839, #35182 ),
 ( #33679, #89464 ),
 ( #26572, #65653 ),
 ( #64658, #56529 ),
 ( #96565, #10337 ) ),
 .UNSPECIFIED., .F., .F., .F.,
 ( 4, 1, 1, 1, 1, 1, 1, 1, 1, 1, 1, 1, 1, 1, 1, 1, 4 ),
 ( 2, 2 ),
 ( 0.000000000000000000, 0.06761452606740248061, 0.1311670463014500410, 0.1902933887105124899, 0.2450610151831994488, 0.2960272302790624144, 0.3428447301738887232, 0.3860527037713296084, 0.4255709801320516350, 0.4995034801514134370, 0.5702922612469545349, 0.6402757819125004524, 0.7105295546786234429, 0.7812030014762999519, 0.8520349845172642267, 0.9243956695042543359, 1.000000000000000000 ),
 ( 0.000000000000000000, 1.000000000000000000 ),
 .UNSPECIFIED. ) ;
#30349=ORIENTED_EDGE ( 'NONE', *, *, #24946, .T. ) ;
#30359=CARTESIAN_POINT ( 'NONE',  ( 5.864225667603142789, -6.376774720514424288, 21.27837265517432996 ) ) ;
#30361=ORIENTED_EDGE ( 'NONE', *, *, #68696, .T. ) ;
#30363=CARTESIAN_POINT ( 'NONE',  ( 5.250998264632097623, -5.356774720514425603, -25.47015671074452925 ) ) ;
#30382=DIRECTION ( 'NONE',  ( 0.000000000000000000, 0.000000000000000000, -1.000000000000000000 ) ) ;
#30387=DIRECTION ( 'NONE',  ( 0.000000000000000000, 0.000000000000000000, -1.000000000000000000 ) ) ;
#30396=( BOUNDED_SURFACE ( )  B_SPLINE_SURFACE ( 3, 2, ( 
 ( #100077, #38200, #91991 ),
 ( #30091, #38702, #22462 ),
 ( #53450, #54945, #85885 ),
 ( #69666, #47830, #93481 ),
 ( #143, #30592, #84378 ),
 ( #85374, #24479, #78752 ) ),
 .UNSPECIFIED., .F., .F., .T. ) 
 B_SPLINE_SURFACE_WITH_KNOTS ( ( 4, 2, 4 ),
 ( 3, 3 ),
 ( 0.001113071882895040263, 0.001219813747004279327, 0.001326555611113518392 ),
 ( 0.000000000000000000, 1.000000000000000000 ),
 .UNSPECIFIED. ) 
 GEOMETRIC_REPRESENTATION_ITEM ( )  RATIONAL_B_SPLINE_SURFACE ( (
 ( 1.000000000000000000, 0.7071067811865114905, 1.000000000000000000),
 ( 1.000000000000000000, 0.7264088502634352684, 1.000000000000000000),
 ( 1.000000000000000000, 0.7445305694446069378, 1.000000000000000000),
 ( 1.000000000000000000, 0.7788548593121751296, 1.000000000000000000),
 ( 1.000000000000000000, 0.7952519535464425138, 1.000000000000000000),
 ( 1.000000000000000000, 0.8096947957033885368, 1.000000000000000000) ) ) 
 REPRESENTATION_ITEM ( '' )  SURFACE ( )  );
#30416=CARTESIAN_POINT ( 'NONE',  ( 33.10022444407529463, -4.633339536272139902, -11.64480304263449106 ) ) ;
#30427=LINE ( 'NONE', #52777, #51605 ) ;
#30428=ORIENTED_EDGE ( 'NONE', *, *, #45047, .F. ) ;
#30429=DIRECTION ( 'NONE',  ( 0.000000000000000000, 0.000000000000000000, -1.000000000000000000 ) ) ;
#30435=CARTESIAN_POINT ( 'NONE',  ( -10.16634758543296613, 5.965225279485572685, 30.00402280011862288 ) ) ;
#30436=CARTESIAN_POINT ( 'NONE',  ( 6.044119082205957838, -5.876774720514424288, 21.40268112089023589 ) ) ;
#30440=CARTESIAN_POINT ( 'NONE',  ( -16.22218391600152643, -6.376774720514426953, -54.85883559227303863 ) ) ;
#30444=VECTOR ( 'NONE', #54555, 999.9999999999998863 ) ;
#30449=DIRECTION ( 'NONE',  ( -0.000000000000000000, -1.000000000000000000, -0.000000000000000000 ) ) ;
#30451=CARTESIAN_POINT ( 'NONE',  ( -24.97666371003640151, 5.965225279485592225, -15.72894043976419098 ) ) ;
#30458=ORIENTED_EDGE ( 'NONE', *, *, #87604, .T. ) ;
#30464=ADVANCED_FACE ( 'NONE', ( #32761 ), #78926, .F. ) ;
#30469=LINE ( 'NONE', #84247, #42182 ) ;
#30492=VERTEX_POINT ( 'NONE', #17539 ) ;
#30514=EDGE_CURVE ( 'NONE', #93024, #20487, #12008, .T. ) ;
#30515=CARTESIAN_POINT ( 'NONE',  ( -27.25988310792305214, -0.3587747205144265483, 30.32664379231667695 ) ) ;
#30516=ORIENTED_EDGE ( 'NONE', *, *, #66200, .F. ) ;
#30530=DIRECTION ( 'NONE',  ( 0.000000000000000000, -1.000000000000000000, 0.000000000000000000 ) ) ;
#30534=DIRECTION ( 'NONE',  ( 0.000000000000000000, -1.000000000000000000, 0.000000000000000000 ) ) ;
#30536=CARTESIAN_POINT ( 'NONE',  ( -10.21384395349174490, -6.376774720514426953, 29.49402280011861777 ) ) ;
#30546=CARTESIAN_POINT ( 'NONE',  ( 4.653846153846159517, -5.876774720514419847, 19.99999999999999289 ) ) ;
#30573=ORIENTED_EDGE ( 'NONE', *, *, #82640, .F. ) ;
#30574=CARTESIAN_POINT ( 'NONE',  ( -6.499903988472228278, -6.376774720514408301, 19.18381548539529646 ) ) ;
#30582=CARTESIAN_POINT ( 'NONE',  ( 14.76093561896379214, 6.475225279485574248, -27.37148769130089931 ) ) ;
#30586=DIRECTION ( 'NONE',  ( 0.000000000000000000, 1.000000000000000000, 0.000000000000000000 ) ) ;
#30592=CARTESIAN_POINT ( 'NONE',  ( 33.34043384136952426, -4.658726884274800639, -12.67806891602219821 ) ) ;
#30593=FACE_OUTER_BOUND ( 'NONE', #83227, .T. ) ;
#30611=ORIENTED_EDGE ( 'NONE', *, *, #7194, .T. ) ;
#30613=CARTESIAN_POINT ( 'NONE',  ( 0.7051282051282027341, -5.876774720514409189, 19.19230769230768985 ) ) ;
#30614=CARTESIAN_POINT ( 'NONE',  ( 32.15269211224249091, -4.540774720514427543, 3.401810532325273861 ) ) ;
#30617=EDGE_LOOP ( 'NONE', ( #34929, #59658, #6427, #41323, #60113 ) ) ;
#30624=CARTESIAN_POINT ( 'NONE',  ( 5.742690948595683409, -5.876774720514426953, 21.62260900090680593 ) ) ;
#30637=CARTESIAN_POINT ( 'NONE',  ( 2.834823996951755465, -6.376774720514406525, 18.76222163777333307 ) ) ;
#30639=AXIS2_PLACEMENT_3D ( 'NONE', #34850, #97244, #73417 ) ;
#30648=VECTOR ( 'NONE', #83951, 1000.000000000000000 ) ;
#30651=ADVANCED_FACE ( 'NONE', ( #14904 ), #45878, .F. ) ;
#30657=CARTESIAN_POINT ( 'NONE',  ( 4.653726706778644306, -6.376774720514415407, 20.04674869880385302 ) ) ;
#30659=CARTESIAN_POINT ( 'NONE',  ( 6.424528460793287543, -6.376774720514413630, 19.73230822599986212 ) ) ;
#30661=CIRCLE ( 'NONE', #98664, 4.080000000000000071 ) ;
#30678=LINE ( 'NONE', #53536, #38675 ) ;
#30684=CARTESIAN_POINT ( 'NONE',  ( 0.09189959430841809773, -5.876774720514410077, 19.67013632031035542 ) ) ;
#30695=EDGE_CURVE ( 'NONE', #42749, #58613, #32136, .T. ) ;
#30699=EDGE_LOOP ( 'NONE', ( #1008, #61422 ) ) ;
#30709=CARTESIAN_POINT ( 'NONE',  ( 33.74607884027702909, 5.965225279485572685, -4.999864028243830916 ) ) ;
#30710=CARTESIAN_POINT ( 'NONE',  ( -4.141439336867657417, -5.876774720514418071, 20.56083401959468304 ) ) ;
#30713=CARTESIAN_POINT ( 'NONE',  ( 17.47419131657910540, 5.965225279485572685, 28.31804950686278843 ) ) ;
#30716=CARTESIAN_POINT ( 'NONE',  ( -29.49875734969025842, 5.965225279485572685, 25.61802280011862720 ) ) ;
#30745=VERTEX_POINT ( 'NONE', #9296 ) ;
#30746=VERTEX_POINT ( 'NONE', #93028 ) ;
#30747=CARTESIAN_POINT ( 'NONE',  ( -29.49875734969025842, 5.965225279485572685, 17.86602280011862476 ) ) ;
#30751=ORIENTED_EDGE ( 'NONE', *, *, #16895, .F. ) ;
#30769=FACE_OUTER_BOUND ( 'NONE', #883, .T. ) ;
#30772=LINE ( 'NONE', #93660, #95827 ) ;
#30781=LINE ( 'NONE', #46019, #73293 ) ;
#30792=VECTOR ( 'NONE', #15125, 1000.000000000000000 ) ;
#30797=CARTESIAN_POINT ( 'NONE',  ( 3.797776442307698286, -6.376774720514427841, 21.83974358974358410 ) ) ;
#30805=FACE_OUTER_BOUND ( 'NONE', #28609, .T. ) ;
#30826=CARTESIAN_POINT ( 'NONE',  ( 13.91401389203221406, -5.356774720514425603, 158.0376437107427137 ) ) ;
#30845=VERTEX_POINT ( 'NONE', #86926 ) ;
#30847=AXIS2_PLACEMENT_3D ( 'NONE', #15619, #48092, #24731 ) ;
#30855=CARTESIAN_POINT ( 'NONE',  ( 4.190829928318763109, -6.376774720514401196, 18.23548058298382557 ) ) ;
#30863=CARTESIAN_POINT ( 'NONE',  ( -27.96875734969026084, -6.376774720514426953, 26.43402280011862615 ) ) ;
#30864=VERTEX_POINT ( 'NONE', #34157 ) ;
#30867=AXIS2_PLACEMENT_3D ( 'NONE', #96705, #64798, #80483 ) ;
#30869=CARTESIAN_POINT ( 'NONE',  ( 4.784292611718076849, -5.356774720514425603, -25.54547254883186014 ) ) ;
#30889=ADVANCED_FACE ( 'NONE', ( #96540 ), #40758, .F. ) ;
#30895=DIRECTION ( 'NONE',  ( -0.9978940991575085961, 0.000000000000000000, -0.06486421869277853025 ) ) ;
#30904=CARTESIAN_POINT ( 'NONE',  ( -5.960145391809922089, -5.876774720514415407, 20.04104409779160534 ) ) ;
#30905=DIRECTION ( 'NONE',  ( 0.000000000000000000, -1.000000000000000000, 0.000000000000000000 ) ) ;
#30916=CARTESIAN_POINT ( 'NONE',  ( 33.50941771711502071, -4.400593307868461146, -12.46354170163592556 ) ) ;
#30924=ADVANCED_FACE ( 'NONE', ( #71715 ), #57002, .T. ) ;
#30928=AXIS2_PLACEMENT_3D ( 'NONE', #47368, #93022, #23499 ) ;
#30952=ORIENTED_EDGE ( 'NONE', *, *, #32537, .F. ) ;
#30969=CARTESIAN_POINT ( 'NONE',  ( 25.82162523591733816, -4.375719933211353663, -11.31246283257596552 ) ) ;
#30974=CARTESIAN_POINT ( 'NONE',  ( -19.77875734969026311, -5.356774720514425603, 27.31649921512899937 ) ) ;
#30976=DIRECTION ( 'NONE',  ( 0.000000000000000000, -7.805083003223303470E-15, 1.000000000000000000 ) ) ;
#30977=CARTESIAN_POINT ( 'NONE',  ( 4.967622410992271753, -5.876774720514416295, 20.05703257908297843 ) ) ;
#30982=ORIENTED_EDGE ( 'NONE', *, *, #36567, .T. ) ;
#30987=( BOUNDED_SURFACE ( )  B_SPLINE_SURFACE ( 3, 2, ( 
 ( #52270, #59894, #12192 ),
 ( #27930, #58887, #83200 ),
 ( #11696, #20298, #13687 ),
 ( #35051, #44657, #51270 ) ),
 .UNSPECIFIED., .F., .F., .F. ) 
 B_SPLINE_SURFACE_WITH_KNOTS ( ( 4, 4 ),
 ( 3, 3 ),
 ( 0.01105101719324316605, 0.01425305434006712488 ),
 ( 0.000000000000000000, 1.000000000000000000 ),
 .UNSPECIFIED. ) 
 GEOMETRIC_REPRESENTATION_ITEM ( )  RATIONAL_B_SPLINE_SURFACE ( (
 ( 1.000000000000000000, 0.7071067811865476838, 1.000000000000000000),
 ( 1.000000000000000000, 0.7071067811865476838, 1.000000000000000000),
 ( 1.000000000000000000, 0.7071067811865479058, 1.000000000000000000),
 ( 1.000000000000000000, 0.7071067811865479058, 1.000000000000000000) ) ) 
 REPRESENTATION_ITEM ( '' )  SURFACE ( )  );
#30997=CARTESIAN_POINT ( 'NONE',  ( 29.59866736649642860, -4.678593451839772044, 28.90589631152484174 ) ) ;
#30998=AXIS2_PLACEMENT_3D ( 'NONE', #26911, #51752, #88820 ) ;
#31014=LINE ( 'NONE', #61981, #12335 ) ;
#31027=ORIENTED_EDGE ( 'NONE', *, *, #82755, .F. ) ;
#31034=CARTESIAN_POINT ( 'NONE',  ( -13.89275734969026388, -0.3587747205144262708, 31.02402280011862246 ) ) ;
#31037=CARTESIAN_POINT ( 'NONE',  ( 30.93860345374796594, -0.6647747205144265426, 28.83647319851474933 ) ) ;
#31042=LINE ( 'NONE', #78702, #32183 ) ;
#31043=VECTOR ( 'NONE', #11069, 1000.000000000000000 ) ;
#31045=DIRECTION ( 'NONE',  ( -0.000000000000000000, 1.000000000000000000, -0.000000000000000000 ) ) ;
#31048=VERTEX_POINT ( 'NONE', #90426 ) ;
#31053=CARTESIAN_POINT ( 'NONE',  ( -24.57525087998973845, -6.376774720514426953, -15.45548830044933197 ) ) ;
#31061=EDGE_CURVE ( 'NONE', #31540, #44951, #89303, .T. ) ;
#31067=CARTESIAN_POINT ( 'NONE',  ( -6.728471858368818559, -6.376774720514408301, 19.14926908420045137 ) ) ;
#31070=VERTEX_POINT ( 'NONE', #68098 ) ;
#31072=DIRECTION ( 'NONE',  ( -1.000000000000000000, -0.000000000000000000, -7.994117400814786717E-16 ) ) ;
#31086=VERTEX_POINT ( 'NONE', #14287 ) ;
#31096=AXIS2_PLACEMENT_3D ( 'NONE', #28761, #52104, #83030 ) ;
#31100=LINE ( 'NONE', #69677, #25166 ) ;
#31103=DIRECTION ( 'NONE',  ( 0.000000000000000000, 1.000000000000000000, 0.000000000000000000 ) ) ;
#31112=ORIENTED_EDGE ( 'NONE', *, *, #40039, .F. ) ;
#31113=ADVANCED_FACE ( 'NONE', ( #16175 ), #957, .F. ) ;
#31118=VECTOR ( 'NONE', #9198, 1000.000000000000000 ) ;
#31122=CARTESIAN_POINT ( 'NONE',  ( 21.48910942911434319, -4.361838973203037817, -16.63132305728401050 ) ) ;
#31129=CARTESIAN_POINT ( 'NONE',  ( 10.54059822343757880, -6.376774720514426953, 23.12308057603841149 ) ) ;
#31132=CARTESIAN_POINT ( 'NONE',  ( 2.790451961050095520, -5.876774720514409189, 18.85195250256714417 ) ) ;
#31144=CARTESIAN_POINT ( 'NONE',  ( -13.57581083383197296, -5.876774720514426953, 19.78786796564403616 ) ) ;
#31146=EDGE_CURVE ( 'NONE', #43589, #48508, #10564, .T. ) ;
#31147=DIRECTION ( 'NONE',  ( 0.000000000000000000, 0.000000000000000000, 1.000000000000000000 ) ) ;
#31151=CARTESIAN_POINT ( 'NONE',  ( 3.902919446070569176, -6.376774720514427841, 21.47497695444087284 ) ) ;
#31153=DIRECTION ( 'NONE',  ( 1.000000000000000000, -0.000000000000000000, -0.000000000000000000 ) ) ;
#31156=DIRECTION ( 'NONE',  ( 1.000000000000000000, -4.218088402344531063E-15, 0.000000000000000000 ) ) ;
#31160=CARTESIAN_POINT ( 'NONE',  ( 0.3670296583442628213, -5.876774720514417183, 20.26087634804755311 ) ) ;
#31188=DIRECTION ( 'NONE',  ( 0.000000000000000000, -1.000000000000000000, 0.000000000000000000 ) ) ;
#31191=CARTESIAN_POINT ( 'NONE',  ( 4.468667172983064262, -6.376774720514401196, 18.40700896291420463 ) ) ;
#31194=CARTESIAN_POINT ( 'NONE',  ( 22.81105451610979173, 1.477225279485574028, -18.46691820600746681 ) ) ;
#31201=CARTESIAN_POINT ( 'NONE',  ( -4.635780534842457001, -5.876774720514410077, 19.53657742262743113 ) ) ;
#31221=CARTESIAN_POINT ( 'NONE',  ( 3.787259615384621636, -6.376774720514404748, 18.51923076923076650 ) ) ;
#31230=CARTESIAN_POINT ( 'NONE',  ( 8.583179188118256420, -5.356774720514425603, -25.03641645905366886 ) ) ;
#31233=CARTESIAN_POINT ( 'NONE',  ( -20.27875734969026311, -6.376774720514428729, 24.00402280011862288 ) ) ;
#31241=FACE_OUTER_BOUND ( 'NONE', #31960, .T. ) ;
#31242=ORIENTED_EDGE ( 'NONE', *, *, #81684, .F. ) ;
#31243=VERTEX_POINT ( 'NONE', #70472 ) ;
#31252=ORIENTED_EDGE ( 'NONE', *, *, #80822, .F. ) ;
#31276=CARTESIAN_POINT ( 'NONE',  ( 4.263585034174699473, -5.876774720514402972, 18.26968045024142739 ) ) ;
#31284=LINE ( 'NONE', #39401, #75033 ) ;
#31290=CARTESIAN_POINT ( 'NONE',  ( 2.708118538500707828, -5.876774720514424288, 20.94830092343283212 ) ) ;
#31300=CARTESIAN_POINT ( 'NONE',  ( 15.03705075715986972, -3.514354387074007047, -27.31754965648562816 ) ) ;
#31319=ORIENTED_EDGE ( 'NONE', *, *, #78705, .T. ) ;
#31326=ORIENTED_EDGE ( 'NONE', *, *, #52786, .F. ) ;
#31332=AXIS2_PLACEMENT_3D ( 'NONE', #49488, #65227, #3321 ) ;
#31333=EDGE_CURVE ( 'NONE', #79616, #78997, #24783, .T. ) ;
#31339=CARTESIAN_POINT ( 'NONE',  ( 4.627238781264984446, -5.876774720514409189, 19.49219360614394247 ) ) ;
#31343=CARTESIAN_POINT ( 'NONE',  ( 23.91005183030481263, -4.132774720514426292, -14.40591128290692069 ) ) ;
#31345=EDGE_CURVE ( 'NONE', #88329, #86782, #3471, .T. ) ;
#31350=LINE ( 'NONE', #62314, #78221 ) ;
#31356=CARTESIAN_POINT ( 'NONE',  ( 4.967620699791259753, -6.376774720514415407, 19.94530485585548973 ) ) ;
#31365=DIRECTION ( 'NONE',  ( 1.232047923278981953E-16, 1.000000000000000000, 0.000000000000000000 ) ) ;
#31368=LINE ( 'NONE', #15140, #27156 ) ;
#31369=AXIS2_PLACEMENT_3D ( 'NONE', #71978, #49150, #95302 ) ;
#31372=ORIENTED_EDGE ( 'NONE', *, *, #30311, .T. ) ;
#31374=LINE ( 'NONE', #99864, #64456 ) ;
#31382=CARTESIAN_POINT ( 'NONE',  ( 0.3910256410256383042, -6.376774720514408301, 19.19230769230768985 ) ) ;
#31385=PLANE ( 'NONE',  #25436 ) ;
#31386=CARTESIAN_POINT ( 'NONE',  ( -10.24059822343757986, -6.376774720514426953, 22.82308057603840368 ) ) ;
#31401=FACE_OUTER_BOUND ( 'NONE', #35529, .T. ) ;
#31403=CARTESIAN_POINT ( 'NONE',  ( 5.344006250707635353, -6.376774720514418959, 20.55781796641452885 ) ) ;
#31406=CARTESIAN_POINT ( 'NONE',  ( 3.106028565906091998, -6.376774720514426953, 3.106028565906120864 ) ) ;
#31410=DIRECTION ( 'NONE',  ( -0.9888510809027409865, 4.164321980682959710E-15, -0.1489078231574183231 ) ) ;
#31416=ORIENTED_EDGE ( 'NONE', *, *, #1107, .T. ) ;
#31432=LINE ( 'NONE', #72009, #47919 ) ;
#31438=CYLINDRICAL_SURFACE ( 'NONE', #24111, 1.836000000000000743 ) ;
#31444=ORIENTED_EDGE ( 'NONE', *, *, #90843, .T. ) ;
#31459=EDGE_CURVE ( 'NONE', #46359, #41475, #83560, .T. ) ;
#31480=CARTESIAN_POINT ( 'NONE',  ( 4.689770114687411784, -5.876774720514424288, 21.33175327469028915 ) ) ;
#31490=CARTESIAN_POINT ( 'NONE',  ( 2.922108196329484375, -6.376774720514417183, 20.36383711510645256 ) ) ;
#31494=CARTESIAN_POINT ( 'NONE',  ( 3.106028565906091998, -5.876774720514426953, 3.106028565906120864 ) ) ;
#31498=CARTESIAN_POINT ( 'NONE',  ( 31.63608487984670958, -3.398012287350409277, 27.34773272911736797 ) ) ;
#31506=DIRECTION ( 'NONE',  ( -0.000000000000000000, 1.000000000000000000, -0.000000000000000000 ) ) ;
#31507=CARTESIAN_POINT ( 'NONE',  ( -5.576690828732316696, -5.876774720514418071, 20.34213149456667935 ) ) ;
#31513=CARTESIAN_POINT ( 'NONE',  ( 3.085011456917871264, -5.876774720514408301, 19.00082519311127172 ) ) ;
#31540=VERTEX_POINT ( 'NONE', #61751 ) ;
#31551=CARTESIAN_POINT ( 'NONE',  ( -3.108425644221024520, -5.876774720514416295, 20.25188360057253334 ) ) ;
#31552=CARTESIAN_POINT ( 'NONE',  ( 0.06697178475903577122, -5.876774720514410077, 19.29815762497054976 ) ) ;
#31553=VERTEX_POINT ( 'NONE', #52130 ) ;
#31557=ADVANCED_FACE ( 'NONE', ( #92670, #38391 ), #14043, .T. ) ;
#31561=CARTESIAN_POINT ( 'NONE',  ( 31.74473449900405697, -4.976825198871215328, -4.259190951192157293 ) ) ;
#31571=VERTEX_POINT ( 'NONE', #6943 ) ;
#31596=AXIS2_PLACEMENT_3D ( 'NONE', #66040, #18335, #95455 ) ;
#31610=CYLINDRICAL_SURFACE ( 'NONE', #89099, 3.349999999999998757 ) ;
#31612=ORIENTED_EDGE ( 'NONE', *, *, #4107, .F. ) ;
#31614=VECTOR ( 'NONE', #20959, 1000.000000000000114 ) ;
#31623=CARTESIAN_POINT ( 'NONE',  ( -23.71328795744024376, -0.3587747205144057872, -17.58350715675015863 ) ) ;
#31624=FACE_BOUND ( 'NONE', #70374, .T. ) ;
#31652=CARTESIAN_POINT ( 'NONE',  ( 5.642884982650352654, -5.876774720514425177, 20.85668005806743608 ) ) ;
#31663=DIRECTION ( 'NONE',  ( 0.000000000000000000, -1.000000000000000000, 0.000000000000000000 ) ) ;
#31673=DIRECTION ( 'NONE',  ( 1.000000000000000000, 0.000000000000000000, 0.000000000000000000 ) ) ;
#31676=VECTOR ( 'NONE', #51236, 1000.000000000000000 ) ;
#31681=VECTOR ( 'NONE', #84393, 1000.000000000000000 ) ;
#31684=VECTOR ( 'NONE', #28454, 1000.000000000000000 ) ;
#31704=EDGE_LOOP ( 'NONE', ( #8538, #31326, #66042, #49829 ) ) ;
#31705=DIRECTION ( 'NONE',  ( -1.000000000000000000, -9.637352644315600173E-17, 0.000000000000000000 ) ) ;
#31710=CARTESIAN_POINT ( 'NONE',  ( -4.743266218460161276, -5.876774720514413630, 19.49357334786887108 ) ) ;
#31713=VERTEX_POINT ( 'NONE', #93673 ) ;
#31716=LINE ( 'NONE', #8376, #30444 ) ;
#31736=FACE_OUTER_BOUND ( 'NONE', #52373, .T. ) ;
#31739=DIRECTION ( 'NONE',  ( -0.000000000000000000, -1.000000000000000000, -0.000000000000000000 ) ) ;
#31756=CARTESIAN_POINT ( 'NONE',  ( 15.11782173391125639, -3.530785491095171924, -28.35562479723304818 ) ) ;
#31763=CARTESIAN_POINT ( 'NONE',  ( -4.401146115524053215, -6.376774720514411854, 19.34190049657481936 ) ) ;
#31766=VECTOR ( 'NONE', #52152, 1000.000000000000000 ) ;
#31773=DIRECTION ( 'NONE',  ( -6.924038193813838377E-14, 0.000000000000000000, -1.000000000000000000 ) ) ;
#31783=EDGE_CURVE ( 'NONE', #34238, #46809, #78443, .T. ) ;
#31784=EDGE_CURVE ( 'NONE', #44867, #24870, #86569, .T. ) ;
#31794=EDGE_CURVE ( 'NONE', #37689, #63088, #97678, .T. ) ;
#31802=PLANE ( 'NONE',  #42477 ) ;
#31806=ORIENTED_EDGE ( 'NONE', *, *, #77076, .F. ) ;
#31809=CARTESIAN_POINT ( 'NONE',  ( -10.24059822343757808, -5.876774720514426953, 0.000000000000000000 ) ) ;
#31872=CARTESIAN_POINT ( 'NONE',  ( 6.792576760808763936, -6.376774720514415407, 20.16775508794004779 ) ) ;
#31893=DIRECTION ( 'NONE',  ( 0.000000000000000000, 0.000000000000000000, 1.000000000000000000 ) ) ;
#31896=CARTESIAN_POINT ( 'NONE',  ( 30.93860345374796594, 6.475225279485573360, 25.41160796525321430 ) ) ;
#31901=AXIS2_PLACEMENT_3D ( 'NONE', #3760, #9349, #96103 ) ;
#31903=DIRECTION ( 'NONE',  ( 0.000000000000000000, 0.000000000000000000, -1.000000000000000000 ) ) ;
#31905=CARTESIAN_POINT ( 'NONE',  ( 5.326923076923078426, -6.376774720514420736, 20.76772836538461320 ) ) ;
#31907=VECTOR ( 'NONE', #36603, 1000.000000000000000 ) ;
#31912=CARTESIAN_POINT ( 'NONE',  ( -6.680782769985652791, -5.876774720514411854, 19.46295461892502132 ) ) ;
#31918=CIRCLE ( 'NONE', #96738, 1.530000000000002469 ) ;
#31926=LINE ( 'NONE', #54773, #1061 ) ;
#31932=CARTESIAN_POINT ( 'NONE',  ( -1.022535880784302353, -5.876774720514415407, 19.99258394656883908 ) ) ;
#31953=LINE ( 'NONE', #16221, #25873 ) ;
#31960=EDGE_LOOP ( 'NONE', ( #15001, #81754, #7989, #46929 ) ) ;
#31969=ORIENTED_EDGE ( 'NONE', *, *, #74633, .T. ) ;
#31979=DIRECTION ( 'NONE',  ( 0.8813259582271224524, 0.000000000000000000, -0.4725087886537610027 ) ) ;
#31983=CARTESIAN_POINT ( 'NONE',  ( 4.885870204371583370, -5.876774720514420736, 20.85936027411790405 ) ) ;
#31997=CARTESIAN_POINT ( 'NONE',  ( -6.720452724358975338, -5.876774720514411854, 19.46153846153846700 ) ) ;
#32003=LINE ( 'NONE', #54352, #13856 ) ;
#32008=LINE ( 'NONE', #15776, #79045 ) ;
#32014=VERTEX_POINT ( 'NONE', #20543 ) ;
#32015=LINE ( 'NONE', #32519, #82219 ) ;
#32020=ORIENTED_EDGE ( 'NONE', *, *, #51359, .F. ) ;
#32022=CARTESIAN_POINT ( 'NONE',  ( 13.91401389203221406, 5.965225279485572685, 158.0376437107427137 ) ) ;
#32024=VECTOR ( 'NONE', #14778, 1000.000000000000000 ) ;
#32031=ADVANCED_FACE ( 'NONE', ( #37283 ), #21043, .F. ) ;
#32032=VECTOR ( 'NONE', #40330, 1000.000000000000000 ) ;
#32042=LINE ( 'NONE', #39148, #72150 ) ;
#32047=ORIENTED_EDGE ( 'NONE', *, *, #48420, .F. ) ;
#32048=DIRECTION ( 'NONE',  ( 0.000000000000000000, 0.000000000000000000, -1.000000000000000000 ) ) ;
#32054=CARTESIAN_POINT ( 'NONE',  ( -9.278253834636469577, -5.876774720514426953, 18.51871304725684553 ) ) ;
#32062=CARTESIAN_POINT ( 'NONE',  ( 31.10870921191468597, -5.152774720514429418, -4.748485609378566785 ) ) ;
#32067=EDGE_CURVE ( 'NONE', #63660, #67290, #76814, .T. ) ;
#32073=DIRECTION ( 'NONE',  ( -1.000000000000000000, -9.637352644315600173E-17, 0.000000000000000000 ) ) ;
#32077=ORIENTED_EDGE ( 'NONE', *, *, #73998, .T. ) ;
#32079=CARTESIAN_POINT ( 'NONE',  ( 6.963174204274080736, -5.876774720514415407, 20.29202897614545975 ) ) ;
#32085=CARTESIAN_POINT ( 'NONE',  ( -4.141025641025642301, -6.376774720514411854, 19.63681891025641235 ) ) ;
#32087=AXIS2_PLACEMENT_3D ( 'NONE', #83435, #12925, #52006 ) ;
#32100=ORIENTED_EDGE ( 'NONE', *, *, #5944, .T. ) ;
#32106=DIRECTION ( 'NONE',  ( 0.000000000000000000, 0.000000000000000000, 1.000000000000000000 ) ) ;
#32110=CARTESIAN_POINT ( 'NONE',  ( 7.433267315672343223, -5.876774720514418959, 20.43888261666079842 ) ) ;
#32125=CARTESIAN_POINT ( 'NONE',  ( -65.05438548721848235, 6.475225279485573360, 0.7300228001186309656 ) ) ;
#32136=LINE ( 'NONE', #46874, #81186 ) ;
#32148=CARTESIAN_POINT ( 'NONE',  ( 3.036358173076929123, -6.376774720514420736, 20.87990785256409865 ) ) ;
#32157=ADVANCED_FACE ( 'NONE', ( #83948 ), #45403, .F. ) ;
#32161=AXIS2_PLACEMENT_3D ( 'NONE', #10575, #88710, #81593 ) ;
#32162=CARTESIAN_POINT ( 'NONE',  ( 0.09189959430841809773, -5.876774720514410966, 19.67013632031035542 ) ) ;
#32170=ORIENTED_EDGE ( 'NONE', *, *, #13469, .F. ) ;
#32174=AXIS2_PLACEMENT_3D ( 'NONE', #28807, #21185, #14575 ) ;
#32178=ORIENTED_EDGE ( 'NONE', *, *, #60820, .T. ) ;
#32183=VECTOR ( 'NONE', #40171, 1000.000000000000000 ) ;
#32194=ORIENTED_EDGE ( 'NONE', *, *, #35701, .F. ) ;
#32195=CARTESIAN_POINT ( 'NONE',  ( 22.81105451610979173, -1.684774720501991396, -18.46691820600746681 ) ) ;
#32200=LINE ( 'NONE', #47441, #19562 ) ;
#32216=DIRECTION ( 'NONE',  ( 0.9831680378442393398, 0.000000000000000000, 0.1827036106964188000 ) ) ;
#32217=ORIENTED_EDGE ( 'NONE', *, *, #21128, .F. ) ;
#32225=CARTESIAN_POINT ( 'NONE',  ( -9.940598223437577374, -5.876774720514426953, 22.08128695274315945 ) ) ;
#32226=CARTESIAN_POINT ( 'NONE',  ( 7.227401621296005274, -3.316774720515020203, -27.22638491047315767 ) ) ;
#32228=AXIS2_PLACEMENT_3D ( 'NONE', #82667, #29379, #83663 ) ;
#32234=CARTESIAN_POINT ( 'NONE',  ( -20.77875734969026311, -3.316774720514426456, 29.49402280011862487 ) ) ;
#32240=EDGE_CURVE ( 'NONE', #93259, #68647, #54012, .T. ) ;
#32241=CARTESIAN_POINT ( 'NONE',  ( 22.02124265030973760, 7.743225279485574042, 13.95402280011862395 ) ) ;
#32245=AXIS2_PLACEMENT_3D ( 'NONE', #59264, #66890, #44033 ) ;
#32246=LINE ( 'NONE', #1808, #83721 ) ;
#32251=DIRECTION ( 'NONE',  ( -0.9994733861282923959, -0.000000000000000000, -0.03244919754393515293 ) ) ;
#32255=VERTEX_POINT ( 'NONE', #86944 ) ;
#32263=CARTESIAN_POINT ( 'NONE',  ( -5.023036858974361252, -5.876774720514410077, 19.14743589743590846 ) ) ;
#32266=CARTESIAN_POINT ( 'NONE',  ( -2.794793911895765870, -6.376774720514417183, 20.33046051580616265 ) ) ;
#32278=LINE ( 'NONE', #23145, #4098 ) ;
#32280=CARTESIAN_POINT ( 'NONE',  ( 4.967948717948723392, -5.876774720514415407, 20.00140224358974095 ) ) ;
#32286=FACE_OUTER_BOUND ( 'NONE', #89354, .T. ) ;
#32296=CARTESIAN_POINT ( 'NONE',  ( 4.487249349319938574, -6.376774720514420736, 21.01618089687719504 ) ) ;
#32303=CARTESIAN_POINT ( 'NONE',  ( 31.55236408230781819, 5.965225279485572685, 19.84760796525321780 ) ) ;
#32308=ORIENTED_EDGE ( 'NONE', *, *, #7281, .T. ) ;
#32320=CARTESIAN_POINT ( 'NONE',  ( -5.457842845122470976, -6.376774720514411854, 19.25892998154168367 ) ) ;
#32326=LINE ( 'NONE', #79499, #20307 ) ;
#32327=VERTEX_POINT ( 'NONE', #81834 ) ;
#32329=ORIENTED_EDGE ( 'NONE', *, *, #43718, .T. ) ;
#32331=ORIENTED_EDGE ( 'NONE', *, *, #53877, .F. ) ;
#32334=LINE ( 'NONE', #94729, #60071 ) ;
#32340=CARTESIAN_POINT ( 'NONE',  ( 4.572862496014544753, -6.376774720514408301, 19.20224321281611068 ) ) ;
#32350=ADVANCED_FACE ( 'NONE', ( #79826 ), #27559, .T. ) ;
#32353=ORIENTED_EDGE ( 'NONE', *, *, #62859, .T. ) ;
#32354=ORIENTED_EDGE ( 'NONE', *, *, #33564, .T. ) ;
#32355=ADVANCED_FACE ( 'NONE', ( #19925 ), #3237, .F. ) ;
#32356=CARTESIAN_POINT ( 'NONE',  ( 0.000000000000000000, -5.356774720514425603, 0.000000000000000000 ) ) ;
#32363=EDGE_CURVE ( 'NONE', #21350, #67214, #50894, .T. ) ;
#32369=EDGE_CURVE ( 'NONE', #34608, #40266, #10827, .T. ) ;
#32370=CARTESIAN_POINT ( 'NONE',  ( 0.03625801282051022839, -6.376774720514410077, 19.27714342948718240 ) ) ;
#32380=LINE ( 'NONE', #94272, #22730 ) ;
#32383=EDGE_CURVE ( 'NONE', #24606, #65803, #47357, .T. ) ;
#32384=ORIENTED_EDGE ( 'NONE', *, *, #46800, .T. ) ;
#32392=CIRCLE ( 'NONE', #45367, 2.249999999999998668 ) ;
#32394=AXIS2_PLACEMENT_3D ( 'NONE', #75729, #89978, #27589 ) ;
#32401=ADVANCED_FACE ( 'NONE', ( #18929 ), #80842, .F. ) ;
#32405=DIRECTION ( 'NONE',  ( -0.000000000000000000, -1.000000000000000000, -0.000000000000000000 ) ) ;
#32408=DIRECTION ( 'NONE',  ( 1.526034937513432889E-15, 0.000000000000000000, 1.000000000000000000 ) ) ;
#32412=CARTESIAN_POINT ( 'NONE',  ( -6.680782769985652791, -6.376774720514411854, 19.46295461892502132 ) ) ;
#32422=EDGE_CURVE ( 'NONE', #94339, #15795, #36654, .T. ) ;
#32429=CARTESIAN_POINT ( 'NONE',  ( -1.044871794871793602, -5.876774720514418071, 20.44941907051282115 ) ) ;
#32436=ORIENTED_EDGE ( 'NONE', *, *, #75003, .F. ) ;
#32437=DIRECTION ( 'NONE',  ( 0.000000000000000000, 0.000000000000000000, 1.000000000000000000 ) ) ;
#32439=LINE ( 'NONE', #47676, #41960 ) ;
#32440=CARTESIAN_POINT ( 'NONE',  ( 5.395440699609677537, 5.965225279485594001, -28.51842087987364138 ) ) ;
#32441=AXIS2_PLACEMENT_3D ( 'NONE', #62044, #37203, #68156 ) ;
#32452=CARTESIAN_POINT ( 'NONE',  ( -7.131053040288445999, -5.876774720514413630, 19.60308799987318196 ) ) ;
#32453=VERTEX_POINT ( 'NONE', #74706 ) ;
#32459=ORIENTED_EDGE ( 'NONE', *, *, #25660, .F. ) ;
#32464=ORIENTED_EDGE ( 'NONE', *, *, #77949, .F. ) ;
#32465=CARTESIAN_POINT ( 'NONE',  ( -6.369015873774380943, -5.876774720514413630, 19.23384392940399934 ) ) ;
#32467=ORIENTED_EDGE ( 'NONE', *, *, #94038, .F. ) ;
#32469=CARTESIAN_POINT ( 'NONE',  ( -10.21384395349174490, -3.316774720514427344, 29.49402280011862487 ) ) ;
#32476=EDGE_CURVE ( 'NONE', #65705, #88108, #45275, .T. ) ;
#32487=VERTEX_POINT ( 'NONE', #37153 ) ;
#32490=EDGE_LOOP ( 'NONE', ( #12486, #50841, #25225, #48186, #67327 ) ) ;
#32495=FACE_OUTER_BOUND ( 'NONE', #15598, .T. ) ;
#32500=CARTESIAN_POINT ( 'NONE',  ( 2.935461252226840401, -6.376774720514420736, 20.47627681611744777 ) ) ;
#32507=FACE_OUTER_BOUND ( 'NONE', #61044, .T. ) ;
#32519=CARTESIAN_POINT ( 'NONE',  ( 0.3910256410256383042, -5.876774720514409189, 19.19230769230768985 ) ) ;
#32528=EDGE_CURVE ( 'NONE', #45070, #35025, #65208, .T. ) ;
#32531=CIRCLE ( 'NONE', #48777, 28.96799999999999287 ) ;
#32537=EDGE_CURVE ( 'NONE', #33122, #24488, #48960, .T. ) ;
#32544=CARTESIAN_POINT ( 'NONE',  ( -11.64875734969026233, -0.3587747205144265483, 31.02402280011862246 ) ) ;
#32548=ORIENTED_EDGE ( 'NONE', *, *, #81071, .T. ) ;
#32555=CARTESIAN_POINT ( 'NONE',  ( -3.054691362729579751, -5.876774720514413630, 19.78730719034165375 ) ) ;
#32562=ORIENTED_EDGE ( 'NONE', *, *, #66654, .T. ) ;
#32578=EDGE_CURVE ( 'NONE', #22171, #67798, #61503, .T. ) ;
#32579=ORIENTED_EDGE ( 'NONE', *, *, #32067, .T. ) ;
#32580=EDGE_LOOP ( 'NONE', ( #51837, #86845, #58955, #43680 ) ) ;
#32582=CARTESIAN_POINT ( 'NONE',  ( 6.457852148677970305, -6.376774720514415407, 20.09052163342618158 ) ) ;
#32583=CARTESIAN_POINT ( 'NONE',  ( 5.443272695963705665, -5.876774720514417183, 20.27301970143225418 ) ) ;
#32586=ORIENTED_EDGE ( 'NONE', *, *, #59460, .T. ) ;
#32589=CARTESIAN_POINT ( 'NONE',  ( 2.590388488674697953, -5.876774720514415407, 19.94764386045124027 ) ) ;
#32607=VERTEX_POINT ( 'NONE', #100023 ) ;
#32615=ORIENTED_EDGE ( 'NONE', *, *, #45236, .F. ) ;
#32623=DIRECTION ( 'NONE',  ( 1.000000000000000000, 0.000000000000000000, 0.000000000000000000 ) ) ;
#32631=ORIENTED_EDGE ( 'NONE', *, *, #25014, .F. ) ;
#32638=CARTESIAN_POINT ( 'NONE',  ( 4.854822496258163866, -5.876774720514421624, 20.96950945262037891 ) ) ;
#32645=VECTOR ( 'NONE', #94553, 1000.000000000000000 ) ;
#32651=CARTESIAN_POINT ( 'NONE',  ( 4.373554412633047228, -6.376774720514422512, 21.19197260575996822 ) ) ;
#32654=CARTESIAN_POINT ( 'NONE',  ( 5.811591729264017125, -5.876774720514421624, 21.22699980322195046 ) ) ;
#32679=CARTESIAN_POINT ( 'NONE',  ( 6.561060095583167495, -6.376774720514427841, 21.83518827598938117 ) ) ;
#32691=DIRECTION ( 'NONE',  ( 0.000000000000000000, 0.000000000000000000, -1.000000000000000000 ) ) ;
#32698=CARTESIAN_POINT ( 'NONE',  ( 2.884397429187188333, -6.376774720514406525, 18.67943752795919110 ) ) ;
#32707=VERTEX_POINT ( 'NONE', #24425 ) ;
#32721=ORIENTED_EDGE ( 'NONE', *, *, #43319, .T. ) ;
#32722=CARTESIAN_POINT ( 'NONE',  ( -0.4453066574538939171, -6.376774720514410077, 19.14913681718892491 ) ) ;
#32727=ORIENTED_EDGE ( 'NONE', *, *, #1189, .T. ) ;
#32728=CARTESIAN_POINT ( 'NONE',  ( 4.784292611718075072, -6.376774720514426953, -25.54547254883186014 ) ) ;
#32730=CARTESIAN_POINT ( 'NONE',  ( 7.227401621481964966, -5.356774720515139698, -27.22638491171618824 ) ) ;
#32738=DIRECTION ( 'NONE',  ( 0.000000000000000000, 0.000000000000000000, 1.000000000000000000 ) ) ;
#32739=CARTESIAN_POINT ( 'NONE',  ( 30.53060340732036337, 1.477225279485574028, 3.744237563515920634E-15 ) ) ;
#32755=ORIENTED_EDGE ( 'NONE', *, *, #94896, .F. ) ;
#32761=FACE_OUTER_BOUND ( 'NONE', #18318, .T. ) ;
#32773=EDGE_CURVE ( 'NONE', #67333, #73040, #50281, .T. ) ;
#32794=CARTESIAN_POINT ( 'NONE',  ( 2.649863049427662709, -5.876774720514420736, 20.71861240329949538 ) ) ;
#32796=CARTESIAN_POINT ( 'NONE',  ( 4.573489327750471567, -5.876774720514419847, 20.79634280254998657 ) ) ;
#32799=PLANE ( 'NONE',  #23718 ) ;
#32806=DIRECTION ( 'NONE',  ( 0.9921023176230514551, 0.000000000000000000, -0.1254312216594016816 ) ) ;
#32816=LINE ( 'NONE', #72886, #13036 ) ;
#32818=CARTESIAN_POINT ( 'NONE',  ( -3.826923076923074429, -5.876774720514426953, 21.75000000000000355 ) ) ;
#32836=VERTEX_POINT ( 'NONE', #56407 ) ;
#32847=CARTESIAN_POINT ( 'NONE',  ( 4.653846153846159517, -5.876774720514416295, 19.99999999999999289 ) ) ;
#32849=VERTEX_POINT ( 'NONE', #87326 ) ;
#32851=DIRECTION ( 'NONE',  ( 0.000000000000000000, 0.000000000000000000, 1.000000000000000000 ) ) ;
#32852=VERTEX_POINT ( 'NONE', #26444 ) ;
#32855=VERTEX_POINT ( 'NONE', #80220 ) ;
#32870=ADVANCED_FACE ( 'NONE', ( #41167 ), #17315, .T. ) ;
#32887=CARTESIAN_POINT ( 'NONE',  ( -6.989144439031651501, -5.876774720514410077, 19.51167604195716621 ) ) ;
#32892=CARTESIAN_POINT ( 'NONE',  ( 6.437068816671457583, 5.965225279485592225, -28.37834077173919667 ) ) ;
#32896=CARTESIAN_POINT ( 'NONE',  ( 27.53860345374771867, -1.682774720514426114, -9.482392034746242260 ) ) ;
#32897=VECTOR ( 'NONE', #69606, 1000.000000000000000 ) ;
#32902=DIRECTION ( 'NONE',  ( 0.000000000000000000, -1.000000000000000000, 0.000000000000000000 ) ) ;
#32915=DIRECTION ( 'NONE',  ( -0.7071067811865507924, 0.000000000000000000, 0.7071067811865442421 ) ) ;
#32924=LINE ( 'NONE', #26312, #94232 ) ;
#32925=LINE ( 'NONE', #40034, #67486 ) ;
#32931=CARTESIAN_POINT ( 'NONE',  ( 19.75748517575715368, 5.965225279485572685, 28.87153971905864580 ) ) ;
#32932=CARTESIAN_POINT ( 'NONE',  ( 14.76093561896379214, -3.316774720514426456, -28.39148769130089889 ) ) ;
#32936=EDGE_CURVE ( 'NONE', #1896, #32707, #73295, .T. ) ;
#32937=CARTESIAN_POINT ( 'NONE',  ( 0.000000000000000000, -2.056774720514426669, 0.000000000000000000 ) ) ;
#32938=EDGE_CURVE ( 'NONE', #45070, #87231, #29449, .T. ) ;
#32942=ORIENTED_EDGE ( 'NONE', *, *, #69592, .T. ) ;
#32952=CARTESIAN_POINT ( 'NONE',  ( -2.243088942307695177, -6.376774720514408301, 19.14743589743590491 ) ) ;
#32959=CARTESIAN_POINT ( 'NONE',  ( -1.438454482798693146, -6.376774720514410077, 19.55848054040323092 ) ) ;
#32982=CARTESIAN_POINT ( 'NONE',  ( -7.326923076923076650, -5.876774720514418071, 20.36318108974359831 ) ) ;
#32989=EDGE_CURVE ( 'NONE', #65105, #18022, #8462, .T. ) ;
#32992=CARTESIAN_POINT ( 'NONE',  ( 3.825380556292953482, -5.876774720514427841, 21.83927723428477208 ) ) ;
#33010=AXIS2_PLACEMENT_3D ( 'NONE', #29118, #11903, #81916 ) ;
#33013=CARTESIAN_POINT ( 'NONE',  ( 29.64448763235240136, -5.625929005037784592, 28.17618604274316851 ) ) ;
#33025=DIRECTION ( 'NONE',  ( 2.439088438507244272E-15, -7.805083003223181985E-15, 1.000000000000000000 ) ) ;
#33033=DIRECTION ( 'NONE',  ( -0.1593164160933055740, 0.000000000000000000, 0.9872275723272646575 ) ) ;
#33050=ADVANCED_FACE ( 'NONE', ( #82710 ), #27932, .F. ) ;
#33055=CARTESIAN_POINT ( 'NONE',  ( 3.509873074917118085, 5.965225279485572685, 29.15869884040363758 ) ) ;
#33057=VERTEX_POINT ( 'NONE', #12194 ) ;
#33066=FACE_OUTER_BOUND ( 'NONE', #27465, .T. ) ;
#33080=ORIENTED_EDGE ( 'NONE', *, *, #56427, .T. ) ;
#33086=EDGE_LOOP ( 'NONE', ( #82157, #53953, #77529, #54315 ) ) ;
#33087=ORIENTED_EDGE ( 'NONE', *, *, #76000, .F. ) ;
#33089=CARTESIAN_POINT ( 'NONE',  ( 6.658651924251966392, -6.376774720514415407, 20.11748569626183425 ) ) ;
#33090=CARTESIAN_POINT ( 'NONE',  ( 5.495499487697820484, -6.376774720514418959, 20.18701882043406926 ) ) ;
#33099=CARTESIAN_POINT ( 'NONE',  ( 13.10664265030973930, 1.324225279485583551, -28.18129937516353678 ) ) ;
#33100=ORIENTED_EDGE ( 'NONE', *, *, #7526, .F. ) ;
#33108=DIRECTION ( 'NONE',  ( 0.000000000000000000, 0.000000000000000000, -1.000000000000000000 ) ) ;
#33118=ORIENTED_EDGE ( 'NONE', *, *, #2081, .T. ) ;
#33122=VERTEX_POINT ( 'NONE', #86213 ) ;
#33128=LINE ( 'NONE', #18897, #70585 ) ;
#33136=CARTESIAN_POINT ( 'NONE',  ( 31.63608488009066733, -3.316774720514426456, 27.34773273846990094 ) ) ;
#33140=CARTESIAN_POINT ( 'NONE',  ( 4.967622410992271753, -5.876774720514415407, 20.05703257908297843 ) ) ;
#33142=DIRECTION ( 'NONE',  ( 0.000000000000000000, 0.000000000000000000, -1.000000000000000000 ) ) ;
#33150=FACE_OUTER_BOUND ( 'NONE', #98888, .T. ) ;
#33162=ORIENTED_EDGE ( 'NONE', *, *, #69819, .F. ) ;
#33166=CARTESIAN_POINT ( 'NONE',  ( 17.51792015816173986, 5.965225279485572685, 29.01255224319336889 ) ) ;
#33176=DIRECTION ( 'NONE',  ( 0.000000000000000000, -1.000000000000000000, 0.000000000000000000 ) ) ;
#33177=ORIENTED_EDGE ( 'NONE', *, *, #64884, .F. ) ;
#33179=EDGE_CURVE ( 'NONE', #20076, #52968, #71700, .T. ) ;
#33183=CARTESIAN_POINT ( 'NONE',  ( 8.000000000000007105, -6.376774720514426953, 17.49999999999999645 ) ) ;
#33206=CARTESIAN_POINT ( 'NONE',  ( -4.968349358974360364, -5.876774720514411854, 19.46153846153846700 ) ) ;
#33208=ADVANCED_FACE ( 'NONE', ( #19190 ), #80596, .F. ) ;
#33209=CIRCLE ( 'NONE', #60753, 3.500000000000000000 ) ;
#33212=CARTESIAN_POINT ( 'NONE',  ( 7.155337544004596317, -5.876774720514418071, 20.64714842558261765 ) ) ;
#33222=FACE_OUTER_BOUND ( 'NONE', #97832, .T. ) ;
#33224=EDGE_LOOP ( 'NONE', ( #48061, #22984, #65542, #90045 ) ) ;
#33235=DIRECTION ( 'NONE',  ( 0.000000000000000000, -1.000000000000000000, 0.000000000000000000 ) ) ;
#33239=ADVANCED_FACE ( 'NONE', ( #87210 ), #76524, .F. ) ;
#33242=CARTESIAN_POINT ( 'NONE',  ( -6.100820854657341918, -6.376774720514413630, 19.76359802465961124 ) ) ;
#33246=CARTESIAN_POINT ( 'NONE',  ( 30.93898937471034216, -4.884441105398384941, -1.603546260404424606 ) ) ;
#33282=CIRCLE ( 'NONE', #88345, 1.835999999999993859 ) ;
#33290=CARTESIAN_POINT ( 'NONE',  ( 4.127208352283176396, -6.376774720514424288, 21.39624840817692686 ) ) ;
#33294=ORIENTED_EDGE ( 'NONE', *, *, #61018, .F. ) ;
#33301=CARTESIAN_POINT ( 'NONE',  ( 3.787259615384621192, -6.376774720514426065, 21.48076923076922640 ) ) ;
#33302=EDGE_LOOP ( 'NONE', ( #16808, #24198, #15731, #68277 ) ) ;
#33308=VECTOR ( 'NONE', #38284, 1000.000000000000000 ) ;
#33316=VERTEX_POINT ( 'NONE', #32931 ) ;
#33323=VERTEX_POINT ( 'NONE', #64911 ) ;
#33327=DIRECTION ( 'NONE',  ( -0.000000000000000000, 1.000000000000000000, -0.000000000000000000 ) ) ;
#33344=ORIENTED_EDGE ( 'NONE', *, *, #97273, .F. ) ;
#33348=VERTEX_POINT ( 'NONE', #98182 ) ;
#33363=VERTEX_POINT ( 'NONE', #22050 ) ;
#33377=CARTESIAN_POINT ( 'NONE',  ( 11.54156857142115911, -3.316774720514427344, -28.05134709678029381 ) ) ;
#33383=DIRECTION ( 'NONE',  ( -0.000000000000000000, -1.000000000000000000, -0.000000000000000000 ) ) ;
#33395=CARTESIAN_POINT ( 'NONE',  ( 5.873458226074941280, -6.376774720514413630, 19.84669099281175164 ) ) ;
#33414=CARTESIAN_POINT ( 'NONE',  ( -1.140932434931746582E-13, -5.876774720514426953, 21.78128695274321203 ) ) ;
#33415=EDGE_CURVE ( 'NONE', #40153, #71923, #91074, .T. ) ;
#33419=CARTESIAN_POINT ( 'NONE',  ( 7.190659024148910561, -6.376774720514413630, 19.91543959911579620 ) ) ;
#33428=CARTESIAN_POINT ( 'NONE',  ( -29.49875734969026198, 5.965225279485572685, 0.1180228001186258285 ) ) ;
#33429=AXIS2_PLACEMENT_3D ( 'NONE', #20568, #51540, #12952 ) ;
#33433=CARTESIAN_POINT ( 'NONE',  ( 4.189750619059152470, -6.376774720514427841, 21.76591699724029283 ) ) ;
#33434=LINE ( 'NONE', #25824, #78724 ) ;
#33448=ORIENTED_EDGE ( 'NONE', *, *, #61494, .T. ) ;
#33462=CARTESIAN_POINT ( 'NONE',  ( -6.020540257910568904, -6.376774720514411854, 19.49847411603315095 ) ) ;
#33483=ORIENTED_EDGE ( 'NONE', *, *, #31784, .F. ) ;
#33490=ORIENTED_EDGE ( 'NONE', *, *, #71999, .T. ) ;
#33515=CARTESIAN_POINT ( 'NONE',  ( 29.73860345376319003, -5.356774720514425603, -4.021180035027960287 ) ) ;
#33520=CARTESIAN_POINT ( 'NONE',  ( 4.573489327750471567, -5.876774720514419847, 20.79634280254998657 ) ) ;
#33529=CARTESIAN_POINT ( 'NONE',  ( 32.16024265030974050, -0.3587747205144265483, 16.27760796525321751 ) ) ;
#33534=LINE ( 'NONE', #2600, #64288 ) ;
#33564=EDGE_CURVE ( 'NONE', #32852, #76880, #38879, .T. ) ;
#33590=CARTESIAN_POINT ( 'NONE',  ( 6.156881756163101294, -5.876774720514413630, 19.74809127057764968 ) ) ;
#33595=VECTOR ( 'NONE', #74666, 1000.000000000000000 ) ;
#33599=DIRECTION ( 'NONE',  ( 2.327730190238734579E-16, -1.000000000000000000, -8.064610422320895277E-16 ) ) ;
#33602=CARTESIAN_POINT ( 'NONE',  ( 12.00135123753652877, -5.092666038735283784, -26.74699110798160007 ) ) ;
#33608=EDGE_LOOP ( 'NONE', ( #37357, #98834, #93567, #25214, #46038, #79751, #92713, #36311, #26314, #18730, #28930, #8133, #55950, #89272, #96636, #96254, #71561, #9112, #65603, #20506, #28392, #54276, #8890, #83146, #65808, #92721, #5811, #25134 ) ) ;
#33617=CARTESIAN_POINT ( 'NONE',  ( 26.74698519091204574, -1.682774720514426114, -10.98683230472874506 ) ) ;
#33618=CARTESIAN_POINT ( 'NONE',  ( 5.786755829966409692, -5.876774720514414518, 19.89762986309224857 ) ) ;
#33620=CARTESIAN_POINT ( 'NONE',  ( 7.166666666666669627, -6.376774720514420736, 20.78665865384615330 ) ) ;
#33627=EDGE_LOOP ( 'NONE', ( #66325, #28987, #38067, #87510 ) ) ;
#33630=ORIENTED_EDGE ( 'NONE', *, *, #34042, .T. ) ;
#33631=CARTESIAN_POINT ( 'NONE',  ( 9.451856243913134392, 6.475225279485569807, -27.03492916892036746 ) ) ;
#33641=LINE ( 'NONE', #56991, #24729 ) ;
#33645=AXIS2_PLACEMENT_3D ( 'NONE', #68699, #13395, #6783 ) ;
#33649=CARTESIAN_POINT ( 'NONE',  ( 4.967622410992271753, -6.376774720514415407, 20.05703257908297843 ) ) ;
#33661=DIRECTION ( 'NONE',  ( 0.09721092304694055330, 0.000000000000000000, -0.9952638024365006997 ) ) ;
#33663=CARTESIAN_POINT ( 'NONE',  ( -17.64648606763744354, -0.3587747205144061202, -23.04404205923973237 ) ) ;
#33670=VERTEX_POINT ( 'NONE', #76703 ) ;
#33673=ADVANCED_FACE ( 'NONE', ( #52902 ), #58035, .T. ) ;
#33677=CARTESIAN_POINT ( 'NONE',  ( 10.24059822343757808, -5.876774720514426953, 0.000000000000000000 ) ) ;
#33679=CARTESIAN_POINT ( 'NONE',  ( -7.024122139145243082, -6.376774720514408301, 19.17707164986947532 ) ) ;
#33710=ORIENTED_EDGE ( 'NONE', *, *, #79272, .F. ) ;
#33714=CARTESIAN_POINT ( 'NONE',  ( -28.32169924589829080, 5.965225279485592225, -8.244178532169447848 ) ) ;
#33717=EDGE_LOOP ( 'NONE', ( #34759, #23483, #62576, #64956 ) ) ;
#33719=PLANE ( 'NONE',  #90414 ) ;
#33722=CARTESIAN_POINT ( 'NONE',  ( 10.24059822343757986, -5.876774720514426953, 22.82308057603840368 ) ) ;
#33725=CARTESIAN_POINT ( 'NONE',  ( 30.93860345374796594, 0.000000000000000000, 0.000000000000000000 ) ) ;
#33727=VECTOR ( 'NONE', #5700, 1000.000000000000114 ) ;
#33732=EDGE_LOOP ( 'NONE', ( #90771, #67911, #57129, #48988 ) ) ;
#33750=ORIENTED_EDGE ( 'NONE', *, *, #62657, .F. ) ;
#33751=EDGE_CURVE ( 'NONE', #27602, #90358, #92442, .T. ) ;
#33756=EDGE_CURVE ( 'NONE', #74029, #21350, #85820, .T. ) ;
#33766=LINE ( 'NONE', #79931, #55655 ) ;
#33769=VECTOR ( 'NONE', #91682, 1000.000000000000000 ) ;
#33786=AXIS2_PLACEMENT_3D ( 'NONE', #53576, #61191, #62180 ) ;
#33794=AXIS2_PLACEMENT_3D ( 'NONE', #50407, #58523, #88467 ) ;
#33795=PLANE ( 'NONE',  #53207 ) ;
#33798=CARTESIAN_POINT ( 'NONE',  ( 3.202571139211427553, -6.376774720514406525, 18.81074098386681470 ) ) ;
#33800=CARTESIAN_POINT ( 'NONE',  ( 4.373554412633047228, -6.376774720514422512, 21.19197260575996822 ) ) ;
#33801=ADVANCED_FACE ( 'NONE', ( #54902 ), #86836, .T. ) ;
#33804=ORIENTED_EDGE ( 'NONE', *, *, #69988, .T. ) ;
#33811=ORIENTED_EDGE ( 'NONE', *, *, #56400, .T. ) ;
#33821=DIRECTION ( 'NONE',  ( 0.1254312216594016538, 0.000000000000000000, 0.9921023176230513441 ) ) ;
#33822=CARTESIAN_POINT ( 'NONE',  ( 22.81105451610979173, -500000.0000000000582, -18.46691820600746681 ) ) ;
#33826=CARTESIAN_POINT ( 'NONE',  ( -0.3544984435505275644, -6.376774720514408301, 19.15251819062245531 ) ) ;
#33839=DIRECTION ( 'NONE',  ( 0.000000000000000000, -3.740886741919572836E-15, -1.000000000000000000 ) ) ;
#33840=VECTOR ( 'NONE', #37464, 1000.000000000000000 ) ;
#33847=CARTESIAN_POINT ( 'NONE',  ( -9.278253834636469577, -5.876774720514426953, 21.48128695274316158 ) ) ;
#33852=ORIENTED_EDGE ( 'NONE', *, *, #35569, .T. ) ;
#33855=CARTESIAN_POINT ( 'NONE',  ( 28.87399897812680649, -1.682774720514426114, -12.57761096169975801 ) ) ;
#33858=ORIENTED_EDGE ( 'NONE', *, *, #84533, .F. ) ;
#33877=DIRECTION ( 'NONE',  ( 0.000000000000000000, 0.000000000000000000, 1.000000000000000000 ) ) ;
#33878=ORIENTED_EDGE ( 'NONE', *, *, #42606, .F. ) ;
#33880=CARTESIAN_POINT ( 'NONE',  ( 29.70397367894831930, -3.853389802531868469, 28.15179473738050220 ) ) ;
#33894=CARTESIAN_POINT ( 'NONE',  ( -0.5830141525297981575, -5.876774720514410077, 19.15054976246387497 ) ) ;
#33901=LINE ( 'NONE', #19164, #37890 ) ;
#33904=VECTOR ( 'NONE', #83475, 1000.000000000000000 ) ;
#33914=VECTOR ( 'NONE', #19369, 1000.000000000000114 ) ;
#33925=EDGE_CURVE ( 'NONE', #82260, #9871, #84215, .T. ) ;
#33938=CARTESIAN_POINT ( 'NONE',  ( 4.585161930874343206, -6.376774720514427841, 21.47592444013076118 ) ) ;
#33939=CARTESIAN_POINT ( 'NONE',  ( -28.84663072490566194, -0.3587747205144265483, 28.73989617533406715 ) ) ;
#33956=ORIENTED_EDGE ( 'NONE', *, *, #12416, .F. ) ;
#33980=PLANE ( 'NONE',  #66175 ) ;
#33985=CARTESIAN_POINT ( 'NONE',  ( -15.82668884360736961, 6.475225279485576024, 42.07822029717483758 ) ) ;
#34000=CARTESIAN_POINT ( 'NONE',  ( 30.53060340732036337, -5.329285123471891872, 3.289350009555732868 ) ) ;
#34003=CARTESIAN_POINT ( 'NONE',  ( 3.113719597313231002, -6.376774720514426065, 21.58936759753562029 ) ) ;
#34015=PLANE ( 'NONE',  #83785 ) ;
#34017=CARTESIAN_POINT ( 'NONE',  ( 4.967948717948723392, -5.876774720514415407, 20.00140224358974095 ) ) ;
#34030=EDGE_CURVE ( 'NONE', #36077, #81218, #94784, .T. ) ;
#34034=CARTESIAN_POINT ( 'NONE',  ( -10.54059822343757880, -6.376774720514426953, 22.82308057603841078 ) ) ;
#34039=CARTESIAN_POINT ( 'NONE',  ( -13.89275734969026388, -0.3587747205144262708, 31.02402280011862246 ) ) ;
#34042=EDGE_CURVE ( 'NONE', #90256, #62112, #41939, .T. ) ;
#34050=DIRECTION ( 'NONE',  ( -1.334402673828313093E-16, 0.000000000000000000, -1.000000000000000000 ) ) ;
#34052=DIRECTION ( 'NONE',  ( 0.6599726524652410609, 0.000000000000000000, -0.7512896232465839930 ) ) ;
#34058=EDGE_LOOP ( 'NONE', ( #58689, #75922, #47194, #97498 ) ) ;
#34061=DIRECTION ( 'NONE',  ( -1.000000000000000000, 0.000000000000000000, -0.000000000000000000 ) ) ;
#34073=EDGE_CURVE ( 'NONE', #94109, #40447, #2449, .T. ) ;
#34075=ORIENTED_EDGE ( 'NONE', *, *, #18704, .F. ) ;
#34078=EDGE_CURVE ( 'NONE', #9871, #79973, #64784, .T. ) ;
#34081=EDGE_CURVE ( 'NONE', #17533, #96649, #64371, .T. ) ;
#34091=CARTESIAN_POINT ( 'NONE',  ( 7.136624701378261548, -6.376774720514420736, 20.99078681144753844 ) ) ;
#34098=CARTESIAN_POINT ( 'NONE',  ( 6.910430652544937935, -6.376774720514418959, 20.24472806504191169 ) ) ;
#34101=EDGE_CURVE ( 'NONE', #13389, #99974, #57253, .T. ) ;
#34103=ORIENTED_EDGE ( 'NONE', *, *, #13552, .F. ) ;
#34107=CARTESIAN_POINT ( 'NONE',  ( -22.05275734969026047, 5.965225279485572685, 31.02402280011862246 ) ) ;
#34113=ORIENTED_EDGE ( 'NONE', *, *, #85418, .T. ) ;
#34114=CIRCLE ( 'NONE', #14686, 6.000000000000000888 ) ;
#34116=EDGE_CURVE ( 'NONE', #69928, #98963, #65369, .T. ) ;
#34136=VECTOR ( 'NONE', #68089, 1000.000000000000000 ) ;
#34142=CARTESIAN_POINT ( 'NONE',  ( -29.49875734969025842, -0.3587747205144265483, 25.61802280011862720 ) ) ;
#34152=CARTESIAN_POINT ( 'NONE',  ( -5.568927889719891944, -6.376774720514417183, 20.14881673916291760 ) ) ;
#34157=CARTESIAN_POINT ( 'NONE',  ( 16.15056352287345121, -3.622774720514426949, -27.77856273171767398 ) ) ;
#34166=CARTESIAN_POINT ( 'NONE',  ( -1.649669150391666506, -6.376774720514411854, 19.67464842890028365 ) ) ;
#34183=AXIS2_PLACEMENT_3D ( 'NONE', #9382, #32216, #77880 ) ;
#34190=VERTEX_POINT ( 'NONE', #19650 ) ;
#34194=EDGE_CURVE ( 'NONE', #61919, #19444, #89089, .T. ) ;
#34195=EDGE_CURVE ( 'NONE', #37098, #29344, #51116, .T. ) ;
#34199=CARTESIAN_POINT ( 'NONE',  ( -24.90875734969025501, 5.965225279485572685, 26.43402280011862615 ) ) ;
#34201=VECTOR ( 'NONE', #17548, 1000.000000000000000 ) ;
#34206=CARTESIAN_POINT ( 'NONE',  ( -25.92875734969026524, -6.376774720514426953, -0.08597719988137648983 ) ) ;
#34216=ORIENTED_EDGE ( 'NONE', *, *, #32383, .F. ) ;
#34224=FACE_BOUND ( 'NONE', #62336, .T. ) ;
#34228=LINE ( 'NONE', #10378, #95132 ) ;
#34238=VERTEX_POINT ( 'NONE', #2956 ) ;
#34241=EDGE_LOOP ( 'NONE', ( #11415, #51178, #65584 ) ) ;
#34243=LINE ( 'NONE', #24608, #93549 ) ;
#34252=FACE_OUTER_BOUND ( 'NONE', #67816, .T. ) ;
#34256=ADVANCED_FACE ( 'NONE', ( #72963 ), #3457, .F. ) ;
#34262=AXIS2_PLACEMENT_3D ( 'NONE', #80319, #10308, #33142 ) ;
#34274=CARTESIAN_POINT ( 'NONE',  ( 2.591645189881369493, -5.876774720514412742, 19.84288601127407148 ) ) ;
#34279=DIRECTION ( 'NONE',  ( 0.000000000000000000, 0.000000000000000000, 1.000000000000000000 ) ) ;
#34281=ORIENTED_EDGE ( 'NONE', *, *, #68203, .T. ) ;
#34295=CARTESIAN_POINT ( 'NONE',  ( -24.90875734969025501, 5.965225279485572685, 30.51402280011862089 ) ) ;
#34300=DIRECTION ( 'NONE',  ( 2.417950247244706201E-16, 0.000000000000000000, -1.000000000000000000 ) ) ;
#34303=CARTESIAN_POINT ( 'NONE',  ( 2.968164339864655332, -6.376774720514408301, 19.33154224050496595 ) ) ;
#34315=CARTESIAN_POINT ( 'NONE',  ( -2.283364382221138467, -6.376774720514411854, 19.46427715384223944 ) ) ;
#34325=FACE_OUTER_BOUND ( 'NONE', #81410, .T. ) ;
#34332=VERTEX_POINT ( 'NONE', #19519 ) ;
#34334=DIRECTION ( 'NONE',  ( 0.000000000000000000, 0.000000000000000000, -1.000000000000000000 ) ) ;
#34340=ORIENTED_EDGE ( 'NONE', *, *, #75672, .T. ) ;
#34342=CARTESIAN_POINT ( 'NONE',  ( -0.02075734969026423599, -6.376774720514426953, -0.08597719988137648983 ) ) ;
#34349=VECTOR ( 'NONE', #79590, 1000.000000000000000 ) ;
#34353=LINE ( 'NONE', #79517, #63034 ) ;
#34354=FACE_OUTER_BOUND ( 'NONE', #43050, .T. ) ;
#34356=ORIENTED_EDGE ( 'NONE', *, *, #82673, .T. ) ;
#34361=DIRECTION ( 'NONE',  ( -0.000000000000000000, 1.000000000000000000, -0.000000000000000000 ) ) ;
#34363=ORIENTED_EDGE ( 'NONE', *, *, #58309, .T. ) ;
#34364=ORIENTED_EDGE ( 'NONE', *, *, #53937, .F. ) ;
#34369=ORIENTED_EDGE ( 'NONE', *, *, #58997, .T. ) ;
#34375=ORIENTED_EDGE ( 'NONE', *, *, #65518, .F. ) ;
#34380=CARTESIAN_POINT ( 'NONE',  ( 22.81105451610979173, -2.682774720514426559, -18.46691820600746681 ) ) ;
#34388=VERTEX_POINT ( 'NONE', #88547 ) ;
#34389=CARTESIAN_POINT ( 'NONE',  ( -5.568927889719891944, -6.376774720514417183, 20.14881673916291760 ) ) ;
#34416=DIRECTION ( 'NONE',  ( -0.6392559695863496705, -0.000000000000000000, -0.7689940216596069522 ) ) ;
#34417=AXIS2_PLACEMENT_3D ( 'NONE', #83329, #75707, #99042 ) ;
#34418=ORIENTED_EDGE ( 'NONE', *, *, #60888, .T. ) ;
#34426=FACE_OUTER_BOUND ( 'NONE', #80225, .T. ) ;
#34427=CARTESIAN_POINT ( 'NONE',  ( 5.802984775641024662, -6.376774720514402972, 18.35026041666666430 ) ) ;
#34428=EDGE_CURVE ( 'NONE', #73685, #18831, #12901, .T. ) ;
#34438=CARTESIAN_POINT ( 'NONE',  ( 4.527536911777373163, -6.376774720514422512, 21.53954785142818196 ) ) ;
#34462=DIRECTION ( 'NONE',  ( -0.000000000000000000, 1.000000000000000000, -0.000000000000000000 ) ) ;
#34465=CARTESIAN_POINT ( 'NONE',  ( 3.509873074917118085, 5.965225279485572685, 29.15869884040363758 ) ) ;
#34469=AXIS2_PLACEMENT_3D ( 'NONE', #42300, #88947, #56512 ) ;
#34470=ORIENTED_EDGE ( 'NONE', *, *, #23087, .T. ) ;
#34477=VERTEX_POINT ( 'NONE', #5382 ) ;
#34478=DIRECTION ( 'NONE',  ( 0.000000000000000000, 0.000000000000000000, 1.000000000000000000 ) ) ;
#34482=DIRECTION ( 'NONE',  ( 0.000000000000000000, 0.000000000000000000, 1.000000000000000000 ) ) ;
#34485=CARTESIAN_POINT ( 'NONE',  ( -3.108974358974359475, -6.376774720514417183, 20.36458333333334281 ) ) ;
#34486=EDGE_CURVE ( 'NONE', #12639, #5619, #67293, .T. ) ;
#34488=VECTOR ( 'NONE', #49002, 1000.000000000000000 ) ;
#34492=ORIENTED_EDGE ( 'NONE', *, *, #64854, .T. ) ;
#34498=EDGE_CURVE ( 'NONE', #54462, #51886, #17817, .T. ) ;
#34500=CARTESIAN_POINT ( 'NONE',  ( 0.2196812790064107401, -5.876774720514408301, 19.42522865122897002 ) ) ;
#34503=DIRECTION ( 'NONE',  ( 0.000000000000000000, 1.000000000000000000, 0.000000000000000000 ) ) ;
#34508=AXIS2_PLACEMENT_3D ( 'NONE', #99350, #60316, #93241 ) ;
#34515=DIRECTION ( 'NONE',  ( 0.000000000000000000, 0.000000000000000000, -1.000000000000000000 ) ) ;
#34520=DIRECTION ( 'NONE',  ( 0.7689940216596065081, 7.885106708985488048E-16, -0.6392559695863502256 ) ) ;
#34525=CARTESIAN_POINT ( 'NONE',  ( 10.24059822343757808, -5.876774720514426953, 0.000000000000000000 ) ) ;
#34526=EDGE_LOOP ( 'NONE', ( #52747, #62696, #41095, #22719 ) ) ;
#34535=AXIS2_PLACEMENT_3D ( 'NONE', #38830, #23591, #85501 ) ;
#34546=CARTESIAN_POINT ( 'NONE',  ( -7.640838998533831194, -5.876774720514417183, 20.32624910079993086 ) ) ;
#34547=B_SPLINE_CURVE_WITH_KNOTS ( 'NONE', 3,
 ( #10140, #88273, #49226, #86759, #16743, #17248, #55330 ),
 .UNSPECIFIED., .F., .F.,
 ( 4, 3, 4 ),
 ( 0.000000000000000000, 1.195459452644217715E-05, 2.107775188753445374E-05 ),
 .UNSPECIFIED. ) ;
#34549=CARTESIAN_POINT ( 'NONE',  ( 28.87399897812680649, 1.477225279485574028, -12.57761096169975445 ) ) ;
#34561=CONICAL_SURFACE ( 'NONE', #91260, 2.999999999999999112, 0.7853981633974412846 ) ;
#34572=CARTESIAN_POINT ( 'NONE',  ( 282.9764569301858046, -0.6647747205144264315, 20.79159422840526616 ) ) ;
#34580=ORIENTED_EDGE ( 'NONE', *, *, #16895, .T. ) ;
#34606=CARTESIAN_POINT ( 'NONE',  ( 11.56983764158150407, -0.3587747205144265483, 28.29037853177889517 ) ) ;
#34608=VERTEX_POINT ( 'NONE', #58673 ) ;
#34609=ADVANCED_FACE ( 'NONE', ( #44955 ), #89127, .F. ) ;
#34628=CARTESIAN_POINT ( 'NONE',  ( 7.164812103570541879, -5.876774720514421624, 20.85668272347560404 ) ) ;
#34632=ORIENTED_EDGE ( 'NONE', *, *, #35892, .F. ) ;
#34634=ORIENTED_EDGE ( 'NONE', *, *, #44352, .F. ) ;
#34639=CARTESIAN_POINT ( 'NONE',  ( -53.01255352321339842, -5.356774720514425603, 35.59556822165056644 ) ) ;
#34650=ORIENTED_EDGE ( 'NONE', *, *, #75336, .T. ) ;
#34655=CARTESIAN_POINT ( 'NONE',  ( 31.79364159983995464, 5.965225279485572685, -11.59305536555894278 ) ) ;
#34659=CARTESIAN_POINT ( 'NONE',  ( 31.88667425545052581, -1.682774720514426114, -9.651215965565016930 ) ) ;
#34660=CARTESIAN_POINT ( 'NONE',  ( 2.976770017179964700, -5.876774720514419847, 20.68690469677381927 ) ) ;
#34666=LINE ( 'NONE', #33663, #37983 ) ;
#34668=CARTESIAN_POINT ( 'NONE',  ( 0.000000000000000000, -2.682774720514426559, 0.000000000000000000 ) ) ;
#34671=EDGE_CURVE ( 'NONE', #54808, #40322, #35344, .T. ) ;
#34678=CARTESIAN_POINT ( 'NONE',  ( 14.02639803017889086, -6.376774720514426065, -25.20535965011783119 ) ) ;
#34680=CARTESIAN_POINT ( 'NONE',  ( -7.338700834008208496, -5.876774720514410077, 19.35116211686183263 ) ) ;
#34682=CARTESIAN_POINT ( 'NONE',  ( 30.09341516180546350, -1.684774720514424562, -11.39311774897855933 ) ) ;
#34686=EDGE_CURVE ( 'NONE', #58859, #99983, #54549, .T. ) ;
#34690=CARTESIAN_POINT ( 'NONE',  ( 6.830155907162054341, -5.876774720514427841, 21.76451523534627341 ) ) ;
#34691=EDGE_CURVE ( 'NONE', #86012, #49051, #87562, .T. ) ;
#34692=FACE_OUTER_BOUND ( 'NONE', #79928, .T. ) ;
#34694=FACE_OUTER_BOUND ( 'NONE', #27834, .T. ) ;
#34695=VERTEX_POINT ( 'NONE', #30709 ) ;
#34711=DIRECTION ( 'NONE',  ( 1.988296846060374587E-13, 1.000000000000000000, -1.446139281080278507E-13 ) ) ;
#34716=CARTESIAN_POINT ( 'NONE',  ( 7.052174998393318184, -5.876774720514418071, 20.39928653130861136 ) ) ;
#34719=CARTESIAN_POINT ( 'NONE',  ( 29.72843915439144524, -4.948038888671026037, 27.41656699113896067 ) ) ;
#34732=ORIENTED_EDGE ( 'NONE', *, *, #97527, .T. ) ;
#34737=DIRECTION ( 'NONE',  ( -0.000000000000000000, 1.000000000000000000, -0.000000000000000000 ) ) ;
#34741=CARTESIAN_POINT ( 'NONE',  ( 7.344278919687202922, -6.376774720514417183, 20.19896341048075783 ) ) ;
#34747=PLANE ( 'NONE',  #20033 ) ;
#34750=AXIS2_PLACEMENT_3D ( 'NONE', #82994, #13487, #75383 ) ;
#34751=LINE ( 'NONE', #12397, #52315 ) ;
#34753=EDGE_LOOP ( 'NONE', ( #41379, #76753, #86601, #86256, #100240, #15289, #56457, #98055 ) ) ;
#34756=ADVANCED_FACE ( 'NONE', ( #7867 ), #70276, .F. ) ;
#34759=ORIENTED_EDGE ( 'NONE', *, *, #45266, .T. ) ;
#34762=VERTEX_POINT ( 'NONE', #83995 ) ;
#34763=DIRECTION ( 'NONE',  ( -0.000000000000000000, 1.000000000000000000, -0.000000000000000000 ) ) ;
#34764=CARTESIAN_POINT ( 'NONE',  ( -0.02075734969026423599, 5.965225279485572685, -0.08597719988137648983 ) ) ;
#34780=DIRECTION ( 'NONE',  ( 0.000000000000000000, 0.000000000000000000, -1.000000000000000000 ) ) ;
#34784=DIRECTION ( 'NONE',  ( 1.611864046919725738E-15, -7.253388211138766116E-15, 1.000000000000000000 ) ) ;
#34796=LINE ( 'NONE', #96681, #28543 ) ;
#34815=EDGE_CURVE ( 'NONE', #81032, #78995, #2276, .T. ) ;
#34817=CARTESIAN_POINT ( 'NONE',  ( 0.3791100739519297491, -6.376774720514418959, 20.35309744218306349 ) ) ;
#34819=DIRECTION ( 'NONE',  ( -0.000000000000000000, 1.000000000000000000, -0.000000000000000000 ) ) ;
#34833=FACE_OUTER_BOUND ( 'NONE', #64451, .T. ) ;
#34845=CARTESIAN_POINT ( 'NONE',  ( -20.27875734969026311, 7.743225279485574042, 24.00402280011862288 ) ) ;
#34850=CARTESIAN_POINT ( 'NONE',  ( 282.9764569301858046, 6.475225279485573360, 20.79159422840526616 ) ) ;
#34852=AXIS2_PLACEMENT_3D ( 'NONE', #48901, #58513, #26559 ) ;
#34853=VERTEX_POINT ( 'NONE', #80385 ) ;
#34858=DIRECTION ( 'NONE',  ( 0.000000000000000000, 0.000000000000000000, -1.000000000000000000 ) ) ;
#34863=( BOUNDED_SURFACE ( )  B_SPLINE_SURFACE ( 3, 2, ( 
 ( #73362, #96685, #72366 ),
 ( #80466, #40904, #19558 ),
 ( #17566, #27187, #25676 ),
 ( #4354, #95692, #2862 ) ),
 .UNSPECIFIED., .F., .F., .T. ) 
 B_SPLINE_SURFACE_WITH_KNOTS ( ( 4, 4 ),
 ( 3, 3 ),
 ( 0.0009756167707891351057, 0.001181474220861217402 ),
 ( 0.000000000000000000, 1.000000000000000000 ),
 .UNSPECIFIED. ) 
 GEOMETRIC_REPRESENTATION_ITEM ( )  RATIONAL_B_SPLINE_SURFACE ( (
 ( 1.000000000000000000, 0.8117984224361689538, 1.000000000000000000),
 ( 1.000000000000000000, 0.7811245729408042848, 1.000000000000000000),
 ( 1.000000000000000000, 0.7458076110977214235, 1.000000000000000000),
 ( 1.000000000000000000, 0.7071067811865522357, 1.000000000000000000) ) ) 
 REPRESENTATION_ITEM ( '' )  SURFACE ( )  );
#34877=FACE_OUTER_BOUND ( 'NONE', #1980, .T. ) ;
#34881=CARTESIAN_POINT ( 'NONE',  ( -7.131053040288445999, -5.876774720514413630, 19.60308799987318196 ) ) ;
#34887=EDGE_CURVE ( 'NONE', #21668, #5151, #86989, .T. ) ;
#34890=DIRECTION ( 'NONE',  ( 0.000000000000000000, 0.000000000000000000, 1.000000000000000000 ) ) ;
#34929=ORIENTED_EDGE ( 'NONE', *, *, #84709, .T. ) ;
#34930=CARTESIAN_POINT ( 'NONE',  ( 6.431189903846153300, -6.376774720514415407, 20.08974358974358765 ) ) ;
#34931=EDGE_CURVE ( 'NONE', #27382, #12529, #19973, .T. ) ;
#34935=CARTESIAN_POINT ( 'NONE',  ( 30.45304879119406039, 1.477225279485574028, -10.07140455160086390 ) ) ;
#34936=CARTESIAN_POINT ( 'NONE',  ( -25.92875734969025814, -3.316774720514426456, 24.50402280011861933 ) ) ;
#34943=CARTESIAN_POINT ( 'NONE',  ( 8.978253834636468866, -5.876774720514426953, 18.51871304725684553 ) ) ;
#34948=ORIENTED_EDGE ( 'NONE', *, *, #44720, .F. ) ;
#34949=CIRCLE ( 'NONE', #30074, 2.040000000000000036 ) ;
#34957=ORIENTED_EDGE ( 'NONE', *, *, #60394, .F. ) ;
#34959=CARTESIAN_POINT ( 'NONE',  ( -9.940598223437573822, -5.876774720514426953, 18.21871304725684837 ) ) ;
#34973=VERTEX_POINT ( 'NONE', #20465 ) ;
#34976=CARTESIAN_POINT ( 'NONE',  ( 5.851028665930490646, 6.475225279485576024, -27.43979700150094558 ) ) ;
#34983=FACE_OUTER_BOUND ( 'NONE', #7906, .T. ) ;
#34992=EDGE_CURVE ( 'NONE', #64204, #32607, #72947, .T. ) ;
#35025=VERTEX_POINT ( 'NONE', #12357 ) ;
#35030=LINE ( 'NONE', #44137, #61804 ) ;
#35033=VERTEX_POINT ( 'NONE', #98589 ) ;
#35042=CARTESIAN_POINT ( 'NONE',  ( -10.26072176705811145, -4.666310954396869271, 28.98969649327457532 ) ) ;
#35051=CARTESIAN_POINT ( 'NONE',  ( 14.78484767477524819, -3.316774720514429120, -28.43034250232787841 ) ) ;
#35058=EDGE_LOOP ( 'NONE', ( #22785, #45855, #34, #60298 ) ) ;
#35064=CARTESIAN_POINT ( 'NONE',  ( -9.940598223437577374, -5.876774720514426953, 17.91871304725684766 ) ) ;
#35066=EDGE_CURVE ( 'NONE', #31571, #54541, #90750, .T. ) ;
#35068=ADVANCED_FACE ( 'NONE', ( #90984 ), #21455, .F. ) ;
#35093=ORIENTED_EDGE ( 'NONE', *, *, #37973, .T. ) ;
#35094=VECTOR ( 'NONE', #83873, 1000.000000000000000 ) ;
#35095=ORIENTED_EDGE ( 'NONE', *, *, #74802, .F. ) ;
#35098=CARTESIAN_POINT ( 'NONE',  ( 14.70028154892705707, -3.418387289272210250, -28.41026772490150876 ) ) ;
#35113=VERTEX_POINT ( 'NONE', #82865 ) ;
#35117=ORIENTED_EDGE ( 'NONE', *, *, #69596, .T. ) ;
#35122=DIRECTION ( 'NONE',  ( -0.9161084732596777025, 4.164321980682960499E-15, 0.4009304992412306978 ) ) ;
#35125=CARTESIAN_POINT ( 'NONE',  ( 7.081057417352553784, -6.376774720514424288, 21.11453472826393352 ) ) ;
#35130=VECTOR ( 'NONE', #45957, 1000.000000000000000 ) ;
#35147=CARTESIAN_POINT ( 'NONE',  ( 29.73860345376319358, -5.356774720496559894, 7.190646357373898680E-15 ) ) ;
#35148=LINE ( 'NONE', #67107, #30159 ) ;
#35163=VERTEX_POINT ( 'NONE', #22943 ) ;
#35170=CIRCLE ( 'NONE', #43285, 3.060000000000000053 ) ;
#35180=CARTESIAN_POINT ( 'NONE',  ( 9.146648804574669001, -3.316774720514593433, -28.07004961703220758 ) ) ;
#35182=CARTESIAN_POINT ( 'NONE',  ( -7.138063944469604571, -5.876774720514408301, 19.21974929698718881 ) ) ;
#35186=CARTESIAN_POINT ( 'NONE',  ( 30.53060340732036337, -5.022552014119394670, -1.287656715832136367 ) ) ;
#35188=ORIENTED_EDGE ( 'NONE', *, *, #85418, .F. ) ;
#35192=CARTESIAN_POINT ( 'NONE',  ( 13.57581083383197296, -5.876774720514426953, 19.78786796564403616 ) ) ;
#35194=CARTESIAN_POINT ( 'NONE',  ( -23.62875734969026453, 6.143225279485574397, 23.50402280011862288 ) ) ;
#35195=EDGE_LOOP ( 'NONE', ( #37674, #88259 ) ) ;
#35197=CARTESIAN_POINT ( 'NONE',  ( -1.836964591723098117, -6.376774720514410077, 19.23384392940399223 ) ) ;
#35201=LINE ( 'NONE', #75242, #46955 ) ;
#35206=DIRECTION ( 'NONE',  ( -9.779078418496698369E-14, 0.000000000000000000, -1.000000000000000000 ) ) ;
#35208=ORIENTED_EDGE ( 'NONE', *, *, #81857, .F. ) ;
#35213=FACE_OUTER_BOUND ( 'NONE', #48423, .T. ) ;
#35221=CARTESIAN_POINT ( 'NONE',  ( 6.910430652544937935, -5.876774720514418071, 20.24472806504191169 ) ) ;
#35222=PLANE ( 'NONE',  #5900 ) ;
#35225=CARTESIAN_POINT ( 'NONE',  ( 29.71608694565284026, -4.561299274004467996, 27.78615310300602559 ) ) ;
#35229=CARTESIAN_POINT ( 'NONE',  ( -29.49875734969026198, 5.965225279485572685, 10.11402280011862587 ) ) ;
#35232=LINE ( 'NONE', #66204, #70124 ) ;
#35238=EDGE_LOOP ( 'NONE', ( #40570, #19350, #59968, #13628 ) ) ;
#35242=AXIS2_PLACEMENT_3D ( 'NONE', #45117, #15645, #16143 ) ;
#35244=CARTESIAN_POINT ( 'NONE',  ( 7.089543269230769162, -6.376774720514413630, 19.75741185897435415 ) ) ;
#35252=CARTESIAN_POINT ( 'NONE',  ( 7.087697398486194622, -6.376774720514418959, 20.45710073441444621 ) ) ;
#35253=CYLINDRICAL_SURFACE ( 'NONE', #87760, 0.3000000000000016542 ) ;
#35266=CARTESIAN_POINT ( 'NONE',  ( -16.89397143409390623, -5.876774720514426953, 16.89397143409405899 ) ) ;
#35269=CARTESIAN_POINT ( 'NONE',  ( -22.05275734969026047, -0.3587747205144262708, 31.02402280011862246 ) ) ;
#35273=DIRECTION ( 'NONE',  ( -0.000000000000000000, -1.000000000000000000, -0.000000000000000000 ) ) ;
#35275=VECTOR ( 'NONE', #94763, 1000.000000000000000 ) ;
#35293=CARTESIAN_POINT ( 'NONE',  ( 30.53060340732036337, -5.297812262124697469, 1.539714685317310483 ) ) ;
#35298=DIRECTION ( 'NONE',  ( 0.000000000000000000, -1.000000000000000000, 0.000000000000000000 ) ) ;
#35307=FACE_OUTER_BOUND ( 'NONE', #7859, .T. ) ;
#35312=EDGE_CURVE ( 'NONE', #34388, #44867, #19462, .T. ) ;
#35315=CARTESIAN_POINT ( 'NONE',  ( 6.365284455128204399, -5.876774720514413630, 19.73076923076922640 ) ) ;
#35319=ORIENTED_EDGE ( 'NONE', *, *, #91098, .T. ) ;
#35326=LINE ( 'NONE', #98702, #90610 ) ;
#35328=VERTEX_POINT ( 'NONE', #14347 ) ;
#35339=ADVANCED_FACE ( 'NONE', ( #29581 ), #44298, .T. ) ;
#35344=LINE ( 'NONE', #74878, #85888 ) ;
#35355=ORIENTED_EDGE ( 'NONE', *, *, #89586, .T. ) ;
#35370=CARTESIAN_POINT ( 'NONE',  ( 29.73860345376319003, -1.682774720514426114, -1.272392034746785860 ) ) ;
#35381=ORIENTED_EDGE ( 'NONE', *, *, #82988, .F. ) ;
#35382=CARTESIAN_POINT ( 'NONE',  ( -10.11875734969026297, -3.316774720514426456, 30.51402280011862089 ) ) ;
#35390=CARTESIAN_POINT ( 'NONE',  ( 6.132272708306365949, -5.876774720514424288, 21.80683391321003839 ) ) ;
#35394=PLANE ( 'NONE',  #24114 ) ;
#35401=DIRECTION ( 'NONE',  ( 0.000000000000000000, -1.000000000000000000, 0.000000000000000000 ) ) ;
#35406=CARTESIAN_POINT ( 'NONE',  ( -0.9988807608215116707, -6.376774720514411854, 19.30497968945844889 ) ) ;
#35419=DIRECTION ( 'NONE',  ( 0.7071067811865507924, 0.000000000000000000, -0.7071067811865442421 ) ) ;
#35422=DIRECTION ( 'NONE',  ( -0.000000000000000000, 1.000000000000000000, -0.000000000000000000 ) ) ;
#35429=DIRECTION ( 'NONE',  ( -0.7071067811865475727, 0.000000000000000000, 0.7071067811865475727 ) ) ;
#35437=CARTESIAN_POINT ( 'NONE',  ( 5.817949855437939632, -6.376774720514417183, 20.34349022145623209 ) ) ;
#35456=ORIENTED_EDGE ( 'NONE', *, *, #84590, .F. ) ;
#35460=LINE ( 'NONE', #50683, #79465 ) ;
#35462=ORIENTED_EDGE ( 'NONE', *, *, #48652, .F. ) ;
#35467=CARTESIAN_POINT ( 'NONE',  ( 13.10664265030973930, 5.965225279485574461, -27.62597719988137612 ) ) ;
#35473=ORIENTED_EDGE ( 'NONE', *, *, #6931, .T. ) ;
#35476=ORIENTED_EDGE ( 'NONE', *, *, #31459, .T. ) ;
#35481=VERTEX_POINT ( 'NONE', #74639 ) ;
#35482=CARTESIAN_POINT ( 'NONE',  ( 10.62437663934349530, -3.316774720514425567, -27.03002426119959978 ) ) ;
#35484=EDGE_CURVE ( 'NONE', #90130, #90525, #74591, .T. ) ;
#35490=DIRECTION ( 'NONE',  ( 0.7682573101345365751, 0.000000000000000000, -0.6401411605457395515 ) ) ;
#35495=VERTEX_POINT ( 'NONE', #77511 ) ;
#35496=VERTEX_POINT ( 'NONE', #8012 ) ;
#35502=ORIENTED_EDGE ( 'NONE', *, *, #48658, .F. ) ;
#35506=CARTESIAN_POINT ( 'NONE',  ( 13.59451591917074431, -3.316774720514426456, -28.23515841827053308 ) ) ;
#35512=FACE_OUTER_BOUND ( 'NONE', #61178, .T. ) ;
#35513=CARTESIAN_POINT ( 'NONE',  ( -3.108974358974359475, -6.376774720514417183, 20.36458333333334281 ) ) ;
#35524=ADVANCED_FACE ( 'NONE', ( #49596 ), #65828, .T. ) ;
#35529=EDGE_LOOP ( 'NONE', ( #97128, #97085, #58370, #66425 ) ) ;
#35534=VECTOR ( 'NONE', #65426, 1000.000000000000000 ) ;
#35536=ORIENTED_EDGE ( 'NONE', *, *, #10631, .T. ) ;
#35544=DIRECTION ( 'NONE',  ( 0.000000000000000000, 0.000000000000000000, 1.000000000000000000 ) ) ;
#35550=CARTESIAN_POINT ( 'NONE',  ( 5.811591729264017125, -6.376774720514422512, 21.22699980322195046 ) ) ;
#35551=ORIENTED_EDGE ( 'NONE', *, *, #63314, .F. ) ;
#35560=ORIENTED_EDGE ( 'NONE', *, *, #52774, .F. ) ;
#35569=EDGE_CURVE ( 'NONE', #1158, #24982, #56714, .T. ) ;
#35581=AXIS2_PLACEMENT_3D ( 'NONE', #4740, #35688, #42814 ) ;
#35589=ORIENTED_EDGE ( 'NONE', *, *, #66648, .T. ) ;
#35590=VERTEX_POINT ( 'NONE', #71934 ) ;
#35592=EDGE_CURVE ( 'NONE', #9229, #46643, #64995, .T. ) ;
#35598=FACE_OUTER_BOUND ( 'NONE', #129, .T. ) ;
#35610=CARTESIAN_POINT ( 'NONE',  ( 10.86264265030973952, -0.3587747205144257157, -27.62597719988137612 ) ) ;
#35615=EDGE_LOOP ( 'NONE', ( #21297, #64594, #86854, #87810, #95761, #99691, #54305, #817, #93887, #80026, #12864, #50434, #40813, #62926, #6883, #6399, #91186, #30458 ) ) ;
#35623=CARTESIAN_POINT ( 'NONE',  ( 5.705253819860196529, -5.876774720514416295, 19.95963554344900714 ) ) ;
#35632=CARTESIAN_POINT ( 'NONE',  ( 6.671786015990716301, 6.475225279485573360, -27.29955796265488033 ) ) ;
#35637=VECTOR ( 'NONE', #22909, 1000.000000000000000 ) ;
#35644=LINE ( 'NONE', #35147, #34136 ) ;
#35645=VECTOR ( 'NONE', #91979, 1000.000000000000227 ) ;
#35655=VERTEX_POINT ( 'NONE', #33855 ) ;
#35658=CARTESIAN_POINT ( 'NONE',  ( 30.59073162224239084, -4.540774720514408891, 26.30400772315274338 ) ) ;
#35659=AXIS2_PLACEMENT_3D ( 'NONE', #68444, #75041, #5537 ) ;
#35661=VERTEX_POINT ( 'NONE', #56211 ) ;
#35672=ORIENTED_EDGE ( 'NONE', *, *, #5693, .T. ) ;
#35674=CARTESIAN_POINT ( 'NONE',  ( 4.653494883475234545, -5.876774720514415407, 20.13747874360300116 ) ) ;
#35676=CARTESIAN_POINT ( 'NONE',  ( 8.655157120194559184, -6.376774720514430506, -28.10018424674326099 ) ) ;
#35681=ORIENTED_EDGE ( 'NONE', *, *, #76347, .F. ) ;
#35683=CARTESIAN_POINT ( 'NONE',  ( 6.371704462700114924, -5.876774720514426953, 21.83798798526824214 ) ) ;
#35688=DIRECTION ( 'NONE',  ( -0.000000000000000000, -1.000000000000000000, -0.000000000000000000 ) ) ;
#35689=ADVANCED_FACE ( 'NONE', ( #19120 ), #18130, .T. ) ;
#35698=CARTESIAN_POINT ( 'NONE',  ( -0.02075734969026423599, 5.965225279485572685, -0.08597719988137648983 ) ) ;
#35701=EDGE_CURVE ( 'NONE', #75743, #70312, #35780, .T. ) ;
#35705=LINE ( 'NONE', #96108, #50903 ) ;
#35708=B_SPLINE_CURVE_WITH_KNOTS ( 'NONE', 3,
 ( #21982, #76763, #92007, #22478 ),
 .UNSPECIFIED., .F., .F.,
 ( 4, 4 ),
 ( 0.6459941988912109023, 0.6543842573219610381 ),
 .UNSPECIFIED. ) ;
#35713=DIRECTION ( 'NONE',  ( -0.000000000000000000, 1.000000000000000000, -0.000000000000000000 ) ) ;
#35724=CARTESIAN_POINT ( 'NONE',  ( 282.9764569301858046, -4.540774720514427543, 20.79159422840526616 ) ) ;
#35738=VECTOR ( 'NONE', #99324, 1000.000000000000000 ) ;
#35744=CARTESIAN_POINT ( 'NONE',  ( 7.141559373243376641, -5.876774720514415407, 19.83742167145384983 ) ) ;
#35749=LINE ( 'NONE', #91509, #98792 ) ;
#35750=CARTESIAN_POINT ( 'NONE',  ( 6.910430652544937935, -6.376774720514418959, 20.24472806504191169 ) ) ;
#35751=EDGE_CURVE ( 'NONE', #29704, #30337, #34114, .T. ) ;
#35758=CARTESIAN_POINT ( 'NONE',  ( 32.16024265030974050, -0.3587747205144265483, 16.27760796525321751 ) ) ;
#35762=EDGE_CURVE ( 'NONE', #4160, #50305, #41558, .T. ) ;
#35764=EDGE_LOOP ( 'NONE', ( #24525, #44085, #68120, #47940 ) ) ;
#35769=CARTESIAN_POINT ( 'NONE',  ( 3.121233215686890272, -6.376774720514404748, 18.93204046835445808 ) ) ;
#35779=LINE ( 'NONE', #20046, #21650 ) ;
#35780=CIRCLE ( 'NONE', #90821, 129.7684398600581517 ) ;
#35788=CARTESIAN_POINT ( 'NONE',  ( 25.61870917940689196, 5.965225279485572685, 29.49402280011862487 ) ) ;
#35789=CARTESIAN_POINT ( 'NONE',  ( 27.86270917940689174, -0.3587747205144265483, 29.49402280011862487 ) ) ;
#35797=CARTESIAN_POINT ( 'NONE',  ( -4.968349358974361252, -6.376774720514411854, 19.46153846153847056 ) ) ;
#35804=ORIENTED_EDGE ( 'NONE', *, *, #57378, .F. ) ;
#35807=EDGE_CURVE ( 'NONE', #5267, #77096, #27743, .T. ) ;
#35817=PLANE ( 'NONE',  #4714 ) ;
#35820=VERTEX_POINT ( 'NONE', #42980 ) ;
#35823=EDGE_CURVE ( 'NONE', #78258, #70560, #56874, .T. ) ;
#35827=DIRECTION ( 'NONE',  ( 1.000000000000000000, 0.000000000000000000, 0.000000000000000000 ) ) ;
#35832=ORIENTED_EDGE ( 'NONE', *, *, #72938, .T. ) ;
#35846=EDGE_LOOP ( 'NONE', ( #74395, #46560, #42754, #41331 ) ) ;
#35851=ORIENTED_EDGE ( 'NONE', *, *, #75212, .T. ) ;
#35852=CARTESIAN_POINT ( 'NONE',  ( 30.35461040182540415, -5.059010452157854942, 19.84760796525321425 ) ) ;
#35860=DIRECTION ( 'NONE',  ( 0.000000000000000000, 0.000000000000000000, -1.000000000000000000 ) ) ;
#35863=VERTEX_POINT ( 'NONE', #66327 ) ;
#35872=CARTESIAN_POINT ( 'NONE',  ( -10.40290173325841216, -6.376774720514426953, 27.45402280011861862 ) ) ;
#35876=ORIENTED_EDGE ( 'NONE', *, *, #85630, .F. ) ;
#35890=FACE_BOUND ( 'NONE', #32490, .T. ) ;
#35892=EDGE_CURVE ( 'NONE', #66793, #18886, #45474, .T. ) ;
#35893=EDGE_CURVE ( 'NONE', #65974, #91108, #7886, .T. ) ;
#35895=DIRECTION ( 'NONE',  ( -1.000000000000000000, -0.000000000000000000, 0.000000000000000000 ) ) ;
#35902=CARTESIAN_POINT ( 'NONE',  ( 10.84340024150424497, -4.021317321268781164, -26.91457715659927175 ) ) ;
#35908=CARTESIAN_POINT ( 'NONE',  ( -20.27875734969026311, 6.143225279485574397, 24.00402280011862288 ) ) ;
#35910=ORIENTED_EDGE ( 'NONE', *, *, #18035, .F. ) ;
#35923=ORIENTED_EDGE ( 'NONE', *, *, #34671, .T. ) ;
#35924=CARTESIAN_POINT ( 'NONE',  ( 10.54059822343757880, -6.376774720514426953, 22.82308057603841078 ) ) ;
#35928=DIRECTION ( 'NONE',  ( 0.000000000000000000, -1.000000000000000000, 0.000000000000000000 ) ) ;
#35942=EDGE_LOOP ( 'NONE', ( #76286, #7061, #30072, #22467, #21335, #27360 ) ) ;
#35944=ORIENTED_EDGE ( 'NONE', *, *, #5960, .T. ) ;
#35947=ORIENTED_EDGE ( 'NONE', *, *, #95872, .F. ) ;
#35964=ORIENTED_EDGE ( 'NONE', *, *, #45668, .T. ) ;
#35966=CARTESIAN_POINT ( 'NONE',  ( 15.29947330337542688, -3.316774720514426456, -27.16854002387010070 ) ) ;
#35967=VERTEX_POINT ( 'NONE', #55582 ) ;
#35981=ORIENTED_EDGE ( 'NONE', *, *, #11572, .F. ) ;
#35983=VECTOR ( 'NONE', #3117, 1000.000000000000000 ) ;
#35999=DIRECTION ( 'NONE',  ( 4.089440751051245812E-15, 1.000000000000000000, -1.042451643221144600E-15 ) ) ;
#36005=DIRECTION ( 'NONE',  ( -0.000000000000000000, 1.000000000000000000, -0.000000000000000000 ) ) ;
#36051=LINE ( 'NONE', #29428, #15995 ) ;
#36056=DIRECTION ( 'NONE',  ( 0.000000000000000000, -1.000000000000000000, 0.000000000000000000 ) ) ;
#36063=ORIENTED_EDGE ( 'NONE', *, *, #58868, .T. ) ;
#36077=VERTEX_POINT ( 'NONE', #75276 ) ;
#36079=ORIENTED_EDGE ( 'NONE', *, *, #2578, .F. ) ;
#36080=CARTESIAN_POINT ( 'NONE',  ( 14.52511747680497933, 5.965225279485572685, -27.86035006098926559 ) ) ;
#36096=CARTESIAN_POINT ( 'NONE',  ( -20.27875734969026311, -6.376774720514428729, 21.00402280011862644 ) ) ;
#36100=B_SPLINE_SURFACE_WITH_KNOTS ( 'NONE', 3, 1, ( 
 ( #36474, #66946 ),
 ( #90763, #27373 ),
 ( #28360, #27865 ),
 ( #13623, #59321 ),
 ( #20740, #65961 ),
 ( #51708, #81157 ),
 ( #96881, #88781 ),
 ( #13126, #82646 ),
 ( #75022, #65463 ),
 ( #75523, #42612 ),
 ( #96380, #89269 ),
 ( #50710, #5521 ),
 ( #67437, #19247 ),
 ( #74047, #28867 ),
 ( #50215, #12131 ),
 ( #4545, #58823 ),
 ( #59829, #21238 ),
 ( #19738, #44595 ),
 ( #73548, #76024 ) ),
 .UNSPECIFIED., .F., .F., .F.,
 ( 4, 1, 1, 1, 1, 1, 1, 1, 1, 1, 1, 1, 1, 1, 1, 1, 4 ),
 ( 2, 2 ),
 ( 0.000000000000000000, 0.06891237672743111276, 0.1352246433344312937, 0.2001606018079680194, 0.2639831308323357106, 0.3270287715257772510, 0.3902418945738325151, 0.4541682297891322939, 0.5193355915291701930, 0.5832703360758352273, 0.6452842511902443512, 0.7050706230450887180, 0.7637435797381000313, 0.8217746784923816161, 0.8800061561487860784, 0.9388620850843768517, 1.000000000000000000 ),
 ( 0.000000000000000000, 1.000000000000000000 ),
 .UNSPECIFIED. ) ;
#36101=ORIENTED_EDGE ( 'NONE', *, *, #24053, .T. ) ;
#36102=ORIENTED_EDGE ( 'NONE', *, *, #34081, .T. ) ;
#36114=CARTESIAN_POINT ( 'NONE',  ( 22.02124265030973760, -4.776774720514394446, 16.20402280011862217 ) ) ;
#36119=CARTESIAN_POINT ( 'NONE',  ( 8.000000000000003553, -5.876774720514426953, 17.50000000000000000 ) ) ;
#36120=VECTOR ( 'NONE', #79518, 1000.000000000000000 ) ;
#36121=B_SPLINE_CURVE_WITH_KNOTS ( 'NONE', 3,
 ( #63158, #52169, #91219, #94086, #29323, #21695, #72771 ),
 .UNSPECIFIED., .F., .F.,
 ( 4, 1, 1, 1, 4 ),
 ( 0.000000000000000000, 0.2835948081386949760, 0.5433948405759660982, 0.7806456291745647036, 1.000000000000000000 ),
 .UNSPECIFIED. ) ;
#36122=ORIENTED_EDGE ( 'NONE', *, *, #29854, .T. ) ;
#36142=CARTESIAN_POINT ( 'NONE',  ( 4.400426145423703694, -5.876774720514425177, 21.64763382324305852 ) ) ;
#36151=ORIENTED_EDGE ( 'NONE', *, *, #2762, .T. ) ;
#36153=CARTESIAN_POINT ( 'NONE',  ( 3.004381791450704942, -5.876774720514420736, 20.78526834885430219 ) ) ;
#36156=ORIENTED_EDGE ( 'NONE', *, *, #73631, .T. ) ;
#36158=CARTESIAN_POINT ( 'NONE',  ( -1.359251851468251449, -6.376774720514420736, 20.71116975788854120 ) ) ;
#36161=CARTESIAN_POINT ( 'NONE',  ( -7.282824509310913186, -6.376774720514415407, 19.84584863393302356 ) ) ;
#36178=CARTESIAN_POINT ( 'NONE',  ( -1.743696941008423984, -6.376774720514413630, 19.59984006504825160 ) ) ;
#36182=CARTESIAN_POINT ( 'NONE',  ( 5.994920710892026605, -5.876774720514428729, 21.76186867112717138 ) ) ;
#36186=CARTESIAN_POINT ( 'NONE',  ( 12.16765770914787304, 6.475225279485573360, -27.57618308014988173 ) ) ;
#36187=CIRCLE ( 'NONE', #62127, 0.3000000000000016542 ) ;
#36192=CARTESIAN_POINT ( 'NONE',  ( -1.967852706420949005, -6.376774720514408301, 19.18381548539530357 ) ) ;
#36194=AXIS2_PLACEMENT_3D ( 'NONE', #84950, #98678, #6336 ) ;
#36204=CARTESIAN_POINT ( 'NONE',  ( 33.13288845015618023, 5.965225279485572685, -0.1650522222209214185 ) ) ;
#36206=VERTEX_POINT ( 'NONE', #17380 ) ;
#36208=DIRECTION ( 'NONE',  ( -0.000000000000000000, -1.000000000000000000, -0.000000000000000000 ) ) ;
#36228=ORIENTED_EDGE ( 'NONE', *, *, #22043, .T. ) ;
#36229=AXIS2_PLACEMENT_3D ( 'NONE', #6430, #37384, #67342 ) ;
#36238=AXIS2_PLACEMENT_3D ( 'NONE', #73207, #89918, #89421 ) ;
#36241=DIRECTION ( 'NONE',  ( 7.109281096390894329E-15, 0.000000000000000000, 1.000000000000000000 ) ) ;
#36245=ORIENTED_EDGE ( 'NONE', *, *, #28067, .F. ) ;
#36247=CARTESIAN_POINT ( 'NONE',  ( 7.052174998393318184, -6.376774720514418959, 20.39928653130861136 ) ) ;
#36253=DIRECTION ( 'NONE',  ( -0.000000000000000000, 1.000000000000000000, -0.000000000000000000 ) ) ;
#36254=CARTESIAN_POINT ( 'NONE',  ( 30.62809631291915835, -4.628857374213141362, 27.84496821199607908 ) ) ;
#36255=CARTESIAN_POINT ( 'NONE',  ( -29.49875734969025842, 5.965225279485572685, 17.86602280011862476 ) ) ;
#36257=DIRECTION ( 'NONE',  ( -0.7071067811865507924, -0.000000000000000000, -0.7071067811865442421 ) ) ;
#36263=VECTOR ( 'NONE', #75783, 1000.000000000000000 ) ;
#36264=CARTESIAN_POINT ( 'NONE',  ( 2.932009311892267434, -6.376774720514410077, 19.53174284846577891 ) ) ;
#36267=CARTESIAN_POINT ( 'NONE',  ( 3.509873074917118085, -0.3587747205144265483, 29.15869884040363758 ) ) ;
#36272=ADVANCED_FACE ( 'NONE', ( #71678 ), #2175, .F. ) ;
#36289=CARTESIAN_POINT ( 'NONE',  ( -4.152941208099351300, -5.876774720514416295, 20.35309744218305639 ) ) ;
#36291=CARTESIAN_POINT ( 'NONE',  ( -24.90875734969025501, 5.965225279485572685, 26.43402280011862615 ) ) ;
#36297=CARTESIAN_POINT ( 'NONE',  ( 30.53060340732035982, 1.477225279485574028, 19.84760796525321425 ) ) ;
#36299=CARTESIAN_POINT ( 'NONE',  ( -2.243088942307695177, -6.376774720514408301, 19.14743589743590491 ) ) ;
#36309=DIRECTION ( 'NONE',  ( 0.000000000000000000, 0.000000000000000000, -1.000000000000000000 ) ) ;
#36311=ORIENTED_EDGE ( 'NONE', *, *, #18756, .T. ) ;
#36317=CARTESIAN_POINT ( 'NONE',  ( 13.91401389203221406, 6.475225279485573360, 158.0376437107427137 ) ) ;
#36332=VERTEX_POINT ( 'NONE', #25494 ) ;
#36341=CARTESIAN_POINT ( 'NONE',  ( -2.606012662418322634, -5.876774720514409189, 19.21974929698718881 ) ) ;
#36349=VERTEX_POINT ( 'NONE', #64592 ) ;
#36351=DIRECTION ( 'NONE',  ( 0.9921023176230513441, 0.000000000000000000, -0.1254312216594016538 ) ) ;
#36354=CARTESIAN_POINT ( 'NONE',  ( -28.98875734969026396, -0.3587747205144265483, 2.362022800118626531 ) ) ;
#36360=DIRECTION ( 'NONE',  ( 0.000000000000000000, -1.000000000000000000, 0.000000000000000000 ) ) ;
#36371=B_SPLINE_SURFACE_WITH_KNOTS ( 'NONE', 3, 1, ( 
 ( #64069, #72661 ),
 ( #96485, #11252 ),
 ( #9749, #87371 ),
 ( #71158, #73161 ),
 ( #25470, #55941 ),
 ( #25974, #79251 ),
 ( #41211, #32583 ),
 ( #33090, #95488 ),
 ( #26976, #17866 ),
 ( #47817, #94983 ),
 ( #80264, #94483 ),
 ( #63563, #17361 ),
 ( #56946, #40704 ),
 ( #80770, #3652 ),
 ( #78739, #48323 ),
 ( #72164, #33590 ),
 ( #87880, #9240 ),
 ( #3158, #41721 ),
 ( #2654, #10249 ) ),
 .UNSPECIFIED., .F., .F., .F.,
 ( 4, 1, 1, 1, 1, 1, 1, 1, 1, 1, 1, 1, 1, 1, 1, 1, 4 ),
 ( 2, 2 ),
 ( 0.000000000000000000, 0.06565904849408699118, 0.1292578964840137568, 0.1914365047840415057, 0.2527174969864875997, 0.3133199640703511202, 0.3744898936696244851, 0.4369089249503372852, 0.5009282752929569149, 0.5649763261437619200, 0.6271371978431706795, 0.6884541671478572322, 0.7490566342317193094, 0.8099329284035216014, 0.8715951039967769765, 0.9347691962579698366, 1.000000000000000000 ),
 ( 0.000000000000000000, 1.000000000000000000 ),
 .UNSPECIFIED. ) ;
#36377=ORIENTED_EDGE ( 'NONE', *, *, #51609, .T. ) ;
#36378=DIRECTION ( 'NONE',  ( 0.000000000000000000, -1.000000000000000000, 0.000000000000000000 ) ) ;
#36384=ADVANCED_FACE ( 'NONE', ( #25993 ), #63072, .T. ) ;
#36388=CARTESIAN_POINT ( 'NONE',  ( 24.71017632900190719, -3.356774720514427379, 1.647607965253211848 ) ) ;
#36394=DIRECTION ( 'NONE',  ( -0.000000000000000000, 1.000000000000000000, -0.000000000000000000 ) ) ;
#36399=VERTEX_POINT ( 'NONE', #46453 ) ;
#36411=DIRECTION ( 'NONE',  ( -0.9994733861282923959, 0.000000000000000000, -0.03244919754393515293 ) ) ;
#36415=VERTEX_POINT ( 'NONE', #76876 ) ;
#36425=CARTESIAN_POINT ( 'NONE',  ( 3.063121397228215859, -6.376774720514420736, 20.95210102656095685 ) ) ;
#36433=CARTESIAN_POINT ( 'NONE',  ( 6.561060095583167495, -5.876774720514427841, 21.83518827598938117 ) ) ;
#36437=CARTESIAN_POINT ( 'NONE',  ( -0.02075734969026423599, -0.3587747205144213303, -0.08597719988137648983 ) ) ;
#36465=EDGE_LOOP ( 'NONE', ( #13565, #93225, #48807, #11261 ) ) ;
#36472=CIRCLE ( 'NONE', #15451, 7.652410033082758467 ) ;
#36474=CARTESIAN_POINT ( 'NONE',  ( 6.431189903846153300, -6.376774720514415407, 20.08974358974358765 ) ) ;
#36476=CARTESIAN_POINT ( 'NONE',  ( -8.978253834636468866, -5.876774720514426953, 21.48128695274316158 ) ) ;
#36477=ORIENTED_EDGE ( 'NONE', *, *, #89716, .F. ) ;
#36487=CYLINDRICAL_SURFACE ( 'NONE', #82656, 1.530000000000001359 ) ;
#36492=EDGE_CURVE ( 'NONE', #12606, #93033, #29306, .T. ) ;
#36495=CARTESIAN_POINT ( 'NONE',  ( -9.940598223437577374, -5.876774720514426953, 22.08128695274315945 ) ) ;
#36511=CARTESIAN_POINT ( 'NONE',  ( 10.86264265030973952, -0.3587747205144257157, -28.64597719988137570 ) ) ;
#36513=EDGE_CURVE ( 'NONE', #41593, #62694, #23094, .T. ) ;
#36514=CARTESIAN_POINT ( 'NONE',  ( -5.891025641025639636, -6.376774720514420736, 20.75510817307693046 ) ) ;
#36521=CARTESIAN_POINT ( 'NONE',  ( -10.28806225508158612, -4.941275956067651798, 28.69510307482446976 ) ) ;
#36528=VECTOR ( 'NONE', #8357, 1000.000000000000000 ) ;
#36534=DIRECTION ( 'NONE',  ( 0.000000000000000000, 1.000000000000000000, 0.000000000000000000 ) ) ;
#36543=LINE ( 'NONE', #38045, #25875 ) ;
#36545=DIRECTION ( 'NONE',  ( 0.6451914333552788428, 0.000000000000000000, 0.7640209514960704107 ) ) ;
#36546=CARTESIAN_POINT ( 'NONE',  ( 5.981014360695730225, -5.876774720514425177, 21.36744920115099333 ) ) ;
#36558=DIRECTION ( 'NONE',  ( -0.000000000000000000, 1.000000000000000000, -0.000000000000000000 ) ) ;
#36567=EDGE_CURVE ( 'NONE', #8977, #66223, #119, .T. ) ;
#36569=ORIENTED_EDGE ( 'NONE', *, *, #89257, .F. ) ;
#36570=CARTESIAN_POINT ( 'NONE',  ( 6.403846153846157740, -6.376774720514426065, 21.48076923076922995 ) ) ;
#36571=CARTESIAN_POINT ( 'NONE',  ( 2.708118538500707828, -5.876774720514424288, 20.94830092343283212 ) ) ;
#36575=CARTESIAN_POINT ( 'NONE',  ( 30.57144966832858302, 5.048887879205125273, 25.33340266839140398 ) ) ;
#36585=ADVANCED_FACE ( 'NONE', ( #72297 ), #95628, .T. ) ;
#36586=EDGE_CURVE ( 'NONE', #96543, #6499, #26060, .T. ) ;
#36588=ORIENTED_EDGE ( 'NONE', *, *, #13718, .T. ) ;
#36592=EDGE_CURVE ( 'NONE', #53085, #18133, #1782, .T. ) ;
#36596=ORIENTED_EDGE ( 'NONE', *, *, #807, .F. ) ;
#36603=DIRECTION ( 'NONE',  ( -0.000000000000000000, 1.000000000000000000, -0.000000000000000000 ) ) ;
#36610=VERTEX_POINT ( 'NONE', #63193 ) ;
#36612=EDGE_CURVE ( 'NONE', #26949, #30746, #19606, .T. ) ;
#36625=ADVANCED_FACE ( 'NONE', ( #33222 ), #2292, .F. ) ;
#36645=B_SPLINE_CURVE_WITH_KNOTS ( 'NONE', 3,
 ( #13999, #37361, #45477, #46459, #77389, #98238, #53089, #59706 ),
 .UNSPECIFIED., .F., .F.,
 ( 4, 2, 2, 4 ),
 ( 0.000000000000000000, 0.003897507692133500394, 0.005846261538200250157, 0.007795015384267000788 ),
 .UNSPECIFIED. ) ;
#36653=CARTESIAN_POINT ( 'NONE',  ( -7.188523146553190912, -6.376774720514413630, 19.66116880005639800 ) ) ;
#36654=LINE ( 'NONE', #91426, #91095 ) ;
#36655=CARTESIAN_POINT ( 'NONE',  ( 22.81105451610979173, -2.682774720540237468, -18.46691820600746681 ) ) ;
#36659=VERTEX_POINT ( 'NONE', #88519 ) ;
#36661=LINE ( 'NONE', #90449, #47377 ) ;
#36664=CARTESIAN_POINT ( 'NONE',  ( -19.69812919673063689, 5.965225279485592225, -22.00173861453435720 ) ) ;
#36689=DIRECTION ( 'NONE',  ( -0.000000000000000000, 1.000000000000000000, -0.000000000000000000 ) ) ;
#36697=DIRECTION ( 'NONE',  ( -0.000000000000000000, 0.000000000000000000, -1.000000000000000000 ) ) ;
#36701=VERTEX_POINT ( 'NONE', #59076 ) ;
#36716=PLANE ( 'NONE',  #15670 ) ;
#36718=CARTESIAN_POINT ( 'NONE',  ( -20.27875734969026311, -6.376774720514428729, 21.00402280011862644 ) ) ;
#36730=CARTESIAN_POINT ( 'NONE',  ( 6.727764423076923350, -5.876774720514413630, 19.76442307692307665 ) ) ;
#36733=CARTESIAN_POINT ( 'NONE',  ( 7.477175500793984853, -6.376774720514417183, 20.66439772633092176 ) ) ;
#36740=ADVANCED_FACE ( 'NONE', ( #5269 ), #79768, .F. ) ;
#36742=ORIENTED_EDGE ( 'NONE', *, *, #29307, .F. ) ;
#36743=AXIS2_PLACEMENT_3D ( 'NONE', #36388, #67351, #98269 ) ;
#36745=EDGE_CURVE ( 'NONE', #100069, #41697, #35232, .T. ) ;
#36749=CARTESIAN_POINT ( 'NONE',  ( 29.77147767949870882, -5.356774720514427379, 26.15915692125050995 ) ) ;
#36752=CIRCLE ( 'NONE', #80493, 0.3000000000000016542 ) ;
#36760=EDGE_LOOP ( 'NONE', ( #69798, #40226, #43677, #17818 ) ) ;
#36761=CARTESIAN_POINT ( 'NONE',  ( 3.749014282529493869, -5.876774720514404748, 18.52125941707705792 ) ) ;
#36762=CARTESIAN_POINT ( 'NONE',  ( 3.714584954927674154, -6.376774720514402972, 18.16171433633635246 ) ) ;
#36763=DIRECTION ( 'NONE',  ( 0.000000000000000000, 0.000000000000000000, 1.000000000000000000 ) ) ;
#36775=LINE ( 'NONE', #67739, #9925 ) ;
#36796=AXIS2_PLACEMENT_3D ( 'NONE', #28636, #50480, #28142 ) ;
#36798=LINE ( 'NONE', #12944, #43222 ) ;
#36803=CARTESIAN_POINT ( 'NONE',  ( -0.08860454909227881426, -5.876774720514410077, 19.21747685089457036 ) ) ;
#36819=ORIENTED_EDGE ( 'NONE', *, *, #91036, .F. ) ;
#36825=CARTESIAN_POINT ( 'NONE',  ( -19.80875734969026425, 5.965225279485572685, 31.02402280011862246 ) ) ;
#36827=FACE_OUTER_BOUND ( 'NONE', #85111, .T. ) ;
#36831=ORIENTED_EDGE ( 'NONE', *, *, #77076, .T. ) ;
#36842=CARTESIAN_POINT ( 'NONE',  ( -3.071531057816138333, -6.376774720514413630, 19.86545874326175110 ) ) ;
#36851=ORIENTED_EDGE ( 'NONE', *, *, #36612, .T. ) ;
#36854=CARTESIAN_POINT ( 'NONE',  ( 29.73860345376319003, -5.356471260711259674, 19.84760796525321425 ) ) ;
#36869=VECTOR ( 'NONE', #6308, 1000.000000000000000 ) ;
#36870=CARTESIAN_POINT ( 'NONE',  ( -10.17728017005432228, -5.183720752832764234, 29.88674535377839803 ) ) ;
#36884=CARTESIAN_POINT ( 'NONE',  ( -2.791950601096355733, -5.876774720514415407, 20.17732409774492552 ) ) ;
#36899=ORIENTED_EDGE ( 'NONE', *, *, #94131, .T. ) ;
#36917=PLANE ( 'NONE',  #32245 ) ;
#36920=CARTESIAN_POINT ( 'NONE',  ( -5.891025641025639636, -5.876774720514419847, 20.75510817307693046 ) ) ;
#36924=CARTESIAN_POINT ( 'NONE',  ( 3.094204744773375815, -6.376774720514422512, 21.02053020447315745 ) ) ;
#36931=CARTESIAN_POINT ( 'NONE',  ( 7.480769230769231726, -5.876774720514430506, 20.77403846153845635 ) ) ;
#36943=ORIENTED_EDGE ( 'NONE', *, *, #862, .T. ) ;
#36948=ORIENTED_EDGE ( 'NONE', *, *, #77591, .F. ) ;
#36963=CIRCLE ( 'NONE', #17550, 3.349999999999998757 ) ;
#36968=AXIS2_PLACEMENT_3D ( 'NONE', #38321, #77870, #70781 ) ;
#37015=CARTESIAN_POINT ( 'NONE',  ( 4.373554412633047228, -5.876774720514422512, 21.19197260575996822 ) ) ;
#37018=FACE_OUTER_BOUND ( 'NONE', #55060, .T. ) ;
#37025=VECTOR ( 'NONE', #68109, 1000.000000000000000 ) ;
#37035=CARTESIAN_POINT ( 'NONE',  ( 33.13630134430571417, -3.554473796596999691, -12.85738972836020899 ) ) ;
#37037=FACE_OUTER_BOUND ( 'NONE', #51220, .T. ) ;
#37038=CARTESIAN_POINT ( 'NONE',  ( 6.365284455128204399, -6.376774720514413630, 19.73076923076922640 ) ) ;
#37045=CARTESIAN_POINT ( 'NONE',  ( -3.108974358974355923, -5.876774720514426953, 21.75000000000001066 ) ) ;
#37054=ORIENTED_EDGE ( 'NONE', *, *, #85983, .F. ) ;
#37056=ORIENTED_EDGE ( 'NONE', *, *, #86200, .T. ) ;
#37061=DIRECTION ( 'NONE',  ( -0.9978940991575084851, 0.000000000000000000, -0.06486421869277853025 ) ) ;
#37063=FACE_OUTER_BOUND ( 'NONE', #49335, .T. ) ;
#37065=FACE_OUTER_BOUND ( 'NONE', #8098, .T. ) ;
#37068=ADVANCED_FACE ( 'NONE', ( #18380 ), #66087, .F. ) ;
#37077=ORIENTED_EDGE ( 'NONE', *, *, #13390, .F. ) ;
#37078=CIRCLE ( 'NONE', #32228, 3.500000000000000000 ) ;
#37079=ORIENTED_EDGE ( 'NONE', *, *, #26099, .T. ) ;
#37090=DIRECTION ( 'NONE',  ( -0.000000000000000000, 1.000000000000000000, -0.000000000000000000 ) ) ;
#37091=ORIENTED_EDGE ( 'NONE', *, *, #9801, .F. ) ;
#37098=VERTEX_POINT ( 'NONE', #51333 ) ;
#37101=PLANE ( 'NONE',  #47917 ) ;
#37106=CARTESIAN_POINT ( 'NONE',  ( 15.01415361830768447, -3.567044333682400481, -27.41917996820976811 ) ) ;
#37107=CARTESIAN_POINT ( 'NONE',  ( 5.996070682796505125, -3.316774720514426900, -27.41631156547456882 ) ) ;
#37110=ORIENTED_EDGE ( 'NONE', *, *, #41684, .T. ) ;
#37119=CARTESIAN_POINT ( 'NONE',  ( -27.96875734969026084, 6.475225279485573360, 26.43402280011862615 ) ) ;
#37147=FACE_OUTER_BOUND ( 'NONE', #74963, .T. ) ;
#37150=CARTESIAN_POINT ( 'NONE',  ( 5.326923076923078426, -6.376774720514420736, 20.76772836538461320 ) ) ;
#37152=VECTOR ( 'NONE', #10350, 1000.000000000000000 ) ;
#37153=CARTESIAN_POINT ( 'NONE',  ( 31.84105487026623393, -5.152774720514427642, -11.95870468328481806 ) ) ;
#37159=EDGE_CURVE ( 'NONE', #57446, #97929, #5303, .T. ) ;
#37161=PLANE ( 'NONE',  #29470 ) ;
#37171=CARTESIAN_POINT ( 'NONE',  ( -1.394533802543915124, -6.376774720514413630, 20.19722303762275573 ) ) ;
#37172=VECTOR ( 'NONE', #35860, 1000.000000000000000 ) ;
#37181=VERTEX_POINT ( 'NONE', #67564 ) ;
#37188=EDGE_CURVE ( 'NONE', #47988, #51587, #97984, .T. ) ;
#37191=B_SPLINE_CURVE_WITH_KNOTS ( 'NONE', 3,
 ( #5974, #45053, #27818, #74974, #5477, #66899, #76471, #91206, #67389, #83589, #82600, #36924, #36425, #20692, #59782 ),
 .UNSPECIFIED., .F., .F.,
 ( 4, 1, 1, 1, 1, 1, 1, 1, 1, 1, 1, 1, 4 ),
 ( 0.000000000000000000, 0.1128134007444584058, 0.2253938839207300371, 0.3395948145627014636, 0.4596754102248630236, 0.5217351900879338977, 0.5839258387389175686, 0.6481741447653697197, 0.7138810381130681337, 0.7810044549073911213, 0.8514509275565554924, 0.9240506926641786078, 1.000000000000000000 ),
 .UNSPECIFIED. ) ;
#37192=LINE ( 'NONE', #27594, #29188 ) ;
#37194=FACE_OUTER_BOUND ( 'NONE', #99810, .T. ) ;
#37203=DIRECTION ( 'NONE',  ( -0.000000000000000000, 1.000000000000000000, -0.000000000000000000 ) ) ;
#37213=CARTESIAN_POINT ( 'NONE',  ( 31.79364159983995464, 6.475225279485573360, -11.59305536555894278 ) ) ;
#37242=EDGE_LOOP ( 'NONE', ( #63843, #71280, #63116, #33750 ) ) ;
#37243=VECTOR ( 'NONE', #62205, 1000.000000000000000 ) ;
#37250=LINE ( 'NONE', #83408, #95209 ) ;
#37252=DIRECTION ( 'NONE',  ( 0.000000000000000000, 0.000000000000000000, 1.000000000000000000 ) ) ;
#37255=AXIS2_PLACEMENT_3D ( 'NONE', #64109, #57492, #26526 ) ;
#37262=CARTESIAN_POINT ( 'NONE',  ( 2.920210193027767076, -5.876774720514413630, 19.64065332113010243 ) ) ;
#37263=LINE ( 'NONE', #99140, #18258 ) ;
#37282=CARTESIAN_POINT ( 'NONE',  ( -4.147110899021980934, -5.876774720514418959, 20.45311193189268906 ) ) ;
#37283=FACE_OUTER_BOUND ( 'NONE', #531, .T. ) ;
#37296=CARTESIAN_POINT ( 'NONE',  ( -1.733151984336291695, -6.376774720514408301, 19.29154511076646017 ) ) ;
#37314=DIRECTION ( 'NONE',  ( 0.000000000000000000, 0.000000000000000000, 1.000000000000000000 ) ) ;
#37322=EDGE_LOOP ( 'NONE', ( #82045, #52333, #15836, #33080 ) ) ;
#37323=VECTOR ( 'NONE', #88985, 1000.000000000000000 ) ;
#37344=CARTESIAN_POINT ( 'NONE',  ( -3.108787716482549701, -5.876774720514416295, 20.32624910079993086 ) ) ;
#37349=ORIENTED_EDGE ( 'NONE', *, *, #56908, .T. ) ;
#37357=ORIENTED_EDGE ( 'NONE', *, *, #79461, .T. ) ;
#37358=DIRECTION ( 'NONE',  ( 0.000000000000000000, 0.000000000000000000, -1.000000000000000000 ) ) ;
#37361=CARTESIAN_POINT ( 'NONE',  ( 30.54636625424942764, -6.376774720514426065, 1.976438700016742045 ) ) ;
#37372=VERTEX_POINT ( 'NONE', #26258 ) ;
#37378=ORIENTED_EDGE ( 'NONE', *, *, #52760, .T. ) ;
#37382=ORIENTED_EDGE ( 'NONE', *, *, #72382, .F. ) ;
#37384=DIRECTION ( 'NONE',  ( 0.000000000000000000, 1.000000000000000000, 0.000000000000000000 ) ) ;
#37391=AXIS2_PLACEMENT_3D ( 'NONE', #1533, #63447, #24854 ) ;
#37393=CARTESIAN_POINT ( 'NONE',  ( -2.762050907158362989, -6.376774720514415407, 19.89644244529369033 ) ) ;
#37397=CIRCLE ( 'NONE', #53399, 91.74549126261076992 ) ;
#37406=DIRECTION ( 'NONE',  ( 0.000000000000000000, 0.000000000000000000, -1.000000000000000000 ) ) ;
#37407=ORIENTED_EDGE ( 'NONE', *, *, #99037, .T. ) ;
#37412=CARTESIAN_POINT ( 'NONE',  ( -4.620655831143558601, -6.376774720514410077, 19.21747685089457036 ) ) ;
#37419=CARTESIAN_POINT ( 'NONE',  ( 3.113719597313231002, -6.376774720514426065, 21.58936759753562029 ) ) ;
#37421=DIRECTION ( 'NONE',  ( 1.000000000000000000, 0.000000000000000000, -2.168404344971008868E-16 ) ) ;
#37422=CARTESIAN_POINT ( 'NONE',  ( 29.73860345376319003, -1.682774720514426114, -1.272392034746785860 ) ) ;
#37423=ORIENTED_EDGE ( 'NONE', *, *, #35066, .T. ) ;
#37433=CARTESIAN_POINT ( 'NONE',  ( -5.755030174389611730, -6.376774720514410077, 19.56655654527324728 ) ) ;
#37435=CARTESIAN_POINT ( 'NONE',  ( 2.903846153846159517, -5.876774720514415407, 19.99999999999999289 ) ) ;
#37454=ORIENTED_EDGE ( 'NONE', *, *, #29307, .T. ) ;
#37456=DIRECTION ( 'NONE',  ( 0.000000000000000000, 0.000000000000000000, 1.000000000000000000 ) ) ;
#37464=DIRECTION ( 'NONE',  ( -0.000000000000000000, 1.000000000000000000, -0.000000000000000000 ) ) ;
#37468=ADVANCED_FACE ( 'NONE', ( #31241 ), #7903, .F. ) ;
#37473=CARTESIAN_POINT ( 'NONE',  ( 4.821763668436347849, -5.876774720514404748, 18.93074869776452829 ) ) ;
#37480=CARTESIAN_POINT ( 'NONE',  ( 5.641653616409716854, -6.376774720514420736, 20.81030773351227481 ) ) ;
#37498=ORIENTED_EDGE ( 'NONE', *, *, #23778, .F. ) ;
#37502=DIRECTION ( 'NONE',  ( -0.000000000000000000, 1.000000000000000000, -0.000000000000000000 ) ) ;
#37515=EDGE_CURVE ( 'NONE', #15460, #70350, #68472, .T. ) ;
#37520=CARTESIAN_POINT ( 'NONE',  ( 15.27524774227295978, -2.682774720514427003, -27.18982104163420388 ) ) ;
#37535=LINE ( 'NONE', #84697, #81274 ) ;
#37537=CARTESIAN_POINT ( 'NONE',  ( -19.37210865224160017, -0.3587747205143967943, -21.60955166348796297 ) ) ;
#37556=CARTESIAN_POINT ( 'NONE',  ( -5.576923076923074873, -5.876774720514426953, 21.75000000000000711 ) ) ;
#37578=CARTESIAN_POINT ( 'NONE',  ( -4.537657931416015700, -6.376774720514410077, 19.25713806424188235 ) ) ;
#37581=ORIENTED_EDGE ( 'NONE', *, *, #94468, .F. ) ;
#37584=CARTESIAN_POINT ( 'NONE',  ( 19.72776355195876263, -0.3587747205144265483, 28.39950002376595606 ) ) ;
#37594=DIRECTION ( 'NONE',  ( 0.000000000000000000, -1.000000000000000000, 0.000000000000000000 ) ) ;
#37595=AXIS2_PLACEMENT_3D ( 'NONE', #49755, #25896, #34515 ) ;
#37604=ORIENTED_EDGE ( 'NONE', *, *, #62267, .T. ) ;
#37608=FACE_OUTER_BOUND ( 'NONE', #18374, .T. ) ;
#37613=CARTESIAN_POINT ( 'NONE',  ( 29.74616903497430442, -6.356993644837154456, 26.56043482791313082 ) ) ;
#37615=CARTESIAN_POINT ( 'NONE',  ( -4.686006777320704586, -0.3587747205144265483, 29.60911411231907309 ) ) ;
#37620=CARTESIAN_POINT ( 'NONE',  ( 14.46675407819882331, -3.972730170967898378, -28.29579275198952359 ) ) ;
#37625=ORIENTED_EDGE ( 'NONE', *, *, #3527, .T. ) ;
#37628=PLANE ( 'NONE',  #85975 ) ;
#37638=VECTOR ( 'NONE', #59133, 1000.000000000000000 ) ;
#37639=EDGE_CURVE ( 'NONE', #90018, #76914, #14473, .T. ) ;
#37642=CARTESIAN_POINT ( 'NONE',  ( 0.000000000000000000, -2.056774720514426669, 0.000000000000000000 ) ) ;
#37643=EDGE_CURVE ( 'NONE', #79116, #82889, #10166, .T. ) ;
#37647=LINE ( 'NONE', #20406, #44244 ) ;
#37674=ORIENTED_EDGE ( 'NONE', *, *, #81505, .T. ) ;
#37676=EDGE_CURVE ( 'NONE', #62214, #46809, #86029, .T. ) ;
#37677=CARTESIAN_POINT ( 'NONE',  ( -1.304987980769231948, -5.876774720514412742, 19.76512419871795245 ) ) ;
#37689=VERTEX_POINT ( 'NONE', #2814 ) ;
#37694=ORIENTED_EDGE ( 'NONE', *, *, #67491, .T. ) ;
#37700=VERTEX_POINT ( 'NONE', #32241 ) ;
#37708=CARTESIAN_POINT ( 'NONE',  ( 6.365284455128204399, -6.376774720514413630, 19.73076923076922640 ) ) ;
#37731=CARTESIAN_POINT ( 'NONE',  ( 32.80655795465876423, -4.354682733740601108, -4.311478614910781992 ) ) ;
#37752=EDGE_CURVE ( 'NONE', #91151, #84743, #10407, .T. ) ;
#37754=CARTESIAN_POINT ( 'NONE',  ( 3.116263380642223968, -6.376774720514401196, 18.40799819116699609 ) ) ;
#37755=CARTESIAN_POINT ( 'NONE',  ( -24.90875734969025501, 5.965225279485572685, 26.43402280011862615 ) ) ;
#37761=ORIENTED_EDGE ( 'NONE', *, *, #38769, .T. ) ;
#37776=LINE ( 'NONE', #7312, #29519 ) ;
#37780=EDGE_CURVE ( 'NONE', #81663, #41697, #34751, .T. ) ;
#37789=CARTESIAN_POINT ( 'NONE',  ( -1.595974963000059477, -6.376774720514408301, 19.39236848396478408 ) ) ;
#37796=CARTESIAN_POINT ( 'NONE',  ( -2.794871794871791604, -5.876774720514426953, 21.75000000000001066 ) ) ;
#37804=CARTESIAN_POINT ( 'NONE',  ( 0.2428503871269292180, -6.376774720514413630, 19.85590024959437017 ) ) ;
#37818=LINE ( 'NONE', #14969, #47586 ) ;
#37823=CIRCLE ( 'NONE', #16738, 0.8159999999999469900 ) ;
#37829=EDGE_LOOP ( 'NONE', ( #9486, #8134, #8771, #50419 ) ) ;
#37830=CARTESIAN_POINT ( 'NONE',  ( -3.103301570662693187, -6.376774720514418959, 20.14409848895067512 ) ) ;
#37834=CARTESIAN_POINT ( 'NONE',  ( -27.96875734969026084, 6.143225279485574397, 24.50402280011861933 ) ) ;
#37837=LINE ( 'NONE', #60194, #46794 ) ;
#37859=EDGE_CURVE ( 'NONE', #76045, #79539, #8571, .T. ) ;
#37865=EDGE_LOOP ( 'NONE', ( #34580, #77113, #89237, #72482, #13759, #66104, #12871, #72593, #88000, #99628, #49544, #84903, #45343, #97960, #9865 ) ) ;
#37874=ADVANCED_FACE ( 'NONE', ( #14114 ), #84130, .F. ) ;
#37875=ORIENTED_EDGE ( 'NONE', *, *, #65861, .T. ) ;
#37890=VECTOR ( 'NONE', #35895, 1000.000000000000000 ) ;
#37893=FACE_OUTER_BOUND ( 'NONE', #20743, .T. ) ;
#37899=VERTEX_POINT ( 'NONE', #14620 ) ;
#37901=EDGE_CURVE ( 'NONE', #15617, #81766, #31350, .T. ) ;
#37914=CARTESIAN_POINT ( 'NONE',  ( 29.73860345376319003, -5.356774720514425603, -4.021180035027960287 ) ) ;
#37915=EDGE_CURVE ( 'NONE', #90366, #77603, #39467, .T. ) ;
#37916=ORIENTED_EDGE ( 'NONE', *, *, #1565, .T. ) ;
#37927=CARTESIAN_POINT ( 'NONE',  ( -5.530932042872791499, -6.376774720514408301, 19.30497968945844534 ) ) ;
#37934=CARTESIAN_POINT ( 'NONE',  ( 9.940598223437573822, -5.876774720514426953, 18.21871304725684837 ) ) ;
#37937=ORIENTED_EDGE ( 'NONE', *, *, #34815, .T. ) ;
#37948=CARTESIAN_POINT ( 'NONE',  ( -29.49875734969025842, 5.965225279485572685, 23.37402280011862743 ) ) ;
#37957=ORIENTED_EDGE ( 'NONE', *, *, #51660, .T. ) ;
#37963=CARTESIAN_POINT ( 'NONE',  ( 15.30859874843628354, -3.492299066144916697, -27.16052374892713317 ) ) ;
#37965=ADVANCED_FACE ( 'NONE', ( #7013 ), #29346, .T. ) ;
#37966=CARTESIAN_POINT ( 'NONE',  ( 4.334227700317904386, -6.376774720514402972, 18.30971318885719157 ) ) ;
#37971=PLANE ( 'NONE',  #5825 ) ;
#37973=EDGE_CURVE ( 'NONE', #64840, #26207, #22219, .T. ) ;
#37977=LINE ( 'NONE', #52210, #11922 ) ;
#37983=VECTOR ( 'NONE', #42302, 999.9999999999998863 ) ;
#37993=CARTESIAN_POINT ( 'NONE',  ( -1.174900045708346497, -5.876774720514411854, 19.48569229636960998 ) ) ;
#37997=AXIS2_PLACEMENT_3D ( 'NONE', #24834, #48190, #94848 ) ;
#37998=VERTEX_POINT ( 'NONE', #93740 ) ;
#38002=FACE_OUTER_BOUND ( 'NONE', #59508, .T. ) ;
#38006=CYLINDRICAL_SURFACE ( 'NONE', #17478, 91.74549126261076992 ) ;
#38031=CARTESIAN_POINT ( 'NONE',  ( 33.69795529655567634, 5.515143950957555496, 14.99689261510125249 ) ) ;
#38045=CARTESIAN_POINT ( 'NONE',  ( 32.60294298177596062, -6.376774720514426953, -11.48871326860665043 ) ) ;
#38051=CARTESIAN_POINT ( 'NONE',  ( 26.73860345374794178, -1.682774720514426114, -1.272392034746785860 ) ) ;
#38057=VECTOR ( 'NONE', #88505, 1000.000000000000000 ) ;
#38067=ORIENTED_EDGE ( 'NONE', *, *, #67253, .T. ) ;
#38075=ORIENTED_EDGE ( 'NONE', *, *, #83781, .F. ) ;
#38082=CARTESIAN_POINT ( 'NONE',  ( -20.27875734969026311, -5.356774720514425603, 24.00402280011862288 ) ) ;
#38085=DIRECTION ( 'NONE',  ( -8.659560562354873694E-17, -0.7071067811865525687, -0.7071067811865425767 ) ) ;
#38087=CARTESIAN_POINT ( 'NONE',  ( -4.141025641025642301, -6.376774720514408301, 19.19230769230769695 ) ) ;
#38090=VECTOR ( 'NONE', #22898, 1000.000000000000000 ) ;
#38103=LINE ( 'NONE', #69057, #68986 ) ;
#38113=VECTOR ( 'NONE', #58779, 1000.000000000000114 ) ;
#38118=VERTEX_POINT ( 'NONE', #81535 ) ;
#38124=CIRCLE ( 'NONE', #94846, 8.452410033082760066 ) ;
#38135=EDGE_CURVE ( 'NONE', #66793, #88329, #67307, .T. ) ;
#38140=DIRECTION ( 'NONE',  ( -0.000000000000000000, -1.000000000000000000, -0.000000000000000000 ) ) ;
#38147=VERTEX_POINT ( 'NONE', #51083 ) ;
#38154=EDGE_CURVE ( 'NONE', #92103, #91104, #28738, .T. ) ;
#38155=CARTESIAN_POINT ( 'NONE',  ( -1.359786310227693251, -5.876774720514417183, 20.62654306927474579 ) ) ;
#38158=ORIENTED_EDGE ( 'NONE', *, *, #82355, .F. ) ;
#38162=PLANE ( 'NONE',  #59856 ) ;
#38177=CARTESIAN_POINT ( 'NONE',  ( -5.970505764849975527, -6.376774720514411854, 19.55848054040323802 ) ) ;
#38180=VECTOR ( 'NONE', #3437, 999.9999999999998863 ) ;
#38188=VECTOR ( 'NONE', #37502, 1000.000000000000000 ) ;
#38191=EDGE_CURVE ( 'NONE', #33057, #81742, #45871, .T. ) ;
#38198=DIRECTION ( 'NONE',  ( -1.000000000000000000, 0.000000000000000000, 0.000000000000000000 ) ) ;
#38200=CARTESIAN_POINT ( 'NONE',  ( 32.85081302853786411, -5.152774720514582185, -13.10817780685225031 ) ) ;
#38218=CARTESIAN_POINT ( 'NONE',  ( 8.000000000000003553, -6.376774720514426953, 0.000000000000000000 ) ) ;
#38222=EDGE_CURVE ( 'NONE', #31540, #2778, #94891, .T. ) ;
#38228=ORIENTED_EDGE ( 'NONE', *, *, #36586, .T. ) ;
#38235=CARTESIAN_POINT ( 'NONE',  ( 5.326923076923078426, -5.876774720514419847, 20.76772836538461320 ) ) ;
#38244=CARTESIAN_POINT ( 'NONE',  ( 17.51792015816173986, 5.965225279485572685, 29.01255224319336889 ) ) ;
#38264=CARTESIAN_POINT ( 'NONE',  ( 22.81105451610979173, 1.477225279485574028, -18.46691820600746681 ) ) ;
#38283=ORIENTED_EDGE ( 'NONE', *, *, #79295, .F. ) ;
#38284=DIRECTION ( 'NONE',  ( 0.000000000000000000, -1.000000000000000000, 0.000000000000000000 ) ) ;
#38285=CARTESIAN_POINT ( 'NONE',  ( 32.66876533700882845, 6.475225279485573360, -12.58926540598385557 ) ) ;
#38299=LINE ( 'NONE', #83979, #16066 ) ;
#38307=CARTESIAN_POINT ( 'NONE',  ( 4.967620699791259753, -6.376774720514415407, 19.94530485585548973 ) ) ;
#38308=DIRECTION ( 'NONE',  ( -0.000000000000000000, -1.000000000000000000, -0.000000000000000000 ) ) ;
#38310=CYLINDRICAL_SURFACE ( 'NONE', #72887, 7.652410033082760243 ) ;
#38312=ORIENTED_EDGE ( 'NONE', *, *, #41100, .T. ) ;
#38319=CARTESIAN_POINT ( 'NONE',  ( -2.711489738547795625, -5.876774720514409189, 19.27798293355755632 ) ) ;
#38321=CARTESIAN_POINT ( 'NONE',  ( -13.89275734969026388, 5.965225279485572685, 31.02402280011862246 ) ) ;
#38326=CARTESIAN_POINT ( 'NONE',  ( -4.152941208099351300, -6.376774720514415407, 20.35309744218305639 ) ) ;
#38327=LINE ( 'NONE', #84504, #59354 ) ;
#38336=ORIENTED_EDGE ( 'NONE', *, *, #38426, .T. ) ;
#38337=CIRCLE ( 'NONE', #48055, 3.060000000000000053 ) ;
#38368=DIRECTION ( 'NONE',  ( 0.000000000000000000, -1.000000000000000000, 0.000000000000000000 ) ) ;
#38369=LINE ( 'NONE', #45005, #19997 ) ;
#38377=AXIS2_PLACEMENT_3D ( 'NONE', #52476, #85403, #68196 ) ;
#38390=CARTESIAN_POINT ( 'NONE',  ( 4.886128916861816052, -5.876774720514411854, 19.14085035285361514 ) ) ;
#38391=FACE_OUTER_BOUND ( 'NONE', #44701, .T. ) ;
#38404=CARTESIAN_POINT ( 'NONE',  ( 3.050049012211247579, -5.876774720514426065, 21.53019692557248632 ) ) ;
#38414=CARTESIAN_POINT ( 'NONE',  ( 15.06054736595347343, -3.522115819418385030, -27.30839264876215466 ) ) ;
#38426=EDGE_CURVE ( 'NONE', #50071, #9886, #79903, .T. ) ;
#38432=CARTESIAN_POINT ( 'NONE',  ( -5.053929855541893446, -5.876774720514408301, 19.14848118821636547 ) ) ;
#38448=AXIS2_PLACEMENT_3D ( 'NONE', #10766, #19366, #49845 ) ;
#38466=CARTESIAN_POINT ( 'NONE',  ( 8.000000000000003553, -5.876774720514426953, 17.50000000000000000 ) ) ;
#38485=DIRECTION ( 'NONE',  ( 0.000000000000000000, 0.000000000000000000, -1.000000000000000000 ) ) ;
#38506=CARTESIAN_POINT ( 'NONE',  ( 19.75748517575715368, -0.3587747205144265483, 28.87153971905864580 ) ) ;
#38509=CARTESIAN_POINT ( 'NONE',  ( 32.98733314340959311, -0.3587747205144265483, 2.074222136288530027 ) ) ;
#38512=CARTESIAN_POINT ( 'NONE',  ( -24.90875734969025501, 5.965225279485572685, 26.43402280011862615 ) ) ;
#38518=LINE ( 'NONE', #69470, #9113 ) ;
#38520=VECTOR ( 'NONE', #47465, 1000.000000000000000 ) ;
#38529=CARTESIAN_POINT ( 'NONE',  ( 33.60454178612405229, -3.597323055450746487, -11.40641020892026170 ) ) ;
#38531=EDGE_LOOP ( 'NONE', ( #55602, #19613, #80905, #53104, #16217, #84918, #27436, #52674, #41977 ) ) ;
#38539=VERTEX_POINT ( 'NONE', #7040 ) ;
#38560=ORIENTED_EDGE ( 'NONE', *, *, #88090, .T. ) ;
#38581=ORIENTED_EDGE ( 'NONE', *, *, #71100, .F. ) ;
#38586=CARTESIAN_POINT ( 'NONE',  ( 25.03579691670893936, -5.064143700970446638, -9.488111998929152691 ) ) ;
#38595=B_SPLINE_SURFACE_WITH_KNOTS ( 'NONE', 3, 1, ( 
 ( #77543, #95288 ),
 ( #87172, #95783 ),
 ( #33377, #42515 ),
 ( #19151, #25772 ),
 ( #57248, #32892 ),
 ( #18650, #71461 ) ),
 .UNSPECIFIED., .F., .F., .F.,
 ( 4, 1, 1, 4 ),
 ( 2, 2 ),
 ( 0.000000000000000000, 0.1985723521474869191, 0.3687871234093659245, 0.5983641756130111400 ),
 ( 0.000000000000000000, 1.000000000000000000 ),
 .UNSPECIFIED. ) ;
#38613=CARTESIAN_POINT ( 'NONE',  ( 31.63187483939985256, -3.931892516571728446, 27.18445229901795557 ) ) ;
#38619=CARTESIAN_POINT ( 'NONE',  ( 15.97264542221207151, -3.406413700670978262, -27.93485542787877662 ) ) ;
#38628=CARTESIAN_POINT ( 'NONE',  ( 14.76093561896379214, 6.475225279485573360, -26.55548769130089681 ) ) ;
#38643=LINE ( 'NONE', #8206, #72043 ) ;
#38653=ORIENTED_EDGE ( 'NONE', *, *, #98501, .F. ) ;
#38662=CARTESIAN_POINT ( 'NONE',  ( -3.095730855174848362, -5.876774720514413630, 20.04377961306771638 ) ) ;
#38675=VECTOR ( 'NONE', #70243, 1000.000000000000000 ) ;
#38685=ORIENTED_EDGE ( 'NONE', *, *, #37752, .T. ) ;
#38697=ADVANCED_FACE ( 'NONE', ( #26767 ), #52400, .T. ) ;
#38700=ORIENTED_EDGE ( 'NONE', *, *, #5089, .F. ) ;
#38702=CARTESIAN_POINT ( 'NONE',  ( 32.96821357219067750, -5.071478440980570213, -13.00504694253962867 ) ) ;
#38723=CARTESIAN_POINT ( 'NONE',  ( -2.704906987277321040, -0.3587747205144061757, -28.92935364444904778 ) ) ;
#38725=VERTEX_POINT ( 'NONE', #76780 ) ;
#38728=CARTESIAN_POINT ( 'NONE',  ( 22.81105451610979173, 6.475225279485573360, -18.46691820600746681 ) ) ;
#38732=CARTESIAN_POINT ( 'NONE',  ( 20.57455539870830208, -4.132774720514426292, -18.22080502500661581 ) ) ;
#38740=AXIS2_PLACEMENT_3D ( 'NONE', #73082, #95902, #96404 ) ;
#38769=EDGE_CURVE ( 'NONE', #43985, #9229, #30123, .T. ) ;
#38770=LINE ( 'NONE', #60639, #30648 ) ;
#38775=EDGE_CURVE ( 'NONE', #59162, #24461, #69286, .T. ) ;
#38789=EDGE_CURVE ( 'NONE', #94651, #19111, #52386, .T. ) ;
#38790=CARTESIAN_POINT ( 'NONE',  ( -10.24059822343757808, -5.876774720514426953, 17.17691942396160698 ) ) ;
#38807=DIRECTION ( 'NONE',  ( 0.000000000000000000, 0.000000000000000000, -1.000000000000000000 ) ) ;
#38815=CARTESIAN_POINT ( 'NONE',  ( -4.147110899021980934, -6.376774720514418959, 20.45311193189268906 ) ) ;
#38826=CARTESIAN_POINT ( 'NONE',  ( -1.743696941008423984, -5.876774720514413630, 19.59984006504825160 ) ) ;
#38830=CARTESIAN_POINT ( 'NONE',  ( 22.02124265030973760, -4.776774720514394446, 16.20402280011862217 ) ) ;
#38831=CIRCLE ( 'NONE', #93947, 3.060000000000000053 ) ;
#38837=DIRECTION ( 'NONE',  ( 0.000000000000000000, 0.000000000000000000, -1.000000000000000000 ) ) ;
#38841=LINE ( 'NONE', #70302, #13781 ) ;
#38845=DIRECTION ( 'NONE',  ( -0.000000000000000000, 1.000000000000000000, -0.000000000000000000 ) ) ;
#38857=DIRECTION ( 'NONE',  ( 0.000000000000000000, 0.000000000000000000, 1.000000000000000000 ) ) ;
#38866=ORIENTED_EDGE ( 'NONE', *, *, #15538, .T. ) ;
#38868=CARTESIAN_POINT ( 'NONE',  ( 32.16024265030974050, 5.965225279485572685, 14.03360796525321774 ) ) ;
#38869=DIRECTION ( 'NONE',  ( 0.000000000000000000, 0.000000000000000000, 1.000000000000000000 ) ) ;
#38877=PLANE ( 'NONE',  #2059 ) ;
#38879=CIRCLE ( 'NONE', #46926, 2.500000000000002220 ) ;
#38883=DIRECTION ( 'NONE',  ( -0.000000000000000000, 1.000000000000000000, -0.000000000000000000 ) ) ;
#38884=CARTESIAN_POINT ( 'NONE',  ( -2.750773227259631692, -5.876774720514414518, 19.84584863393302001 ) ) ;
#38889=CARTESIAN_POINT ( 'NONE',  ( 4.039061187531148178, -5.876774720514401196, 18.18637930035166761 ) ) ;
#38906=CARTESIAN_POINT ( 'NONE',  ( 2.745953332610513442, -5.876774720514418959, 21.05053573504278575 ) ) ;
#38915=DIRECTION ( 'NONE',  ( 1.000000000000000000, 0.000000000000000000, 0.000000000000000000 ) ) ;
#38917=EDGE_CURVE ( 'NONE', #36701, #63790, #37823, .T. ) ;
#38935=ORIENTED_EDGE ( 'NONE', *, *, #15077, .T. ) ;
#38945=CARTESIAN_POINT ( 'NONE',  ( 19.75748517575715368, 5.965225279485572685, 28.87153971905864580 ) ) ;
#38951=ORIENTED_EDGE ( 'NONE', *, *, #76220, .T. ) ;
#38957=ORIENTED_EDGE ( 'NONE', *, *, #69534, .T. ) ;
#38965=CARTESIAN_POINT ( 'NONE',  ( 4.115763745420833786, -5.876774720514401196, 18.20859014712428348 ) ) ;
#38968=DIRECTION ( 'NONE',  ( 0.000000000000000000, 1.000000000000000000, 0.000000000000000000 ) ) ;
#38973=CARTESIAN_POINT ( 'NONE',  ( 6.431189903846153300, -6.376774720514415407, 20.08974358974358765 ) ) ;
#38993=CARTESIAN_POINT ( 'NONE',  ( 22.81105451610979173, 8.475225279485572472, -18.46691820600746681 ) ) ;
#39014=ORIENTED_EDGE ( 'NONE', *, *, #4975, .T. ) ;
#39016=CARTESIAN_POINT ( 'NONE',  ( -5.941268476065055815, -6.376774720514417183, 20.11414146978959749 ) ) ;
#39029=ADVANCED_FACE ( 'NONE', ( #48367 ), #79297, .T. ) ;
#39037=CARTESIAN_POINT ( 'NONE',  ( -0.6227173540047638012, -5.876774720514413630, 19.48351902941045211 ) ) ;
#39039=ADVANCED_FACE ( 'NONE', ( #31624, #39737 ), #70693, .F. ) ;
#39044=AXIS2_PLACEMENT_3D ( 'NONE', #84422, #61104, #24015 ) ;
#39047=VERTEX_POINT ( 'NONE', #97030 ) ;
#39071=EDGE_LOOP ( 'NONE', ( #82038, #81256, #99714, #55187 ) ) ;
#39086=DIRECTION ( 'NONE',  ( 0.6599726524652352877, 0.000000000000000000, -0.7512896232465891000 ) ) ;
#39088=ORIENTED_EDGE ( 'NONE', *, *, #18191, .F. ) ;
#39092=EDGE_CURVE ( 'NONE', #57212, #19469, #89689, .T. ) ;
#39099=CARTESIAN_POINT ( 'NONE',  ( 2.904244945035652670, -5.876774720514415407, 20.04207437776001299 ) ) ;
#39109=CARTESIAN_POINT ( 'NONE',  ( 29.77147767949870882, -6.376774720514427841, 26.15915692125050995 ) ) ;
#39117=CARTESIAN_POINT ( 'NONE',  ( -12.84880425037203011, 5.965225279485592225, -26.59900746623528534 ) ) ;
#39123=CARTESIAN_POINT ( 'NONE',  ( 3.672440828437461224, -6.376774720514402972, 18.52532110411518573 ) ) ;
#39125=DIRECTION ( 'NONE',  ( 1.257682986112628908E-16, 0.000000000000000000, 1.000000000000000000 ) ) ;
#39148=CARTESIAN_POINT ( 'NONE',  ( 20.13489193910630703, -2.682774720514426559, -22.92085183005112370 ) ) ;
#39155=EDGE_CURVE ( 'NONE', #17609, #54808, #29007, .T. ) ;
#39165=CARTESIAN_POINT ( 'NONE',  ( 5.541369867593821219, -6.376774720514426065, 21.42815349816763160 ) ) ;
#39180=ORIENTED_EDGE ( 'NONE', *, *, #24360, .T. ) ;
#39183=CARTESIAN_POINT ( 'NONE',  ( -6.265203266387573855, -6.376774720514408301, 19.29154511076646017 ) ) ;
#39194=FACE_OUTER_BOUND ( 'NONE', #15232, .T. ) ;
#39195=CARTESIAN_POINT ( 'NONE',  ( 2.936453026386435017, -5.876774720514406525, 18.60215244312560401 ) ) ;
#39212=EDGE_CURVE ( 'NONE', #70182, #75883, #90913, .T. ) ;
#39221=CARTESIAN_POINT ( 'NONE',  ( 30.53060340732036337, -1.682774720514426114, -8.442346167188910400 ) ) ;
#39222=LINE ( 'NONE', #15885, #26490 ) ;
#39223=ORIENTED_EDGE ( 'NONE', *, *, #82364, .T. ) ;
#39233=VECTOR ( 'NONE', #11818, 1000.000000000000114 ) ;
#39235=DIRECTION ( 'NONE',  ( 0.000000000000000000, 0.000000000000000000, -1.000000000000000000 ) ) ;
#39236=DIRECTION ( 'NONE',  ( -1.000000000000000000, 0.000000000000000000, 0.000000000000000000 ) ) ;
#39249=AXIS2_PLACEMENT_3D ( 'NONE', #9960, #40911, #1855 ) ;
#39252=EDGE_CURVE ( 'NONE', #75907, #91581, #8719, .T. ) ;
#39265=CARTESIAN_POINT ( 'NONE',  ( 5.641025641025643189, -6.376774720514420736, 20.78665865384615330 ) ) ;
#39272=DIRECTION ( 'NONE',  ( -0.000000000000000000, 1.000000000000000000, -0.000000000000000000 ) ) ;
#39274=DIRECTION ( 'NONE',  ( 0.000000000000000000, 0.000000000000000000, -1.000000000000000000 ) ) ;
#39277=CARTESIAN_POINT ( 'NONE',  ( -7.635352852713973348, -5.876774720514415407, 20.14409848895066091 ) ) ;
#39283=VERTEX_POINT ( 'NONE', #2083 ) ;
#39287=DIRECTION ( 'NONE',  ( -0.7512896232465891000, -0.000000000000000000, -0.6599726524652351767 ) ) ;
#39298=CARTESIAN_POINT ( 'NONE',  ( 14.61581676223891613, -3.316774720514426900, -27.35847991879931485 ) ) ;
#39306=LINE ( 'NONE', #70262, #57776 ) ;
#39315=CARTESIAN_POINT ( 'NONE',  ( -27.83739072329610664, -0.3587747205143967943, -8.084349702057700426 ) ) ;
#39316=CARTESIAN_POINT ( 'NONE',  ( -4.289200894924355190, -5.876774720514413630, 19.85590024959437017 ) ) ;
#39326=ORIENTED_EDGE ( 'NONE', *, *, #62657, .T. ) ;
#39327=CARTESIAN_POINT ( 'NONE',  ( 26.73860345374794534, 1.477225279485574028, 3.440769881205036427E-15 ) ) ;
#39331=VERTEX_POINT ( 'NONE', #71085 ) ;
#39335=ORIENTED_EDGE ( 'NONE', *, *, #18044, .T. ) ;
#39340=LINE ( 'NONE', #56083, #72196 ) ;
#39342=EDGE_CURVE ( 'NONE', #59659, #35661, #24892, .T. ) ;
#39343=CARTESIAN_POINT ( 'NONE',  ( 11.25623914429021788, -5.356774720514424715, -27.04805245727492036 ) ) ;
#39346=B_SPLINE_CURVE_WITH_KNOTS ( 'NONE', 3,
 ( #51671, #97828, #36433, #21197, #67397, #59790, #28825, #90724, #52163, #99322, #83093, #44552, #75477, #5982, #36931 ),
 .UNSPECIFIED., .F., .F.,
 ( 4, 1, 1, 1, 1, 1, 1, 1, 1, 1, 1, 1, 4 ),
 ( 0.000000000000000000, 0.08433472199262730118, 0.1670523184160740138, 0.2495660772409658001, 0.3327404818018465660, 0.4159148863627275539, 0.4978280095399964522, 0.5803725886080518537, 0.6646001210565030126, 0.7494666931126164888, 0.8325102339401410090, 0.9156392816681726554, 1.000000000000000000 ),
 .UNSPECIFIED. ) ;
#39351=CARTESIAN_POINT ( 'NONE',  ( -8.978253834636468866, -5.876774720514426953, 21.48128695274316158 ) ) ;
#39358=ORIENTED_EDGE ( 'NONE', *, *, #34195, .T. ) ;
#39366=DIRECTION ( 'NONE',  ( 0.7512896232465892110, 0.000000000000000000, 0.6599726524652351767 ) ) ;
#39374=CARTESIAN_POINT ( 'NONE',  ( -4.401146115524053215, -5.876774720514411854, 19.34190049657481936 ) ) ;
#39380=CARTESIAN_POINT ( 'NONE',  ( -5.457842845122470976, -5.876774720514410966, 19.25892998154168367 ) ) ;
#39382=CARTESIAN_POINT ( 'NONE',  ( -2.794644232660540961, -5.876774720514413630, 20.26757654895259009 ) ) ;
#39396=ORIENTED_EDGE ( 'NONE', *, *, #68696, .F. ) ;
#39401=CARTESIAN_POINT ( 'NONE',  ( 10.86264265030973952, 5.965225279485574461, -28.64597719988137570 ) ) ;
#39407=CARTESIAN_POINT ( 'NONE',  ( -20.77875734969026311, 6.143225279485574397, 27.35402280011862430 ) ) ;
#39410=CARTESIAN_POINT ( 'NONE',  ( 3.787259615384621192, -5.876774720514425177, 21.48076923076922640 ) ) ;
#39421=VECTOR ( 'NONE', #41365, 1000.000000000000000 ) ;
#39427=CARTESIAN_POINT ( 'NONE',  ( 3.825970207471427020, -5.876774720514403860, 18.52126221587801780 ) ) ;
#39437=CARTESIAN_POINT ( 'NONE',  ( -5.837039262820512775, -5.876774720514413630, 19.76512419871795245 ) ) ;
#39442=CARTESIAN_POINT ( 'NONE',  ( 30.53060340732036337, -5.297812262124697469, 1.539714685317310483 ) ) ;
#39457=LINE ( 'NONE', #9503, #23742 ) ;
#39458=CARTESIAN_POINT ( 'NONE',  ( 4.127614219445591814, -6.376774720514408301, 18.60403502951120558 ) ) ;
#39463=VECTOR ( 'NONE', #13813, 1000.000000000000000 ) ;
#39467=LINE ( 'NONE', #70419, #63714 ) ;
#39468=EDGE_LOOP ( 'NONE', ( #81509, #50680, #48785, #31444, #43036, #52216, #87268, #24215, #17376, #58424, #64686, #63798, #12797, #4048, #43232 ) ) ;
#39482=CARTESIAN_POINT ( 'NONE',  ( 6.658651924251966392, -6.376774720514415407, 20.11748569626183425 ) ) ;
#39488=CYLINDRICAL_SURFACE ( 'NONE', #83845, 1.325999999999990298 ) ;
#39489=VECTOR ( 'NONE', #7063, 1000.000000000000000 ) ;
#39490=DIRECTION ( 'NONE',  ( -0.000000000000000000, 1.000000000000000000, -0.000000000000000000 ) ) ;
#39499=AXIS2_PLACEMENT_3D ( 'NONE', #15896, #46859, #93515 ) ;
#39510=DIRECTION ( 'NONE',  ( -0.9980236263794188822, 0.000000000000000000, 0.06283980576413537855 ) ) ;
#39518=CARTESIAN_POINT ( 'NONE',  ( 5.627902640648289712, -6.376774720514413630, 20.02890049923285787 ) ) ;
#39523=CARTESIAN_POINT ( 'NONE',  ( -6.275748223059703257, -5.876774720514411854, 19.59984006504824805 ) ) ;
#39524=CIRCLE ( 'NONE', #52489, 251.4258649670780699 ) ;
#39532=AXIS2_PLACEMENT_3D ( 'NONE', #90112, #90606, #20588 ) ;
#39554=LINE ( 'NONE', #32440, #72471 ) ;
#39562=VERTEX_POINT ( 'NONE', #27407 ) ;
#39563=B_SPLINE_CURVE_WITH_KNOTS ( 'NONE', 3,
 ( #28907, #37520, #61372, #75567, #84687, #5069, #6066, #22770 ),
 .UNSPECIFIED., .F., .F.,
 ( 4, 2, 2, 4 ),
 ( 0.000000000000000000, 0.2499999999999974465, 0.4999999999999948930, 1.000000000000000000 ),
 .UNSPECIFIED. ) ;
#39565=CARTESIAN_POINT ( 'NONE',  ( -7.326695514711824231, -5.876774720514418071, 20.26757654895259719 ) ) ;
#39576=AXIS2_PLACEMENT_3D ( 'NONE', #67999, #46660, #92812 ) ;
#39593=CARTESIAN_POINT ( 'NONE',  ( 4.854822496258163866, -5.876774720514422512, 20.96950945262037891 ) ) ;
#39595=ORIENTED_EDGE ( 'NONE', *, *, #26088, .F. ) ;
#39597=ORIENTED_EDGE ( 'NONE', *, *, #95374, .T. ) ;
#39613=CARTESIAN_POINT ( 'NONE',  ( 31.67047468188982862, -5.333900073052421753, 28.72484383265714314 ) ) ;
#39625=VERTEX_POINT ( 'NONE', #66982 ) ;
#39627=DIRECTION ( 'NONE',  ( 1.000000000000000000, 0.000000000000000000, -1.104558621438292892E-14 ) ) ;
#39631=CARTESIAN_POINT ( 'NONE',  ( 14.47945362154707816, -3.630796101029359679, -28.34983287945845731 ) ) ;
#39634=DIRECTION ( 'NONE',  ( 0.000000000000000000, -1.000000000000000000, 0.000000000000000000 ) ) ;
#39636=CARTESIAN_POINT ( 'NONE',  ( 31.64143112576189765, -6.376774720514426953, 14.03360796525321774 ) ) ;
#39652=CIRCLE ( 'NONE', #78540, 27.94799999999999685 ) ;
#39654=CARTESIAN_POINT ( 'NONE',  ( 31.46635748159467383, -4.132774720514425404, -3.372935991075822759 ) ) ;
#39668=DIRECTION ( 'NONE',  ( 0.000000000000000000, 0.000000000000000000, -1.000000000000000000 ) ) ;
#39672=EDGE_LOOP ( 'NONE', ( #38581, #29233, #81776, #73969 ) ) ;
#39677=CIRCLE ( 'NONE', #13744, 2.500000000000000444 ) ;
#39690=CARTESIAN_POINT ( 'NONE',  ( 7.155337544004596317, -6.376774720514417183, 20.64714842558261765 ) ) ;
#39697=CARTESIAN_POINT ( 'NONE',  ( 2.993128331772667572, -5.876774720514403860, 18.53171057923899312 ) ) ;
#39704=ORIENTED_EDGE ( 'NONE', *, *, #88838, .F. ) ;
#39715=CARTESIAN_POINT ( 'NONE',  ( -7.491187506528125262, -6.376774720514410077, 19.53857357749109980 ) ) ;
#39719=CARTESIAN_POINT ( 'NONE',  ( -1.174900045708346497, -6.376774720514411854, 19.48569229636960998 ) ) ;
#39729=ADVANCED_FACE ( 'NONE', ( #9057 ), #62874, .T. ) ;
#39737=FACE_OUTER_BOUND ( 'NONE', #33, .T. ) ;
#39745=CARTESIAN_POINT ( 'NONE',  ( 4.966987340572156739, -6.376774720514417183, 20.16530235339958210 ) ) ;
#39752=VECTOR ( 'NONE', #22053, 1000.000000000000000 ) ;
#39771=FACE_OUTER_BOUND ( 'NONE', #92885, .T. ) ;
#39774=CIRCLE ( 'NONE', #901, 15.00000000000000178 ) ;
#39784=VECTOR ( 'NONE', #34503, 1000.000000000000000 ) ;
#39794=VERTEX_POINT ( 'NONE', #40523 ) ;
#39799=FACE_OUTER_BOUND ( 'NONE', #89549, .T. ) ;
#39802=ADVANCED_FACE ( 'NONE', ( #92291 ), #22763, .F. ) ;
#39812=CARTESIAN_POINT ( 'NONE',  ( 2.834823996951755465, -6.376774720514406525, 18.76222163777333307 ) ) ;
#39817=CARTESIAN_POINT ( 'NONE',  ( -4.165021623707020559, -6.376774720514417183, 20.26087634804756377 ) ) ;
#39831=VECTOR ( 'NONE', #16829, 1000.000000000000000 ) ;
#39843=LINE ( 'NONE', #1295, #85337 ) ;
#39848=ORIENTED_EDGE ( 'NONE', *, *, #77380, .T. ) ;
#39870=ORIENTED_EDGE ( 'NONE', *, *, #49137, .T. ) ;
#39873=CARTESIAN_POINT ( 'NONE',  ( -4.169309590939843879, -6.376774720514411854, 19.59793130852656518 ) ) ;
#39878=CARTESIAN_POINT ( 'NONE',  ( -5.378122165843598701, -5.876774720514410077, 19.21968329462762526 ) ) ;
#39883=CARTESIAN_POINT ( 'NONE',  ( -19.38764004357183168, -0.3587747205143967943, -21.62823517627351322 ) ) ;
#39888=CARTESIAN_POINT ( 'NONE',  ( -2.283364382221138467, -5.876774720514412742, 19.46427715384223944 ) ) ;
#39891=FACE_OUTER_BOUND ( 'NONE', #6759, .T. ) ;
#39892=CARTESIAN_POINT ( 'NONE',  ( 4.531089049250198286, -5.876774720514405637, 18.46391971337801508 ) ) ;
#39899=AXIS2_PLACEMENT_3D ( 'NONE', #71602, #2100, #33033 ) ;
#39904=CARTESIAN_POINT ( 'NONE',  ( 2.611202098145462891, -6.376774720514420736, 20.45574432200782766 ) ) ;
#39915=DIRECTION ( 'NONE',  ( -0.000000000000000000, -1.000000000000000000, -0.000000000000000000 ) ) ;
#39920=EDGE_CURVE ( 'NONE', #63059, #451, #27779, .T. ) ;
#39925=CARTESIAN_POINT ( 'NONE',  ( 3.903461913076534451, -5.876774720514404748, 18.52532880998198905 ) ) ;
#39930=CARTESIAN_POINT ( 'NONE',  ( 10.24059822343757808, -5.876774720514426953, 17.91871304725684766 ) ) ;
#39932=DIRECTION ( 'NONE',  ( -0.9921023176230514551, 0.000000000000000000, 0.1254312216594016816 ) ) ;
#39943=AXIS2_PLACEMENT_3D ( 'NONE', #95616, #1772, #11377 ) ;
#39951=CARTESIAN_POINT ( 'NONE',  ( 29.73860345376319003, -1.682774720514426114, -1.272392034746785860 ) ) ;
#39955=CARTESIAN_POINT ( 'NONE',  ( 4.639502537026700679, -5.876774720514416295, 19.60647575951318800 ) ) ;
#39957=ORIENTED_EDGE ( 'NONE', *, *, #42476, .F. ) ;
#39960=ORIENTED_EDGE ( 'NONE', *, *, #82673, .F. ) ;
#39966=DIRECTION ( 'NONE',  ( 0.000000000000000000, 0.000000000000000000, 1.000000000000000000 ) ) ;
#39999=DIRECTION ( 'NONE',  ( 0.000000000000000000, 1.000000000000000000, 0.000000000000000000 ) ) ;
#40010=CIRCLE ( 'NONE', #25443, 1.700000000000000178 ) ;
#40021=ORIENTED_EDGE ( 'NONE', *, *, #95038, .F. ) ;
#40023=CARTESIAN_POINT ( 'NONE',  ( -6.100820854657341918, -6.376774720514413630, 19.76359802465961124 ) ) ;
#40034=CARTESIAN_POINT ( 'NONE',  ( -19.77875734969026311, 6.143225279485574397, 27.35402280011862430 ) ) ;
#40039=EDGE_CURVE ( 'NONE', #30746, #21858, #91170, .T. ) ;
#40041=CARTESIAN_POINT ( 'NONE',  ( -0.9827876235267493099, -5.876774720514415407, 19.81240905262004404 ) ) ;
#40048=EDGE_CURVE ( 'NONE', #63904, #9871, #14035, .T. ) ;
#40064=DIRECTION ( 'NONE',  ( -0.000000000000000000, 1.000000000000000000, -0.000000000000000000 ) ) ;
#40068=ADVANCED_FACE ( 'NONE', ( #51624, #43515, #35890, #13040, #90178, #54126, #15038 ), #68840, .T. ) ;
#40070=CARTESIAN_POINT ( 'NONE',  ( -7.234140626586239797, -5.876774720514411854, 19.72789237585158162 ) ) ;
#40083=CARTESIAN_POINT ( 'NONE',  ( 0.3910256410256394144, -6.376774720514411854, 19.63681891025641235 ) ) ;
#40085=ORIENTED_EDGE ( 'NONE', *, *, #27114, .T. ) ;
#40097=EDGE_CURVE ( 'NONE', #3112, #34388, #320, .T. ) ;
#40102=ORIENTED_EDGE ( 'NONE', *, *, #57614, .T. ) ;
#40114=CARTESIAN_POINT ( 'NONE',  ( -11.64875734969026233, -0.3587747205144265483, 30.51402280011862089 ) ) ;
#40117=ORIENTED_EDGE ( 'NONE', *, *, #89874, .T. ) ;
#40122=CARTESIAN_POINT ( 'NONE',  ( 31.69157588112856061, -3.316774720514426456, 29.47507169338741662 ) ) ;
#40124=VECTOR ( 'NONE', #98020, 1000.000000000000000 ) ;
#40125=DIRECTION ( 'NONE',  ( 0.000000000000000000, 0.000000000000000000, 1.000000000000000000 ) ) ;
#40149=ORIENTED_EDGE ( 'NONE', *, *, #8302, .F. ) ;
#40151=CARTESIAN_POINT ( 'NONE',  ( 5.771117285127500551, -5.876774720514418071, 20.39900056875960388 ) ) ;
#40153=VERTEX_POINT ( 'NONE', #77924 ) ;
#40155=FACE_OUTER_BOUND ( 'NONE', #24414, .T. ) ;
#40157=LINE ( 'NONE', #71113, #69582 ) ;
#40158=AXIS2_PLACEMENT_3D ( 'NONE', #87293, #79680, #18289 ) ;
#40162=ADVANCED_FACE ( 'NONE', ( #61242 ), #38877, .F. ) ;
#40171=DIRECTION ( 'NONE',  ( 1.000000000000000000, 0.000000000000000000, 5.238131417152343399E-15 ) ) ;
#40191=CARTESIAN_POINT ( 'NONE',  ( 7.166040305186291093, -5.876774720514420736, 20.81030863372915718 ) ) ;
#40194=ORIENTED_EDGE ( 'NONE', *, *, #69613, .F. ) ;
#40197=VERTEX_POINT ( 'NONE', #8932 ) ;
#40199=VERTEX_POINT ( 'NONE', #39883 ) ;
#40207=DIRECTION ( 'NONE',  ( 0.000000000000000000, -1.000000000000000000, 0.000000000000000000 ) ) ;
#40226=ORIENTED_EDGE ( 'NONE', *, *, #55055, .T. ) ;
#40234=CARTESIAN_POINT ( 'NONE',  ( -1.292025413547811308, -6.376774720514411854, 19.72913074730690752 ) ) ;
#40241=VERTEX_POINT ( 'NONE', #64760 ) ;
#40255=CARTESIAN_POINT ( 'NONE',  ( -5.574014511416001127, -5.876774720514413630, 20.24089781925592391 ) ) ;
#40266=VERTEX_POINT ( 'NONE', #3348 ) ;
#40275=CARTESIAN_POINT ( 'NONE',  ( 5.727631217150810805, -5.876774720514421624, 21.11407618546790133 ) ) ;
#40282=EDGE_LOOP ( 'NONE', ( #5312, #48442, #99080, #8548 ) ) ;
#40285=B_SPLINE_CURVE_WITH_KNOTS ( 'NONE', 3,
 ( #19564, #73859, #43909, #27691, #12940, #3863, #19063, #34303, #96204, #49539, #66771, #74840, #72869, #65775, #33798, #26690, #10962, #57649, #41928, #97689, #50038, #88590, #82461 ),
 .UNSPECIFIED., .F., .F.,
 ( 4, 1, 1, 1, 1, 1, 1, 1, 1, 1, 1, 1, 1, 1, 1, 1, 1, 1, 1, 1, 4 ),
 ( 0.000000000000000000, 0.06568119799063895647, 0.1284864641740642022, 0.1881751303280073950, 0.2451061306699852116, 0.2994484245294744551, 0.3508229360093824134, 0.3999416805337764336, 0.4466717436323716650, 0.4912545333734980035, 0.5333763442704358981, 0.5738527549682231887, 0.6125263117194529316, 0.6495971364453292374, 0.6855320415538496137, 0.7201057860682000822, 0.7538376629736500689, 0.8189254160467134280, 0.8804934616501639555, 0.9403113338460573623, 1.000000000000000000 ),
 .UNSPECIFIED. ) ;
#40287=DIRECTION ( 'NONE',  ( -1.252131230780251939E-15, -0.000000000000000000, -1.000000000000000000 ) ) ;
#40289=DIRECTION ( 'NONE',  ( 0.000000000000000000, 0.000000000000000000, -1.000000000000000000 ) ) ;
#40295=EDGE_CURVE ( 'NONE', #69965, #96767, #60586, .T. ) ;
#40301=ADVANCED_FACE ( 'NONE', ( #88069 ), #72848, .F. ) ;
#40309=CYLINDRICAL_SURFACE ( 'NONE', #86934, 251.4258649670780699 ) ;
#40316=CARTESIAN_POINT ( 'NONE',  ( -28.84663072490566194, 5.965225279485572685, 28.73989617533406715 ) ) ;
#40318=DIRECTION ( 'NONE',  ( 0.000000000000000000, 1.000000000000000000, 0.000000000000000000 ) ) ;
#40319=ORIENTED_EDGE ( 'NONE', *, *, #77466, .F. ) ;
#40322=VERTEX_POINT ( 'NONE', #63752 ) ;
#40330=DIRECTION ( 'NONE',  ( 0.000000000000000000, -1.000000000000000000, 0.000000000000000000 ) ) ;
#40342=CARTESIAN_POINT ( 'NONE',  ( -0.005606649364735081555, -6.376774720514410077, 19.25713806424188235 ) ) ;
#40344=ORIENTED_EDGE ( 'NONE', *, *, #94816, .T. ) ;
#40351=CARTESIAN_POINT ( 'NONE',  ( 9.464509667904351886, -3.316774720514128028, -27.03659963365196717 ) ) ;
#40352=CIRCLE ( 'NONE', #3063, 0.8160000000000007248 ) ;
#40359=CARTESIAN_POINT ( 'NONE',  ( 17.51792015816173986, 5.965225279485572685, 29.01255224319336889 ) ) ;
#40363=AXIS2_PLACEMENT_3D ( 'NONE', #54561, #76872, #7879 ) ;
#40364=CARTESIAN_POINT ( 'NONE',  ( -5.912814555383966386, -6.376774720514418959, 20.28973052848695602 ) ) ;
#40377=PLANE ( 'NONE',  #19059 ) ;
#40383=EDGE_CURVE ( 'NONE', #41593, #95277, #35779, .T. ) ;
#40388=EDGE_CURVE ( 'NONE', #87273, #20975, #28659, .T. ) ;
#40392=DIRECTION ( 'NONE',  ( -1.104558621438292892E-14, 0.000000000000000000, -1.000000000000000000 ) ) ;
#40397=DIRECTION ( 'NONE',  ( 0.7071067811865476838, 0.000000000000000000, -0.7071067811865474617 ) ) ;
#40402=CARTESIAN_POINT ( 'NONE',  ( 4.821763668436347849, -5.876774720514406525, 18.93074869776452829 ) ) ;
#40407=LINE ( 'NONE', #1848, #67461 ) ;
#40414=DIRECTION ( 'NONE',  ( 0.000000000000000000, 0.000000000000000000, 1.000000000000000000 ) ) ;
#40416=CARTESIAN_POINT ( 'NONE',  ( 4.547994309883463870, -6.376774720514422512, 20.87593061325451416 ) ) ;
#40425=VECTOR ( 'NONE', #27206, 1000.000000000000000 ) ;
#40435=AXIS2_PLACEMENT_3D ( 'NONE', #9218, #71634, #48808 ) ;
#40439=ORIENTED_EDGE ( 'NONE', *, *, #25531, .T. ) ;
#40446=CARTESIAN_POINT ( 'NONE',  ( -24.90875734969025501, -3.316774720514426456, 27.45402280011862572 ) ) ;
#40447=VERTEX_POINT ( 'NONE', #6317 ) ;
#40449=CARTESIAN_POINT ( 'NONE',  ( -9.940598223437573822, -6.376774720514426953, 18.21871304725684837 ) ) ;
#40453=EDGE_LOOP ( 'NONE', ( #91618, #21712, #32615, #11414 ) ) ;
#40455=ORIENTED_EDGE ( 'NONE', *, *, #69335, .F. ) ;
#40473=ORIENTED_EDGE ( 'NONE', *, *, #72382, .T. ) ;
#40474=DIRECTION ( 'NONE',  ( 0.000000000000000000, 0.000000000000000000, -1.000000000000000000 ) ) ;
#40490=ORIENTED_EDGE ( 'NONE', *, *, #26053, .F. ) ;
#40491=CARTESIAN_POINT ( 'NONE',  ( 33.10875634548599322, 5.965225279485572685, -11.42349945801155719 ) ) ;
#40493=CARTESIAN_POINT ( 'NONE',  ( -28.98875734969026396, -0.3587747205144262708, 7.870022800118625206 ) ) ;
#40496=DIRECTION ( 'NONE',  ( -0.000000000000000000, -1.000000000000000000, -0.000000000000000000 ) ) ;
#40516=AXIS2_PLACEMENT_3D ( 'NONE', #88996, #18972, #19468 ) ;
#40518=CIRCLE ( 'NONE', #1617, 28.45799999999999486 ) ;
#40523=CARTESIAN_POINT ( 'NONE',  ( 29.70220533433691301, -3.316774720514426456, 28.20564067601639735 ) ) ;
#40535=CARTESIAN_POINT ( 'NONE',  ( -6.275748223059703257, -6.376774720514411854, 19.59984006504824805 ) ) ;
#40570=ORIENTED_EDGE ( 'NONE', *, *, #20905, .F. ) ;
#40575=CARTESIAN_POINT ( 'NONE',  ( -6.905879715866854340, -5.876774720514411854, 19.48240003225459560 ) ) ;
#40597=DIRECTION ( 'NONE',  ( 0.7863974287229266169, 0.000000000000000000, -0.6177208787939496570 ) ) ;
#40601=CARTESIAN_POINT ( 'NONE',  ( -65.05438548721848235, -6.376774720514426953, 30.51402280011862089 ) ) ;
#40613=ORIENTED_EDGE ( 'NONE', *, *, #40295, .T. ) ;
#40614=CARTESIAN_POINT ( 'NONE',  ( 32.48849721025742099, -4.168223360657076881, -0.9137309853436130780 ) ) ;
#40617=EDGE_CURVE ( 'NONE', #15460, #42617, #53008, .T. ) ;
#40628=CARTESIAN_POINT ( 'NONE',  ( 31.68813401132623397, -4.191046033661507408, 29.35543347196376729 ) ) ;
#40633=CARTESIAN_POINT ( 'NONE',  ( -19.80875734969026425, 5.965225279485572685, 30.51402280011862089 ) ) ;
#40647=EDGE_CURVE ( 'NONE', #43715, #28435, #91195, .T. ) ;
#40649=ORIENTED_EDGE ( 'NONE', *, *, #60323, .T. ) ;
#40651=DIRECTION ( 'NONE',  ( 0.7512896232465891000, 0.000000000000000000, 0.6599726524652351767 ) ) ;
#40689=CARTESIAN_POINT ( 'NONE',  ( 31.02038118199824268, -5.152774720514427642, -4.893189986691015569 ) ) ;
#40692=AXIS2_PLACEMENT_3D ( 'NONE', #63885, #41526, #30016 ) ;
#40695=FACE_OUTER_BOUND ( 'NONE', #88882, .T. ) ;
#40696=ORIENTED_EDGE ( 'NONE', *, *, #49680, .F. ) ;
#40697=CARTESIAN_POINT ( 'NONE',  ( 7.153659783701941777, -6.376774720514422512, 20.92502190304499265 ) ) ;
#40703=CARTESIAN_POINT ( 'NONE',  ( 6.457852148677970305, -5.876774720514415407, 20.09052163342618158 ) ) ;
#40704=CARTESIAN_POINT ( 'NONE',  ( 5.873458226074941280, -5.876774720514413630, 19.84669099281175164 ) ) ;
#40715=AXIS2_PLACEMENT_3D ( 'NONE', #18302, #24901, #1585 ) ;
#40720=VERTEX_POINT ( 'NONE', #88832 ) ;
#40723=EDGE_LOOP ( 'NONE', ( #16447, #79436, #96440, #12720 ) ) ;
#40728=CARTESIAN_POINT ( 'NONE',  ( 29.80070917940689768, -3.316774720514426456, 27.39560796525317343 ) ) ;
#40735=ORIENTED_EDGE ( 'NONE', *, *, #41684, .F. ) ;
#40745=DIRECTION ( 'NONE',  ( -1.000000000000000000, 0.000000000000000000, 2.000709955812756815E-15 ) ) ;
#40751=CARTESIAN_POINT ( 'NONE',  ( -5.154768636056045850, -5.876774720514411854, 19.48351902941045921 ) ) ;
#40758=CYLINDRICAL_SURFACE ( 'NONE', #77970, 3.500000000000000000 ) ;
#40766=CARTESIAN_POINT ( 'NONE',  ( 3.206569032998081603, -5.876774720514423400, 21.19686455982786200 ) ) ;
#40790=ORIENTED_EDGE ( 'NONE', *, *, #36513, .F. ) ;
#40793=VERTEX_POINT ( 'NONE', #18803 ) ;
#40797=ORIENTED_EDGE ( 'NONE', *, *, #68506, .T. ) ;
#40799=LINE ( 'NONE', #24565, #95625 ) ;
#40803=CARTESIAN_POINT ( 'NONE',  ( 5.399550031317769339, 5.965225279485594001, -28.54570968858208246 ) ) ;
#40807=CARTESIAN_POINT ( 'NONE',  ( 30.00738719773715601, -4.772774720514425972, -9.049252915307082645 ) ) ;
#40813=ORIENTED_EDGE ( 'NONE', *, *, #24780, .T. ) ;
#40814=CARTESIAN_POINT ( 'NONE',  ( 3.475076759263674209, -6.376774720514401196, 18.20843037655054530 ) ) ;
#40816=ORIENTED_EDGE ( 'NONE', *, *, #24330, .F. ) ;
#40824=DIRECTION ( 'NONE',  ( 0.000000000000000000, 0.000000000000000000, 1.000000000000000000 ) ) ;
#40833=AXIS2_PLACEMENT_3D ( 'NONE', #34668, #4216, #57519 ) ;
#40835=DIRECTION ( 'NONE',  ( -0.000000000000000000, 1.000000000000000000, -0.000000000000000000 ) ) ;
#40857=CARTESIAN_POINT ( 'NONE',  ( -5.903826827417286260, -6.376774720514418959, 20.39230070883895252 ) ) ;
#40861=ORIENTED_EDGE ( 'NONE', *, *, #51327, .T. ) ;
#40876=CARTESIAN_POINT ( 'NONE',  ( -16.22218391600152643, 6.475225279485573360, -54.85883559227303863 ) ) ;
#40878=EDGE_CURVE ( 'NONE', #26965, #18629, #76616, .T. ) ;
#40887=CARTESIAN_POINT ( 'NONE',  ( 282.9764569301858046, -0.3587747205144265483, 20.79159422840526616 ) ) ;
#40892=CARTESIAN_POINT ( 'NONE',  ( -2.791950601096355733, -5.876774720514417183, 20.17732409774492552 ) ) ;
#40894=CARTESIAN_POINT ( 'NONE',  ( 3.787259615384621636, -5.876774720514405637, 18.51923076923076650 ) ) ;
#40904=CARTESIAN_POINT ( 'NONE',  ( 15.77315497053730020, -4.795106742339615202, -28.11009842133895731 ) ) ;
#40905=CARTESIAN_POINT ( 'NONE',  ( 0.000000000000000000, -4.132774720514426292, 0.000000000000000000 ) ) ;
#40909=FACE_OUTER_BOUND ( 'NONE', #83145, .T. ) ;
#40911=DIRECTION ( 'NONE',  ( 0.000000000000000000, -1.000000000000000000, 0.000000000000000000 ) ) ;
#40938=DIRECTION ( 'NONE',  ( 0.000000000000000000, -1.000000000000000000, 0.000000000000000000 ) ) ;
#40941=ORIENTED_EDGE ( 'NONE', *, *, #99918, .F. ) ;
#40949=ORIENTED_EDGE ( 'NONE', *, *, #83388, .F. ) ;
#40952=CARTESIAN_POINT ( 'NONE',  ( 27.53860345374808105, -1.682774720514426114, -1.272392034746785860 ) ) ;
#40961=CARTESIAN_POINT ( 'NONE',  ( 4.593956459244529889, -5.876774720514410966, 19.29001220640957115 ) ) ;
#40969=VERTEX_POINT ( 'NONE', #53764 ) ;
#40974=CARTESIAN_POINT ( 'NONE',  ( 5.641025641025643189, -6.376774720514420736, 20.78665865384615330 ) ) ;
#40976=ORIENTED_EDGE ( 'NONE', *, *, #16638, .F. ) ;
#40977=ORIENTED_EDGE ( 'NONE', *, *, #66812, .F. ) ;
#41000=CARTESIAN_POINT ( 'NONE',  ( -7.304748120944324796, -5.876774720514417183, 19.95463486386180563 ) ) ;
#41004=ADVANCED_FACE ( 'NONE', ( #78068 ), #17689, .F. ) ;
#41005=ORIENTED_EDGE ( 'NONE', *, *, #66400, .F. ) ;
#41025=CARTESIAN_POINT ( 'NONE',  ( -20.27875734969026311, 7.743225279485574042, 24.00402280011862288 ) ) ;
#41042=DIRECTION ( 'NONE',  ( -0.000000000000000000, -1.000000000000000000, -0.000000000000000000 ) ) ;
#41046=CARTESIAN_POINT ( 'NONE',  ( 7.370931459274800090, -6.376774720514417183, 20.26286690110499578 ) ) ;
#41064=LINE ( 'NONE', #2506, #75987 ) ;
#41076=ADVANCED_FACE ( 'NONE', ( #81592 ), #50148, .T. ) ;
#41077=CARTESIAN_POINT ( 'NONE',  ( 26.73860345374794534, -5.356774720514427379, -3.111611894936215705 ) ) ;
#41091=CARTESIAN_POINT ( 'NONE',  ( -6.636054160061366503, -5.876774720514411854, 19.15289935703627933 ) ) ;
#41095=ORIENTED_EDGE ( 'NONE', *, *, #53140, .F. ) ;
#41098=FACE_OUTER_BOUND ( 'NONE', #82768, .T. ) ;
#41100=EDGE_CURVE ( 'NONE', #15238, #47938, #79586, .T. ) ;
#41128=TOROIDAL_SURFACE ( 'NONE', #31332, 80.18232118519038920, 8.160000000000000142 ) ;
#41134=VECTOR ( 'NONE', #62290, 1000.000000000000114 ) ;
#41145=ORIENTED_EDGE ( 'NONE', *, *, #96959, .F. ) ;
#41150=CARTESIAN_POINT ( 'NONE',  ( 14.67302116299744519, -4.477500275188337930, -27.99481486150953558 ) ) ;
#41156=CARTESIAN_POINT ( 'NONE',  ( 22.02124265030973760, 6.143225279485574397, 16.20402280011862217 ) ) ;
#41164=FACE_OUTER_BOUND ( 'NONE', #5155, .T. ) ;
#41167=FACE_OUTER_BOUND ( 'NONE', #65565, .T. ) ;
#41170=B_SPLINE_CURVE_WITH_KNOTS ( 'NONE', 3,
 ( #54871, #79192, #85811, #41150, #79692, #8691, #16291, #39631, #48260, #70 ),
 .UNSPECIFIED., .F., .F.,
 ( 4, 2, 2, 2, 4 ),
 ( 0.000000000000000000, 0.0004686948575969757699, 0.0009373897151939515398, 0.001406084572790927256, 0.001874779430387901779 ),
 .UNSPECIFIED. ) ;
#41174=CARTESIAN_POINT ( 'NONE',  ( -24.90875734969025501, 6.475225279485573360, 30.00402280011862288 ) ) ;
#41183=ADVANCED_FACE ( 'NONE', ( #49653 ), #80586, .F. ) ;
#41198=EDGE_CURVE ( 'NONE', #65732, #94122, #84744, .T. ) ;
#41203=CARTESIAN_POINT ( 'NONE',  ( 4.784292611718076849, -5.356774720514425603, -25.54547254883186014 ) ) ;
#41208=ORIENTED_EDGE ( 'NONE', *, *, #26970, .T. ) ;
#41210=CARTESIAN_POINT ( 'NONE',  ( 6.792576760808763936, -5.876774720514415407, 20.16775508794004779 ) ) ;
#41211=CARTESIAN_POINT ( 'NONE',  ( 5.443272695963705665, -6.376774720514417183, 20.27301970143225418 ) ) ;
#41224=ORIENTED_EDGE ( 'NONE', *, *, #84330, .T. ) ;
#41237=CARTESIAN_POINT ( 'NONE',  ( 6.944081373883786767, -5.876774720514423400, 21.27829155525578031 ) ) ;
#41239=LINE ( 'NONE', #87912, #56748 ) ;
#41242=VERTEX_POINT ( 'NONE', #67368 ) ;
#41243=LINE ( 'NONE', #44243, #70816 ) ;
#41259=CARTESIAN_POINT ( 'NONE',  ( -5.568927889719891944, -5.876774720514415407, 20.14881673916291760 ) ) ;
#41261=ORIENTED_EDGE ( 'NONE', *, *, #75336, .F. ) ;
#41272=CARTESIAN_POINT ( 'NONE',  ( 3.448102555317568374, -6.376774720514424288, 21.39871091031772110 ) ) ;
#41277=CARTESIAN_POINT ( 'NONE',  ( 5.654014271574485662, -6.376774720514420736, 20.92503208403226722 ) ) ;
#41288=LINE ( 'NONE', #33677, #13514 ) ;
#41294=LINE ( 'NONE', #89468, #91616 ) ;
#41295=FACE_OUTER_BOUND ( 'NONE', #75893, .T. ) ;
#41319=FACE_OUTER_BOUND ( 'NONE', #20706, .T. ) ;
#41323=ORIENTED_EDGE ( 'NONE', *, *, #70885, .T. ) ;
#41324=ORIENTED_EDGE ( 'NONE', *, *, #86346, .T. ) ;
#41331=ORIENTED_EDGE ( 'NONE', *, *, #15175, .F. ) ;
#41334=CARTESIAN_POINT ( 'NONE',  ( -29.49875734969026198, -0.3587747205144265483, 2.362022800118626531 ) ) ;
#41361=CARTESIAN_POINT ( 'NONE',  ( 6.457852148677970305, -6.376774720514415407, 20.09052163342618158 ) ) ;
#41365=DIRECTION ( 'NONE',  ( 1.000000000000000000, 0.000000000000000000, 0.000000000000000000 ) ) ;
#41367=EDGE_CURVE ( 'NONE', #94938, #2928, #74951, .T. ) ;
#41371=CARTESIAN_POINT ( 'NONE',  ( 31.21829842716237735, -4.540774721315884221, 2.131740660352481775 ) ) ;
#41375=VERTEX_POINT ( 'NONE', #69354 ) ;
#41379=ORIENTED_EDGE ( 'NONE', *, *, #33564, .F. ) ;
#41387=CARTESIAN_POINT ( 'NONE',  ( -20.27875734969026311, -6.376774720514428729, 24.00402280011862288 ) ) ;
#41390=DIRECTION ( 'NONE',  ( 1.250865172912931245E-15, 0.000000000000000000, 1.000000000000000000 ) ) ;
#41401=CARTESIAN_POINT ( 'NONE',  ( 32.42932432802503939, -0.3587747205144265483, -0.2107846672978405389 ) ) ;
#41404=DIRECTION ( 'NONE',  ( -1.000000000000000000, 0.000000000000000000, -0.000000000000000000 ) ) ;
#41407=VECTOR ( 'NONE', #14872, 1000.000000000000000 ) ;
#41411=FACE_OUTER_BOUND ( 'NONE', #66803, .T. ) ;
#41417=FACE_OUTER_BOUND ( 'NONE', #59574, .T. ) ;
#41445=CARTESIAN_POINT ( 'NONE',  ( -0.4453066574538939171, -6.376774720514410077, 19.14913681718892491 ) ) ;
#41463=ORIENTED_EDGE ( 'NONE', *, *, #94500, .T. ) ;
#41470=ORIENTED_EDGE ( 'NONE', *, *, #93180, .F. ) ;
#41475=VERTEX_POINT ( 'NONE', #23155 ) ;
#41485=AXIS2_PLACEMENT_3D ( 'NONE', #97988, #68065, #59450 ) ;
#41494=LINE ( 'NONE', #11532, #84633 ) ;
#41499=CARTESIAN_POINT ( 'NONE',  ( -7.324001883147635894, -6.376774720514413630, 20.17732409774492197 ) ) ;
#41504=CARTESIAN_POINT ( 'NONE',  ( -5.574014511416001127, -6.376774720514415407, 20.24089781925592391 ) ) ;
#41507=CARTESIAN_POINT ( 'NONE',  ( 32.06540688909004189, -1.682774720514426114, -12.44045471929205249 ) ) ;
#41526=DIRECTION ( 'NONE',  ( 0.000000000000000000, -1.000000000000000000, 0.000000000000000000 ) ) ;
#41531=EDGE_CURVE ( 'NONE', #69943, #30492, #31284, .T. ) ;
#41536=DIRECTION ( 'NONE',  ( -0.000000000000000000, 1.000000000000000000, -0.000000000000000000 ) ) ;
#41537=ORIENTED_EDGE ( 'NONE', *, *, #53877, .T. ) ;
#41549=AXIS2_PLACEMENT_3D ( 'NONE', #47192, #2523, #17736 ) ;
#41550=CARTESIAN_POINT ( 'NONE',  ( 5.271800844963591359, -3.316774720514426456, -28.56638892015329034 ) ) ;
#41557=TOROIDAL_SURFACE ( 'NONE', #59370, 132.8284398600581540, 2.040000000000000036 ) ;
#41558=B_SPLINE_CURVE_WITH_KNOTS ( 'NONE', 3,
 ( #36854, #83511, #97251, #35852, #44471, #13499, #67818, #91129 ),
 .UNSPECIFIED., .F., .F.,
 ( 4, 2, 2, 4 ),
 ( 0.004987975423754770384, 0.005587860113707344804, 0.005887802458683627678, 0.006187744803659911419 ),
 .UNSPECIFIED. ) ;
#41562=DIRECTION ( 'NONE',  ( 0.000000000000000000, -1.000000000000000000, 0.000000000000000000 ) ) ;
#41586=LINE ( 'NONE', #55812, #99737 ) ;
#41590=ORIENTED_EDGE ( 'NONE', *, *, #76504, .T. ) ;
#41593=VERTEX_POINT ( 'NONE', #18561 ) ;
#41594=CARTESIAN_POINT ( 'NONE',  ( -5.877732331298974877, -6.376774720514411854, 19.69174559449349005 ) ) ;
#41600=CARTESIAN_POINT ( 'NONE',  ( 7.805843057017202824, -3.316774720514425567, -27.15467198446602026 ) ) ;
#41606=CARTESIAN_POINT ( 'NONE',  ( 15.27779656932134067, -3.574456261761478792, -27.18758201676848785 ) ) ;
#41608=VECTOR ( 'NONE', #23282, 1000.000000000000000 ) ;
#41621=CARTESIAN_POINT ( 'NONE',  ( 0.2196812790064107401, -6.376774720514408301, 19.42522865122897002 ) ) ;
#41626=DIRECTION ( 'NONE',  ( 0.000000000000000000, 0.000000000000000000, -1.000000000000000000 ) ) ;
#41627=VECTOR ( 'NONE', #57224, 1000.000000000000000 ) ;
#41635=VECTOR ( 'NONE', #5464, 1000.000000000000000 ) ;
#41638=DIRECTION ( 'NONE',  ( -0.000000000000000000, 1.000000000000000000, -0.000000000000000000 ) ) ;
#41655=DIRECTION ( 'NONE',  ( 0.000000000000000000, 0.000000000000000000, 1.000000000000000000 ) ) ;
#41657=ADVANCED_FACE ( 'NONE', ( #41411 ), #34863, .T. ) ;
#41659=ADVANCED_FACE ( 'NONE', ( #58145 ), #94684, .F. ) ;
#41667=ORIENTED_EDGE ( 'NONE', *, *, #57122, .T. ) ;
#41668=ADVANCED_FACE ( 'NONE', ( #28677 ), #74351, .F. ) ;
#41669=AXIS2_PLACEMENT_3D ( 'NONE', #79291, #25515, #16898 ) ;
#41671=CARTESIAN_POINT ( 'NONE',  ( 6.199338013146583393, -5.876774720514415407, 20.11757922567734980 ) ) ;
#41683=VECTOR ( 'NONE', #45151, 1000.000000000000000 ) ;
#41684=EDGE_CURVE ( 'NONE', #81663, #50305, #67252, .T. ) ;
#41685=CARTESIAN_POINT ( 'NONE',  ( -0.02075734969026423599, 5.965225279485572685, -0.08597719988137648983 ) ) ;
#41691=VECTOR ( 'NONE', #50173, 1000.000000000000000 ) ;
#41697=VERTEX_POINT ( 'NONE', #43417 ) ;
#41701=ORIENTED_EDGE ( 'NONE', *, *, #17964, .T. ) ;
#41705=CARTESIAN_POINT ( 'NONE',  ( -19.69812919673063689, -0.3587747205143964613, -22.00173861453436430 ) ) ;
#41708=EDGE_CURVE ( 'NONE', #30045, #43147, #83448, .T. ) ;
#41713=ORIENTED_EDGE ( 'NONE', *, *, #43593, .T. ) ;
#41714=CARTESIAN_POINT ( 'NONE',  ( 7.166666666666668739, -6.376774720514414518, 20.78665865384614975 ) ) ;
#41720=CARTESIAN_POINT ( 'NONE',  ( 6.727829057902616761, -6.376774720514417183, 20.13865202822440281 ) ) ;
#41721=CARTESIAN_POINT ( 'NONE',  ( 6.329711958793041049, -5.876774720514411854, 19.73172534246499765 ) ) ;
#41742=CARTESIAN_POINT ( 'NONE',  ( 22.81105451610979173, 8.475225279485572472, -19.61691820600746539 ) ) ;
#41749=CARTESIAN_POINT ( 'NONE',  ( 6.697025426467099862, -6.376774720514424288, 21.43052570396496037 ) ) ;
#41750=VERTEX_POINT ( 'NONE', #55016 ) ;
#41751=CARTESIAN_POINT ( 'NONE',  ( 29.58031977903354459, -3.717801497966991775, 29.19834312781581076 ) ) ;
#41755=LINE ( 'NONE', #26007, #82104 ) ;
#41758=CARTESIAN_POINT ( 'NONE',  ( -7.641025641025638748, -6.376774720514427841, 21.75000000000001066 ) ) ;
#41768=EDGE_CURVE ( 'NONE', #81441, #18133, #83263, .T. ) ;
#41770=CARTESIAN_POINT ( 'NONE',  ( -5.000686017310577824, -5.876774720514410077, 19.46274624311237034 ) ) ;
#41771=VECTOR ( 'NONE', #10796, 1000.000000000000000 ) ;
#41778=EDGE_CURVE ( 'NONE', #19254, #98127, #30163, .T. ) ;
#41780=CARTESIAN_POINT ( 'NONE',  ( 13.31108137134011393, -2.682774720514426559, -27.16778744938429924 ) ) ;
#41783=CARTESIAN_POINT ( 'NONE',  ( -41.32836283488544638, -5.152774720514427642, 39.26872235229541985 ) ) ;
#41785=B_SPLINE_CURVE_WITH_KNOTS ( 'NONE', 3,
 ( #58127, #72346, #89064, #57132 ),
 .UNSPECIFIED., .F., .F.,
 ( 4, 4 ),
 ( 8.673617379884035472E-19, 0.0002632372126714214219 ),
 .UNSPECIFIED. ) ;
#41788=ORIENTED_EDGE ( 'NONE', *, *, #98152, .T. ) ;
#41789=CARTESIAN_POINT ( 'NONE',  ( 3.128267882468583228, -6.376774720514424288, 21.08409277973916218 ) ) ;
#41793=CARTESIAN_POINT ( 'NONE',  ( -20.27875734969026311, 7.743225279485574042, 21.75402280011862644 ) ) ;
#41815=CYLINDRICAL_SURFACE ( 'NONE', #14427, 3.349999999999998757 ) ;
#41817=AXIS2_PLACEMENT_3D ( 'NONE', #59128, #44398, #89070 ) ;
#41819=EDGE_CURVE ( 'NONE', #98879, #55323, #87962, .T. ) ;
#41838=VECTOR ( 'NONE', #82824, 1000.000000000000000 ) ;
#41840=CARTESIAN_POINT ( 'NONE',  ( 13.55016566187448923, 5.965225279485570908, -28.22449608469281657 ) ) ;
#41846=CARTESIAN_POINT ( 'NONE',  ( 6.509931258083027750, -5.876774720514417183, 20.09204137875607188 ) ) ;
#41852=ORIENTED_EDGE ( 'NONE', *, *, #79295, .T. ) ;
#41855=VECTOR ( 'NONE', #63126, 1000.000000000000000 ) ;
#41878=EDGE_LOOP ( 'NONE', ( #43427, #8815, #60054, #81011 ) ) ;
#41879=B_SPLINE_CURVE_WITH_KNOTS ( 'NONE', 3,
 ( #35966, #76510, #37963, #7015 ),
 .UNSPECIFIED., .F., .F.,
 ( 4, 4 ),
 ( 0.000000000000000000, 0.0002633127703855885223 ),
 .UNSPECIFIED. ) ;
#41890=ORIENTED_EDGE ( 'NONE', *, *, #50843, .F. ) ;
#41895=LINE ( 'NONE', #72840, #70839 ) ;
#41900=EDGE_CURVE ( 'NONE', #33323, #95752, #86952, .T. ) ;
#41915=CARTESIAN_POINT ( 'NONE',  ( 13.57581083383197296, -5.876774720514426953, 19.78786796564403616 ) ) ;
#41928=CARTESIAN_POINT ( 'NONE',  ( 3.450324536843889067, -6.376774720514404748, 18.60429515659643229 ) ) ;
#41930=CARTESIAN_POINT ( 'NONE',  ( -24.90875734969025501, 5.965225279485572685, 30.51402280011862089 ) ) ;
#41937=DIRECTION ( 'NONE',  ( 0.000000000000000000, 0.000000000000000000, -1.000000000000000000 ) ) ;
#41939=B_SPLINE_CURVE_WITH_KNOTS ( 'NONE', 3,
 ( #93276, #70458, #93783, #9549, #8048, #71967 ),
 .UNSPECIFIED., .F., .F.,
 ( 4, 2, 4 ),
 ( 0.000000000000000000, 0.5000000000000000000, 1.000000000000000000 ),
 .UNSPECIFIED. ) ;
#41957=CARTESIAN_POINT ( 'NONE',  ( 22.81105451610979173, -1.682774720514426114, -18.46691820600746681 ) ) ;
#41958=ORIENTED_EDGE ( 'NONE', *, *, #63883, .T. ) ;
#41960=VECTOR ( 'NONE', #70505, 1000.000000000000000 ) ;
#41965=EDGE_LOOP ( 'NONE', ( #56109, #98367, #37382 ) ) ;
#41973=VECTOR ( 'NONE', #73038, 1000.000000000000114 ) ;
#41977=ORIENTED_EDGE ( 'NONE', *, *, #30514, .F. ) ;
#41980=VERTEX_POINT ( 'NONE', #79833 ) ;
#41981=AXIS2_PLACEMENT_3D ( 'NONE', #10343, #73251, #55533 ) ;
#41994=AXIS2_PLACEMENT_3D ( 'NONE', #46063, #83601, #100307 ) ;
#42003=ORIENTED_EDGE ( 'NONE', *, *, #13390, .T. ) ;
#42004=ORIENTED_EDGE ( 'NONE', *, *, #34078, .F. ) ;
#42010=CARTESIAN_POINT ( 'NONE',  ( -7.064692883725313344, -5.876774720514411854, 19.55266968305501862 ) ) ;
#42021=ADVANCED_FACE ( 'NONE', ( #90944 ), #4223, .T. ) ;
#42034=CIRCLE ( 'NONE', #38740, 3.979149600822063704 ) ;
#42039=PLANE ( 'NONE',  #62374 ) ;
#42043=CIRCLE ( 'NONE', #1539, 2.040000000000001368 ) ;
#42046=ORIENTED_EDGE ( 'NONE', *, *, #93972, .T. ) ;
#42053=PLANE ( 'NONE',  #85341 ) ;
#42054=AXIS2_PLACEMENT_3D ( 'NONE', #9392, #29111, #60086 ) ;
#42062=ADVANCED_FACE ( 'NONE', ( #43785 ), #89455, .F. ) ;
#42065=CARTESIAN_POINT ( 'NONE',  ( 4.638796026491669444, -6.376774720514424288, 21.40644651702305268 ) ) ;
#42081=VERTEX_POINT ( 'NONE', #97064 ) ;
#42085=ORIENTED_EDGE ( 'NONE', *, *, #19206, .F. ) ;
#42091=ORIENTED_EDGE ( 'NONE', *, *, #23043, .F. ) ;
#42100=CARTESIAN_POINT ( 'NONE',  ( -5.850750514176234596, -5.876774720514411854, 19.74039977944280366 ) ) ;
#42102=ORIENTED_EDGE ( 'NONE', *, *, #68237, .F. ) ;
#42105=CARTESIAN_POINT ( 'NONE',  ( 9.016989526679575206, 6.475225279485574248, -27.05137190084761301 ) ) ;
#42113=EDGE_CURVE ( 'NONE', #78770, #59659, #29042, .T. ) ;
#42125=ORIENTED_EDGE ( 'NONE', *, *, #31146, .F. ) ;
#42133=CARTESIAN_POINT ( 'NONE',  ( 2.832419239133125544, -6.376774720514422512, 21.23415460623727213 ) ) ;
#42163=CARTESIAN_POINT ( 'NONE',  ( -7.641025641025640525, -6.376774720514417183, 20.36458333333334281 ) ) ;
#42170=CARTESIAN_POINT ( 'NONE',  ( 27.86270917940689174, -0.3587747205144265483, 29.49402280011862487 ) ) ;
#42173=EDGE_LOOP ( 'NONE', ( #142, #51094, #87716, #91726 ) ) ;
#42176=AXIS2_PLACEMENT_3D ( 'NONE', #11371, #34711, #65685 ) ;
#42178=CARTESIAN_POINT ( 'NONE',  ( 32.53135143123563466, -0.3587747205144265483, 6.926385399448451885 ) ) ;
#42181=DIRECTION ( 'NONE',  ( -0.9997753877537052247, 0.000000000000000000, 0.02119372647573814633 ) ) ;
#42182=VECTOR ( 'NONE', #5629, 1000.000000000000000 ) ;
#42188=VECTOR ( 'NONE', #82719, 1000.000000000000114 ) ;
#42192=VECTOR ( 'NONE', #86165, 1000.000000000000000 ) ;
#42193=DIRECTION ( 'NONE',  ( -0.9913618264504691080, 0.000000000000000000, 0.1311553622875927805 ) ) ;
#42199=AXIS2_PLACEMENT_3D ( 'NONE', #3558, #65477, #53228 ) ;
#42201=EDGE_CURVE ( 'NONE', #96767, #26965, #38369, .T. ) ;
#42222=CARTESIAN_POINT ( 'NONE',  ( 2.611202098145462891, -5.876774720514419847, 20.45574432200782766 ) ) ;
#42226=LINE ( 'NONE', #19357, #8110 ) ;
#42239=DIRECTION ( 'NONE',  ( -0.000000000000000000, 0.000000000000000000, -1.000000000000000000 ) ) ;
#42244=ADVANCED_FACE ( 'NONE', ( #20643 ), #5427, .T. ) ;
#42247=VERTEX_POINT ( 'NONE', #29259 ) ;
#42248=AXIS2_PLACEMENT_3D ( 'NONE', #73426, #34858, #49099 ) ;
#42257=PLANE ( 'NONE',  #82196 ) ;
#42259=CARTESIAN_POINT ( 'NONE',  ( 7.111284305517425075, -5.876774720514421624, 21.05363841023157434 ) ) ;
#42262=DIRECTION ( 'NONE',  ( 0.000000000000000000, 0.000000000000000000, -1.000000000000000000 ) ) ;
#42269=CARTESIAN_POINT ( 'NONE',  ( 30.53060340732036693, -4.905826575867056505, 14.32820694822485841 ) ) ;
#42274=DIRECTION ( 'NONE',  ( -0.000000000000000000, 1.000000000000000000, -0.000000000000000000 ) ) ;
#42290=EDGE_CURVE ( 'NONE', #87149, #56850, #100243, .T. ) ;
#42296=CARTESIAN_POINT ( 'NONE',  ( 30.58729439590577570, -4.540774720514427543, 26.14186284044645703 ) ) ;
#42300=CARTESIAN_POINT ( 'NONE',  ( 9.543201319291914093E-14, -5.876774720514426953, 18.21871304725679508 ) ) ;
#42302=DIRECTION ( 'NONE',  ( -0.6392559695863496705, 6.845827386180411947E-16, -0.7689940216596069522 ) ) ;
#42304=DIRECTION ( 'NONE',  ( -1.000000000000000000, -0.000000000000000000, -7.994117400814786717E-16 ) ) ;
#42319=CARTESIAN_POINT ( 'NONE',  ( 30.09341516180546350, -1.682774720514426114, -13.09311774897855862 ) ) ;
#42321=ORIENTED_EDGE ( 'NONE', *, *, #42290, .T. ) ;
#42323=CARTESIAN_POINT ( 'NONE',  ( 7.072045900997899537, -5.876774720514427841, 21.62824307385093192 ) ) ;
#42324=CARTESIAN_POINT ( 'NONE',  ( 7.462166178408539352, 6.475225279485573360, -27.67315496249664974 ) ) ;
#42332=DIRECTION ( 'NONE',  ( 1.700709290173338723E-14, 0.000000000000000000, 1.000000000000000000 ) ) ;
#42336=ADVANCED_FACE ( 'NONE', ( #8422 ), #45137, .T. ) ;
#42349=EDGE_CURVE ( 'NONE', #75496, #28958, #49211, .T. ) ;
#42351=FACE_OUTER_BOUND ( 'NONE', #33302, .T. ) ;
#42361=CARTESIAN_POINT ( 'NONE',  ( 33.62089986283198328, -3.615790004618635312, -11.40738377976237494 ) ) ;
#42364=ORIENTED_EDGE ( 'NONE', *, *, #80875, .F. ) ;
#42372=CARTESIAN_POINT ( 'NONE',  ( 31.31283134548411340, -1.682774720514426114, -10.20862453625735533 ) ) ;
#42376=CARTESIAN_POINT ( 'NONE',  ( 7.234974673537251100, -6.376774720514415407, 19.99114326857715795 ) ) ;
#42383=EDGE_CURVE ( 'NONE', #64208, #47314, #33766, .T. ) ;
#42390=CARTESIAN_POINT ( 'NONE',  ( 31.10634905326439181, -4.583458114012134210, -2.800232393899708683 ) ) ;
#42401=CARTESIAN_POINT ( 'NONE',  ( 2.610950917001260141, -6.376774720514411854, 19.54489930512155027 ) ) ;
#42402=DIRECTION ( 'NONE',  ( -0.000000000000000000, 1.000000000000000000, -0.000000000000000000 ) ) ;
#42420=CARTESIAN_POINT ( 'NONE',  ( 15.14080536460164694, -3.622774720514426949, -26.62908960815038384 ) ) ;
#42426=CARTESIAN_POINT ( 'NONE',  ( -20.27875734969026311, 7.743225279485574042, 24.00402280011862288 ) ) ;
#42431=CARTESIAN_POINT ( 'NONE',  ( 6.727764423076923350, -5.876774720514413630, 19.76442307692307665 ) ) ;
#42436=CIRCLE ( 'NONE', #3530, 251.4258649670780699 ) ;
#42452=DIRECTION ( 'NONE',  ( -1.743630241030147277E-15, -0.000000000000000000, -1.000000000000000000 ) ) ;
#42457=ADVANCED_FACE ( 'NONE', ( #96167 ), #50491, .T. ) ;
#42459=FACE_OUTER_BOUND ( 'NONE', #39468, .T. ) ;
#42476=EDGE_CURVE ( 'NONE', #70312, #88108, #68211, .T. ) ;
#42477=AXIS2_PLACEMENT_3D ( 'NONE', #63777, #72373, #93688 ) ;
#42506=AXIS2_PLACEMENT_3D ( 'NONE', #10035, #2942, #96772 ) ;
#42507=CARTESIAN_POINT ( 'NONE',  ( -7.347880794884120722E-16, -4.056774720514426669, -6.000000000000000888 ) ) ;
#42514=EDGE_LOOP ( 'NONE', ( #46654, #11482, #98917, #59398 ) ) ;
#42515=CARTESIAN_POINT ( 'NONE',  ( 11.54156857142115911, 5.965225279485592225, -28.05134709678029381 ) ) ;
#42523=CARTESIAN_POINT ( 'NONE',  ( -1.064504969004270052, -5.876774720514408301, 19.35667676486395905 ) ) ;
#42527=ADVANCED_FACE ( 'NONE', ( #82918 ), #92941, .T. ) ;
#42546=CARTESIAN_POINT ( 'NONE',  ( 31.82032313667048484, -0.3587747205144265483, 9.148483289431938559 ) ) ;
#42573=CARTESIAN_POINT ( 'NONE',  ( -24.97666371003640506, -0.3587747205143964613, -15.72894043976419454 ) ) ;
#42575=VERTEX_POINT ( 'NONE', #87302 ) ;
#42578=VERTEX_POINT ( 'NONE', #24402 ) ;
#42591=EDGE_LOOP ( 'NONE', ( #26584, #46559, #43814, #9288 ) ) ;
#42599=EDGE_LOOP ( 'NONE', ( #26954, #64225, #67569, #67471 ) ) ;
#42604=CARTESIAN_POINT ( 'NONE',  ( 11.41483471809167405, -3.316774720514427344, -27.05170832580397189 ) ) ;
#42606=EDGE_CURVE ( 'NONE', #35113, #76129, #16789, .T. ) ;
#42612=CARTESIAN_POINT ( 'NONE',  ( 5.872047395031165351, -5.876774720514415407, 20.29192741308114734 ) ) ;
#42614=FACE_OUTER_BOUND ( 'NONE', #35238, .T. ) ;
#42617=VERTEX_POINT ( 'NONE', #70582 ) ;
#42622=AXIS2_PLACEMENT_3D ( 'NONE', #72989, #3478, #34416 ) ;
#42623=CARTESIAN_POINT ( 'NONE',  ( 282.9764569301858046, -0.3587747205144265483, 20.79159422840526616 ) ) ;
#42626=CARTESIAN_POINT ( 'NONE',  ( 3.714529970114099022, -6.376774720514426065, 21.83853177191107520 ) ) ;
#42659=CARTESIAN_POINT ( 'NONE',  ( -13.57581083383196940, -6.376774720514426953, 20.21213203435597094 ) ) ;
#42662=CARTESIAN_POINT ( 'NONE',  ( -29.49875734969026198, 5.965225279485572685, 7.870022800118625206 ) ) ;
#42672=DIRECTION ( 'NONE',  ( 0.000000000000000000, 0.000000000000000000, -1.000000000000000000 ) ) ;
#42677=CARTESIAN_POINT ( 'NONE',  ( 11.03981094302168842, -0.3587747205144256601, -28.06140118199223465 ) ) ;
#42688=CYLINDRICAL_SURFACE ( 'NONE', #56259, 0.3000000000000016542 ) ;
#42700=ORIENTED_EDGE ( 'NONE', *, *, #57122, .F. ) ;
#42701=LINE ( 'NONE', #44185, #18517 ) ;
#42712=LINE ( 'NONE', #49324, #59298 ) ;
#42714=EDGE_LOOP ( 'NONE', ( #22692, #16214, #90855, #47347 ) ) ;
#42720=CARTESIAN_POINT ( 'NONE',  ( 14.66599494348457888, -4.455096676454772364, -28.01208847159967164 ) ) ;
#42725=AXIS2_PLACEMENT_3D ( 'NONE', #74671, #12766, #42262 ) ;
#42729=DIRECTION ( 'NONE',  ( 0.000000000000000000, 0.000000000000000000, 1.000000000000000000 ) ) ;
#42730=CARTESIAN_POINT ( 'NONE',  ( -9.150000000000000355, -6.376774720514426953, -15.69999999999999929 ) ) ;
#42731=VERTEX_POINT ( 'NONE', #5562 ) ;
#42734=CIRCLE ( 'NONE', #94563, 1.149999999999998135 ) ;
#42745=CARTESIAN_POINT ( 'NONE',  ( 7.448826589983275959, -6.376774720514420736, 21.05250386848070221 ) ) ;
#42749=VERTEX_POINT ( 'NONE', #26909 ) ;
#42754=ORIENTED_EDGE ( 'NONE', *, *, #18704, .T. ) ;
#42762=AXIS2_PLACEMENT_3D ( 'NONE', #24290, #78054, #10064 ) ;
#42771=VERTEX_POINT ( 'NONE', #66502 ) ;
#42772=CARTESIAN_POINT ( 'NONE',  ( 4.332134589405623792, -6.376774720514427841, 21.69242924468134959 ) ) ;
#42792=VECTOR ( 'NONE', #57544, 1000.000000000000000 ) ;
#42796=EDGE_CURVE ( 'NONE', #97929, #7781, #21273, .T. ) ;
#42797=CARTESIAN_POINT ( 'NONE',  ( 16.89397143409390623, -5.876774720514426953, 16.89397143409405899 ) ) ;
#42798=EDGE_CURVE ( 'NONE', #18086, #22543, #52249, .T. ) ;
#42802=CARTESIAN_POINT ( 'NONE',  ( 9.313311959400177642, -6.376774720514677419, -28.06297399545715976 ) ) ;
#42807=DIRECTION ( 'NONE',  ( -0.9978940991575084851, 0.000000000000000000, -0.06486421869277853025 ) ) ;
#42814=DIRECTION ( 'NONE',  ( 0.000000000000000000, 0.000000000000000000, -1.000000000000000000 ) ) ;
#42816=VERTEX_POINT ( 'NONE', #61367 ) ;
#42818=CARTESIAN_POINT ( 'NONE',  ( -2.243088942307695177, -5.876774720514407413, 19.14743589743590491 ) ) ;
#42821=DIRECTION ( 'NONE',  ( -0.000000000000000000, -1.000000000000000000, -0.000000000000000000 ) ) ;
#42834=CARTESIAN_POINT ( 'NONE',  ( 15.58962545129234556, -1.684774720514426560, -26.91365498785467736 ) ) ;
#42842=CARTESIAN_POINT ( 'NONE',  ( 6.658651924251966392, -5.876774720514415407, 20.11748569626183425 ) ) ;
#42850=CARTESIAN_POINT ( 'NONE',  ( -6.914873625533462409, 5.965225279485572685, 29.95171384920748281 ) ) ;
#42855=CARTESIAN_POINT ( 'NONE',  ( 15.10352928271630724, -3.582999323269832725, -27.29968155418892195 ) ) ;
#42857=ORIENTED_EDGE ( 'NONE', *, *, #56433, .F. ) ;
#42861=DIRECTION ( 'NONE',  ( -0.000000000000000000, -0.000000000000000000, -1.000000000000000000 ) ) ;
#42871=CARTESIAN_POINT ( 'NONE',  ( 29.68479148105952703, 1.477225279485574028, -9.431263391055123790 ) ) ;
#42874=AXIS2_PLACEMENT_3D ( 'NONE', #87123, #25725, #56702 ) ;
#42879=CARTESIAN_POINT ( 'NONE',  ( 13.10664265030973930, -0.3587747205144256601, -27.62597719988137612 ) ) ;
#42889=LINE ( 'NONE', #75807, #36869 ) ;
#42902=EDGE_CURVE ( 'NONE', #39331, #77715, #63851, .T. ) ;
#42904=DIRECTION ( 'NONE',  ( 0.000000000000000000, 0.000000000000000000, 1.000000000000000000 ) ) ;
#42922=CARTESIAN_POINT ( 'NONE',  ( -4.926336369345164279, 5.965225279485592225, -28.61095484066304451 ) ) ;
#42938=ADVANCED_FACE ( 'NONE', ( #31401 ), #56262, .T. ) ;
#42950=DIRECTION ( 'NONE',  ( 0.000000000000000000, 0.000000000000000000, 1.000000000000000000 ) ) ;
#42952=ORIENTED_EDGE ( 'NONE', *, *, #16891, .F. ) ;
#42954=DIRECTION ( 'NONE',  ( 0.000000000000000000, 0.000000000000000000, -1.000000000000000000 ) ) ;
#42965=CARTESIAN_POINT ( 'NONE',  ( -0.9827876235267493099, -5.876774720514415407, 19.81240905262004404 ) ) ;
#42971=DIRECTION ( 'NONE',  ( 0.000000000000000000, -1.000000000000000000, 0.000000000000000000 ) ) ;
#42976=ADVANCED_FACE ( 'NONE', ( #62878 ), #93286, .T. ) ;
#42980=CARTESIAN_POINT ( 'NONE',  ( 5.097264368846952998, 6.475225279485573360, -27.56135813788808164 ) ) ;
#42986=CARTESIAN_POINT ( 'NONE',  ( -4.495793269230770939, -5.876774720514410077, 19.27714342948718595 ) ) ;
#43001=CARTESIAN_POINT ( 'NONE',  ( 5.402409956206937203, -5.876774720514424288, 21.18719775722114917 ) ) ;
#43015=CARTESIAN_POINT ( 'NONE',  ( -0.6735982426299428338, -5.876774720514410077, 19.16400979764068069 ) ) ;
#43023=EDGE_CURVE ( 'NONE', #65522, #82260, #54754, .T. ) ;
#43030=EDGE_CURVE ( 'NONE', #50095, #881, #88099, .T. ) ;
#43036=ORIENTED_EDGE ( 'NONE', *, *, #2351, .T. ) ;
#43046=DIRECTION ( 'NONE',  ( 0.8369330630277727057, 0.000000000000000000, -0.5473052603538087757 ) ) ;
#43050=EDGE_LOOP ( 'NONE', ( #49179, #42321, #28749, #2951 ) ) ;
#43051=CARTESIAN_POINT ( 'NONE',  ( 5.730633878096764278, -6.376774720514418959, 20.45679216967608838 ) ) ;
#43054=CARTESIAN_POINT ( 'NONE',  ( 3.879810481058463711, -6.376774720514427841, 21.83835767234735670 ) ) ;
#43061=CIRCLE ( 'NONE', #26828, 0.2999999999999981570 ) ;
#43063=CARTESIAN_POINT ( 'NONE',  ( 25.05730599792488178, -500000.0000000000582, -18.59674224247031304 ) ) ;
#43090=EDGE_CURVE ( 'NONE', #35820, #36659, #44349, .T. ) ;
#43096=CARTESIAN_POINT ( 'NONE',  ( 10.22568704553358643, -3.316774720514425567, -27.02513721610328901 ) ) ;
#43105=FACE_OUTER_BOUND ( 'NONE', #79995, .T. ) ;
#43116=DIRECTION ( 'NONE',  ( 0.000000000000000000, 0.000000000000000000, -1.000000000000000000 ) ) ;
#43118=DIRECTION ( 'NONE',  ( -0.000000000000000000, 1.000000000000000000, -0.000000000000000000 ) ) ;
#43121=ORIENTED_EDGE ( 'NONE', *, *, #47630, .T. ) ;
#43123=CARTESIAN_POINT ( 'NONE',  ( -3.071531057816138333, -6.376774720514413630, 19.86545874326175110 ) ) ;
#43132=LINE ( 'NONE', #20270, #26018 ) ;
#43135=VECTOR ( 'NONE', #240, 1000.000000000000000 ) ;
#43138=ORIENTED_EDGE ( 'NONE', *, *, #94359, .T. ) ;
#43147=VERTEX_POINT ( 'NONE', #43520 ) ;
#43148=CIRCLE ( 'NONE', #82039, 84.48086791635432746 ) ;
#43158=CARTESIAN_POINT ( 'NONE',  ( -10.35374248095108030, -5.304213687372781649, 27.98611676734227771 ) ) ;
#43166=CARTESIAN_POINT ( 'NONE',  ( 6.377880655330028681, -6.376774720514424288, 21.48000012937543346 ) ) ;
#43171=DIRECTION ( 'NONE',  ( -0.000000000000000000, -1.000000000000000000, -0.000000000000000000 ) ) ;
#43175=CARTESIAN_POINT ( 'NONE',  ( 32.59332756141819232, -1.682774720514426114, -11.41404606144471146 ) ) ;
#43178=PLANE ( 'NONE',  #69624 ) ;
#43189=EDGE_CURVE ( 'NONE', #48082, #37098, #26528, .T. ) ;
#43214=CARTESIAN_POINT ( 'NONE',  ( 15.12110981444473623, -4.119741627009104512, -28.36351442485851138 ) ) ;
#43222=VECTOR ( 'NONE', #98181, 1000.000000000000114 ) ;
#43232=ORIENTED_EDGE ( 'NONE', *, *, #48669, .F. ) ;
#43243=CARTESIAN_POINT ( 'NONE',  ( 6.887358010905132666, -6.376774720514426065, 21.32574817943157086 ) ) ;
#43250=CARTESIAN_POINT ( 'NONE',  ( 30.53060340732036337, -4.751397487713028944, 17.08790783164733895 ) ) ;
#43265=CARTESIAN_POINT ( 'NONE',  ( 4.189750619059152470, -6.376774720514427841, 21.76591699724029283 ) ) ;
#43272=EDGE_CURVE ( 'NONE', #51886, #63566, #33901, .T. ) ;
#43282=CARTESIAN_POINT ( 'NONE',  ( 32.76111974776238611, -3.316774720514426900, -3.850861272813261849 ) ) ;
#43284=VECTOR ( 'NONE', #33235, 1000.000000000000000 ) ;
#43285=AXIS2_PLACEMENT_3D ( 'NONE', #59582, #50971, #90513 ) ;
#43292=ORIENTED_EDGE ( 'NONE', *, *, #48972, .F. ) ;
#43294=CARTESIAN_POINT ( 'NONE',  ( 4.628547153713393314, -6.376774720514418959, 20.50654586986123817 ) ) ;
#43295=CARTESIAN_POINT ( 'NONE',  ( 8.817327481845893544, -6.376774720514593930, -28.08864864928871086 ) ) ;
#43303=ORIENTED_EDGE ( 'NONE', *, *, #60832, .F. ) ;
#43306=DIRECTION ( 'NONE',  ( 0.1489078231574191002, 0.000000000000000000, -0.9888510809027407644 ) ) ;
#43316=CARTESIAN_POINT ( 'NONE',  ( 30.54440242517687665, -0.2147811518489095850, 23.45430928465147247 ) ) ;
#43319=EDGE_CURVE ( 'NONE', #46585, #13448, #96301, .T. ) ;
#43323=DIRECTION ( 'NONE',  ( 0.000000000000000000, -1.000000000000000000, 0.000000000000000000 ) ) ;
#43335=DIRECTION ( 'NONE',  ( 0.000000000000000000, 0.000000000000000000, -1.000000000000000000 ) ) ;
#43340=CARTESIAN_POINT ( 'NONE',  ( 32.33408272158504815, -4.458032690740698634, 0.9207958043952065852 ) ) ;
#43348=CARTESIAN_POINT ( 'NONE',  ( 15.22325621495362391, -3.582999323269832725, -27.23549315679322547 ) ) ;
#43378=DIRECTION ( 'NONE',  ( -0.000000000000000000, 0.000000000000000000, -1.000000000000000000 ) ) ;
#43383=DIRECTION ( 'NONE',  ( -0.000000000000000000, 0.000000000000000000, -1.000000000000000000 ) ) ;
#43384=ADVANCED_FACE ( 'NONE', ( #37893 ), #68348, .T. ) ;
#43386=CARTESIAN_POINT ( 'NONE',  ( 2.968164339864655332, -5.876774720514408301, 19.33154224050496595 ) ) ;
#43387=CARTESIAN_POINT ( 'NONE',  ( 2.589743589743596086, -5.876774720514416295, 20.00140224358974095 ) ) ;
#43389=CARTESIAN_POINT ( 'NONE',  ( 26.73860345374794534, -5.356774720514427379, -3.111611894936215705 ) ) ;
#43401=ADVANCED_FACE ( 'NONE', ( #84060 ), #67857, .F. ) ;
#43403=DIRECTION ( 'NONE',  ( 0.000000000000000000, 0.000000000000000000, 1.000000000000000000 ) ) ;
#43414=DIRECTION ( 'NONE',  ( 0.000000000000000000, 0.000000000000000000, 1.000000000000000000 ) ) ;
#43416=CIRCLE ( 'NONE', #75835, 3.060000000000000053 ) ;
#43417=CARTESIAN_POINT ( 'NONE',  ( 30.53060340732035982, 1.477225279485574028, -1.272392034746785860 ) ) ;
#43420=LINE ( 'NONE', #74352, #98565 ) ;
#43427=ORIENTED_EDGE ( 'NONE', *, *, #67457, .T. ) ;
#43430=VECTOR ( 'NONE', #39510, 1000.000000000000114 ) ;
#43436=EDGE_CURVE ( 'NONE', #29097, #10925, #68845, .T. ) ;
#43441=AXIS2_PLACEMENT_3D ( 'NONE', #29161, #53016, #4835 ) ;
#43452=DIRECTION ( 'NONE',  ( -0.000000000000000000, -1.000000000000000000, -0.000000000000000000 ) ) ;
#43459=LINE ( 'NONE', #60683, #8197 ) ;
#43461=ORIENTED_EDGE ( 'NONE', *, *, #9373, .F. ) ;
#43466=ORIENTED_EDGE ( 'NONE', *, *, #19174, .T. ) ;
#43488=EDGE_CURVE ( 'NONE', #83993, #87855, #16635, .T. ) ;
#43491=EDGE_CURVE ( 'NONE', #56620, #94842, #84142, .T. ) ;
#43496=LINE ( 'NONE', #90648, #70984 ) ;
#43505=LINE ( 'NONE', #29258, #7615 ) ;
#43513=CARTESIAN_POINT ( 'NONE',  ( -1.292025413547811308, -6.376774720514413630, 19.72913074730690752 ) ) ;
#43515=FACE_OUTER_BOUND ( 'NONE', #54417, .T. ) ;
#43520=CARTESIAN_POINT ( 'NONE',  ( -29.49875734969025842, -0.3587747205144262708, 15.62202280011862321 ) ) ;
#43527=CARTESIAN_POINT ( 'NONE',  ( 10.54812756816019892, -3.634129942730893070, -27.00766266717979747 ) ) ;
#43558=LINE ( 'NONE', #12091, #38113 ) ;
#43561=CARTESIAN_POINT ( 'NONE',  ( 30.61643171304413613, 6.475225279485573360, 27.37433008668288181 ) ) ;
#43580=ORIENTED_EDGE ( 'NONE', *, *, #92413, .T. ) ;
#43589=VERTEX_POINT ( 'NONE', #80957 ) ;
#43593=EDGE_CURVE ( 'NONE', #30864, #96155, #26351, .T. ) ;
#43603=EDGE_LOOP ( 'NONE', ( #72433, #69247, #22701, #3276 ) ) ;
#43604=ORIENTED_EDGE ( 'NONE', *, *, #11312, .T. ) ;
#43619=CYLINDRICAL_SURFACE ( 'NONE', #72735, 0.3000000000000016542 ) ;
#43623=VECTOR ( 'NONE', #87512, 1000.000000000000000 ) ;
#43629=LINE ( 'NONE', #97407, #56036 ) ;
#43645=CARTESIAN_POINT ( 'NONE',  ( -29.49875734969026198, 5.965225279485572685, 7.870022800118625206 ) ) ;
#43660=CARTESIAN_POINT ( 'NONE',  ( -28.98875734969026396, 5.965225279485572685, -0.08597719988137648983 ) ) ;
#43664=CARTESIAN_POINT ( 'NONE',  ( -1.304987980769231948, -6.376774720514413630, 19.76512419871795245 ) ) ;
#43677=ORIENTED_EDGE ( 'NONE', *, *, #67328, .T. ) ;
#43680=ORIENTED_EDGE ( 'NONE', *, *, #6591, .F. ) ;
#43685=CARTESIAN_POINT ( 'NONE',  ( 33.74607884027702909, 5.965225279485572685, -4.999864028243830916 ) ) ;
#43695=CARTESIAN_POINT ( 'NONE',  ( 13.74975846015576586, 5.965225279485572685, -27.72022515045486557 ) ) ;
#43703=CARTESIAN_POINT ( 'NONE',  ( 14.83405752585475135, -4.881907540128472611, -27.54622755360324859 ) ) ;
#43715=VERTEX_POINT ( 'NONE', #60631 ) ;
#43718=EDGE_CURVE ( 'NONE', #2778, #26032, #100134, .T. ) ;
#43727=CARTESIAN_POINT ( 'NONE',  ( -5.891837592278976743, -5.876774720514418959, 20.62654306927474934 ) ) ;
#43747=AXIS2_PLACEMENT_3D ( 'NONE', #92940, #47791, #78215 ) ;
#43759=VECTOR ( 'NONE', #79785, 1000.000000000000000 ) ;
#43768=CARTESIAN_POINT ( 'NONE',  ( 30.61238849909758031, -3.934983946744459171, 27.21775687185679615 ) ) ;
#43777=DIRECTION ( 'NONE',  ( 0.000000000000000000, 0.000000000000000000, -1.000000000000000000 ) ) ;
#43781=EDGE_CURVE ( 'NONE', #93033, #68551, #68518, .T. ) ;
#43785=FACE_OUTER_BOUND ( 'NONE', #22329, .T. ) ;
#43786=DIRECTION ( 'NONE',  ( 0.000000000000000000, 0.000000000000000000, 1.000000000000000000 ) ) ;
#43800=CARTESIAN_POINT ( 'NONE',  ( 25.61870917940689196, 5.965225279485572685, 29.49402280011862487 ) ) ;
#43804=CARTESIAN_POINT ( 'NONE',  ( 22.02124265030973760, 6.143225279485574397, 19.55402280011862004 ) ) ;
#43814=ORIENTED_EDGE ( 'NONE', *, *, #35751, .T. ) ;
#43828=CARTESIAN_POINT ( 'NONE',  ( -4.401146115524053215, -6.376774720514411854, 19.34190049657481936 ) ) ;
#43832=EDGE_LOOP ( 'NONE', ( #65399, #3703, #73312, #72320 ) ) ;
#43835=CARTESIAN_POINT ( 'NONE',  ( 3.557932825399831689, -5.876774720514428729, 21.44518044978141091 ) ) ;
#43844=EDGE_LOOP ( 'NONE', ( #5728, #92950, #266, #92140 ) ) ;
#43845=AXIS2_PLACEMENT_3D ( 'NONE', #48757, #56875, #10178 ) ;
#43865=DIRECTION ( 'NONE',  ( -1.000000000000000000, 0.000000000000000000, 0.000000000000000000 ) ) ;
#43875=ORIENTED_EDGE ( 'NONE', *, *, #23087, .F. ) ;
#43876=CARTESIAN_POINT ( 'NONE',  ( 3.296033061219842519, -5.876774720514406525, 18.71226942120119574 ) ) ;
#43890=CARTESIAN_POINT ( 'NONE',  ( -10.59832330691884117, -6.376774720514425177, -27.05373799718301697 ) ) ;
#43894=CARTESIAN_POINT ( 'NONE',  ( 30.45304879119406039, -1.682774720514426114, -10.07140455160086390 ) ) ;
#43899=LINE ( 'NONE', #4345, #16552 ) ;
#43900=DIRECTION ( 'NONE',  ( 0.000000000000000000, 0.000000000000000000, -1.000000000000000000 ) ) ;
#43908=CARTESIAN_POINT ( 'NONE',  ( -1.012926118674504883, -6.376774720514415407, 19.92818918856637822 ) ) ;
#43909=CARTESIAN_POINT ( 'NONE',  ( 2.905472630834636139, -6.376774720514415407, 19.87563926270137671 ) ) ;
#43911=CARTESIAN_POINT ( 'NONE',  ( 20.57455539870795036, -2.682774720514426559, -18.22080502500658739 ) ) ;
#43921=CARTESIAN_POINT ( 'NONE',  ( 29.80070917940689412, 5.965225279485572685, 27.39560796525321607 ) ) ;
#43925=CARTESIAN_POINT ( 'NONE',  ( 0.3849403830293018358, -6.376774720514418959, 20.45311193189268906 ) ) ;
#43932=ORIENTED_EDGE ( 'NONE', *, *, #85743, .T. ) ;
#43937=ORIENTED_EDGE ( 'NONE', *, *, #60330, .F. ) ;
#43946=DIRECTION ( 'NONE',  ( 0.000000000000000000, 0.000000000000000000, -1.000000000000000000 ) ) ;
#43950=CARTESIAN_POINT ( 'NONE',  ( -3.095730855174848362, -6.376774720514413630, 20.04377961306771638 ) ) ;
#43955=CYLINDRICAL_SURFACE ( 'NONE', #20854, 12.65241003308275758 ) ;
#43968=ORIENTED_EDGE ( 'NONE', *, *, #9000, .T. ) ;
#43970=CARTESIAN_POINT ( 'NONE',  ( 13.87573923102662121, -3.316774720514425123, -28.27006591627376508 ) ) ;
#43984=CYLINDRICAL_SURFACE ( 'NONE', #87833, 130.7884398600581335 ) ;
#43985=VERTEX_POINT ( 'NONE', #73229 ) ;
#43992=CARTESIAN_POINT ( 'NONE',  ( 27.53860345374808105, -5.356774720496559894, 0.000000000000000000 ) ) ;
#43993=CARTESIAN_POINT ( 'NONE',  ( -0.02075734969026423599, 5.965225279485572685, -29.05397719988136984 ) ) ;
#43994=DIRECTION ( 'NONE',  ( 0.000000000000000000, -1.000000000000000000, 0.000000000000000000 ) ) ;
#43997=CARTESIAN_POINT ( 'NONE',  ( -2.457093156980370452, -5.876774720514410077, 19.51167604195716976 ) ) ;
#43999=CARTESIAN_POINT ( 'NONE',  ( -9.940598223437573822, -5.876774720514426953, 21.78128695274315874 ) ) ;
#44002=ADVANCED_FACE ( 'NONE', ( #96550 ), #48895, .T. ) ;
#44012=ORIENTED_EDGE ( 'NONE', *, *, #45929, .T. ) ;
#44024=VECTOR ( 'NONE', #55761, 999.9999999999998863 ) ;
#44029=ORIENTED_EDGE ( 'NONE', *, *, #41819, .F. ) ;
#44032=ADVANCED_FACE ( 'NONE', ( #58014 ), #79821, .F. ) ;
#44033=DIRECTION ( 'NONE',  ( 0.000000000000000000, 0.000000000000000000, -1.000000000000000000 ) ) ;
#44054=CARTESIAN_POINT ( 'NONE',  ( -24.90875734969025501, -0.3587747205144265483, 26.43402280011862615 ) ) ;
#44060=ORIENTED_EDGE ( 'NONE', *, *, #38135, .F. ) ;
#44062=ADVANCED_FACE ( 'NONE', ( #33150 ), #58508, .F. ) ;
#44079=EDGE_CURVE ( 'NONE', #93291, #94756, #90080, .T. ) ;
#44085=ORIENTED_EDGE ( 'NONE', *, *, #39920, .F. ) ;
#44086=CARTESIAN_POINT ( 'NONE',  ( 0.000000000000000000, -4.056774720514426669, 0.000000000000000000 ) ) ;
#44094=ADVANCED_FACE ( 'NONE', ( #37147 ), #5200, .F. ) ;
#44106=EDGE_CURVE ( 'NONE', #1512, #95782, #76197, .T. ) ;
#44111=B_SPLINE_CURVE_WITH_KNOTS ( 'NONE', 3,
 ( #25907, #4581, #96919, #65999, #57385, #81194, #65499, #26908, #33520, #57879, #11671, #19283, #19778, #56881, #37015, #44631, #45139, #13163, #6565, #59867, #20274, #58860, #6059 ),
 .UNSPECIFIED., .F., .F.,
 ( 4, 1, 1, 1, 1, 1, 1, 1, 1, 1, 1, 1, 1, 1, 1, 1, 1, 1, 1, 1, 4 ),
 ( 0.000000000000000000, 0.07295106587586808189, 0.1415836941865457888, 0.2059264601708682696, 0.2653013571846069008, 0.3205972327139294809, 0.3718165030988108688, 0.4187897697094533633, 0.4616987286157644976, 0.5021335821035667335, 0.5408043152926478303, 0.5781805253279665990, 0.6142968652075149194, 0.6496782432647882910, 0.6842994600896379342, 0.7183589527723613921, 0.7520808646475963810, 0.8176524386023853452, 0.8797220764054369813, 0.9399655597309874988, 1.000000000000000000 ),
 .UNSPECIFIED. ) ;
#44115=CARTESIAN_POINT ( 'NONE',  ( -1.267404104715736279, -5.876774720514411854, 19.66076420632889921 ) ) ;
#44117=DIRECTION ( 'NONE',  ( 0.000000000000000000, 0.000000000000000000, 1.000000000000000000 ) ) ;
#44123=VECTOR ( 'NONE', #21179, 1000.000000000000000 ) ;
#44127=LINE ( 'NONE', #13652, #27200 ) ;
#44137=CARTESIAN_POINT ( 'NONE',  ( -5.891025641025639636, -6.376774720514420736, 20.75510817307693046 ) ) ;
#44139=ORIENTED_EDGE ( 'NONE', *, *, #55984, .T. ) ;
#44152=FACE_OUTER_BOUND ( 'NONE', #14444, .T. ) ;
#44153=AXIS2_PLACEMENT_3D ( 'NONE', #2579, #86300, #87299 ) ;
#44159=EDGE_CURVE ( 'NONE', #34973, #27382, #37647, .T. ) ;
#44163=EDGE_CURVE ( 'NONE', #60109, #44429, #82815, .T. ) ;
#44174=CARTESIAN_POINT ( 'NONE',  ( 6.403846153846157740, -5.876774720514425177, 21.48076923076922995 ) ) ;
#44185=CARTESIAN_POINT ( 'NONE',  ( 9.150000000000000355, -5.876774720514426953, -15.70000000000000284 ) ) ;
#44202=CARTESIAN_POINT ( 'NONE',  ( 2.989331223418256744, -5.876774720514424288, 21.46569930292093886 ) ) ;
#44235=DIRECTION ( 'NONE',  ( 1.000000000000000000, 0.000000000000000000, 0.000000000000000000 ) ) ;
#44241=AXIS2_PLACEMENT_3D ( 'NONE', #54834, #24862, #92872 ) ;
#44243=CARTESIAN_POINT ( 'NONE',  ( -25.92875734969025814, -3.316774720514426456, 30.51402280011862089 ) ) ;
#44244=VECTOR ( 'NONE', #5697, 1000.000000000000227 ) ;
#44269=CARTESIAN_POINT ( 'NONE',  ( 30.61558314414154580, -3.638221654638376990, 27.34201279177319321 ) ) ;
#44279=EDGE_CURVE ( 'NONE', #55323, #79408, #99271, .T. ) ;
#44289=CARTESIAN_POINT ( 'NONE',  ( 12.46200043076872888, -4.205547148226783882, -28.02060279727989922 ) ) ;
#44296=CARTESIAN_POINT ( 'NONE',  ( -1.394533802543915124, -5.876774720514413630, 20.19722303762275573 ) ) ;
#44298=B_SPLINE_SURFACE_WITH_KNOTS ( 'NONE', 3, 1, ( 
 ( #49331, #87879 ),
 ( #95487, #86373 ),
 ( #71657, #16351 ),
 ( #39690, #79250 ),
 ( #64068, #94982 ),
 ( #18363, #17865 ),
 ( #71157, #1647 ),
 ( #25973, #80263 ),
 ( #47317, #10756 ),
 ( #56945, #32079 ),
 ( #34098, #70649 ),
 ( #3157, #24468 ),
 ( #8752, #41210 ),
 ( #41720, #9748 ),
 ( #33089, #48829 ),
 ( #17360, #72660 ),
 ( #16857, #65070 ),
 ( #32582, #40703 ),
 ( #23962, #79755 ) ),
 .UNSPECIFIED., .F., .F., .F.,
 ( 4, 1, 1, 1, 1, 1, 1, 1, 1, 1, 1, 1, 1, 1, 1, 1, 4 ),
 ( 2, 2 ),
 ( 0.000000000000000000, 0.06318289109391794778, 0.1237330903858703257, 0.1836062326498469899, 0.2427039625557292357, 0.3016492823581786720, 0.3610699883815534639, 0.4220736591995472020, 0.4842519596996277542, 0.5473469430655184542, 0.6093464547651399332, 0.6708936127785768422, 0.7332102753497369285, 0.7968038021902664747, 0.8620990789963799417, 0.9294007105664079393, 1.000000000000000000 ),
 ( 0.000000000000000000, 1.000000000000000000 ),
 .UNSPECIFIED. ) ;
#44299=CARTESIAN_POINT ( 'NONE',  ( -2.606012662418322634, -5.876774720514410077, 19.21974929698718881 ) ) ;
#44321=LINE ( 'NONE', #75249, #80090 ) ;
#44334=CARTESIAN_POINT ( 'NONE',  ( -4.495793269230770939, -6.376774720514410077, 19.27714342948718595 ) ) ;
#44338=CARTESIAN_POINT ( 'NONE',  ( 3.787259615384621192, -5.876774720514425177, 21.48076923076922640 ) ) ;
#44342=B_SPLINE_CURVE_WITH_KNOTS ( 'NONE', 3,
 ( #74562, #20760, #52234, #68950 ),
 .UNSPECIFIED., .F., .F.,
 ( 4, 4 ),
 ( 0.000000000000000000, 1.000000000000000000 ),
 .UNSPECIFIED. ) ;
#44347=ORIENTED_EDGE ( 'NONE', *, *, #63416, .F. ) ;
#44349=CIRCLE ( 'NONE', #42762, 27.94799999999999685 ) ;
#44352=EDGE_CURVE ( 'NONE', #94222, #24461, #86821, .T. ) ;
#44370=CARTESIAN_POINT ( 'NONE',  ( 14.52511747680497933, 6.475225279485573360, -27.86035006098926559 ) ) ;
#44373=LINE ( 'NONE', #75298, #97222 ) ;
#44380=AXIS2_PLACEMENT_3D ( 'NONE', #95585, #26072, #17965 ) ;
#44381=CARTESIAN_POINT ( 'NONE',  ( 3.202571139211427553, -5.876774720514406525, 18.81074098386681470 ) ) ;
#44382=CARTESIAN_POINT ( 'NONE',  ( 2.591645189881369493, -6.376774720514411854, 19.84288601127407148 ) ) ;
#44383=PLANE ( 'NONE',  #30341 ) ;
#44393=CARTESIAN_POINT ( 'NONE',  ( 30.93860345374796594, -0.6647747205144264315, 19.84760796525321780 ) ) ;
#44394=CARTESIAN_POINT ( 'NONE',  ( 1.305682803664691249, 5.965225279485572685, 29.57950906855421991 ) ) ;
#44398=DIRECTION ( 'NONE',  ( 0.2488812114211667315, 0.000000000000000000, 0.9685340172660600322 ) ) ;
#44415=CARTESIAN_POINT ( 'NONE',  ( -0.4362980769230789257, -6.376774720514411854, 19.46153846153846345 ) ) ;
#44416=CARTESIAN_POINT ( 'NONE',  ( -1.390986686320385468, -6.376774720514413630, 19.62288733224860948 ) ) ;
#44419=EDGE_CURVE ( 'NONE', #35655, #81742, #87322, .T. ) ;
#44429=VERTEX_POINT ( 'NONE', #49289 ) ;
#44438=ORIENTED_EDGE ( 'NONE', *, *, #5353, .T. ) ;
#44451=DIRECTION ( 'NONE',  ( 1.000000000000000000, 0.000000000000000000, 0.000000000000000000 ) ) ;
#44452=CARTESIAN_POINT ( 'NONE',  ( -20.27875734969026311, 7.743225279485574042, 22.60402280011862430 ) ) ;
#44456=CARTESIAN_POINT ( 'NONE',  ( -2.243088942307695621, -6.376774720514410077, 19.14743589743590846 ) ) ;
#44461=CARTESIAN_POINT ( 'NONE',  ( -4.440151687742864617, -6.376774720514411854, 19.67013632031035897 ) ) ;
#44469=CARTESIAN_POINT ( 'NONE',  ( 4.281720980632043094, -6.376774720514408301, 18.71132571341777151 ) ) ;
#44471=CARTESIAN_POINT ( 'NONE',  ( 30.41387671341004761, -4.976059279456417350, 19.84760796525321425 ) ) ;
#44476=CARTESIAN_POINT ( 'NONE',  ( -4.752075056065355518, -5.876774720514407413, 19.17724329193115551 ) ) ;
#44490=B_SPLINE_SURFACE_WITH_KNOTS ( 'NONE', 3, 1, ( 
 ( #12328, #74240 ),
 ( #4735, #35683 ),
 ( #66660, #51408 ),
 ( #74724, #5226 ),
 ( #98057, #36182 ),
 ( #90957, #67149 ),
 ( #28556, #22912 ),
 ( #69629, #16328 ),
 ( #39165, #604 ),
 ( #62516, #46282 ),
 ( #6714, #77210 ),
 ( #7208, #23938 ),
 ( #30044, #46786 ),
 ( #29552, #15318 ),
 ( #83840, #77714 ) ),
 .UNSPECIFIED., .F., .F., .F.,
 ( 4, 1, 1, 1, 1, 1, 1, 1, 1, 1, 1, 1, 4 ),
 ( 2, 2 ),
 ( 0.000000000000000000, 0.08597245417931687061, 0.1699564070247753245, 0.2542168740862559284, 0.3392430307459933791, 0.4239782646133617439, 0.5058277166288100979, 0.5866357120841194650, 0.6677102638611641661, 0.7496008928139508143, 0.8308747881193089269, 0.9140520568558714309, 1.000000000000000000 ),
 ( 0.000000000000000000, 1.000000000000000000 ),
 .UNSPECIFIED. ) ;
#44493=DIRECTION ( 'NONE',  ( 0.000000000000000000, 0.000000000000000000, -1.000000000000000000 ) ) ;
#44497=ORIENTED_EDGE ( 'NONE', *, *, #26099, .F. ) ;
#44517=EDGE_CURVE ( 'NONE', #8365, #72161, #49787, .T. ) ;
#44518=EDGE_LOOP ( 'NONE', ( #72982, #83986, #86856, #57106 ) ) ;
#44520=CARTESIAN_POINT ( 'NONE',  ( 10.95759398273795249, -4.132774720514426292, -26.86884997114579932 ) ) ;
#44528=EDGE_CURVE ( 'NONE', #68153, #69965, #94939, .T. ) ;
#44548=VECTOR ( 'NONE', #27560, 1000.000000000000000 ) ;
#44552=CARTESIAN_POINT ( 'NONE',  ( 7.448826589983275959, -5.876774720514420736, 21.05250386848070221 ) ) ;
#44570=CARTESIAN_POINT ( 'NONE',  ( 1.305682803664691249, 5.965225279485572685, 29.57950906855421991 ) ) ;
#44581=AXIS2_PLACEMENT_3D ( 'NONE', #73626, #72137, #96956 ) ;
#44586=CARTESIAN_POINT ( 'NONE',  ( 4.334227700317904386, -5.876774720514401196, 18.30971318885719157 ) ) ;
#44593=AXIS2_PLACEMENT_3D ( 'NONE', #82860, #36697, #68151 ) ;
#44595=CARTESIAN_POINT ( 'NONE',  ( 5.641575934020636396, -5.876774720514419847, 20.76276410292889096 ) ) ;
#44597=DIRECTION ( 'NONE',  ( -0.6599726524652340665, 3.117967031984456719E-15, 0.7512896232465900992 ) ) ;
#44600=EDGE_LOOP ( 'NONE', ( #61992, #9405, #27722, #59381 ) ) ;
#44618=CARTESIAN_POINT ( 'NONE',  ( -24.90875734969025501, 6.475225279485573360, 29.49402280011861777 ) ) ;
#44623=VECTOR ( 'NONE', #25817, 1000.000000000000000 ) ;
#44631=CARTESIAN_POINT ( 'NONE',  ( 4.329581153495547063, -5.876774720514422512, 21.24220543808225869 ) ) ;
#44635=( BOUNDED_SURFACE ( )  B_SPLINE_SURFACE ( 3, 2, ( 
 ( #21296, #29915, #100403 ),
 ( #37035, #30916, #67995 ),
 ( #76577, #99904, #30416 ),
 ( #60882, #51770, #53268 ),
 ( #77078, #21787, #15190 ),
 ( #46152, #5583, #98923 ),
 ( #22784, #91317, #52765 ),
 ( #14688, #53772, #38529 ),
 ( #84197, #67496, #29414 ),
 ( #60395, #45160, #98418 ) ),
 .UNSPECIFIED., .F., .F., .T. ) 
 B_SPLINE_SURFACE_WITH_KNOTS ( ( 4, 2, 2, 2, 4 ),
 ( 3, 3 ),
 ( -1.454863790203986262E-16, 9.770668801556799598E-05, 0.0001954133760312814648, 0.0002931200640469949336, 0.0003908267520627084295 ),
 ( 0.000000000000000000, 1.000000000000000000 ),
 .UNSPECIFIED. ) 
 GEOMETRIC_REPRESENTATION_ITEM ( )  RATIONAL_B_SPLINE_SURFACE ( (
 ( 1.000000000000000000, 0.8096947957034197341, 1.000000000000000000),
 ( 1.000000000000000000, 0.8369431042627567541, 1.000000000000000000),
 ( 1.000000000000000000, 0.8633772427686626783, 1.000000000000000000),
 ( 1.000000000000000000, 0.9107640641016462313, 1.000000000000000000),
 ( 1.000000000000000000, 0.9319105126974177589, 1.000000000000000000),
 ( 1.000000000000000000, 0.9655776140384774164, 1.000000000000000000),
 ( 1.000000000000000000, 0.9783528158684996479, 1.000000000000000000),
 ( 1.000000000000000000, 0.9955824377509593370, 1.000000000000000000),
 ( 1.000000000000000000, 1.000024029240739631, 1.000000000000000000),
 ( 1.000000000000000000, 1.000000000000000000, 1.000000000000000000) ) ) 
 REPRESENTATION_ITEM ( '' )  SURFACE ( )  );
#44647=ORIENTED_EDGE ( 'NONE', *, *, #19522, .F. ) ;
#44651=ADVANCED_FACE ( 'NONE', ( #45533 ), #75896, .T. ) ;
#44652=CIRCLE ( 'NONE', #10683, 0.3000000000000016542 ) ;
#44653=DIRECTION ( 'NONE',  ( 3.639962309748244178E-15, 1.000000000000000000, -2.135627652102599075E-15 ) ) ;
#44654=ADVANCED_FACE ( 'NONE', ( #47030 ), #24175, .F. ) ;
#44657=CARTESIAN_POINT ( 'NONE',  ( 14.78484767477524819, -5.152774720514425866, -28.43034250232787485 ) ) ;
#44664=AXIS2_PLACEMENT_3D ( 'NONE', #54575, #2298, #69799 ) ;
#44665=CARTESIAN_POINT ( 'NONE',  ( 13.91401389203221406, -3.316774720514426456, 158.0376437107427137 ) ) ;
#44671=ADVANCED_FACE ( 'NONE', ( #40909 ), #94183, .T. ) ;
#44691=EDGE_LOOP ( 'NONE', ( #23497, #15887, #11015, #72193 ) ) ;
#44701=EDGE_LOOP ( 'NONE', ( #92248, #35095 ) ) ;
#44704=CARTESIAN_POINT ( 'NONE',  ( 15.99960863614693274, -3.577630190449808012, -27.91116951066528173 ) ) ;
#44711=CARTESIAN_POINT ( 'NONE',  ( 33.00535138976592719, -3.570691370340881576, -12.97242311383975988 ) ) ;
#44713=PLANE ( 'NONE',  #58260 ) ;
#44718=EDGE_LOOP ( 'NONE', ( #63325, #78300, #10344, #20618, #99332, #31416, #78910, #93262, #650, #75764, #82625, #13296, #34340, #16971, #38951, #60794, #76881, #51814, #84262, #69704 ) ) ;
#44720=EDGE_CURVE ( 'NONE', #3112, #49156, #18377, .T. ) ;
#44728=AXIS2_PLACEMENT_3D ( 'NONE', #87180, #32902, #47131 ) ;
#44731=LINE ( 'NONE', #14257, #18785 ) ;
#44737=CIRCLE ( 'NONE', #51258, 0.3000000000000016542 ) ;
#44740=CARTESIAN_POINT ( 'NONE',  ( -27.25988310792305214, 5.965225279485572685, 30.32664379231667695 ) ) ;
#44742=CARTESIAN_POINT ( 'NONE',  ( 3.252401863874215593, -0.3587747205143964613, -29.35688408629929214 ) ) ;
#44750=ORIENTED_EDGE ( 'NONE', *, *, #6591, .T. ) ;
#44756=VERTEX_POINT ( 'NONE', #16555 ) ;
#44758=DIRECTION ( 'NONE',  ( 0.000000000000000000, 0.000000000000000000, 1.000000000000000000 ) ) ;
#44759=LINE ( 'NONE', #52367, #72365 ) ;
#44772=CARTESIAN_POINT ( 'NONE',  ( -1.380763273332680896, -6.376774720514418959, 20.28973052848695602 ) ) ;
#44783=CARTESIAN_POINT ( 'NONE',  ( 4.647438682898014761, -6.376774720514417183, 20.26932200457894950 ) ) ;
#44784=CIRCLE ( 'NONE', #17183, 251.4258649670780699 ) ;
#44785=ADVANCED_FACE ( 'NONE', ( #35307 ), #4844, .T. ) ;
#44788=LINE ( 'NONE', #91437, #20228 ) ;
#44791=DIRECTION ( 'NONE',  ( -1.000000000000000000, -0.000000000000000000, -5.238131417152343399E-15 ) ) ;
#44792=CARTESIAN_POINT ( 'NONE',  ( -1.501937386944296460, -6.376774720514415407, 19.86422795159478483 ) ) ;
#44798=AXIS2_PLACEMENT_3D ( 'NONE', #90990, #89007, #52440 ) ;
#44809=DIRECTION ( 'NONE',  ( 0.000000000000000000, -1.000000000000000000, 0.000000000000000000 ) ) ;
#44817=DIRECTION ( 'NONE',  ( 0.000000000000000000, 0.000000000000000000, -1.000000000000000000 ) ) ;
#44825=CARTESIAN_POINT ( 'NONE',  ( -0.3225169060639742624, -6.376774720514411854, 19.46611907402017749 ) ) ;
#44831=CARTESIAN_POINT ( 'NONE',  ( -4.465079497292244959, -6.376774720514410077, 19.29815762497054976 ) ) ;
#44843=ORIENTED_EDGE ( 'NONE', *, *, #81320, .F. ) ;
#44861=LINE ( 'NONE', #92015, #94264 ) ;
#44863=EDGE_CURVE ( 'NONE', #3925, #12606, #40285, .T. ) ;
#44867=VERTEX_POINT ( 'NONE', #64781 ) ;
#44868=LINE ( 'NONE', #53485, #56231 ) ;
#44871=CARTESIAN_POINT ( 'NONE',  ( 30.63935204725980554, -3.888906929512149446, 28.25823861891851507 ) ) ;
#44878=VERTEX_POINT ( 'NONE', #13442 ) ;
#44879=AXIS2_PLACEMENT_3D ( 'NONE', #15859, #70158, #641 ) ;
#44884=CARTESIAN_POINT ( 'NONE',  ( 3.051095722660301934, -5.876774720514410077, 19.07493897947323092 ) ) ;
#44888=CARTESIAN_POINT ( 'NONE',  ( 26.73860345374794178, -5.334136533370936739, -4.444819549327402086 ) ) ;
#44893=MANIFOLD_SOLID_BREP ( 'Kes-Ekstr\X2\00fc\X0\zyon28', #82466 ) ;
#44894=DIRECTION ( 'NONE',  ( 0.000000000000000000, 0.000000000000000000, 1.000000000000000000 ) ) ;
#44900=CARTESIAN_POINT ( 'NONE',  ( 32.25183987940364005, -6.376774720514426953, 2.026414261721653176 ) ) ;
#44911=AXIS2_PLACEMENT_3D ( 'NONE', #13756, #28494, #99492 ) ;
#44912=CARTESIAN_POINT ( 'NONE',  ( -29.49875734969025842, -0.3587747205144265483, 17.86602280011862476 ) ) ;
#44943=VECTOR ( 'NONE', #37456, 1000.000000000000000 ) ;
#44947=CARTESIAN_POINT ( 'NONE',  ( 3.879812756903532556, -6.376774720514401196, 18.16163344421570969 ) ) ;
#44951=VERTEX_POINT ( 'NONE', #15436 ) ;
#44952=AXIS2_PLACEMENT_3D ( 'NONE', #65976, #88795, #51222 ) ;
#44955=FACE_OUTER_BOUND ( 'NONE', #51145, .T. ) ;
#44958=VERTEX_POINT ( 'NONE', #76333 ) ;
#44959=CARTESIAN_POINT ( 'NONE',  ( -3.108425644221024520, -5.876774720514414518, 20.25188360057253334 ) ) ;
#44962=CARTESIAN_POINT ( 'NONE',  ( -4.289200894924355190, -6.376774720514413630, 19.85590024959437017 ) ) ;
#44977=DIRECTION ( 'NONE',  ( 0.5473052603538087757, -5.646564643389147554E-15, 0.8369330630277725946 ) ) ;
#44993=ADVANCED_FACE ( 'NONE', ( #99172 ), #92560, .F. ) ;
#45004=DIRECTION ( 'NONE',  ( -1.000000000000000000, -0.000000000000000000, 0.000000000000000000 ) ) ;
#45005=CARTESIAN_POINT ( 'NONE',  ( 31.82032313667048484, -6.376774720514426953, 9.148483289431936782 ) ) ;
#45006=CARTESIAN_POINT ( 'NONE',  ( -65.05438548721848235, -5.356774720514425603, 0.7300228001186309656 ) ) ;
#45009=DIRECTION ( 'NONE',  ( 1.156482317317878549E-14, 0.000000000000000000, 1.000000000000000000 ) ) ;
#45015=DIRECTION ( 'NONE',  ( -0.000000000000000000, 1.000000000000000000, -0.000000000000000000 ) ) ;
#45023=AXIS2_PLACEMENT_3D ( 'NONE', #17165, #48131, #95295 ) ;
#45028=EDGE_CURVE ( 'NONE', #13059, #95824, #59716, .T. ) ;
#45035=ORIENTED_EDGE ( 'NONE', *, *, #9060, .F. ) ;
#45037=LINE ( 'NONE', #75955, #62974 ) ;
#45038=CARTESIAN_POINT ( 'NONE',  ( 3.113719597313231002, -5.876774720514426065, 21.58936759753562029 ) ) ;
#45040=DIRECTION ( 'NONE',  ( -1.334402673828313093E-16, 0.000000000000000000, -1.000000000000000000 ) ) ;
#45042=VERTEX_POINT ( 'NONE', #67255 ) ;
#45044=DIRECTION ( 'NONE',  ( 0.000000000000000000, -1.000000000000000000, 0.000000000000000000 ) ) ;
#45047=EDGE_CURVE ( 'NONE', #43147, #73685, #9324, .T. ) ;
#45053=CARTESIAN_POINT ( 'NONE',  ( 3.748501943728875574, -6.376774720514426065, 21.47917144995767558 ) ) ;
#45056=CARTESIAN_POINT ( 'NONE',  ( 17.51792015816173986, -0.3587747205144265483, 29.01255224319336889 ) ) ;
#45061=DIRECTION ( 'NONE',  ( 0.000000000000000000, -1.000000000000000000, 0.000000000000000000 ) ) ;
#45069=VERTEX_POINT ( 'NONE', #77822 ) ;
#45070=VERTEX_POINT ( 'NONE', #220 ) ;
#45072=ORIENTED_EDGE ( 'NONE', *, *, #30185, .T. ) ;
#45093=CARTESIAN_POINT ( 'NONE',  ( 4.912344403463128728, -6.376774720514408301, 19.26008510998990886 ) ) ;
#45098=ADVANCED_FACE ( 'NONE', ( #39771 ), #15933, .F. ) ;
#45103=DIRECTION ( 'NONE',  ( -0.5630016722799281448, -5.365801633547210331E-16, 0.8264557562326034779 ) ) ;
#45105=CARTESIAN_POINT ( 'NONE',  ( 5.727631217150810805, -6.376774720514422512, 21.11407618546790133 ) ) ;
#45110=ORIENTED_EDGE ( 'NONE', *, *, #66428, .T. ) ;
#45117=CARTESIAN_POINT ( 'NONE',  ( 282.9764569301858046, 5.965225279485572685, 20.79159422840526616 ) ) ;
#45134=DIRECTION ( 'NONE',  ( -0.1254312216594016538, 0.000000000000000000, -0.9921023176230513441 ) ) ;
#45137=B_SPLINE_SURFACE_WITH_KNOTS ( 'NONE', 3, 1, ( 
 ( #25136, #85037 ),
 ( #17535, #56119 ),
 ( #31763, #39374 ),
 ( #24636, #79427 ),
 ( #9921, #1319 ),
 ( #39873, #70328 ),
 ( #24142, #62729 ) ),
 .UNSPECIFIED., .F., .F., .F.,
 ( 4, 1, 1, 1, 4 ),
 ( 2, 2 ),
 ( 0.000000000000000000, 0.2193543708254352964, 0.4566051594240339018, 0.7164051918613050240, 1.000000000000000000 ),
 ( 0.000000000000000000, 1.000000000000000000 ),
 .UNSPECIFIED. ) ;
#45139=CARTESIAN_POINT ( 'NONE',  ( 4.281508569253434260, -5.876774720514422512, 21.28700241941785265 ) ) ;
#45143=ORIENTED_EDGE ( 'NONE', *, *, #19881, .F. ) ;
#45151=DIRECTION ( 'NONE',  ( 0.000000000000000000, 1.000000000000000000, 0.000000000000000000 ) ) ;
#45160=CARTESIAN_POINT ( 'NONE',  ( 33.61456970919608978, -3.316774720514426900, -11.35828564741662028 ) ) ;
#45185=CARTESIAN_POINT ( 'NONE',  ( -53.01255352321339842, -4.772774720514425972, 35.59556822165056644 ) ) ;
#45201=CIRCLE ( 'NONE', #3131, 0.3000000000000016542 ) ;
#45218=AXIS2_PLACEMENT_3D ( 'NONE', #69735, #213, #69228 ) ;
#45221=EDGE_CURVE ( 'NONE', #12529, #86771, #86456, .T. ) ;
#45224=ADVANCED_FACE ( 'NONE', ( #71241 ), #9664, .T. ) ;
#45225=EDGE_LOOP ( 'NONE', ( #25447, #24240, #73157, #37110, #2809, #18393, #29585, #49565, #1013, #94922, #29209 ) ) ;
#45226=CARTESIAN_POINT ( 'NONE',  ( -6.602379858799704238, -5.876774720514410966, 19.46575348430202723 ) ) ;
#45229=CIRCLE ( 'NONE', #41994, 1.399999999999998579 ) ;
#45236=EDGE_CURVE ( 'NONE', #87855, #22734, #41288, .T. ) ;
#45243=LINE ( 'NONE', #68577, #68988 ) ;
#45259=EDGE_CURVE ( 'NONE', #77096, #45042, #67629, .T. ) ;
#45266=EDGE_CURVE ( 'NONE', #4283, #18679, #29046, .T. ) ;
#45273=CARTESIAN_POINT ( 'NONE',  ( -7.234140626586239797, -6.376774720514411854, 19.72789237585158162 ) ) ;
#45274=CIRCLE ( 'NONE', #66373, 1.835999999999993859 ) ;
#45275=LINE ( 'NONE', #59502, #27872 ) ;
#45282=CARTESIAN_POINT ( 'NONE',  ( 8.868390920966309210, -6.053523946337313610, -26.43277665853620206 ) ) ;
#45290=CARTESIAN_POINT ( 'NONE',  ( -1.359786310227693251, -6.376774720514417183, 20.62654306927474579 ) ) ;
#45292=AXIS2_PLACEMENT_3D ( 'NONE', #92502, #31103, #21483 ) ;
#45298=DIRECTION ( 'NONE',  ( -1.000000000000000000, -0.000000000000000000, -0.000000000000000000 ) ) ;
#45299=EDGE_CURVE ( 'NONE', #54223, #90167, #98550, .T. ) ;
#45303=ORIENTED_EDGE ( 'NONE', *, *, #96787, .T. ) ;
#45327=EDGE_CURVE ( 'NONE', #497, #77260, #90451, .T. ) ;
#45337=CARTESIAN_POINT ( 'NONE',  ( 6.424528460793287543, -5.876774720514413630, 19.73230822599986212 ) ) ;
#45339=ORIENTED_EDGE ( 'NONE', *, *, #8796, .T. ) ;
#45343=ORIENTED_EDGE ( 'NONE', *, *, #11715, .F. ) ;
#45344=ORIENTED_EDGE ( 'NONE', *, *, #48432, .F. ) ;
#45352=CARTESIAN_POINT ( 'NONE',  ( -19.77875734969026311, 6.143225279485574397, 29.49402280011862487 ) ) ;
#45355=CARTESIAN_POINT ( 'NONE',  ( -0.8460708837923186509, -6.376774720514410077, 19.21968329462762526 ) ) ;
#45360=CARTESIAN_POINT ( 'NONE',  ( 27.53860345374808105, -3.356774720514427379, 1.647607965253212514 ) ) ;
#45362=ORIENTED_EDGE ( 'NONE', *, *, #80751, .T. ) ;
#45367=AXIS2_PLACEMENT_3D ( 'NONE', #32195, #48942, #31705 ) ;
#45370=DIRECTION ( 'NONE',  ( 0.000000000000000000, 0.000000000000000000, 1.000000000000000000 ) ) ;
#45372=CYLINDRICAL_SURFACE ( 'NONE', #33645, 0.3000000000000016542 ) ;
#45374=CARTESIAN_POINT ( 'NONE',  ( 30.09341516180546350, -1.682774720514426114, -11.39311774897855933 ) ) ;
#45376=CIRCLE ( 'NONE', #25946, 2.499999999999972911 ) ;
#45402=DIRECTION ( 'NONE',  ( 0.000000000000000000, -1.000000000000000000, 0.000000000000000000 ) ) ;
#45403=PLANE ( 'NONE',  #6709 ) ;
#45416=ORIENTED_EDGE ( 'NONE', *, *, #1041, .F. ) ;
#45427=EDGE_CURVE ( 'NONE', #63059, #9746, #63829, .T. ) ;
#45429=B_SPLINE_CURVE_WITH_KNOTS ( 'NONE', 3,
 ( #16479, #87509, #95119, #9877, #7877, #38826, #768, #54559, #16986, #47954, #71791, #62686, #2286, #77874, #48457, #79385, #69788, #25608, #265 ),
 .UNSPECIFIED., .F., .F.,
 ( 4, 1, 1, 1, 1, 1, 1, 1, 1, 1, 1, 1, 1, 1, 1, 1, 4 ),
 ( 0.000000000000000000, 0.06815824415599749941, 0.1347066022023570842, 0.2018649976035983007, 0.2707882662774625526, 0.3400242943604910306, 0.4080827390537214439, 0.4768131952581447508, 0.5473460643070945375, 0.5856397954238962145, 0.6288649531777642521, 0.6771532033637908121, 0.7308028113651056090, 0.7898066155325017546, 0.8543250087420143357, 0.9243651340575425035, 1.000000000000000000 ),
 .UNSPECIFIED. ) ;
#45431=EDGE_LOOP ( 'NONE', ( #3563, #80932, #71648, #41537 ) ) ;
#45432=CARTESIAN_POINT ( 'NONE',  ( 0.1739078616027790736, -6.376774720514415407, 19.75705121608222115 ) ) ;
#45435=AXIS2_PLACEMENT_3D ( 'NONE', #29758, #74437, #44493 ) ;
#45438=CARTESIAN_POINT ( 'NONE',  ( -4.286263797015736595E-16, -2.056774720514426669, -3.500000000000000000 ) ) ;
#45440=ORIENTED_EDGE ( 'NONE', *, *, #38191, .T. ) ;
#45444=VECTOR ( 'NONE', #3082, 1000.000000000000114 ) ;
#45448=CARTESIAN_POINT ( 'NONE',  ( 4.334227700317904386, -6.376774720514402972, 18.30971318885719157 ) ) ;
#45460=CARTESIAN_POINT ( 'NONE',  ( -0.9078848932494473223, -5.876774720514411854, 19.67454710845354171 ) ) ;
#45462=DIRECTION ( 'NONE',  ( -0.6451914333552788428, 0.000000000000000000, -0.7640209514960702997 ) ) ;
#45463=CARTESIAN_POINT ( 'NONE',  ( -4.533825836049095059, -6.376774720514411854, 19.59623724171353132 ) ) ;
#45466=ORIENTED_EDGE ( 'NONE', *, *, #20827, .T. ) ;
#45474=LINE ( 'NONE', #23598, #48756 ) ;
#45477=CARTESIAN_POINT ( 'NONE',  ( 30.77956504631911017, -6.277769580494330093, 0.6965969997247714041 ) ) ;
#45478=LINE ( 'NONE', #92621, #57740 ) ;
#45505=DIRECTION ( 'NONE',  ( -0.000000000000000000, 1.000000000000000000, -0.000000000000000000 ) ) ;
#45512=CARTESIAN_POINT ( 'NONE',  ( -2.732037236150805626, -6.376774720514411854, 19.78976258633487717 ) ) ;
#45514=DIRECTION ( 'NONE',  ( 0.000000000000000000, 1.000000000000000000, 0.000000000000000000 ) ) ;
#45525=CARTESIAN_POINT ( 'NONE',  ( 10.48383480065558615, -3.481296116130239149, -27.02502823977714286 ) ) ;
#45533=FACE_OUTER_BOUND ( 'NONE', #12283, .T. ) ;
#45552=CARTESIAN_POINT ( 'NONE',  ( -5.706951327759631099, -6.376774720514411854, 19.48569229636961353 ) ) ;
#45555=EDGE_CURVE ( 'NONE', #60162, #55041, #46624, .T. ) ;
#45557=AXIS2_PLACEMENT_3D ( 'NONE', #20901, #21391, #12291 ) ;
#45563=CARTESIAN_POINT ( 'NONE',  ( 22.02124265030973760, 6.143225279485574397, 16.20402280011862217 ) ) ;
#45588=DIRECTION ( 'NONE',  ( 0.000000000000000000, -1.000000000000000000, 0.000000000000000000 ) ) ;
#45592=CARTESIAN_POINT ( 'NONE',  ( 4.642799911345256270, -6.376774720514408301, 18.59646607068888713 ) ) ;
#45599=CARTESIAN_POINT ( 'NONE',  ( 5.811591729264017125, -6.376774720514422512, 21.22699980322195046 ) ) ;
#45600=ORIENTED_EDGE ( 'NONE', *, *, #66405, .F. ) ;
#45617=VERTEX_POINT ( 'NONE', #63363 ) ;
#45628=CARTESIAN_POINT ( 'NONE',  ( 33.00535138976610483, 5.965225279485572685, -12.97242311383961066 ) ) ;
#45633=LINE ( 'NONE', #98901, #83875 ) ;
#45636=CARTESIAN_POINT ( 'NONE',  ( 3.509873074917118085, -0.3587747205144265483, 29.15869884040363758 ) ) ;
#45643=LINE ( 'NONE', #14174, #41683 ) ;
#45647=VERTEX_POINT ( 'NONE', #64367 ) ;
#45651=PLANE ( 'NONE',  #14959 ) ;
#45653=VERTEX_POINT ( 'NONE', #31386 ) ;
#45658=CARTESIAN_POINT ( 'NONE',  ( -0.7827064370038755436, -6.376774720514410077, 19.55912026249540148 ) ) ;
#45668=EDGE_CURVE ( 'NONE', #55838, #53330, #42734, .T. ) ;
#45674=AXIS2_PLACEMENT_3D ( 'NONE', #12395, #98123, #58586 ) ;
#45679=ADVANCED_FACE ( 'NONE', ( #72960 ), #88680, .F. ) ;
#45682=ORIENTED_EDGE ( 'NONE', *, *, #13909, .F. ) ;
#45695=CARTESIAN_POINT ( 'NONE',  ( 3.797776442307698286, -6.376774720514427841, 21.83974358974358410 ) ) ;
#45708=ADVANCED_FACE ( 'NONE', ( #66852 ), #73951, .F. ) ;
#45718=ORIENTED_EDGE ( 'NONE', *, *, #52873, .F. ) ;
#45723=CARTESIAN_POINT ( 'NONE',  ( 14.62591090210861999, -3.611920024593927803, -27.34381298535168270 ) ) ;
#45724=CARTESIAN_POINT ( 'NONE',  ( 2.903846153846159517, -6.376774720514415407, 19.99999999999999289 ) ) ;
#45736=CARTESIAN_POINT ( 'NONE',  ( 15.30669617938070459, -3.316774720514427344, -28.51986056384665957 ) ) ;
#45760=VERTEX_POINT ( 'NONE', #18160 ) ;
#45762=CARTESIAN_POINT ( 'NONE',  ( 6.420673076923079314, -6.376774720514427841, 21.83974358974358765 ) ) ;
#45765=CARTESIAN_POINT ( 'NONE',  ( -1.595974963000059477, -5.876774720514409189, 19.39236848396478408 ) ) ;
#45769=EDGE_CURVE ( 'NONE', #56886, #12265, #57249, .T. ) ;
#45786=CARTESIAN_POINT ( 'NONE',  ( 0.2196812790064107401, -5.876774720514409189, 19.42522865122897002 ) ) ;
#45801=DIRECTION ( 'NONE',  ( 0.000000000000000000, 0.000000000000000000, 1.000000000000000000 ) ) ;
#45803=DIRECTION ( 'NONE',  ( 0.000000000000000000, 0.000000000000000000, 1.000000000000000000 ) ) ;
#45836=EDGE_CURVE ( 'NONE', #30845, #100399, #87677, .T. ) ;
#45849=CARTESIAN_POINT ( 'NONE',  ( 7.370931459274800090, -5.876774720514417183, 20.26286690110499578 ) ) ;
#45851=CARTESIAN_POINT ( 'NONE',  ( 282.9764569301858046, -5.152774720514427642, 20.79159422840526616 ) ) ;
#45853=ORIENTED_EDGE ( 'NONE', *, *, #86200, .F. ) ;
#45855=ORIENTED_EDGE ( 'NONE', *, *, #90583, .F. ) ;
#45861=LINE ( 'NONE', #180, #56760 ) ;
#45863=ADVANCED_FACE ( 'NONE', ( #4935 ), #95784, .F. ) ;
#45867=ORIENTED_EDGE ( 'NONE', *, *, #91640, .T. ) ;
#45871=CIRCLE ( 'NONE', #11819, 1.700000000000000178 ) ;
#45874=CARTESIAN_POINT ( 'NONE',  ( 3.052815417670126319, -5.876774720514407413, 18.46676085997033923 ) ) ;
#45876=DIRECTION ( 'NONE',  ( -0.9994733861282923959, 0.000000000000000000, -0.03244919754393515293 ) ) ;
#45878=PLANE ( 'NONE',  #29315 ) ;
#45881=B_SPLINE_SURFACE_WITH_KNOTS ( 'NONE', 3, 1, ( 
 ( #82001, #27221 ),
 ( #41445, #72402 ),
 ( #33826, #51060 ),
 ( #65312, #81508 ),
 ( #88124, #64813 ),
 ( #26217, #2897 ),
 ( #49567, #65802 ) ),
 .UNSPECIFIED., .F., .F., .F.,
 ( 4, 1, 1, 1, 4 ),
 ( 2, 2 ),
 ( 0.000000000000000000, 0.2499864026691206442, 0.4969648798681433055, 0.7462659243093390238, 1.000000000000000000 ),
 ( 0.000000000000000000, 1.000000000000000000 ),
 .UNSPECIFIED. ) ;
#45895=DIRECTION ( 'NONE',  ( 0.000000000000000000, 1.000000000000000000, -0.000000000000000000 ) ) ;
#45898=DIRECTION ( 'NONE',  ( 0.000000000000000000, 1.000000000000000000, -0.000000000000000000 ) ) ;
#45902=LINE ( 'NONE', #710, #57764 ) ;
#45904=CARTESIAN_POINT ( 'NONE',  ( 0.3849403830293018358, -5.876774720514418959, 20.45311193189268906 ) ) ;
#45905=VECTOR ( 'NONE', #98050, 1000.000000000000000 ) ;
#45914=VERTEX_POINT ( 'NONE', #91710 ) ;
#45929=EDGE_CURVE ( 'NONE', #88329, #44867, #76981, .T. ) ;
#45950=CARTESIAN_POINT ( 'NONE',  ( -4.243469080022288509, -5.876774720514411854, 19.94806476610987644 ) ) ;
#45953=CARTESIAN_POINT ( 'NONE',  ( 10.54059822343757880, -5.876774720514426953, 22.82308057603841078 ) ) ;
#45957=DIRECTION ( 'NONE',  ( 0.000000000000000000, -1.000000000000000000, 0.000000000000000000 ) ) ;
#45964=CARTESIAN_POINT ( 'NONE',  ( 4.627238781264984446, -6.376774720514408301, 19.49219360614394247 ) ) ;
#45972=CARTESIAN_POINT ( 'NONE',  ( 9.405830370894557646, -5.356774720514425603, -24.99732136569351226 ) ) ;
#45979=AXIS2_PLACEMENT_3D ( 'NONE', #4796, #59092, #19011 ) ;
#45989=CARTESIAN_POINT ( 'NONE',  ( 33.00535138976610483, 5.965225279485572685, -12.97242311383961066 ) ) ;
#45991=CARTESIAN_POINT ( 'NONE',  ( 15.77421270221671179, -3.602820947333605250, -28.08718493694522422 ) ) ;
#45997=FACE_BOUND ( 'NONE', #48863, .T. ) ;
#46001=EDGE_CURVE ( 'NONE', #38118, #2589, #93715, .T. ) ;
#46005=EDGE_CURVE ( 'NONE', #3440, #79116, #9487, .T. ) ;
#46014=CARTESIAN_POINT ( 'NONE',  ( -2.794871794871795156, -5.876774720514418071, 20.36318108974359475 ) ) ;
#46018=VECTOR ( 'NONE', #21151, 1000.000000000000000 ) ;
#46019=CARTESIAN_POINT ( 'NONE',  ( -29.49875734969026198, 5.965225279485572685, 0.1180228001186258285 ) ) ;
#46032=CARTESIAN_POINT ( 'NONE',  ( 29.73860345376319003, -4.772774720514425972, -4.021180035027960287 ) ) ;
#46033=CARTESIAN_POINT ( 'NONE',  ( 2.787364042957740651, -6.376774720514424288, 21.14548745790758488 ) ) ;
#46038=ORIENTED_EDGE ( 'NONE', *, *, #60918, .F. ) ;
#46039=( NAMED_UNIT ( * ) PLANE_ANGLE_UNIT ( ) SI_UNIT ( $, .RADIAN. ) );
#46041=CARTESIAN_POINT ( 'NONE',  ( -9.940598223437577374, -6.376774720514426953, 17.91871304725684766 ) ) ;
#46043=DIRECTION ( 'NONE',  ( 0.000000000000000000, 0.000000000000000000, -1.000000000000000000 ) ) ;
#46050=CARTESIAN_POINT ( 'NONE',  ( 4.547289707988324103, -5.876774720514410966, 19.12266226838056582 ) ) ;
#46052=CARTESIAN_POINT ( 'NONE',  ( 15.63605935613269438, 5.965225279485572685, -27.55169773172585934 ) ) ;
#46059=CARTESIAN_POINT ( 'NONE',  ( -5.115065434581078208, -5.876774720514408301, 19.15054976246387497 ) ) ;
#46063=CARTESIAN_POINT ( 'NONE',  ( 22.02124265030973760, 7.743225279485574042, 16.20402280011862217 ) ) ;
#46069=ORIENTED_EDGE ( 'NONE', *, *, #11312, .F. ) ;
#46072=B_SPLINE_CURVE_WITH_KNOTS ( 'NONE', 3,
 ( #86819, #72114, #3110, #10203, #73114, #2605, #65022, #48271, #95936, #64524, #57403, #88331, #3601, #9700, #80718, #95436, #18807, #34546, #79202 ),
 .UNSPECIFIED., .F., .F.,
 ( 4, 1, 1, 1, 1, 1, 1, 1, 1, 1, 1, 1, 1, 1, 1, 1, 4 ),
 ( 0.000000000000000000, 0.07560433049574560860, 0.1479650154827357456, 0.2187969985237000203, 0.2894704453213765016, 0.3597242180874995476, 0.4297077387530455206, 0.5004965198485865630, 0.5744290198679483650, 0.6139472962286703916, 0.6571552698261112768, 0.7039727697209375856, 0.7549389848168005512, 0.8097066112894875101, 0.8688329536985499590, 0.9323854739325975194, 1.000000000000000000 ),
 .UNSPECIFIED. ) ;
#46086=DIRECTION ( 'NONE',  ( 0.000000000000000000, -1.000000000000000000, 0.000000000000000000 ) ) ;
#46091=CARTESIAN_POINT ( 'NONE',  ( 4.931982383686722926, -5.876774720514410077, 19.38944687450761961 ) ) ;
#46098=PLANE ( 'NONE',  #13509 ) ;
#46100=EDGE_LOOP ( 'NONE', ( #33858, #37054, #17748, #92361 ) ) ;
#46115=EDGE_CURVE ( 'NONE', #89719, #74381, #83266, .T. ) ;
#46117=VECTOR ( 'NONE', #37061, 1000.000000000000114 ) ;
#46118=ADVANCED_FACE ( 'NONE', ( #4880 ), #26715, .F. ) ;
#46129=CARTESIAN_POINT ( 'NONE',  ( 28.87399897812680649, -4.772774720514425972, -12.57761096169975623 ) ) ;
#46138=ORIENTED_EDGE ( 'NONE', *, *, #96965, .T. ) ;
#46152=CARTESIAN_POINT ( 'NONE',  ( 33.57588617459661151, -3.431642488465076912, -12.05779067269562255 ) ) ;
#46157=CARTESIAN_POINT ( 'NONE',  ( 3.787259615384621636, -6.376774720514404748, 18.51923076923076650 ) ) ;
#46159=CARTESIAN_POINT ( 'NONE',  ( -0.7067007548136460260, -6.376774720514410077, 19.51517878119693350 ) ) ;
#46166=ORIENTED_EDGE ( 'NONE', *, *, #88846, .F. ) ;
#46170=LINE ( 'NONE', #92329, #18919 ) ;
#46192=CARTESIAN_POINT ( 'NONE',  ( 3.797776442307698286, -5.876774720514427841, 21.83974358974358410 ) ) ;
#46196=CARTESIAN_POINT ( 'NONE',  ( 30.57287095715025416, 6.119174785681471995, 25.41160796525320720 ) ) ;
#46224=EDGE_CURVE ( 'NONE', #15357, #100201, #52052, .T. ) ;
#46227=CARTESIAN_POINT ( 'NONE',  ( 29.68632914399157130, -6.069062472358077720, 27.51067976151145800 ) ) ;
#46235=CIRCLE ( 'NONE', #72180, 251.4258649670780699 ) ;
#46237=CARTESIAN_POINT ( 'NONE',  ( -5.154768636056045850, -5.876774720514414518, 19.48351902941045921 ) ) ;
#46264=DIRECTION ( 'NONE',  ( -0.000000000000000000, 1.000000000000000000, -0.000000000000000000 ) ) ;
#46268=ADVANCED_FACE ( 'NONE', ( #42459 ), #88619, .T. ) ;
#46280=CARTESIAN_POINT ( 'NONE',  ( -3.004714864173751998, -5.876774720514412742, 19.63296556618507083 ) ) ;
#46282=CARTESIAN_POINT ( 'NONE',  ( 5.464387484610083057, -5.876774720514419847, 21.31215092858952431 ) ) ;
#46286=EDGE_CURVE ( 'NONE', #32487, #45617, #96253, .T. ) ;
#46297=AXIS2_PLACEMENT_3D ( 'NONE', #53174, #53674, #75980 ) ;
#46299=ORIENTED_EDGE ( 'NONE', *, *, #27244, .F. ) ;
#46300=DIRECTION ( 'NONE',  ( -1.250865172912931245E-15, 6.879758451021121945E-15, -1.000000000000000000 ) ) ;
#46305=AXIS2_PLACEMENT_3D ( 'NONE', #57340, #87259, #34482 ) ;
#46306=ORIENTED_EDGE ( 'NONE', *, *, #12289, .F. ) ;
#46307=AXIS2_PLACEMENT_3D ( 'NONE', #66012, #57892, #58875 ) ;
#46317=CARTESIAN_POINT ( 'NONE',  ( 3.252808283508203058, -5.876774720514402972, 18.30939203766361345 ) ) ;
#46319=CIRCLE ( 'NONE', #13938, 129.7684398600581233 ) ;
#46322=ORIENTED_EDGE ( 'NONE', *, *, #43272, .T. ) ;
#46324=CARTESIAN_POINT ( 'NONE',  ( -29.49875734969026198, 5.965225279485572685, 2.362022800118626531 ) ) ;
#46338=CARTESIAN_POINT ( 'NONE',  ( 7.460332110455646593, -6.376774720514418959, 20.55293369838740247 ) ) ;
#46341=EDGE_CURVE ( 'NONE', #94971, #37998, #37818, .T. ) ;
#46343=CARTESIAN_POINT ( 'NONE',  ( 7.402957069319889172, -5.876774720514418959, 20.34212842306459024 ) ) ;
#46353=EDGE_CURVE ( 'NONE', #86043, #94109, #81359, .T. ) ;
#46359=VERTEX_POINT ( 'NONE', #76852 ) ;
#46371=DIRECTION ( 'NONE',  ( -0.000000000000000000, 1.000000000000000000, -0.000000000000000000 ) ) ;
#46385=VECTOR ( 'NONE', #90265, 1000.000000000000000 ) ;
#46405=DIRECTION ( 'NONE',  ( 0.9913618264504691080, 7.885106708985488048E-16, -0.1311553622875927805 ) ) ;
#46406=ORIENTED_EDGE ( 'NONE', *, *, #47764, .F. ) ;
#46417=CARTESIAN_POINT ( 'NONE',  ( -29.49875734969025842, -0.3587747205144262708, 23.37402280011862743 ) ) ;
#46426=ORIENTED_EDGE ( 'NONE', *, *, #97352, .F. ) ;
#46428=CARTESIAN_POINT ( 'NONE',  ( -9.278253834636469577, -6.376774720514426953, 21.48128695274316158 ) ) ;
#46432=VERTEX_POINT ( 'NONE', #75370 ) ;
#46436=CARTESIAN_POINT ( 'NONE',  ( -4.533825836049095059, -5.876774720514411854, 19.59623724171353132 ) ) ;
#46440=EDGE_CURVE ( 'NONE', #14898, #24603, #5868, .T. ) ;
#46444=ADVANCED_FACE ( 'NONE', ( #41319 ), #1758, .T. ) ;
#46453=CARTESIAN_POINT ( 'NONE',  ( -29.49875734969026198, -0.3587747205144262708, 0.1180228001186258285 ) ) ;
#46458=CIRCLE ( 'NONE', #83746, 1.325999999999969647 ) ;
#46459=CARTESIAN_POINT ( 'NONE',  ( 31.13709916799238897, -5.945958180706680807, -1.190136329645604230 ) ) ;
#46461=CARTESIAN_POINT ( 'NONE',  ( 9.214646252612421762, -3.316774720514544583, -27.04520690475792222 ) ) ;
#46465=CARTESIAN_POINT ( 'NONE',  ( 25.61870917940689196, -0.3587747205144265483, 29.49402280011862487 ) ) ;
#46470=ORIENTED_EDGE ( 'NONE', *, *, #60948, .T. ) ;
#46473=DIRECTION ( 'NONE',  ( 1.000000000000000000, 0.000000000000000000, 0.000000000000000000 ) ) ;
#46477=EDGE_CURVE ( 'NONE', #98350, #97460, #2767, .T. ) ;
#46492=EDGE_CURVE ( 'NONE', #42771, #404, #78359, .T. ) ;
#46523=CARTESIAN_POINT ( 'NONE',  ( 2.832419239133125544, -5.876774720514422512, 21.23415460623727213 ) ) ;
#46533=CARTESIAN_POINT ( 'NONE',  ( 20.57455539870835182, -3.407774720514426647, -18.22080502500614330 ) ) ;
#46535=VECTOR ( 'NONE', #24752, 1000.000000000000000 ) ;
#46536=B_SPLINE_CURVE_WITH_KNOTS ( 'NONE', 3,
 ( #43282, #74221, #100019, #22895, #76199, #23399, #85826, #47272, #78197, #61996 ),
 .UNSPECIFIED., .F., .F.,
 ( 4, 2, 2, 2, 4 ),
 ( -1.423960876792978737E-05, 0.0005136504108877040049, 0.001041540430543337831, 0.001569430450198971549, 0.002097320469854605483 ),
 .UNSPECIFIED. ) ;
#46541=CARTESIAN_POINT ( 'NONE',  ( 4.653846153846159517, -5.876774720514419847, 19.99999999999999289 ) ) ;
#46550=CARTESIAN_POINT ( 'NONE',  ( -19.80875734969026425, 5.965225279485572685, 31.02402280011862246 ) ) ;
#46556=ORIENTED_EDGE ( 'NONE', *, *, #533, .T. ) ;
#46559=ORIENTED_EDGE ( 'NONE', *, *, #70799, .T. ) ;
#46560=ORIENTED_EDGE ( 'NONE', *, *, #11723, .T. ) ;
#46571=EDGE_CURVE ( 'NONE', #75883, #87540, #35705, .T. ) ;
#46575=ORIENTED_EDGE ( 'NONE', *, *, #6946, .T. ) ;
#46582=ORIENTED_EDGE ( 'NONE', *, *, #35762, .T. ) ;
#46585=VERTEX_POINT ( 'NONE', #88994 ) ;
#46591=LINE ( 'NONE', #77515, #16979 ) ;
#46598=TOROIDAL_SURFACE ( 'NONE', #93568, 253.2618649670780826, 1.835999999999999854 ) ;
#46604=EDGE_CURVE ( 'NONE', #66723, #34190, #96593, .T. ) ;
#46605=VERTEX_POINT ( 'NONE', #28091 ) ;
#46623=DIRECTION ( 'NONE',  ( -0.000000000000000000, -1.000000000000000000, -0.000000000000000000 ) ) ;
#46624=LINE ( 'NONE', #56247, #71926 ) ;
#46637=B_SPLINE_CURVE_WITH_KNOTS ( 'NONE', 3,
 ( #97544, #4206, #36153, #34660, #81328, #97047, #20401, #73224, #26547, #5194, #66130 ),
 .UNSPECIFIED., .F., .F.,
 ( 4, 1, 1, 1, 1, 1, 1, 1, 4 ),
 ( 0.000000000000000000, 0.1105883385953350950, 0.2245417540535963874, 0.3425034940501046066, 0.4643240984173571118, 0.5907560327017662427, 0.7222274753555133486, 0.8588428362087243695, 1.000000000000000000 ),
 .UNSPECIFIED. ) ;
#46643=VERTEX_POINT ( 'NONE', #26596 ) ;
#46645=CARTESIAN_POINT ( 'NONE',  ( -6.100820854657341918, -5.876774720514413630, 19.76359802465961124 ) ) ;
#46648=AXIS2_PLACEMENT_3D ( 'NONE', #20492, #51463, #80907 ) ;
#46654=ORIENTED_EDGE ( 'NONE', *, *, #47939, .F. ) ;
#46660=DIRECTION ( 'NONE',  ( -0.000000000000000000, 0.000000000000000000, -1.000000000000000000 ) ) ;
#46663=CARTESIAN_POINT ( 'NONE',  ( -9.150000000000000355, -5.876774720514426953, -15.69999999999999929 ) ) ;
#46668=VECTOR ( 'NONE', #40397, 1000.000000000000000 ) ;
#46672=CARTESIAN_POINT ( 'NONE',  ( -23.59123376470063960, 6.143225279485574397, 24.50402280011862288 ) ) ;
#46679=ORIENTED_EDGE ( 'NONE', *, *, #37915, .F. ) ;
#46680=EDGE_CURVE ( 'NONE', #46766, #59937, #99479, .T. ) ;
#46691=CARTESIAN_POINT ( 'NONE',  ( 3.004381791450704942, -6.376774720514420736, 20.78526834885430219 ) ) ;
#46700=ORIENTED_EDGE ( 'NONE', *, *, #71886, .F. ) ;
#46705=ORIENTED_EDGE ( 'NONE', *, *, #57570, .F. ) ;
#46716=CARTESIAN_POINT ( 'NONE',  ( 4.967948717948723392, -5.876774720514415407, 20.00140224358974095 ) ) ;
#46737=CARTESIAN_POINT ( 'NONE',  ( 31.65328924465878302, -5.892800044774432422, 28.08003312682333785 ) ) ;
#46745=CARTESIAN_POINT ( 'NONE',  ( -5.533628790199073499, -5.876774720514418071, 19.87297243748313491 ) ) ;
#46762=B_SPLINE_CURVE_WITH_KNOTS ( 'NONE', 3,
 ( #8064, #9561, #448, #8570, #48651, #87189, #33395, #71480, #17173, #39518, #63882, #24292, #94293, #64387, #70470, #31403, #94796, #955, #31905 ),
 .UNSPECIFIED., .F., .F.,
 ( 4, 1, 1, 1, 1, 1, 1, 1, 1, 1, 1, 1, 1, 1, 1, 1, 4 ),
 ( 0.000000000000000000, 0.06523080374203017728, 0.1284048960032230235, 0.1900670715964783708, 0.2509433657682806351, 0.3115458328521427123, 0.3728628021568293205, 0.4350236738562381356, 0.4990717247070431406, 0.5630910750496627148, 0.6255101063303755149, 0.6866800359296488798, 0.7472825030135124003, 0.8085634952159584943, 0.8707421035159862432, 0.9343409515059130088, 1.000000000000000000 ),
 .UNSPECIFIED. ) ;
#46766=VERTEX_POINT ( 'NONE', #13844 ) ;
#46785=CARTESIAN_POINT ( 'NONE',  ( -2.959136224476847765, -5.876774720514413630, 19.53857357749110335 ) ) ;
#46786=CARTESIAN_POINT ( 'NONE',  ( 5.331146515430939203, -5.876774720514419847, 20.91308853528358469 ) ) ;
#46788=VECTOR ( 'NONE', #36545, 1000.000000000000000 ) ;
#46794=VECTOR ( 'NONE', #21103, 1000.000000000000000 ) ;
#46800=EDGE_CURVE ( 'NONE', #26363, #54720, #83860, .T. ) ;
#46802=VECTOR ( 'NONE', #4486, 1000.000000000000000 ) ;
#46804=ADVANCED_FACE ( 'NONE', ( #37194 ), #7227, .F. ) ;
#46809=VERTEX_POINT ( 'NONE', #68149 ) ;
#46817=ORIENTED_EDGE ( 'NONE', *, *, #22863, .T. ) ;
#46818=CARTESIAN_POINT ( 'NONE',  ( -23.62875734969026453, 6.143225279485574397, 24.50402280011862288 ) ) ;
#46820=CARTESIAN_POINT ( 'NONE',  ( -19.77875734969026311, -3.316774720514426456, 27.45402280011862572 ) ) ;
#46823=ORIENTED_EDGE ( 'NONE', *, *, #91704, .T. ) ;
#46825=CARTESIAN_POINT ( 'NONE',  ( 3.183477995988301945, -5.876774720514404748, 18.35601591497023577 ) ) ;
#46839=ORIENTED_EDGE ( 'NONE', *, *, #73631, .F. ) ;
#46846=CARTESIAN_POINT ( 'NONE',  ( 6.429811694900724461, -5.876774720514425177, 21.48000018967326596 ) ) ;
#46848=CARTESIAN_POINT ( 'NONE',  ( 7.107139210497321002, -5.876774720514413630, 19.78447747620696617 ) ) ;
#46850=ORIENTED_EDGE ( 'NONE', *, *, #24568, .F. ) ;
#46851=ORIENTED_EDGE ( 'NONE', *, *, #34078, .T. ) ;
#46859=DIRECTION ( 'NONE',  ( -0.000000000000000000, -1.000000000000000000, -0.000000000000000000 ) ) ;
#46869=EDGE_CURVE ( 'NONE', #97499, #41750, #44321, .T. ) ;
#46872=DIRECTION ( 'NONE',  ( 0.9980236263794188822, 0.000000000000000000, -0.06283980576413539243 ) ) ;
#46874=CARTESIAN_POINT ( 'NONE',  ( -3.826923076923078426, -6.376774720514408301, 19.19230769230769695 ) ) ;
#46883=CARTESIAN_POINT ( 'NONE',  ( 8.000000000000003553, -5.876774720514426953, 0.000000000000000000 ) ) ;
#46888=CARTESIAN_POINT ( 'NONE',  ( 4.639188450898540594, -6.376774720514418959, 20.39229233339611014 ) ) ;
#46901=CARTESIAN_POINT ( 'NONE',  ( -7.640476926272304681, -6.376774720514415407, 20.25188360057253689 ) ) ;
#46907=DIRECTION ( 'NONE',  ( 0.7512896232465892110, 0.000000000000000000, 0.6599726524652350657 ) ) ;
#46908=ORIENTED_EDGE ( 'NONE', *, *, #91847, .F. ) ;
#46911=CARTESIAN_POINT ( 'NONE',  ( -19.37210865224160017, 5.965225279485592225, -21.60955166348795586 ) ) ;
#46926=AXIS2_PLACEMENT_3D ( 'NONE', #34682, #72753, #89466 ) ;
#46927=CARTESIAN_POINT ( 'NONE',  ( 9.940598223437577374, -6.376774720514426953, 22.08128695274315945 ) ) ;
#46929=ORIENTED_EDGE ( 'NONE', *, *, #62159, .T. ) ;
#46935=VECTOR ( 'NONE', #57066, 1000.000000000000000 ) ;
#46938=DIRECTION ( 'NONE',  ( 1.955152872784845154E-15, 1.000000000000000000, -3.740001113483016365E-15 ) ) ;
#46939=CARTESIAN_POINT ( 'NONE',  ( -4.147110899021980934, -5.876774720514418071, 20.45311193189268906 ) ) ;
#46943=ORIENTED_EDGE ( 'NONE', *, *, #87867, .F. ) ;
#46949=CARTESIAN_POINT ( 'NONE',  ( -28.32169924589829080, -0.3587747205143964613, -8.244178532169451401 ) ) ;
#46955=VECTOR ( 'NONE', #44809, 1000.000000000000000 ) ;
#46957=ORIENTED_EDGE ( 'NONE', *, *, #20955, .T. ) ;
#46967=CARTESIAN_POINT ( 'NONE',  ( 10.22845072388260768, -5.356774720514425603, -24.98266432381545954 ) ) ;
#46977=DIRECTION ( 'NONE',  ( 0.000000000000000000, 0.000000000000000000, 1.000000000000000000 ) ) ;
#46978=ORIENTED_EDGE ( 'NONE', *, *, #87257, .F. ) ;
#46988=ORIENTED_EDGE ( 'NONE', *, *, #34691, .F. ) ;
#46999=DIRECTION ( 'NONE',  ( 0.000000000000000000, -1.000000000000000000, 0.000000000000000000 ) ) ;
#47001=AXIS2_PLACEMENT_3D ( 'NONE', #39315, #46938, #54065 ) ;
#47004=ADVANCED_FACE ( 'NONE', ( #40695 ), #71148, .F. ) ;
#47012=CARTESIAN_POINT ( 'NONE',  ( 30.09341516180546350, 1.477225279485574028, -11.39311774897855933 ) ) ;
#47017=ORIENTED_EDGE ( 'NONE', *, *, #75034, .T. ) ;
#47030=FACE_OUTER_BOUND ( 'NONE', #73024, .T. ) ;
#47032=LINE ( 'NONE', #21665, #14905 ) ;
#47045=ORIENTED_EDGE ( 'NONE', *, *, #56427, .F. ) ;
#47054=DIRECTION ( 'NONE',  ( 0.1875268396392987258, 0.000000000000000000, 0.9822594791677485837 ) ) ;
#47059=CARTESIAN_POINT ( 'NONE',  ( -5.023036858974360364, -5.876774720514408301, 19.14743589743590491 ) ) ;
#47062=ORIENTED_EDGE ( 'NONE', *, *, #69130, .T. ) ;
#47064=CARTESIAN_POINT ( 'NONE',  ( 30.53060340732036337, -5.329285123471891872, 3.289350009555732868 ) ) ;
#47075=ORIENTED_EDGE ( 'NONE', *, *, #26088, .T. ) ;
#47080=CARTESIAN_POINT ( 'NONE',  ( 4.281720980632043094, -6.376774720514408301, 18.71132571341777151 ) ) ;
#47092=CARTESIAN_POINT ( 'NONE',  ( 13.91401389203221406, -0.3587747205144265483, 158.0376437107427137 ) ) ;
#47097=FACE_OUTER_BOUND ( 'NONE', #93433, .T. ) ;
#47102=DIRECTION ( 'NONE',  ( 0.000000000000000000, -1.000000000000000000, 0.000000000000000000 ) ) ;
#47119=CARTESIAN_POINT ( 'NONE',  ( -0.02075734969026423599, 5.965225279485572685, -28.54397719988136828 ) ) ;
#47121=FACE_OUTER_BOUND ( 'NONE', #39672, .T. ) ;
#47122=ORIENTED_EDGE ( 'NONE', *, *, #52101, .T. ) ;
#47126=CARTESIAN_POINT ( 'NONE',  ( -29.49875734969026198, 5.965225279485572685, 2.362022800118626531 ) ) ;
#47127=CARTESIAN_POINT ( 'NONE',  ( 3.797776442307698286, -6.376774720514401196, 18.16025641025640525 ) ) ;
#47131=DIRECTION ( 'NONE',  ( 0.000000000000000000, 0.000000000000000000, 1.000000000000000000 ) ) ;
#47133=CARTESIAN_POINT ( 'NONE',  ( -20.27875734969026311, 7.743225279485574042, 24.00402280011862288 ) ) ;
#47143=ORIENTED_EDGE ( 'NONE', *, *, #52231, .F. ) ;
#47162=CARTESIAN_POINT ( 'NONE',  ( -0.9540731552372990754, -6.376774720514411854, 19.74568812963596542 ) ) ;
#47167=DIRECTION ( 'NONE',  ( 0.000000000000000000, 1.000000000000000000, -0.000000000000000000 ) ) ;
#47175=FACE_OUTER_BOUND ( 'NONE', #91267, .T. ) ;
#47183=ORIENTED_EDGE ( 'NONE', *, *, #43781, .F. ) ;
#47185=CARTESIAN_POINT ( 'NONE',  ( -7.318926569091948942, -5.876774720514417183, 20.09505574050193033 ) ) ;
#47187=CARTESIAN_POINT ( 'NONE',  ( 26.73860345374794534, -5.356774720496559894, 3.440769881205036427E-15 ) ) ;
#47192=CARTESIAN_POINT ( 'NONE',  ( 30.93860345374796594, 6.475225279485573360, 19.84760796525321780 ) ) ;
#47194=ORIENTED_EDGE ( 'NONE', *, *, #72810, .T. ) ;
#47199=CARTESIAN_POINT ( 'NONE',  ( -4.752075056065355518, -5.876774720514406525, 19.17724329193115551 ) ) ;
#47204=ORIENTED_EDGE ( 'NONE', *, *, #32369, .T. ) ;
#47205=CARTESIAN_POINT ( 'NONE',  ( 27.86270917940689174, -0.3587747205144265483, 29.49402280011862487 ) ) ;
#47209=CARTESIAN_POINT ( 'NONE',  ( 25.06060784212036907, -5.114160763660862585, -9.130698857930203971 ) ) ;
#47214=CARTESIAN_POINT ( 'NONE',  ( -13.36367879947601445, -5.876774720514426953, 20.00000000000000355 ) ) ;
#47215=VERTEX_POINT ( 'NONE', #72154 ) ;
#47230=VERTEX_POINT ( 'NONE', #31343 ) ;
#47236=CARTESIAN_POINT ( 'NONE',  ( 33.12653832968932477, 5.965225279485572685, -7.315055336576597789 ) ) ;
#47238=CARTESIAN_POINT ( 'NONE',  ( 29.73860345376316872, -5.356774720514427379, 17.30421508979847189 ) ) ;
#47250=CARTESIAN_POINT ( 'NONE',  ( 2.905472630834636139, -5.876774720514415407, 19.87563926270137671 ) ) ;
#47253=FACE_OUTER_BOUND ( 'NONE', #1683, .T. ) ;
#47269=DIRECTION ( 'NONE',  ( -1.000000000000000000, 0.000000000000000000, 0.000000000000000000 ) ) ;
#47272=CARTESIAN_POINT ( 'NONE',  ( 32.04341656622251122, -4.806217029847265287, -4.198923130344409671 ) ) ;
#47273=CARTESIAN_POINT ( 'NONE',  ( -1.653359744423585465, -5.876774720514413630, 19.34586827028017098 ) ) ;
#47281=ORIENTED_EDGE ( 'NONE', *, *, #15169, .T. ) ;
#47297=ADVANCED_FACE ( 'NONE', ( #34354 ), #64330, .F. ) ;
#47311=CARTESIAN_POINT ( 'NONE',  ( -29.49875734969025842, -0.3587747205144265483, 25.61802280011862720 ) ) ;
#47313=VERTEX_POINT ( 'NONE', #26736 ) ;
#47314=VERTEX_POINT ( 'NONE', #17116 ) ;
#47317=CARTESIAN_POINT ( 'NONE',  ( 7.010993867624484288, -6.376774720514417183, 20.34381700913260715 ) ) ;
#47347=ORIENTED_EDGE ( 'NONE', *, *, #73163, .F. ) ;
#47350=EDGE_LOOP ( 'NONE', ( #57424, #83637, #94751, #1563 ) ) ;
#47351=ORIENTED_EDGE ( 'NONE', *, *, #6847, .F. ) ;
#47357=CIRCLE ( 'NONE', #78115, 0.8159999999999660858 ) ;
#47363=EDGE_CURVE ( 'NONE', #56601, #89282, #28078, .T. ) ;
#47368=CARTESIAN_POINT ( 'NONE',  ( 5.395440699609677537, 5.965225279485594001, -28.51842087987364138 ) ) ;
#47375=EDGE_CURVE ( 'NONE', #15961, #82260, #63828, .T. ) ;
#47377=VECTOR ( 'NONE', #67627, 1000.000000000000000 ) ;
#47380=LINE ( 'NONE', #694, #83350 ) ;
#47382=ORIENTED_EDGE ( 'NONE', *, *, #7474, .T. ) ;
#47400=CARTESIAN_POINT ( 'NONE',  ( -23.59123376470063960, 6.143225279485574397, 24.50402280011862288 ) ) ;
#47417=ORIENTED_EDGE ( 'NONE', *, *, #12453, .F. ) ;
#47441=CARTESIAN_POINT ( 'NONE',  ( -25.92875734969026524, -5.356774720514425603, 0.7300228001186309656 ) ) ;
#47446=FACE_OUTER_BOUND ( 'NONE', #44691, .T. ) ;
#47456=VERTEX_POINT ( 'NONE', #98733 ) ;
#47463=VERTEX_POINT ( 'NONE', #50085 ) ;
#47465=DIRECTION ( 'NONE',  ( -1.286817348990133655E-16, 0.000000000000000000, 1.000000000000000000 ) ) ;
#47466=DIRECTION ( 'NONE',  ( -0.000000000000000000, -1.000000000000000000, -0.000000000000000000 ) ) ;
#47478=DIRECTION ( 'NONE',  ( 0.000000000000000000, 0.000000000000000000, -1.000000000000000000 ) ) ;
#47504=CARTESIAN_POINT ( 'NONE',  ( -2.794871794871795156, -5.876774720514415407, 20.36318108974359475 ) ) ;
#47507=CARTESIAN_POINT ( 'NONE',  ( 13.91401389203221406, -6.376774720514426953, 28.26920385068457264 ) ) ;
#47533=CARTESIAN_POINT ( 'NONE',  ( 4.215004826710222474, -5.876774720514426953, 21.34072927444733381 ) ) ;
#47540=PLANE ( 'NONE',  #61448 ) ;
#47543=EDGE_CURVE ( 'NONE', #92467, #14570, #96744, .T. ) ;
#47550=CARTESIAN_POINT ( 'NONE',  ( 4.653733606810938284, -5.876774720514412742, 19.95301661664751336 ) ) ;
#47569=EDGE_LOOP ( 'NONE', ( #30213, #4925, #34281, #61542, #16111 ) ) ;
#47578=DIRECTION ( 'NONE',  ( -0.000000000000000000, 1.000000000000000000, -0.000000000000000000 ) ) ;
#47581=CARTESIAN_POINT ( 'NONE',  ( 3.825970207471427020, -6.376774720514402972, 18.52126221587801780 ) ) ;
#47586=VECTOR ( 'NONE', #92587, 1000.000000000000000 ) ;
#47592=ORIENTED_EDGE ( 'NONE', *, *, #97236, .F. ) ;
#47595=ORIENTED_EDGE ( 'NONE', *, *, #22042, .F. ) ;
#47606=ORIENTED_EDGE ( 'NONE', *, *, #90467, .T. ) ;
#47615=DIRECTION ( 'NONE',  ( -0.000000000000000000, 1.000000000000000000, -0.000000000000000000 ) ) ;
#47630=EDGE_CURVE ( 'NONE', #92987, #30745, #91229, .T. ) ;
#47643=CARTESIAN_POINT ( 'NONE',  ( 1.175186991919855872, -6.376774720514426953, 28.89597625626659649 ) ) ;
#47646=DIRECTION ( 'NONE',  ( -0.000000000000000000, -1.000000000000000000, -0.000000000000000000 ) ) ;
#47647=CARTESIAN_POINT ( 'NONE',  ( -5.960145391809922089, -6.376774720514415407, 20.04104409779160534 ) ) ;
#47653=CARTESIAN_POINT ( 'NONE',  ( 19.75748517575715368, -0.3587747205144265483, 28.87153971905864580 ) ) ;
#47666=EDGE_CURVE ( 'NONE', #29733, #70312, #18494, .T. ) ;
#47668=ORIENTED_EDGE ( 'NONE', *, *, #53162, .T. ) ;
#47676=CARTESIAN_POINT ( 'NONE',  ( 32.45853543194704116, 5.965225279485572685, 9.169203677920338080 ) ) ;
#47690=CARTESIAN_POINT ( 'NONE',  ( -28.47875734969025885, 5.965225279485572685, -0.08597719988137300651 ) ) ;
#47694=ORIENTED_EDGE ( 'NONE', *, *, #15668, .T. ) ;
#47700=CARTESIAN_POINT ( 'NONE',  ( -4.620655831143558601, -5.876774720514410077, 19.21747685089457036 ) ) ;
#47712=CARTESIAN_POINT ( 'NONE',  ( 31.63608488009066733, -3.316774720514426456, 27.34773273846990094 ) ) ;
#47715=EDGE_CURVE ( 'NONE', #26949, #99423, #10381, .T. ) ;
#47722=VERTEX_POINT ( 'NONE', #86007 ) ;
#47731=CARTESIAN_POINT ( 'NONE',  ( 3.004381791450704942, -5.876774720514419847, 20.78526834885430219 ) ) ;
#47735=FACE_OUTER_BOUND ( 'NONE', #25710, .T. ) ;
#47739=CARTESIAN_POINT ( 'NONE',  ( 31.62831224182126988, -4.127879075750807480, 27.04291028225966542 ) ) ;
#47741=CIRCLE ( 'NONE', #25049, 0.3000000000000016542 ) ;
#47752=ORIENTED_EDGE ( 'NONE', *, *, #22778, .F. ) ;
#47764=EDGE_CURVE ( 'NONE', #5650, #34190, #69116, .T. ) ;
#47791=DIRECTION ( 'NONE',  ( -0.6392559695863502256, 6.454799914155189828E-16, -0.7689940216596065081 ) ) ;
#47805=EDGE_CURVE ( 'NONE', #83635, #27797, #89652, .T. ) ;
#47806=CARTESIAN_POINT ( 'NONE',  ( 6.763596848542221984, -5.876774720514426065, 21.40271460634751577 ) ) ;
#47807=ORIENTED_EDGE ( 'NONE', *, *, #4355, .F. ) ;
#47811=DIRECTION ( 'NONE',  ( -1.000000000000000000, -0.000000000000000000, 0.000000000000000000 ) ) ;
#47817=CARTESIAN_POINT ( 'NONE',  ( 5.627902640648289712, -6.376774720514413630, 20.02890049923285787 ) ) ;
#47821=EDGE_CURVE ( 'NONE', #34695, #68647, #19488, .T. ) ;
#47822=DIRECTION ( 'NONE',  ( 1.330598087067427724E-14, 0.000000000000000000, -1.000000000000000000 ) ) ;
#47825=EDGE_CURVE ( 'NONE', #94137, #83680, #51451, .T. ) ;
#47828=PLANE ( 'NONE',  #44879 ) ;
#47830=CARTESIAN_POINT ( 'NONE',  ( 33.25738712673413033, -4.772289986317655774, -12.75102155484566424 ) ) ;
#47835=AXIS2_PLACEMENT_3D ( 'NONE', #58137, #2345, #11443 ) ;
#47840=ORIENTED_EDGE ( 'NONE', *, *, #71144, .T. ) ;
#47852=B_SPLINE_CURVE_WITH_KNOTS ( 'NONE', 3,
 ( #41714, #9742, #72654, #40697, #34091, #65064, #26479, #88371, #18850, #4637, #58435, #89865, #67540, #21833, #27479, #50814, #52809, #98964, #36570 ),
 .UNSPECIFIED., .F., .F.,
 ( 4, 1, 1, 1, 1, 1, 1, 1, 1, 1, 1, 1, 1, 1, 1, 1, 4 ),
 ( 0.000000000000000000, 0.06184170298390879311, 0.1212623730944467210, 0.1807459488653150592, 0.2392309018221055461, 0.2983075587884643221, 0.3581827976158475924, 0.4203592307800689265, 0.4847924155141841718, 0.5499384837666866366, 0.6137182775404276258, 0.6766807072496321407, 0.7391541704483172159, 0.8021997032403536121, 0.8667401776163008442, 0.9320496524002468419, 1.000000000000000000 ),
 .UNSPECIFIED. ) ;
#47853=ORIENTED_EDGE ( 'NONE', *, *, #35066, .F. ) ;
#47855=DIRECTION ( 'NONE',  ( 0.000000000000000000, 0.000000000000000000, 1.000000000000000000 ) ) ;
#47866=DIRECTION ( 'NONE',  ( -0.9685340172660600322, 0.000000000000000000, 0.2488812114211667315 ) ) ;
#47867=CARTESIAN_POINT ( 'NONE',  ( 31.79364159983995464, -2.682774720514426559, -11.59305536555894278 ) ) ;
#47876=CARTESIAN_POINT ( 'NONE',  ( 4.948291700218025113, -6.376774720514418959, 20.47145334051262111 ) ) ;
#47880=FACE_OUTER_BOUND ( 'NONE', #10030, .T. ) ;
#47890=CARTESIAN_POINT ( 'NONE',  ( 4.547994309883463870, -6.376774720514422512, 20.87593061325451416 ) ) ;
#47909=AXIS2_PLACEMENT_3D ( 'NONE', #46927, #31188, #93086 ) ;
#47910=ORIENTED_EDGE ( 'NONE', *, *, #68203, .F. ) ;
#47917=AXIS2_PLACEMENT_3D ( 'NONE', #83274, #6150, #12755 ) ;
#47918=FACE_OUTER_BOUND ( 'NONE', #89864, .T. ) ;
#47919=VECTOR ( 'NONE', #18692, 1000.000000000000000 ) ;
#47935=ORIENTED_EDGE ( 'NONE', *, *, #69471, .F. ) ;
#47936=CARTESIAN_POINT ( 'NONE',  ( 3.052815417670126319, -6.376774720514406525, 18.46676085997033923 ) ) ;
#47937=ADVANCED_FACE ( 'NONE', ( #30593 ), #60528, .T. ) ;
#47938=VERTEX_POINT ( 'NONE', #30092 ) ;
#47939=EDGE_CURVE ( 'NONE', #54059, #12619, #75761, .T. ) ;
#47940=ORIENTED_EDGE ( 'NONE', *, *, #87635, .T. ) ;
#47943=CARTESIAN_POINT ( 'NONE',  ( -4.194375271223358403, -5.876774720514417183, 20.09898898868106087 ) ) ;
#47953=LINE ( 'NONE', #46949, #93412 ) ;
#47954=CARTESIAN_POINT ( 'NONE',  ( -1.456683411003494966, -5.876774720514416295, 19.95737465391042775 ) ) ;
#47960=CARTESIAN_POINT ( 'NONE',  ( 0.3910256410256418569, -6.376774720514420736, 20.67377804487180271 ) ) ;
#47962=ORIENTED_EDGE ( 'NONE', *, *, #3873, .F. ) ;
#47975=DIRECTION ( 'NONE',  ( -0.000000000000000000, -1.000000000000000000, -0.000000000000000000 ) ) ;
#47987=CARTESIAN_POINT ( 'NONE',  ( 29.73860345376318293, -5.356774720514426491, 17.72811386545585322 ) ) ;
#47988=VERTEX_POINT ( 'NONE', #79767 ) ;
#47990=CARTESIAN_POINT ( 'NONE',  ( 15.52291915823243507, -3.595107466738250768, -28.22347026866546216 ) ) ;
#47993=AXIS2_PLACEMENT_3D ( 'NONE', #49273, #88317, #57883 ) ;
#48004=CARTESIAN_POINT ( 'NONE',  ( -5.824076695599092801, -5.876774720514412742, 19.72913074730691108 ) ) ;
#48005=EDGE_LOOP ( 'NONE', ( #20000, #37937, #46575, #90684 ) ) ;
#48019=CARTESIAN_POINT ( 'NONE',  ( 4.740341618695937065, -5.876774720514404748, 18.75174579344860248 ) ) ;
#48020=CARTESIAN_POINT ( 'NONE',  ( 11.56983764158150407, -6.376774720514426953, 28.29037853177889517 ) ) ;
#48031=CARTESIAN_POINT ( 'NONE',  ( 2.590395174287518643, -5.876774720514416295, 20.05492615153064762 ) ) ;
#48042=CARTESIAN_POINT ( 'NONE',  ( 4.878909776184770742E-15, -5.876774720514426953, 22.50000000000000355 ) ) ;
#48047=CARTESIAN_POINT ( 'NONE',  ( 4.486687842132109694, -5.876774720514410077, 18.98221446873611029 ) ) ;
#48055=AXIS2_PLACEMENT_3D ( 'NONE', #80204, #39634, #41655 ) ;
#48060=CARTESIAN_POINT ( 'NONE',  ( 14.76093561896379214, 5.965225279485572685, -26.55548769130089681 ) ) ;
#48061=ORIENTED_EDGE ( 'NONE', *, *, #4355, .T. ) ;
#48062=VECTOR ( 'NONE', #71028, 1000.000000000000000 ) ;
#48065=ORIENTED_EDGE ( 'NONE', *, *, #12644, .F. ) ;
#48066=AXIS2_PLACEMENT_3D ( 'NONE', #21461, #20474, #28599 ) ;
#48073=EDGE_CURVE ( 'NONE', #47456, #57568, #9636, .T. ) ;
#48080=CARTESIAN_POINT ( 'NONE',  ( 4.613443512364428400, -6.376774720514411854, 19.38647409819875733 ) ) ;
#48082=VERTEX_POINT ( 'NONE', #12746 ) ;
#48092=DIRECTION ( 'NONE',  ( -0.000000000000000000, -1.000000000000000000, -0.000000000000000000 ) ) ;
#48101=ORIENTED_EDGE ( 'NONE', *, *, #60245, .F. ) ;
#48107=ORIENTED_EDGE ( 'NONE', *, *, #34498, .F. ) ;
#48108=ORIENTED_EDGE ( 'NONE', *, *, #7647, .T. ) ;
#48111=DIRECTION ( 'NONE',  ( 0.02119372647572909107, 0.000000000000000000, 0.9997753877537054468 ) ) ;
#48116=DIRECTION ( 'NONE',  ( 0.000000000000000000, 0.000000000000000000, 1.000000000000000000 ) ) ;
#48117=CARTESIAN_POINT ( 'NONE',  ( -7.064692883725313344, -6.376774720514411854, 19.55266968305501862 ) ) ;
#48123=CARTESIAN_POINT ( 'NONE',  ( -5.554587162835583847, -6.376774720514417183, 19.99258394656885329 ) ) ;
#48125=CARTESIAN_POINT ( 'NONE',  ( 0.000000000000000000, -2.056774720514426669, 0.000000000000000000 ) ) ;
#48131=DIRECTION ( 'NONE',  ( 0.9161084732596779245, 5.365801633547218220E-16, -0.4009304992412300317 ) ) ;
#48143=AXIS2_PLACEMENT_3D ( 'NONE', #51341, #98489, #28990 ) ;
#48146=ORIENTED_EDGE ( 'NONE', *, *, #12471, .F. ) ;
#48147=CARTESIAN_POINT ( 'NONE',  ( 22.02124265030973760, 7.743225279485574042, 16.20402280011862217 ) ) ;
#48149=CARTESIAN_POINT ( 'NONE',  ( -6.602379858799704238, -5.876774720514410077, 19.46575348430202723 ) ) ;
#48150=CARTESIAN_POINT ( 'NONE',  ( -28.98875734969026396, 5.965225279485572685, 2.362022800118626531 ) ) ;
#48155=ORIENTED_EDGE ( 'NONE', *, *, #74122, .F. ) ;
#48166=CARTESIAN_POINT ( 'NONE',  ( -24.90875734969025501, 5.965225279485572685, 30.00402280011862288 ) ) ;
#48186=ORIENTED_EDGE ( 'NONE', *, *, #63416, .T. ) ;
#48190=DIRECTION ( 'NONE',  ( -0.4009304992412306978, 6.454799914155190814E-16, -0.9161084732596777025 ) ) ;
#48202=AXIS2_PLACEMENT_3D ( 'NONE', #26845, #19714, #57812 ) ;
#48204=CARTESIAN_POINT ( 'NONE',  ( -6.775140224358976226, -5.876774720514408301, 19.14743589743590846 ) ) ;
#48209=ORIENTED_EDGE ( 'NONE', *, *, #87257, .T. ) ;
#48210=CARTESIAN_POINT ( 'NONE',  ( 6.646494591716556322, -3.316774720514426900, -28.33840132637671161 ) ) ;
#48221=ORIENTED_EDGE ( 'NONE', *, *, #41708, .T. ) ;
#48240=AXIS2_PLACEMENT_3D ( 'NONE', #32225, #71808, #63201 ) ;
#48242=DIRECTION ( 'NONE',  ( 0.000000000000000000, -1.000000000000000000, 0.000000000000000000 ) ) ;
#48254=PLANE ( 'NONE',  #44153 ) ;
#48260=CARTESIAN_POINT ( 'NONE',  ( 14.45468597507908903, -3.471643246632547974, -28.36588305008921651 ) ) ;
#48265=AXIS2_PLACEMENT_3D ( 'NONE', #28901, #12671, #97415 ) ;
#48271=CARTESIAN_POINT ( 'NONE',  ( -7.421417143192116761, -5.876774720514411854, 19.43823095447975291 ) ) ;
#48285=LINE ( 'NONE', #25434, #46802 ) ;
#48288=FACE_OUTER_BOUND ( 'NONE', #97763, .T. ) ;
#48303=ORIENTED_EDGE ( 'NONE', *, *, #93676, .T. ) ;
#48311=CARTESIAN_POINT ( 'NONE',  ( 7.111284305517425075, -5.876774720514421624, 21.05363841023157434 ) ) ;
#48314=EDGE_LOOP ( 'NONE', ( #19741, #10387, #35319, #54818, #36948 ) ) ;
#48323=CARTESIAN_POINT ( 'NONE',  ( 6.058092820189922456, -5.876774720514413630, 19.77091638250125882 ) ) ;
#48328=CARTESIAN_POINT ( 'NONE',  ( 22.02124265030973760, 6.143225279485574397, 16.20402280011862217 ) ) ;
#48338=ORIENTED_EDGE ( 'NONE', *, *, #68355, .F. ) ;
#48339=EDGE_LOOP ( 'NONE', ( #43875, #67639, #73215, #63391, #55594, #19122, #885, #60026, #20840, #37077, #17117, #55657, #97363, #55136, #23600 ) ) ;
#48342=ORIENTED_EDGE ( 'NONE', *, *, #29700, .F. ) ;
#48356=DIRECTION ( 'NONE',  ( 0.000000000000000000, 0.000000000000000000, 1.000000000000000000 ) ) ;
#48359=VECTOR ( 'NONE', #53776, 1000.000000000000000 ) ;
#48360=VERTEX_POINT ( 'NONE', #84259 ) ;
#48361=CARTESIAN_POINT ( 'NONE',  ( -0.02075734969026423599, 5.965225279485572685, -0.08597719988137648983 ) ) ;
#48367=FACE_OUTER_BOUND ( 'NONE', #78778, .T. ) ;
#48377=CARTESIAN_POINT ( 'NONE',  ( 4.780030342074717886, -5.876774720514423400, 21.16398229115527130 ) ) ;
#48406=ADVANCED_FACE ( 'NONE', ( #1542 ), #23858, .F. ) ;
#48413=ORIENTED_EDGE ( 'NONE', *, *, #9893, .F. ) ;
#48420=EDGE_CURVE ( 'NONE', #41980, #63083, #52059, .T. ) ;
#48423=EDGE_LOOP ( 'NONE', ( #98124, #25763, #3627, #8997 ) ) ;
#48432=EDGE_CURVE ( 'NONE', #24870, #25405, #99337, .T. ) ;
#48438=EDGE_CURVE ( 'NONE', #6989, #16640, #70150, .T. ) ;
#48439=DIRECTION ( 'NONE',  ( 0.000000000000000000, 0.000000000000000000, 1.000000000000000000 ) ) ;
#48441=CARTESIAN_POINT ( 'NONE',  ( 3.797776442307698286, -6.376774720514401196, 18.16025641025640525 ) ) ;
#48442=ORIENTED_EDGE ( 'NONE', *, *, #77473, .F. ) ;
#48444=DIRECTION ( 'NONE',  ( -1.000000000000000000, -8.503546450866701308E-16, 0.000000000000000000 ) ) ;
#48448=ADVANCED_FACE ( 'NONE', ( #43105 ), #66466, .F. ) ;
#48452=CARTESIAN_POINT ( 'NONE',  ( 27.86270917940689174, 5.965225279485572685, 29.02104833056109001 ) ) ;
#48457=CARTESIAN_POINT ( 'NONE',  ( -1.371775545366004545, -5.876774720514414518, 20.39230070883894186 ) ) ;
#48459=ADVANCED_FACE ( 'NONE', ( #42614 ), #58335, .F. ) ;
#48460=CARTESIAN_POINT ( 'NONE',  ( -29.49875734969026198, 5.965225279485572685, 2.362022800118626531 ) ) ;
#48466=ORIENTED_EDGE ( 'NONE', *, *, #49680, .T. ) ;
#48471=CARTESIAN_POINT ( 'NONE',  ( 9.150000000000000355, -5.876774720514426953, -15.70000000000000284 ) ) ;
#48475=AXIS2_PLACEMENT_3D ( 'NONE', #64168, #9845, #64673 ) ;
#48480=CARTESIAN_POINT ( 'NONE',  ( 0.000000000000000000, -2.056774720514426669, 4.299999999999999822 ) ) ;
#48488=CARTESIAN_POINT ( 'NONE',  ( -6.377963355984652694, -6.376774720514411854, 19.53740760792478426 ) ) ;
#48491=AXIS2_PLACEMENT_3D ( 'NONE', #11579, #16819, #3985 ) ;
#48492=DIRECTION ( 'NONE',  ( 0.000000000000000000, -1.000000000000000000, 0.000000000000000000 ) ) ;
#48504=LINE ( 'NONE', #80941, #57897 ) ;
#48507=DIRECTION ( 'NONE',  ( 0.000000000000000000, -1.000000000000000000, 0.000000000000000000 ) ) ;
#48508=VERTEX_POINT ( 'NONE', #4548 ) ;
#48516=CIRCLE ( 'NONE', #51769, 2.499999999999995115 ) ;
#48520=CARTESIAN_POINT ( 'NONE',  ( -2.772696838893043747, -5.876774720514414518, 19.95463486386180207 ) ) ;
#48534=EDGE_CURVE ( 'NONE', #36610, #17395, #49728, .T. ) ;
#48539=ADVANCED_FACE ( 'NONE', ( #26374 ), #19249, .F. ) ;
#48543=CARTESIAN_POINT ( 'NONE',  ( 4.415069475862049231, -5.876774720514423400, 21.13806644168711557 ) ) ;
#48561=VECTOR ( 'NONE', #99936, 1000.000000000000000 ) ;
#48566=AXIS2_PLACEMENT_3D ( 'NONE', #84219, #87738, #16213 ) ;
#48567=DIRECTION ( 'NONE',  ( 0.000000000000000000, 0.000000000000000000, 1.000000000000000000 ) ) ;
#48571=CARTESIAN_POINT ( 'NONE',  ( 22.81105451610979173, 8.475225279485572472, -18.46691820600746681 ) ) ;
#48578=ORIENTED_EDGE ( 'NONE', *, *, #42349, .T. ) ;
#48582=CARTESIAN_POINT ( 'NONE',  ( 2.922108196329484375, -6.376774720514417183, 20.36383711510645256 ) ) ;
#48591=CARTESIAN_POINT ( 'NONE',  ( 3.903461913076534451, -5.876774720514405637, 18.52532880998198905 ) ) ;
#48595=CARTESIAN_POINT ( 'NONE',  ( 27.53860345374808105, -1.682774720514426114, -1.272392034746785860 ) ) ;
#48598=EDGE_CURVE ( 'NONE', #87115, #51471, #73060, .T. ) ;
#48603=CARTESIAN_POINT ( 'NONE',  ( -28.98875734969026396, 5.965225279485572685, 10.11402280011862587 ) ) ;
#48607=DIRECTION ( 'NONE',  ( -0.000000000000000000, 0.000000000000000000, -1.000000000000000000 ) ) ;
#48611=DIRECTION ( 'NONE',  ( 1.000000000000000000, 0.000000000000000000, 0.000000000000000000 ) ) ;
#48618=VECTOR ( 'NONE', #58724, 1000.000000000000000 ) ;
#48646=EDGE_CURVE ( 'NONE', #25101, #1158, #27601, .T. ) ;
#48651=CARTESIAN_POINT ( 'NONE',  ( 6.058092820189922456, -6.376774720514413630, 19.77091638250125882 ) ) ;
#48652=EDGE_CURVE ( 'NONE', #89282, #47313, #66949, .T. ) ;
#48658=EDGE_CURVE ( 'NONE', #1547, #5151, #37977, .T. ) ;
#48666=EDGE_CURVE ( 'NONE', #88122, #59933, #24881, .T. ) ;
#48669=EDGE_CURVE ( 'NONE', #22711, #99954, #83182, .T. ) ;
#48670=CARTESIAN_POINT ( 'NONE',  ( 5.949073730962466833, 6.475225279485573360, -27.94053387008862188 ) ) ;
#48691=DIRECTION ( 'NONE',  ( 0.000000000000000000, 0.000000000000000000, 1.000000000000000000 ) ) ;
#48693=EDGE_LOOP ( 'NONE', ( #62171, #90212, #80436, #41005 ) ) ;
#48698=CARTESIAN_POINT ( 'NONE',  ( -1.653359744423585465, -5.876774720514412742, 19.34586827028017098 ) ) ;
#48712=AXIS2_PLACEMENT_3D ( 'NONE', #76548, #69457, #949 ) ;
#48714=CARTESIAN_POINT ( 'NONE',  ( -6.072964844751159497, -6.376774720514410077, 19.44316438561912008 ) ) ;
#48720=CARTESIAN_POINT ( 'NONE',  ( 5.959527149828093506, -3.316774720514425567, -28.45540529974545407 ) ) ;
#48730=CARTESIAN_POINT ( 'NONE',  ( 4.780030342074717886, -5.876774720514424288, 21.16398229115527130 ) ) ;
#48732=ORIENTED_EDGE ( 'NONE', *, *, #77808, .T. ) ;
#48748=CARTESIAN_POINT ( 'NONE',  ( -2.243088942307695177, -6.376774720514408301, 19.14743589743590491 ) ) ;
#48754=CARTESIAN_POINT ( 'NONE',  ( -9.940598223437573822, -5.876774720514426953, 21.78128695274315874 ) ) ;
#48756=VECTOR ( 'NONE', #23097, 1000.000000000000114 ) ;
#48757=CARTESIAN_POINT ( 'NONE',  ( 22.02124265030973760, -6.376774720514428729, 16.20402280011862217 ) ) ;
#48766=CARTESIAN_POINT ( 'NONE',  ( -28.98875734969026041, 5.965225279485572685, 23.37402280011862743 ) ) ;
#48770=EDGE_CURVE ( 'NONE', #86899, #100313, #55694, .T. ) ;
#48777=AXIS2_PLACEMENT_3D ( 'NONE', #98637, #14401, #66234 ) ;
#48782=CARTESIAN_POINT ( 'NONE',  ( 5.817949855437939632, -5.876774720514417183, 20.34349022145623209 ) ) ;
#48785=ORIENTED_EDGE ( 'NONE', *, *, #29255, .T. ) ;
#48794=EDGE_CURVE ( 'NONE', #58098, #65974, #78521, .T. ) ;
#48805=ORIENTED_EDGE ( 'NONE', *, *, #49340, .T. ) ;
#48807=ORIENTED_EDGE ( 'NONE', *, *, #59759, .T. ) ;
#48808=DIRECTION ( 'NONE',  ( 2.246662546894773332E-15, 0.000000000000000000, 1.000000000000000000 ) ) ;
#48829=CARTESIAN_POINT ( 'NONE',  ( 6.658651924251966392, -5.876774720514415407, 20.11748569626183425 ) ) ;
#48835=CARTESIAN_POINT ( 'NONE',  ( -24.90875734969025501, -6.376774720514426953, 29.49402280011861777 ) ) ;
#48863=EDGE_LOOP ( 'NONE', ( #96520, #64217 ) ) ;
#48865=PLANE ( 'NONE',  #54040 ) ;
#48868=PLANE ( 'NONE',  #92006 ) ;
#48877=CARTESIAN_POINT ( 'NONE',  ( 31.61049571213237641, -4.540774720514426654, 26.28206907949443050 ) ) ;
#48881=CARTESIAN_POINT ( 'NONE',  ( 4.465438306463536122, -6.376774720514426065, 21.59631214011467293 ) ) ;
#48888=AXIS2_PLACEMENT_3D ( 'NONE', #13932, #90564, #43900 ) ;
#48892=B_SPLINE_CURVE_WITH_KNOTS ( 'NONE', 3,
 ( #24254, #16637, #30363, #30869 ),
 .UNSPECIFIED., .F., .F.,
 ( 4, 4 ),
 ( 0.000000000000000000, 0.001418231214350569244 ),
 .UNSPECIFIED. ) ;
#48895=PLANE ( 'NONE',  #78189 ) ;
#48898=DIRECTION ( 'NONE',  ( -0.000000000000000000, -1.000000000000000000, -0.000000000000000000 ) ) ;
#48899=CARTESIAN_POINT ( 'NONE',  ( 6.326958800731953048, -5.876774720514425177, 21.47849181751607972 ) ) ;
#48901=CARTESIAN_POINT ( 'NONE',  ( 27.53860345374771867, -1.682774720514426114, -9.482392034746242260 ) ) ;
#48903=ADVANCED_FACE ( 'NONE', ( #34252 ), #41128, .F. ) ;
#48911=CARTESIAN_POINT ( 'NONE',  ( 7.844850387708879325, -6.376774720514429617, -25.09814097568368751 ) ) ;
#48913=CARTESIAN_POINT ( 'NONE',  ( -7.338700834008208496, -6.376774720514410077, 19.35116211686183263 ) ) ;
#48922=CARTESIAN_POINT ( 'NONE',  ( 7.480769230769231726, -6.376774720514420736, 20.77403846153845635 ) ) ;
#48927=DIRECTION ( 'NONE',  ( -1.000000000000000000, 0.000000000000000000, 0.000000000000000000 ) ) ;
#48936=ORIENTED_EDGE ( 'NONE', *, *, #33179, .T. ) ;
#48939=CARTESIAN_POINT ( 'NONE',  ( -9.149999999999996803, -5.876774720514426953, 11.88602120139452012 ) ) ;
#48942=DIRECTION ( 'NONE',  ( -8.334928612639484546E-17, 1.000000000000000000, -7.321843366904296032E-17 ) ) ;
#48945=CARTESIAN_POINT ( 'NONE',  ( 13.10664265030973930, 5.965225279485574461, -28.18129937516157568 ) ) ;
#48951=DIRECTION ( 'NONE',  ( 0.000000000000000000, 1.000000000000000000, 1.478457507934778393E-16 ) ) ;
#48960=CIRCLE ( 'NONE', #3620, 0.3000000000000016542 ) ;
#48962=DIRECTION ( 'NONE',  ( 1.000000000000000000, 0.000000000000000000, -5.238131417152343399E-15 ) ) ;
#48964=ADVANCED_FACE ( 'NONE', ( #96151 ), #16134, .F. ) ;
#48972=EDGE_CURVE ( 'NONE', #15899, #45653, #8530, .T. ) ;
#48976=CARTESIAN_POINT ( 'NONE',  ( 0.2311345937353457003, -6.376774720514410077, 19.43951662020192828 ) ) ;
#48983=ADVANCED_FACE ( 'NONE', ( #10911 ), #46098, .T. ) ;
#48984=EDGE_CURVE ( 'NONE', #92467, #55695, #91745, .T. ) ;
#48988=ORIENTED_EDGE ( 'NONE', *, *, #46477, .T. ) ;
#48997=EDGE_CURVE ( 'NONE', #47215, #57615, #50979, .T. ) ;
#49002=DIRECTION ( 'NONE',  ( -1.000000000000000000, 0.000000000000000000, -0.000000000000000000 ) ) ;
#49016=VECTOR ( 'NONE', #39490, 1000.000000000000000 ) ;
#49019=CARTESIAN_POINT ( 'NONE',  ( -20.27875734969026311, 7.743225279485574042, 21.75402280011862644 ) ) ;
#49029=EDGE_CURVE ( 'NONE', #5079, #1528, #58934, .T. ) ;
#49033=ADVANCED_FACE ( 'NONE', ( #60093 ), #82901, .T. ) ;
#49041=CARTESIAN_POINT ( 'NONE',  ( 4.453188626415028217, -6.376774720514422512, 21.07953283331298167 ) ) ;
#49050=CARTESIAN_POINT ( 'NONE',  ( -2.791950601096355733, -6.376774720514417183, 20.17732409774492552 ) ) ;
#49051=VERTEX_POINT ( 'NONE', #98624 ) ;
#49070=DIRECTION ( 'NONE',  ( 0.000000000000000000, -1.000000000000000000, 0.000000000000000000 ) ) ;
#49086=CARTESIAN_POINT ( 'NONE',  ( 32.98733314340959311, 5.965225279485572685, 2.074222136288530027 ) ) ;
#49095=AXIS2_PLACEMENT_3D ( 'NONE', #27410, #3582, #91166 ) ;
#49099=DIRECTION ( 'NONE',  ( -1.000000000000000000, 0.000000000000000000, 0.000000000000000000 ) ) ;
#49100=FACE_OUTER_BOUND ( 'NONE', #11071, .T. ) ;
#49109=VECTOR ( 'NONE', #13493, 1000.000000000000000 ) ;
#49111=ADVANCED_FACE ( 'NONE', ( #5286 ), #34747, .T. ) ;
#49116=VECTOR ( 'NONE', #76685, 1000.000000000000000 ) ;
#49117=EDGE_LOOP ( 'NONE', ( #63396, #5016, #21800, #65444 ) ) ;
#49120=CARTESIAN_POINT ( 'NONE',  ( 9.478389368232452483, -2.682774720514426559, -23.17485683983816003 ) ) ;
#49124=CARTESIAN_POINT ( 'NONE',  ( 29.72852606603716552, -4.950008708102185295, 27.41398129243886217 ) ) ;
#49131=CARTESIAN_POINT ( 'NONE',  ( -5.486124437288584232, -6.376774720514417183, 19.74568812963598319 ) ) ;
#49137=EDGE_CURVE ( 'NONE', #34853, #54541, #39222, .T. ) ;
#49149=DIRECTION ( 'NONE',  ( 1.000000000000000000, 0.000000000000000000, 0.000000000000000000 ) ) ;
#49150=DIRECTION ( 'NONE',  ( -0.000000000000000000, 1.000000000000000000, -0.000000000000000000 ) ) ;
#49156=VERTEX_POINT ( 'NONE', #52469 ) ;
#49177=CARTESIAN_POINT ( 'NONE',  ( -29.49875734969025842, 5.965225279485572685, 23.37402280011862743 ) ) ;
#49178=VECTOR ( 'NONE', #74540, 1000.000000000000000 ) ;
#49179=ORIENTED_EDGE ( 'NONE', *, *, #4303, .F. ) ;
#49199=CARTESIAN_POINT ( 'NONE',  ( -6.720452724358975338, -5.876774720514411854, 19.46153846153846700 ) ) ;
#49208=EDGE_LOOP ( 'NONE', ( #90898, #32464, #42091, #12846 ) ) ;
#49211=CIRCLE ( 'NONE', #92853, 28.96799999999999287 ) ;
#49213=CARTESIAN_POINT ( 'NONE',  ( -6.369015873774380943, -6.376774720514413630, 19.23384392940399934 ) ) ;
#49215=EDGE_LOOP ( 'NONE', ( #38075, #18027, #89352, #72600 ) ) ;
#49218=VERTEX_POINT ( 'NONE', #84403 ) ;
#49220=CARTESIAN_POINT ( 'NONE',  ( 13.80377080874918150, 6.475225279485574248, -27.21172484903264532 ) ) ;
#49226=CARTESIAN_POINT ( 'NONE',  ( 5.092794675178905273, -3.306008726340172288, -27.56219045528442280 ) ) ;
#49228=EDGE_CURVE ( 'NONE', #49448, #67210, #77768, .T. ) ;
#49232=CARTESIAN_POINT ( 'NONE',  ( 10.54059822343757702, -5.876774720514426953, 17.17691942396159988 ) ) ;
#49234=ORIENTED_EDGE ( 'NONE', *, *, #23545, .F. ) ;
#49245=CARTESIAN_POINT ( 'NONE',  ( 3.323502641304225236, -6.376774720514426065, 21.72931788002195219 ) ) ;
#49252=AXIS2_PLACEMENT_3D ( 'NONE', #52410, #50920, #81860 ) ;
#49262=CARTESIAN_POINT ( 'NONE',  ( 5.471383689419962337, 5.965225279485594001, -29.02273493113403902 ) ) ;
#49266=B_SPLINE_CURVE_WITH_KNOTS ( 'NONE', 3,
 ( #13576, #39427, #39925, #16078, #68873, #86597, #78977, #54170, #24687, #54661, #15083, #48047, #53665, #46050, #93201, #8972, #70377, #23687, #85092, #93702, #24193, #47550, #46541 ),
 .UNSPECIFIED., .F., .F.,
 ( 4, 1, 1, 1, 1, 1, 1, 1, 1, 1, 1, 1, 1, 1, 1, 1, 1, 1, 1, 1, 4 ),
 ( 0.000000000000000000, 0.06038661931106227565, 0.1208832485859964029, 0.1827546186251403082, 0.2478110297583512034, 0.2812991000432494282, 0.3150876241506579412, 0.3497023955502757131, 0.3848565811185565289, 0.4209661972261032892, 0.4585111882611391243, 0.4971747221273126183, 0.5376020478662695279, 0.5805030184200120624, 0.6274675400267057945, 0.6783882095592440598, 0.7339832205925608255, 0.7937467045508355135, 0.8577136721607333536, 0.9266978643613864586, 1.000000000000000000 ),
 .UNSPECIFIED. ) ;
#49269=LINE ( 'NONE', #95419, #95192 ) ;
#49270=CARTESIAN_POINT ( 'NONE',  ( 2.909586618535765723, -5.876774720514411854, 19.75512108203924200 ) ) ;
#49273=CARTESIAN_POINT ( 'NONE',  ( 282.9764569301858046, -2.682774720514426559, 20.79159422840526616 ) ) ;
#49277=DIRECTION ( 'NONE',  ( -2.501730345825856179E-15, 6.879758451021104590E-15, -1.000000000000000000 ) ) ;
#49286=CARTESIAN_POINT ( 'NONE',  ( 6.351517594976544778, -5.876774720514417183, 20.09206396488320578 ) ) ;
#49289=CARTESIAN_POINT ( 'NONE',  ( 22.33191539159863481, -4.132774720514426292, -16.26852658953813346 ) ) ;
#49324=CARTESIAN_POINT ( 'NONE',  ( -4.568292318365942073, -0.3587747205144265483, 30.06720597538392425 ) ) ;
#49329=ORIENTED_EDGE ( 'NONE', *, *, #47363, .T. ) ;
#49331=CARTESIAN_POINT ( 'NONE',  ( 7.166666666666668739, -6.376774720514420736, 20.78665865384614975 ) ) ;
#49335=EDGE_LOOP ( 'NONE', ( #32436, #40490, #10226, #30516 ) ) ;
#49338=CARTESIAN_POINT ( 'NONE',  ( 2.610950917001260141, -5.876774720514411854, 19.54489930512155027 ) ) ;
#49340=EDGE_CURVE ( 'NONE', #451, #3529, #36187, .T. ) ;
#49341=PLANE ( 'NONE',  #72505 ) ;
#49342=CARTESIAN_POINT ( 'NONE',  ( -10.79305683637731406, 5.965225279485594001, -27.49869550653260930 ) ) ;
#49346=ADVANCED_FACE ( 'NONE', ( #72693 ), #9779, .T. ) ;
#49352=DIRECTION ( 'NONE',  ( 0.000000000000000000, 1.000000000000000000, 0.000000000000000000 ) ) ;
#49354=EDGE_LOOP ( 'NONE', ( #88245, #511, #11147, #84236 ) ) ;
#49360=CARTESIAN_POINT ( 'NONE',  ( 5.400898774349120579, -5.876774720514417183, 20.36357656736558042 ) ) ;
#49362=DIRECTION ( 'NONE',  ( -0.000000000000000000, 1.000000000000000000, -0.000000000000000000 ) ) ;
#49365=CARTESIAN_POINT ( 'NONE',  ( 29.57907552799942508, -3.316774720514426456, 29.21818156447043791 ) ) ;
#49368=CARTESIAN_POINT ( 'NONE',  ( 32.25183987940364005, -0.3587747205144265483, 2.026414261721653176 ) ) ;
#49373=DIRECTION ( 'NONE',  ( 0.000000000000000000, 1.000000000000000000, 1.478457507934778393E-16 ) ) ;
#49382=CARTESIAN_POINT ( 'NONE',  ( -5.533628790199073499, -6.376774720514417183, 19.87297243748313491 ) ) ;
#49388=CARTESIAN_POINT ( 'NONE',  ( 3.960462906497916435, -6.376774720514427841, 21.82884394085917279 ) ) ;
#49402=CARTESIAN_POINT ( 'NONE',  ( -1.955883090540335045, -6.376774720514411854, 19.49432735726521315 ) ) ;
#49417=VECTOR ( 'NONE', #35419, 1000.000000000000114 ) ;
#49418=CARTESIAN_POINT ( 'NONE',  ( 6.055070915967790235, -6.376774720518116446, -28.43998667026512095 ) ) ;
#49434=CARTESIAN_POINT ( 'NONE',  ( 14.43441819135929371, -3.316774720514426456, -28.36222020317710246 ) ) ;
#49448=VERTEX_POINT ( 'NONE', #20375 ) ;
#49456=ORIENTED_EDGE ( 'NONE', *, *, #18826, .T. ) ;
#49457=CARTESIAN_POINT ( 'NONE',  ( -20.27875734969026311, -7.835183881457444599, 24.00402280011862288 ) ) ;
#49462=CARTESIAN_POINT ( 'NONE',  ( 32.64853395142472436, -3.736174708400741729, -2.687157883629963884 ) ) ;
#49463=DIRECTION ( 'NONE',  ( -2.246662546894773332E-15, 7.121496375062676691E-15, -1.000000000000000000 ) ) ;
#49471=CARTESIAN_POINT ( 'NONE',  ( 14.73162737928355170, -3.582999323269832725, -27.37940951657878941 ) ) ;
#49473=ORIENTED_EDGE ( 'NONE', *, *, #29255, .F. ) ;
#49477=DIRECTION ( 'NONE',  ( -1.257682986112628661E-16, 0.000000000000000000, -1.000000000000000000 ) ) ;
#49485=ORIENTED_EDGE ( 'NONE', *, *, #59316, .F. ) ;
#49486=ADVANCED_FACE ( 'NONE', ( #82290 ), #11778, .F. ) ;
#49488=CARTESIAN_POINT ( 'NONE',  ( -41.32836283488544638, 2.803225279485573207, 39.26872235229541985 ) ) ;
#49491=CARTESIAN_POINT ( 'NONE',  ( -5.891837592278976743, -6.376774720514418959, 20.62654306927474934 ) ) ;
#49492=VERTEX_POINT ( 'NONE', #36119 ) ;
#49495=CARTESIAN_POINT ( 'NONE',  ( 31.50451260799805198, -4.115674466082359650, -1.392914706732841790 ) ) ;
#49518=CIRCLE ( 'NONE', #824, 0.3000000000000016542 ) ;
#49520=VECTOR ( 'NONE', #29319, 1000.000000000000114 ) ;
#49539=CARTESIAN_POINT ( 'NONE',  ( 3.020285327128866992, -6.376774720514406525, 19.15473963397401391 ) ) ;
#49544=ORIENTED_EDGE ( 'NONE', *, *, #28353, .F. ) ;
#49548=PLANE ( 'NONE',  #56122 ) ;
#49565=ORIENTED_EDGE ( 'NONE', *, *, #46005, .T. ) ;
#49567=CARTESIAN_POINT ( 'NONE',  ( 0.03625801282051022839, -6.376774720514410077, 19.27714342948718240 ) ) ;
#49594=VECTOR ( 'NONE', #88112, 1000.000000000000000 ) ;
#49596=FACE_OUTER_BOUND ( 'NONE', #7734, .T. ) ;
#49600=VECTOR ( 'NONE', #70937, 1000.000000000000000 ) ;
#49621=CARTESIAN_POINT ( 'NONE',  ( -7.282824509310913186, -6.376774720514415407, 19.84584863393302356 ) ) ;
#49627=CARTESIAN_POINT ( 'NONE',  ( 33.74607884027702909, 5.965225279485572685, -4.999864028243830916 ) ) ;
#49634=CARTESIAN_POINT ( 'NONE',  ( -1.174900045708346497, -5.876774720514411854, 19.48569229636960998 ) ) ;
#49641=CARTESIAN_POINT ( 'NONE',  ( -2.794871794871791604, -6.376774720514427841, 21.75000000000001066 ) ) ;
#49646=ORIENTED_EDGE ( 'NONE', *, *, #77808, .F. ) ;
#49653=FACE_OUTER_BOUND ( 'NONE', #70827, .T. ) ;
#49667=AXIS2_PLACEMENT_3D ( 'NONE', #14126, #45103, #71284 ) ;
#49680=EDGE_CURVE ( 'NONE', #40241, #82993, #90727, .T. ) ;
#49699=VECTOR ( 'NONE', #81892, 1000.000000000000114 ) ;
#49712=VERTEX_POINT ( 'NONE', #11596 ) ;
#49728=LINE ( 'NONE', #95382, #28153 ) ;
#49731=VERTEX_POINT ( 'NONE', #34943 ) ;
#49740=VECTOR ( 'NONE', #33599, 1000.000000000000000 ) ;
#49743=CARTESIAN_POINT ( 'NONE',  ( 3.251543564379332008, -6.376774720514424288, 21.68810402963413964 ) ) ;
#49752=DIRECTION ( 'NONE',  ( 0.9822594791677485837, 0.000000000000000000, -0.1875268396392986980 ) ) ;
#49753=VECTOR ( 'NONE', #80670, 1000.000000000000000 ) ;
#49755=CARTESIAN_POINT ( 'NONE',  ( -0.02075734969026423599, 5.965225279485572685, -0.08597719988137648983 ) ) ;
#49760=LINE ( 'NONE', #3579, #51957 ) ;
#49778=CARTESIAN_POINT ( 'NONE',  ( -41.32836283488544638, 2.803225279485573207, 39.26872235229541985 ) ) ;
#49782=ORIENTED_EDGE ( 'NONE', *, *, #32989, .T. ) ;
#49787=LINE ( 'NONE', #26440, #63746 ) ;
#49790=CARTESIAN_POINT ( 'NONE',  ( 23.91005183030481263, -2.682774720514426559, -14.40591128290692069 ) ) ;
#49792=DIRECTION ( 'NONE',  ( -1.000000000000000000, 0.000000000000000000, -1.334402673828313586E-16 ) ) ;
#49796=ADVANCED_FACE ( 'NONE', ( #64671 ), #87981, .F. ) ;
#49800=AXIS2_PLACEMENT_3D ( 'NONE', #78653, #15267, #62459 ) ;
#49801=ADVANCED_FACE ( 'NONE', ( #26583 ), #365, .F. ) ;
#49802=CARTESIAN_POINT ( 'NONE',  ( -4.993225604111834137, -0.3587747205143964613, -29.11654937215279304 ) ) ;
#49812=VERTEX_POINT ( 'NONE', #33183 ) ;
#49827=ORIENTED_EDGE ( 'NONE', *, *, #16198, .F. ) ;
#49829=ORIENTED_EDGE ( 'NONE', *, *, #15057, .T. ) ;
#49831=CARTESIAN_POINT ( 'NONE',  ( 2.598243466966731585, -5.876774720514413630, 20.31174627870924709 ) ) ;
#49844=EDGE_CURVE ( 'NONE', #8748, #76027, #87473, .T. ) ;
#49845=DIRECTION ( 'NONE',  ( 0.000000000000000000, 0.000000000000000000, 1.000000000000000000 ) ) ;
#49846=PLANE ( 'NONE',  #1116 ) ;
#49849=CARTESIAN_POINT ( 'NONE',  ( 13.59451591917074431, -3.316774720514426456, -28.23515841827053308 ) ) ;
#49854=EDGE_CURVE ( 'NONE', #18022, #36077, #79853, .T. ) ;
#49866=CARTESIAN_POINT ( 'NONE',  ( 6.697025426467099862, -5.876774720514423400, 21.43052570396496037 ) ) ;
#49870=CIRCLE ( 'NONE', #87075, 2.249999999999998668 ) ;
#49871=ORIENTED_EDGE ( 'NONE', *, *, #15169, .F. ) ;
#49886=CARTESIAN_POINT ( 'NONE',  ( -5.439936175300728927, -6.376774720514410077, 19.67454710845353816 ) ) ;
#49895=ORIENTED_EDGE ( 'NONE', *, *, #83330, .T. ) ;
#49908=CARTESIAN_POINT ( 'NONE',  ( 10.24059822343752479, -6.376774720514426953, -2.394817856121274864E-14 ) ) ;
#49920=CARTESIAN_POINT ( 'NONE',  ( 11.22265027772288093, -3.316774720514091612, -28.06709888818796017 ) ) ;
#49933=CARTESIAN_POINT ( 'NONE',  ( 7.267403311989051318, -5.876774720514426065, 21.43157132964656952 ) ) ;
#49942=CARTESIAN_POINT ( 'NONE',  ( 14.76093561896379214, 6.475225279485574248, -26.55548769130089681 ) ) ;
#49960=CARTESIAN_POINT ( 'NONE',  ( 13.91401389203221406, 5.965225279485572685, 158.0376437107427137 ) ) ;
#49961=CARTESIAN_POINT ( 'NONE',  ( 7.116579217368891541, -5.876774720514415407, 20.51774267661129869 ) ) ;
#49974=EDGE_LOOP ( 'NONE', ( #6888, #88242, #10281, #80922 ) ) ;
#49981=CARTESIAN_POINT ( 'NONE',  ( 6.365284455128204399, -5.876774720514413630, 19.73076923076922640 ) ) ;
#49984=CARTESIAN_POINT ( 'NONE',  ( 13.91401389203221406, 6.475225279485573360, 158.0376437107427137 ) ) ;
#49999=CARTESIAN_POINT ( 'NONE',  ( 29.73860345376316872, -5.356774720514427379, 17.30421508979847189 ) ) ;
#50006=CARTESIAN_POINT ( 'NONE',  ( 2.590388488674697953, -6.376774720514415407, 19.94764386045124027 ) ) ;
#50007=CARTESIAN_POINT ( 'NONE',  ( -19.38764004357183524, 5.965225279485572685, -21.62823517627350611 ) ) ;
#50008=AXIS2_PLACEMENT_3D ( 'NONE', #42922, #28678, #82948 ) ;
#50015=LINE ( 'NONE', #72846, #12330 ) ;
#50024=CARTESIAN_POINT ( 'NONE',  ( 282.9764569301858046, -0.3587747205144265483, 20.79159422840526616 ) ) ;
#50025=DIRECTION ( 'NONE',  ( 1.000000000000000000, -1.232047923278981953E-16, 0.000000000000000000 ) ) ;
#50034=AXIS2_PLACEMENT_3D ( 'NONE', #84832, #70617, #69106 ) ;
#50038=CARTESIAN_POINT ( 'NONE',  ( 3.672440828437461224, -6.376774720514402972, 18.52532110411518573 ) ) ;
#50050=CARTESIAN_POINT ( 'NONE',  ( 0.3849403830293018358, -5.876774720514418071, 20.45311193189268906 ) ) ;
#50064=ORIENTED_EDGE ( 'NONE', *, *, #926, .T. ) ;
#50069=VECTOR ( 'NONE', #51109, 1000.000000000000000 ) ;
#50071=VERTEX_POINT ( 'NONE', #51916 ) ;
#50077=CARTESIAN_POINT ( 'NONE',  ( -1.036876607668611117, -5.876774720514417183, 20.14881673916291405 ) ) ;
#50083=VERTEX_POINT ( 'NONE', #97577 ) ;
#50085=CARTESIAN_POINT ( 'NONE',  ( 10.75273025779354796, -6.376774720514426953, 23.03521261039436752 ) ) ;
#50090=ADVANCED_FACE ( 'NONE', ( #34694 ), #98062, .T. ) ;
#50095=VERTEX_POINT ( 'NONE', #75234 ) ;
#50101=ORIENTED_EDGE ( 'NONE', *, *, #41100, .F. ) ;
#50108=DIRECTION ( 'NONE',  ( 2.615445361545220718E-15, -6.974520964120588319E-15, 1.000000000000000000 ) ) ;
#50114=CARTESIAN_POINT ( 'NONE',  ( -6.989144439031651501, -6.376774720514410077, 19.51167604195716621 ) ) ;
#50119=LINE ( 'NONE', #49627, #91917 ) ;
#50120=DIRECTION ( 'NONE',  ( 0.000000000000000000, 0.000000000000000000, -1.000000000000000000 ) ) ;
#50123=DIRECTION ( 'NONE',  ( 1.000000000000000000, 0.000000000000000000, -2.615445361545220718E-15 ) ) ;
#50127=CARTESIAN_POINT ( 'NONE',  ( -0.4909855769230798139, -6.376774720514410077, 19.14743589743590135 ) ) ;
#50148=CYLINDRICAL_SURFACE ( 'NONE', #71803, 28.96799999999999642 ) ;
#50158=ORIENTED_EDGE ( 'NONE', *, *, #1223, .F. ) ;
#50166=CARTESIAN_POINT ( 'NONE',  ( 5.671814302646631667, -6.376774720514418959, 20.58085404595000512 ) ) ;
#50173=DIRECTION ( 'NONE',  ( 1.000000000000000000, -0.000000000000000000, 0.000000000000000000 ) ) ;
#50176=CARTESIAN_POINT ( 'NONE',  ( 27.86270917940689174, 5.965225279485572685, 29.49402280011862487 ) ) ;
#50182=EDGE_LOOP ( 'NONE', ( #20839, #62148, #84993, #65862 ) ) ;
#50183=VERTEX_POINT ( 'NONE', #19950 ) ;
#50201=ADVANCED_FACE ( 'NONE', ( #27079 ), #73746, .T. ) ;
#50202=CARTESIAN_POINT ( 'NONE',  ( 2.920210193027767076, -5.876774720514413630, 19.64065332113010243 ) ) ;
#50203=ORIENTED_EDGE ( 'NONE', *, *, #47825, .T. ) ;
#50204=CARTESIAN_POINT ( 'NONE',  ( -0.02075734969026423599, -3.316774720514426456, -0.08597719988137648983 ) ) ;
#50207=CARTESIAN_POINT ( 'NONE',  ( 5.097264368844749427, 6.475225279485576024, -27.56135813788841560 ) ) ;
#50215=CARTESIAN_POINT ( 'NONE',  ( 5.671814302646631667, -6.376774720514418959, 20.58085404595000512 ) ) ;
#50217=CARTESIAN_POINT ( 'NONE',  ( -7.999999999999996447, -5.876774720514426953, 0.000000000000000000 ) ) ;
#50219=VERTEX_POINT ( 'NONE', #4741 ) ;
#50231=CARTESIAN_POINT ( 'NONE',  ( -0.02075734969026423599, 5.965225279485572685, -0.08597719988137648983 ) ) ;
#50254=DIRECTION ( 'NONE',  ( -0.000000000000000000, 1.000000000000000000, -0.000000000000000000 ) ) ;
#50267=CARTESIAN_POINT ( 'NONE',  ( -10.25272501932627378, -4.561466182953243909, 29.07579354015162210 ) ) ;
#50272=CARTESIAN_POINT ( 'NONE',  ( 5.930937628982182908, -5.876774720514417183, 20.24478033514397524 ) ) ;
#50281=LINE ( 'NONE', #66028, #35983 ) ;
#50287=ADVANCED_FACE ( 'NONE', ( #61531 ), #29558, .F. ) ;
#50305=VERTEX_POINT ( 'NONE', #6720 ) ;
#50309=DIRECTION ( 'NONE',  ( -0.000000000000000000, -1.000000000000000000, -0.000000000000000000 ) ) ;
#50320=ORIENTED_EDGE ( 'NONE', *, *, #83716, .F. ) ;
#50322=DIRECTION ( 'NONE',  ( -0.1875268396392987258, -0.000000000000000000, -0.9822594791677485837 ) ) ;
#50324=DIRECTION ( 'NONE',  ( 0.000000000000000000, -1.000000000000000000, 0.000000000000000000 ) ) ;
#50328=DIRECTION ( 'NONE',  ( 0.9980236263794188822, 0.000000000000000000, -0.06283980576413537855 ) ) ;
#50331=CARTESIAN_POINT ( 'NONE',  ( 27.86270917940689174, 5.965225279485572685, 29.49402280011862487 ) ) ;
#50333=ORIENTED_EDGE ( 'NONE', *, *, #97897, .F. ) ;
#50335=CARTESIAN_POINT ( 'NONE',  ( 12.78578435864683449, -3.995361385602315796, -28.02483137475221397 ) ) ;
#50341=EDGE_CURVE ( 'NONE', #8989, #25591, #39524, .T. ) ;
#50349=CARTESIAN_POINT ( 'NONE',  ( -12.84880425037202656, -0.3587747205143964613, -26.59900746623529244 ) ) ;
#50361=VECTOR ( 'NONE', #56111, 1000.000000000000000 ) ;
#50363=DIRECTION ( 'NONE',  ( 0.03244919754393515293, 0.000000000000000000, -0.9994733861282923959 ) ) ;
#50405=CARTESIAN_POINT ( 'NONE',  ( 9.313311959394031447, -3.316774720514592545, -28.06297399525112013 ) ) ;
#50407=CARTESIAN_POINT ( 'NONE',  ( -3.106028565906091998, -5.876774720514426953, 3.106028565906120864 ) ) ;
#50411=ORIENTED_EDGE ( 'NONE', *, *, #14774, .T. ) ;
#50412=CARTESIAN_POINT ( 'NONE',  ( 30.53060340732036337, -5.297812262124697469, 1.539714685317310483 ) ) ;
#50414=ORIENTED_EDGE ( 'NONE', *, *, #34428, .T. ) ;
#50416=CARTESIAN_POINT ( 'NONE',  ( 6.698292889820671725, -5.876774720514424288, 21.80822233811499444 ) ) ;
#50419=ORIENTED_EDGE ( 'NONE', *, *, #51327, .F. ) ;
#50421=DIRECTION ( 'NONE',  ( -0.000000000000000000, 1.000000000000000000, -0.000000000000000000 ) ) ;
#50422=AXIS2_PLACEMENT_3D ( 'NONE', #55499, #54491, #24030 ) ;
#50427=CARTESIAN_POINT ( 'NONE',  ( 29.64064043116815128, 5.965225279485572685, 28.71191112024341408 ) ) ;
#50430=DIRECTION ( 'NONE',  ( 1.257682986112628661E-16, 0.000000000000000000, 1.000000000000000000 ) ) ;
#50434=ORIENTED_EDGE ( 'NONE', *, *, #8302, .T. ) ;
#50443=CARTESIAN_POINT ( 'NONE',  ( 6.853365600657045142, -5.876774720514416295, 20.20310688689519196 ) ) ;
#50446=CARTESIAN_POINT ( 'NONE',  ( 29.70220533433691301, -3.316774720514426456, 28.20564067601639735 ) ) ;
#50448=ORIENTED_EDGE ( 'NONE', *, *, #81764, .F. ) ;
#50472=CARTESIAN_POINT ( 'NONE',  ( 6.853365600657045142, -6.376774720514415407, 20.20310688689519196 ) ) ;
#50478=ORIENTED_EDGE ( 'NONE', *, *, #68739, .F. ) ;
#50480=DIRECTION ( 'NONE',  ( 0.000000000000000000, -1.000000000000000000, 0.000000000000000000 ) ) ;
#50486=ORIENTED_EDGE ( 'NONE', *, *, #38135, .T. ) ;
#50491=PLANE ( 'NONE',  #510 ) ;
#50500=PLANE ( 'NONE',  #7410 ) ;
#50523=EDGE_CURVE ( 'NONE', #94249, #13162, #42701, .T. ) ;
#50536=ORIENTED_EDGE ( 'NONE', *, *, #19771, .T. ) ;
#50544=ORIENTED_EDGE ( 'NONE', *, *, #23619, .T. ) ;
#50550=DIRECTION ( 'NONE',  ( -0.000000000000000000, 0.000000000000000000, -1.000000000000000000 ) ) ;
#50552=DIRECTION ( 'NONE',  ( 0.000000000000000000, 1.000000000000000000, 0.000000000000000000 ) ) ;
#50553=DIRECTION ( 'NONE',  ( -0.000000000000000000, 1.000000000000000000, -0.000000000000000000 ) ) ;
#50554=VERTEX_POINT ( 'NONE', #73636 ) ;
#50559=CARTESIAN_POINT ( 'NONE',  ( -23.71328795744024021, 5.965225279485594001, -17.58350715675015152 ) ) ;
#50578=ORIENTED_EDGE ( 'NONE', *, *, #17717, .T. ) ;
#50581=CARTESIAN_POINT ( 'NONE',  ( 8.978253834636468866, -5.876774720514426953, 0.000000000000000000 ) ) ;
#50586=EDGE_CURVE ( 'NONE', #26032, #83737, #21322, .T. ) ;
#50598=EDGE_CURVE ( 'NONE', #31243, #57287, #6111, .T. ) ;
#50601=DIRECTION ( 'NONE',  ( 0.000000000000000000, -1.000000000000000000, 0.000000000000000000 ) ) ;
#50615=DIRECTION ( 'NONE',  ( -0.000000000000000000, 1.000000000000000000, -0.000000000000000000 ) ) ;
#50617=AXIS2_PLACEMENT_3D ( 'NONE', #85694, #24293, #32408 ) ;
#50631=ORIENTED_EDGE ( 'NONE', *, *, #91943, .F. ) ;
#50644=DIRECTION ( 'NONE',  ( 0.000000000000000000, 0.000000000000000000, -1.000000000000000000 ) ) ;
#50658=VERTEX_POINT ( 'NONE', #2019 ) ;
#50675=ORIENTED_EDGE ( 'NONE', *, *, #15700, .T. ) ;
#50679=ORIENTED_EDGE ( 'NONE', *, *, #68734, .F. ) ;
#50680=ORIENTED_EDGE ( 'NONE', *, *, #59886, .T. ) ;
#50683=CARTESIAN_POINT ( 'NONE',  ( 29.70220533433691301, -6.376774720514426953, 28.20564067601639735 ) ) ;
#50698=LINE ( 'NONE', #81647, #59923 ) ;
#50702=CARTESIAN_POINT ( 'NONE',  ( 9.069233782100962316, -3.316774720514428232, -28.07145878873749112 ) ) ;
#50710=CARTESIAN_POINT ( 'NONE',  ( 5.771117285127500551, -6.376774720514417183, 20.39900056875960388 ) ) ;
#50719=ADVANCED_FACE ( 'NONE', ( #94347 ), #16721, .T. ) ;
#50733=VECTOR ( 'NONE', #45588, 1000.000000000000000 ) ;
#50734=ORIENTED_EDGE ( 'NONE', *, *, #51149, .T. ) ;
#50776=CARTESIAN_POINT ( 'NONE',  ( 6.251785340501501587, -6.376774720514424288, 21.46941214867599612 ) ) ;
#50781=DIRECTION ( 'NONE',  ( 0.000000000000000000, 1.000000000000000000, 0.000000000000000000 ) ) ;
#50782=FACE_OUTER_BOUND ( 'NONE', #54193, .T. ) ;
#50785=ORIENTED_EDGE ( 'NONE', *, *, #6562, .F. ) ;
#50789=DIRECTION ( 'NONE',  ( -0.000000000000000000, 1.000000000000000000, -0.000000000000000000 ) ) ;
#50790=FACE_OUTER_BOUND ( 'NONE', #53219, .T. ) ;
#50799=ORIENTED_EDGE ( 'NONE', *, *, #79102, .F. ) ;
#50803=ORIENTED_EDGE ( 'NONE', *, *, #4887, .F. ) ;
#50806=CARTESIAN_POINT ( 'NONE',  ( -3.108974358974359475, -5.876774720514418071, 20.36458333333334281 ) ) ;
#50807=DIRECTION ( 'NONE',  ( 1.000000000000000000, 0.000000000000000000, -2.168404344971008868E-16 ) ) ;
#50813=ORIENTED_EDGE ( 'NONE', *, *, #12908, .F. ) ;
#50814=CARTESIAN_POINT ( 'NONE',  ( 6.555906488453394410, -6.376774720514426065, 21.46941147007026274 ) ) ;
#50818=ORIENTED_EDGE ( 'NONE', *, *, #67017, .F. ) ;
#50821=CARTESIAN_POINT ( 'NONE',  ( 15.88393883468596712, -3.596971506839818034, -28.01277999924163709 ) ) ;
#50836=AXIS2_PLACEMENT_3D ( 'NONE', #66358, #50120, #65864 ) ;
#50837=VERTEX_POINT ( 'NONE', #26345 ) ;
#50841=ORIENTED_EDGE ( 'NONE', *, *, #33756, .T. ) ;
#50843=EDGE_CURVE ( 'NONE', #19111, #36659, #88250, .T. ) ;
#50850=CARTESIAN_POINT ( 'NONE',  ( -24.97666371003640151, 5.965225279485592225, -15.72894043976419098 ) ) ;
#50852=CARTESIAN_POINT ( 'NONE',  ( 6.887358010905132666, -5.876774720514425177, 21.32574817943157086 ) ) ;
#50861=CARTESIAN_POINT ( 'NONE',  ( 32.45853543194704116, 5.965225279485572685, 9.169203677920338080 ) ) ;
#50877=CARTESIAN_POINT ( 'NONE',  ( 3.960462906497916435, -5.876774720514426953, 21.82884394085917279 ) ) ;
#50893=CARTESIAN_POINT ( 'NONE',  ( 5.359050311451609261, -6.376774720514420736, 21.05346524168807676 ) ) ;
#50894=LINE ( 'NONE', #96554, #92684 ) ;
#50897=VECTOR ( 'NONE', #83096, 1000.000000000000000 ) ;
#50902=CARTESIAN_POINT ( 'NONE',  ( 4.127208352283176396, -5.876774720514423400, 21.39624840817692686 ) ) ;
#50903=VECTOR ( 'NONE', #43323, 1000.000000000000000 ) ;
#50904=CARTESIAN_POINT ( 'NONE',  ( 9.196673285530609476, -6.376774720514424288, -25.00509208784493964 ) ) ;
#50906=CARTESIAN_POINT ( 'NONE',  ( -7.243541020599075786, -6.376774720514408301, 19.27798293355755632 ) ) ;
#50911=DIRECTION ( 'NONE',  ( 0.000000000000000000, 0.000000000000000000, 1.000000000000000000 ) ) ;
#50912=FACE_OUTER_BOUND ( 'NONE', #81665, .T. ) ;
#50917=CARTESIAN_POINT ( 'NONE',  ( 5.184553252003285984, 5.965225279485572685, -28.06387035751381731 ) ) ;
#50920=DIRECTION ( 'NONE',  ( 0.000000000000000000, -1.000000000000000000, 0.000000000000000000 ) ) ;
#50923=VERTEX_POINT ( 'NONE', #89746 ) ;
#50935=ORIENTED_EDGE ( 'NONE', *, *, #47715, .T. ) ;
#50945=EDGE_CURVE ( 'NONE', #88122, #31070, #20215, .T. ) ;
#50950=CARTESIAN_POINT ( 'NONE',  ( -4.286263797015736595E-16, -2.056774720514426669, -3.500000000000000000 ) ) ;
#50953=FACE_OUTER_BOUND ( 'NONE', #58046, .T. ) ;
#50956=LINE ( 'NONE', #6258, #72823 ) ;
#50970=PLANE ( 'NONE',  #46648 ) ;
#50971=DIRECTION ( 'NONE',  ( -0.000000000000000000, -0.000000000000000000, 1.000000000000000000 ) ) ;
#50973=CARTESIAN_POINT ( 'NONE',  ( 7.190659024148910561, -6.376774720514413630, 19.91543959911579620 ) ) ;
#50979=LINE ( 'NONE', #42871, #63818 ) ;
#51000=DIRECTION ( 'NONE',  ( 0.000000000000000000, -1.000000000000000000, 0.000000000000000000 ) ) ;
#51022=PLANE ( 'NONE',  #73903 ) ;
#51033=ORIENTED_EDGE ( 'NONE', *, *, #69613, .T. ) ;
#51060=CARTESIAN_POINT ( 'NONE',  ( -0.3544984435505275644, -5.876774720514408301, 19.15251819062245531 ) ) ;
#51071=DIRECTION ( 'NONE',  ( -1.955152872784845154E-15, -1.000000000000000000, 3.740001113483016365E-15 ) ) ;
#51082=ORIENTED_EDGE ( 'NONE', *, *, #43593, .F. ) ;
#51083=CARTESIAN_POINT ( 'NONE',  ( -29.49875734969026198, -0.3587747205144265483, 10.11402280011862587 ) ) ;
#51089=CARTESIAN_POINT ( 'NONE',  ( 3.180076745125953508, -0.3587747205143968499, -28.87659520466658236 ) ) ;
#51091=CARTESIAN_POINT ( 'NONE',  ( -4.537657931416015700, -5.876774720514410077, 19.25713806424188235 ) ) ;
#51094=ORIENTED_EDGE ( 'NONE', *, *, #72694, .F. ) ;
#51101=DIRECTION ( 'NONE',  ( -0.000000000000000000, -1.000000000000000000, -0.000000000000000000 ) ) ;
#51102=ADVANCED_FACE ( 'NONE', ( #93727 ), #2402, .T. ) ;
#51109=DIRECTION ( 'NONE',  ( -0.000000000000000000, 1.000000000000000000, -0.000000000000000000 ) ) ;
#51111=ORIENTED_EDGE ( 'NONE', *, *, #62509, .T. ) ;
#51116=LINE ( 'NONE', #26778, #22638 ) ;
#51127=DIRECTION ( 'NONE',  ( -0.000000000000000000, -1.000000000000000000, -0.000000000000000000 ) ) ;
#51131=DIRECTION ( 'NONE',  ( 0.000000000000000000, 0.000000000000000000, 1.000000000000000000 ) ) ;
#51132=CARTESIAN_POINT ( 'NONE',  ( 0.000000000000000000, -2.056774720514426669, 3.500000000000000000 ) ) ;
#51140=B_SPLINE_CURVE_WITH_KNOTS ( 'NONE', 3,
 ( #48945, #41840, #16467, #3280 ),
 .UNSPECIFIED., .F., .F.,
 ( 4, 4 ),
 ( 0.007875538328797549587, 0.009214210883376282302 ),
 .UNSPECIFIED. ) ;
#51143=LINE ( 'NONE', #73984, #44123 ) ;
#51145=EDGE_LOOP ( 'NONE', ( #26375, #11861, #95203, #15942 ) ) ;
#51149=EDGE_CURVE ( 'NONE', #33316, #12604, #86124, .T. ) ;
#51153=ORIENTED_EDGE ( 'NONE', *, *, #74616, .F. ) ;
#51154=CARTESIAN_POINT ( 'NONE',  ( 5.872047395031165351, -6.376774720514415407, 20.29192741308114734 ) ) ;
#51159=EDGE_CURVE ( 'NONE', #89315, #78100, #93226, .T. ) ;
#51169=DIRECTION ( 'NONE',  ( -0.8264557562326038109, 6.454799914155187856E-16, -0.5630016722799275897 ) ) ;
#51176=EDGE_LOOP ( 'NONE', ( #59918, #97243, #72844, #45718 ) ) ;
#51178=ORIENTED_EDGE ( 'NONE', *, *, #7281, .F. ) ;
#51181=CARTESIAN_POINT ( 'NONE',  ( 15.08554537508440774, -5.152774720514413431, -26.79085230644761495 ) ) ;
#51188=EDGE_CURVE ( 'NONE', #29733, #65705, #16600, .T. ) ;
#51192=ORIENTED_EDGE ( 'NONE', *, *, #67886, .F. ) ;
#51193=CARTESIAN_POINT ( 'NONE',  ( 6.826756808399247589, -5.876774720514423400, 21.36722843294932161 ) ) ;
#51198=CARTESIAN_POINT ( 'NONE',  ( 2.905472630834636139, -5.876774720514415407, 19.87563926270137671 ) ) ;
#51212=DIRECTION ( 'NONE',  ( 0.000000000000000000, 0.000000000000000000, 1.000000000000000000 ) ) ;
#51213=ORIENTED_EDGE ( 'NONE', *, *, #51359, .T. ) ;
#51218=ADVANCED_FACE ( 'NONE', ( #94732 ), #62814, .F. ) ;
#51220=EDGE_LOOP ( 'NONE', ( #7175, #96514, #28714, #93768 ) ) ;
#51222=DIRECTION ( 'NONE',  ( 0.000000000000000000, 0.000000000000000000, -1.000000000000000000 ) ) ;
#51223=CARTESIAN_POINT ( 'NONE',  ( 3.797776442307698286, -6.376774720514427841, 21.83974358974358410 ) ) ;
#51228=CARTESIAN_POINT ( 'NONE',  ( 9.940598223437577374, -5.876774720514426953, 17.91871304725684766 ) ) ;
#51229=EDGE_CURVE ( 'NONE', #60724, #13389, #87633, .T. ) ;
#51236=DIRECTION ( 'NONE',  ( -1.000000000000000000, 1.232047923278981953E-16, 0.000000000000000000 ) ) ;
#51247=CARTESIAN_POINT ( 'NONE',  ( -4.968349358974361252, -6.376774720514411854, 19.46153846153847056 ) ) ;
#51258=AXIS2_PLACEMENT_3D ( 'NONE', #35924, #98306, #88722 ) ;
#51261=CARTESIAN_POINT ( 'NONE',  ( -10.23311166579590825, -4.222446552888387217, 29.28685113854110966 ) ) ;
#51262=CARTESIAN_POINT ( 'NONE',  ( 282.9764569301858046, -5.356774720514427379, 20.79159422840526616 ) ) ;
#51267=CARTESIAN_POINT ( 'NONE',  ( 6.044119082205957838, -6.376774720514424288, 21.40268112089023589 ) ) ;
#51270=CARTESIAN_POINT ( 'NONE',  ( 15.15958133180904355, -5.152774720514426754, -26.63299148310929709 ) ) ;
#51272=DIRECTION ( 'NONE',  ( 0.000000000000000000, 0.000000000000000000, -1.000000000000000000 ) ) ;
#51277=VECTOR ( 'NONE', #30905, 1000.000000000000000 ) ;
#51279=ADVANCED_FACE ( 'NONE', ( #18604 ), #28289, .T. ) ;
#51281=CARTESIAN_POINT ( 'NONE',  ( -3.106028565906091998, -5.876774720514426953, 3.106028565906120864 ) ) ;
#51311=ORIENTED_EDGE ( 'NONE', *, *, #78969, .F. ) ;
#51319=ORIENTED_EDGE ( 'NONE', *, *, #22163, .F. ) ;
#51327=EDGE_CURVE ( 'NONE', #57623, #75580, #89851, .T. ) ;
#51333=CARTESIAN_POINT ( 'NONE',  ( 25.61870917940689196, -0.3587747205144265483, 28.79814474876424768 ) ) ;
#51341=CARTESIAN_POINT ( 'NONE',  ( -3.826923076923078426, -6.376774720514408301, 19.19230769230769695 ) ) ;
#51348=CARTESIAN_POINT ( 'NONE',  ( 29.70917971445138051, -6.219445159570049064, 27.14760184111773356 ) ) ;
#51350=VECTOR ( 'NONE', #80516, 1000.000000000000000 ) ;
#51353=CARTESIAN_POINT ( 'NONE',  ( 5.097264368846952998, 6.475225279485573360, -27.56135813788808164 ) ) ;
#51354=AXIS2_PLACEMENT_3D ( 'NONE', #60720, #70820, #29752 ) ;
#51359=EDGE_CURVE ( 'NONE', #42617, #99563, #83323, .T. ) ;
#51368=ORIENTED_EDGE ( 'NONE', *, *, #58290, .F. ) ;
#51369=CARTESIAN_POINT ( 'NONE',  ( 4.332134589405623792, -5.876774720514426953, 21.69242924468134959 ) ) ;
#51372=CIRCLE ( 'NONE', #62762, 2.249999999999998668 ) ;
#51387=AXIS2_PLACEMENT_3D ( 'NONE', #17513, #62707, #63718 ) ;
#51393=EDGE_CURVE ( 'NONE', #88212, #81441, #85350, .T. ) ;
#51398=DIRECTION ( 'NONE',  ( 1.000000000000000000, 0.000000000000000000, 0.000000000000000000 ) ) ;
#51402=ADVANCED_FACE ( 'NONE', ( #29718 ), #100209, .T. ) ;
#51403=CARTESIAN_POINT ( 'NONE',  ( -2.070328576748420524, -6.376774720514410077, 19.46575348430201657 ) ) ;
#51408=CARTESIAN_POINT ( 'NONE',  ( 6.274899854645557440, -5.876774720514428729, 21.83451738260096775 ) ) ;
#51416=ADVANCED_FACE ( 'NONE', ( #28728 ), #76374, .F. ) ;
#51420=FACE_OUTER_BOUND ( 'NONE', #64052, .T. ) ;
#51432=LINE ( 'NONE', #21945, #5685 ) ;
#51435=ORIENTED_EDGE ( 'NONE', *, *, #97339, .F. ) ;
#51436=CARTESIAN_POINT ( 'NONE',  ( 16.26279755680690542, -1.684774720514426560, -27.67997040356620531 ) ) ;
#51448=CARTESIAN_POINT ( 'NONE',  ( -20.77875734969026311, 6.143225279485574397, 27.35402280011862430 ) ) ;
#51449=ORIENTED_EDGE ( 'NONE', *, *, #11070, .T. ) ;
#51450=DIRECTION ( 'NONE',  ( -0.1593164160933057683, 0.000000000000000000, 0.9872275723272647685 ) ) ;
#51451=LINE ( 'NONE', #35229, #96093 ) ;
#51456=CIRCLE ( 'NONE', #48202, 4.299999999999999822 ) ;
#51458=EDGE_CURVE ( 'NONE', #32849, #33122, #80153, .T. ) ;
#51463=DIRECTION ( 'NONE',  ( 1.000000000000000000, 0.000000000000000000, 0.000000000000000000 ) ) ;
#51467=CARTESIAN_POINT ( 'NONE',  ( 7.107139210497321002, -5.876774720514413630, 19.78447747620696617 ) ) ;
#51471=VERTEX_POINT ( 'NONE', #30713 ) ;
#51475=ORIENTED_EDGE ( 'NONE', *, *, #37639, .T. ) ;
#51478=PLANE ( 'NONE',  #70760 ) ;
#51480=CARTESIAN_POINT ( 'NONE',  ( 30.59430046144282400, -4.508643932895013862, 26.46466010020539272 ) ) ;
#51490=CARTESIAN_POINT ( 'NONE',  ( 3.202571139211427553, -6.376774720514406525, 18.81074098386681470 ) ) ;
#51491=CARTESIAN_POINT ( 'NONE',  ( 2.710830299132254595, -5.876774720514410966, 19.05039662921485544 ) ) ;
#51515=PRODUCT ( 'Plastic Part 2', 'Plastic Part 2', '', ( #74216 ) ) ;
#51525=CARTESIAN_POINT ( 'NONE',  ( -0.4686347352592966087, -6.376774720514411854, 19.46274624311237034 ) ) ;
#51534=CARTESIAN_POINT ( 'NONE',  ( -1.044871794871793602, -6.376774720514418959, 20.44941907051282115 ) ) ;
#51540=DIRECTION ( 'NONE',  ( 0.000000000000000000, -1.000000000000000000, 0.000000000000000000 ) ) ;
#51541=ORIENTED_EDGE ( 'NONE', *, *, #30695, .T. ) ;
#51571=CARTESIAN_POINT ( 'NONE',  ( -2.889365861140832159, -6.376774720514410077, 19.43823095447973870 ) ) ;
#51587=VERTEX_POINT ( 'NONE', #81886 ) ;
#51598=ORIENTED_EDGE ( 'NONE', *, *, #53511, .T. ) ;
#51605=VECTOR ( 'NONE', #51779, 1000.000000000000000 ) ;
#51608=CARTESIAN_POINT ( 'NONE',  ( -24.90875734969025501, -3.316774720514426456, 26.43402280011862615 ) ) ;
#51609=EDGE_CURVE ( 'NONE', #3529, #45653, #4765, .T. ) ;
#51619=CIRCLE ( 'NONE', #77528, 1.835999999999999632 ) ;
#51623=DIRECTION ( 'NONE',  ( 0.000000000000000000, 0.000000000000000000, -1.000000000000000000 ) ) ;
#51624=FACE_BOUND ( 'NONE', #10379, .T. ) ;
#51634=CARTESIAN_POINT ( 'NONE',  ( 33.69795529655567634, -0.6647747205144264315, 23.11160796525322070 ) ) ;
#51644=ORIENTED_EDGE ( 'NONE', *, *, #35484, .F. ) ;
#51655=VECTOR ( 'NONE', #92388, 1000.000000000000114 ) ;
#51658=DIRECTION ( 'NONE',  ( 0.000000000000000000, 0.000000000000000000, 1.000000000000000000 ) ) ;
#51660=EDGE_CURVE ( 'NONE', #18886, #47314, #12126, .T. ) ;
#51666=VECTOR ( 'NONE', #31673, 1000.000000000000000 ) ;
#51671=CARTESIAN_POINT ( 'NONE',  ( 6.420673076923079314, -5.876774720514427841, 21.83974358974358765 ) ) ;
#51675=DIRECTION ( 'NONE',  ( -4.015954566446630556E-15, -1.000000000000000000, -1.297050502119899750E-15 ) ) ;
#51676=ORIENTED_EDGE ( 'NONE', *, *, #52866, .T. ) ;
#51708=CARTESIAN_POINT ( 'NONE',  ( 6.127395130496778641, -6.376774720514417183, 20.13872869980892943 ) ) ;
#51723=ADVANCED_FACE ( 'NONE', ( #42351 ), #79878, .F. ) ;
#51725=VECTOR ( 'NONE', #59155, 1000.000000000000000 ) ;
#51730=DIRECTION ( 'NONE',  ( 0.000000000000000000, -1.000000000000000000, 0.000000000000000000 ) ) ;
#51752=DIRECTION ( 'NONE',  ( 0.000000000000000000, 1.000000000000000000, 0.000000000000000000 ) ) ;
#51753=CONICAL_SURFACE ( 'NONE', #67909, 2.999999999999999112, 0.7853981633974412846 ) ;
#51760=CARTESIAN_POINT ( 'NONE',  ( -0.02075734969026423599, -3.316774720514426456, -0.08597719988137648983 ) ) ;
#51765=ORIENTED_EDGE ( 'NONE', *, *, #69369, .T. ) ;
#51769=AXIS2_PLACEMENT_3D ( 'NONE', #63631, #45895, #8824 ) ;
#51770=CARTESIAN_POINT ( 'NONE',  ( 33.62145766639996936, -4.037870770857248104, -12.08356088300365094 ) ) ;
#51771=ORIENTED_EDGE ( 'NONE', *, *, #48794, .T. ) ;
#51776=DIRECTION ( 'NONE',  ( 0.000000000000000000, 0.000000000000000000, -1.000000000000000000 ) ) ;
#51779=DIRECTION ( 'NONE',  ( 0.000000000000000000, 0.000000000000000000, 1.000000000000000000 ) ) ;
#51795=ORIENTED_EDGE ( 'NONE', *, *, #86346, .F. ) ;
#51807=CIRCLE ( 'NONE', #63190, 0.8160000000000007248 ) ;
#51814=ORIENTED_EDGE ( 'NONE', *, *, #8697, .T. ) ;
#51837=ORIENTED_EDGE ( 'NONE', *, *, #63163, .F. ) ;
#51840=CARTESIAN_POINT ( 'NONE',  ( -6.377963355984652694, -5.876774720514412742, 19.53740760792478426 ) ) ;
#51846=LINE ( 'NONE', #68561, #59609 ) ;
#51848=DIRECTION ( 'NONE',  ( 0.000000000000000000, 1.000000000000000000, -8.673617379884035472E-16 ) ) ;
#51852=EDGE_CURVE ( 'NONE', #99333, #58343, #92359, .T. ) ;
#51861=DIRECTION ( 'NONE',  ( -3.017716325409535726E-14, 0.000000000000000000, -1.000000000000000000 ) ) ;
#51881=AXIS2_PLACEMENT_3D ( 'NONE', #79355, #71256, #80869 ) ;
#51883=CARTESIAN_POINT ( 'NONE',  ( 30.60113388085891017, -4.386958714992013952, 26.76092701747204927 ) ) ;
#51886=VERTEX_POINT ( 'NONE', #32469 ) ;
#51888=CARTESIAN_POINT ( 'NONE',  ( 22.33191539159816585, -3.407774720514426647, -16.26852658953824360 ) ) ;
#51891=CARTESIAN_POINT ( 'NONE',  ( -6.989144439031651501, -6.376774720514410077, 19.51167604195716621 ) ) ;
#51896=LINE ( 'NONE', #19929, #41838 ) ;
#51900=CARTESIAN_POINT ( 'NONE',  ( 4.653494883475234545, -6.376774720514415407, 20.13747874360300116 ) ) ;
#51910=CARTESIAN_POINT ( 'NONE',  ( -2.369893591381136755, -5.876774720514410966, 19.15221817653405623 ) ) ;
#51916=CARTESIAN_POINT ( 'NONE',  ( 14.76093561896379214, -3.316774720514426456, -28.39148769130088468 ) ) ;
#51923=CARTESIAN_POINT ( 'NONE',  ( -24.90875734969025501, 5.965225279485572685, 26.43402280011862615 ) ) ;
#51931=PLANE ( 'NONE',  #44593 ) ;
#51934=ORIENTED_EDGE ( 'NONE', *, *, #31794, .T. ) ;
#51942=CARTESIAN_POINT ( 'NONE',  ( 22.33191539159856731, -2.682774720514426559, -16.26852658953777109 ) ) ;
#51949=CARTESIAN_POINT ( 'NONE',  ( 33.74607884027702909, 5.965225279485572685, -4.999864028243830916 ) ) ;
#51951=AXIS2_PLACEMENT_3D ( 'NONE', #12733, #50324, #81260 ) ;
#51953=ORIENTED_EDGE ( 'NONE', *, *, #74190, .T. ) ;
#51957=VECTOR ( 'NONE', #34520, 1000.000000000000000 ) ;
#51970=VERTEX_POINT ( 'NONE', #16736 ) ;
#51981=CARTESIAN_POINT ( 'NONE',  ( 30.61558003201036726, -3.638743767327229151, 27.34189434213806535 ) ) ;
#51990=CARTESIAN_POINT ( 'NONE',  ( -6.914873625533457968, -6.376774720514426953, 29.95171384920748281 ) ) ;
#51995=CARTESIAN_POINT ( 'NONE',  ( 7.089543269230769162, -6.376774720514413630, 19.75741185897435415 ) ) ;
#52000=DIRECTION ( 'NONE',  ( 0.000000000000000000, 1.000000000000000000, 0.000000000000000000 ) ) ;
#52002=AXIS2_PLACEMENT_3D ( 'NONE', #50581, #94748, #11020 ) ;
#52006=DIRECTION ( 'NONE',  ( 0.9994733861282923959, 0.000000000000000000, 0.03244919754393515293 ) ) ;
#52013=DIRECTION ( 'NONE',  ( 0.000000000000000000, 0.000000000000000000, 1.000000000000000000 ) ) ;
#52022=CARTESIAN_POINT ( 'NONE',  ( -0.8502773128684013582, -6.376774720514413630, 19.61227901093089798 ) ) ;
#52036=B_SPLINE_CURVE_WITH_KNOTS ( 'NONE', 3,
 ( #80320, #41780, #96541, #72720 ),
 .UNSPECIFIED., .F., .F.,
 ( 4, 4 ),
 ( 0.000000000000000000, 1.000000000000000000 ),
 .UNSPECIFIED. ) ;
#52037=ORIENTED_EDGE ( 'NONE', *, *, #26586, .T. ) ;
#52052=LINE ( 'NONE', #20092, #62213 ) ;
#52059=B_SPLINE_CURVE_WITH_KNOTS ( 'NONE', 3,
 ( #85769, #32992, #63966, #94874, #25367, #56344, #8650, #9140, #86268, #8151, #87265, #23350, #54333, #17762, #31480, #85259, #48730, #1035, #39593, #31983, #79648, #10147, #72064, #15752, #62441, #30977, #46716 ),
 .UNSPECIFIED., .F., .F.,
 ( 4, 1, 1, 1, 1, 1, 1, 1, 1, 1, 1, 1, 1, 1, 1, 1, 1, 1, 1, 1, 1, 1, 1, 1, 4 ),
 ( 0.000000000000000000, 0.03378714634699089836, 0.06662165772429383404, 0.09928487809597265346, 0.1313611650426506072, 0.1635851875953436008, 0.1961039269870681889, 0.2289022543238170004, 0.2621580559050075143, 0.2959912222583161445, 0.3302178457247997301, 0.3650598258919544037, 0.4009507373401082209, 0.4376203820767376462, 0.4757075294370921026, 0.5153806916250490699, 0.5564135414931649093, 0.5997648298727309424, 0.6464241555840876119, 0.6964314445175666668, 0.7497815178015586612, 0.8065733069755320894, 0.8674355315653994314, 0.9318867532508745555, 1.000000000000000000 ),
 .UNSPECIFIED. ) ;
#52066=CARTESIAN_POINT ( 'NONE',  ( -2.959136224476847765, -5.876774720514412742, 19.53857357749110335 ) ) ;
#52091=CARTESIAN_POINT ( 'NONE',  ( -2.701720430790308214, -0.3587747205144061202, -28.90526747363640681 ) ) ;
#52101=EDGE_CURVE ( 'NONE', #19111, #71424, #39652, .T. ) ;
#52103=EDGE_CURVE ( 'NONE', #40197, #45760, #33209, .T. ) ;
#52104=DIRECTION ( 'NONE',  ( 0.000000000000000000, 1.000000000000000000, 0.000000000000000000 ) ) ;
#52110=FACE_OUTER_BOUND ( 'NONE', #99842, .T. ) ;
#52119=CARTESIAN_POINT ( 'NONE',  ( -2.373828433815573735, -6.376774720514410077, 19.48240003225459915 ) ) ;
#52123=AXIS2_PLACEMENT_3D ( 'NONE', #32739, #56094, #63722 ) ;
#52130=CARTESIAN_POINT ( 'NONE',  ( 10.46399479596398052, -3.316774720514422903, -27.03001098546561209 ) ) ;
#52131=EDGE_LOOP ( 'NONE', ( #18479, #10261, #79752, #40816, #83871, #51153, #33100, #8991, #81854, #15845, #11996, #9785, #1710, #21613, #14981, #3546, #37581, #56537, #46166, #1200 ) ) ;
#52143=PLANE ( 'NONE',  #53831 ) ;
#52147=CARTESIAN_POINT ( 'NONE',  ( 31.24279708945211098, -4.510509370595455536, 1.827416827591516357 ) ) ;
#52152=DIRECTION ( 'NONE',  ( 1.743630241030147080E-15, -6.974520964120588319E-15, 1.000000000000000000 ) ) ;
#52157=DIRECTION ( 'NONE',  ( -0.09721092304694051167, 0.000000000000000000, 0.9952638024365005887 ) ) ;
#52163=CARTESIAN_POINT ( 'NONE',  ( 7.267403311989051318, -5.876774720514425177, 21.43157132964656952 ) ) ;
#52169=CARTESIAN_POINT ( 'NONE',  ( -4.169309590939843879, -5.876774720514412742, 19.59793130852656518 ) ) ;
#52173=EDGE_LOOP ( 'NONE', ( #62207, #98737, #66869, #82273 ) ) ;
#52189=VERTEX_POINT ( 'NONE', #5020 ) ;
#52199=VERTEX_POINT ( 'NONE', #59822 ) ;
#52200=CARTESIAN_POINT ( 'NONE',  ( 4.039061187531148178, -5.876774720514399419, 18.18637930035166761 ) ) ;
#52210=CARTESIAN_POINT ( 'NONE',  ( -27.83739072329610664, 5.965225279485592225, -8.084349702057698650 ) ) ;
#52212=ADVANCED_FACE ( 'NONE', ( #66939 ), #56298, .T. ) ;
#52213=VECTOR ( 'NONE', #2972, 1000.000000000000000 ) ;
#52216=ORIENTED_EDGE ( 'NONE', *, *, #43488, .T. ) ;
#52231=EDGE_CURVE ( 'NONE', #94339, #35113, #46591, .T. ) ;
#52232=CARTESIAN_POINT ( 'NONE',  ( -3.004714864173751998, -6.376774720514411854, 19.63296556618507083 ) ) ;
#52234=CARTESIAN_POINT ( 'NONE',  ( 10.46399479596398052, -3.105441387181091084, -27.03001098546561209 ) ) ;
#52249=LINE ( 'NONE', #7563, #91334 ) ;
#52252=VECTOR ( 'NONE', #94136, 1000.000000000000000 ) ;
#52256=LINE ( 'NONE', #91306, #9326 ) ;
#52260=CARTESIAN_POINT ( 'NONE',  ( -10.27832545704433365, -4.855524038559839717, 28.80005113363453972 ) ) ;
#52265=CARTESIAN_POINT ( 'NONE',  ( 29.73860345376319358, -3.356774720514428267, 1.647607965253212958 ) ) ;
#52267=CIRCLE ( 'NONE', #65260, 1.700000000000000178 ) ;
#52270=CARTESIAN_POINT ( 'NONE',  ( 11.86515846156731335, -3.316774720514427788, -28.09350142571734921 ) ) ;
#52280=AXIS2_PLACEMENT_3D ( 'NONE', #30269, #61247, #92170 ) ;
#52283=CARTESIAN_POINT ( 'NONE',  ( 5.864225667603142789, -5.876774720514424288, 21.27837265517432996 ) ) ;
#52291=EDGE_CURVE ( 'NONE', #30337, #29704, #26699, .T. ) ;
#52315=VECTOR ( 'NONE', #11413, 1000.000000000000000 ) ;
#52318=CARTESIAN_POINT ( 'NONE',  ( 15.63775912259741041, -4.567193422986002282, -28.22903731538627525 ) ) ;
#52333=ORIENTED_EDGE ( 'NONE', *, *, #27621, .F. ) ;
#52334=CONICAL_SURFACE ( 'NONE', #70133, 2.999999999999999112, 0.7853981633974412846 ) ;
#52336=ORIENTED_EDGE ( 'NONE', *, *, #52291, .T. ) ;
#52337=FACE_OUTER_BOUND ( 'NONE', #15702, .T. ) ;
#52342=DIRECTION ( 'NONE',  ( 0.000000000000000000, -1.000000000000000000, 0.000000000000000000 ) ) ;
#52347=VECTOR ( 'NONE', #1284, 1000.000000000000227 ) ;
#52356=EDGE_CURVE ( 'NONE', #42247, #9388, #95959, .T. ) ;
#52360=ORIENTED_EDGE ( 'NONE', *, *, #29611, .F. ) ;
#52367=CARTESIAN_POINT ( 'NONE',  ( -29.49875734969026198, 5.965225279485572685, 2.362022800118626531 ) ) ;
#52373=EDGE_LOOP ( 'NONE', ( #76404, #64511, #91508, #59800 ) ) ;
#52375=FACE_OUTER_BOUND ( 'NONE', #37242, .T. ) ;
#52380=DIRECTION ( 'NONE',  ( -0.000000000000000000, 1.000000000000000000, -0.000000000000000000 ) ) ;
#52385=DIRECTION ( 'NONE',  ( 1.000000000000000000, 0.000000000000000000, -1.104558621438292892E-14 ) ) ;
#52386=CIRCLE ( 'NONE', #78297, 27.94799999999999685 ) ;
#52387=CARTESIAN_POINT ( 'NONE',  ( 25.05730599792488533, -1.684774720501991174, -18.59674224247030239 ) ) ;
#52393=CARTESIAN_POINT ( 'NONE',  ( 4.653846153846159517, -6.376774720514415407, 19.99999999999999289 ) ) ;
#52399=CARTESIAN_POINT ( 'NONE',  ( -2.148731487934370410, -5.876774720514411854, 19.46295461892501422 ) ) ;
#52400=B_SPLINE_SURFACE_WITH_KNOTS ( 'NONE', 3, 1, ( 
 ( #86662, #2438 ),
 ( #63859, #10040 ),
 ( #19146, #64360 ),
 ( #95778, #73448 ),
 ( #50114, #32887 ),
 ( #48117, #42010 ),
 ( #81053, #34881 ),
 ( #25261, #10538 ),
 ( #56240, #56739 ),
 ( #95282, #72953 ),
 ( #49621, #80052 ),
 ( #88674, #25767 ),
 ( #71455, #41000 ),
 ( #11535, #1943 ),
 ( #3941, #65857 ),
 ( #41499, #72452 ),
 ( #3449, #96775 ),
 ( #27274, #18643 ),
 ( #88174, #64865 ) ),
 .UNSPECIFIED., .F., .F., .F.,
 ( 4, 1, 1, 1, 1, 1, 1, 1, 1, 1, 1, 1, 1, 1, 1, 1, 4 ),
 ( 2, 2 ),
 ( 0.000000000000000000, 0.07735147826526211912, 0.1497817737883345712, 0.2198699552839545879, 0.2879755066202366320, 0.3546781060271970709, 0.4187834319376942949, 0.4827347082469880535, 0.5473072519464166064, 0.5826981022599677651, 0.6240955651677915217, 0.6712929496345372282, 0.7243202075485738467, 0.7838489433400219752, 0.8494366971205808969, 0.9216570148062976919, 1.000000000000000000 ),
 ( 0.000000000000000000, 1.000000000000000000 ),
 .UNSPECIFIED. ) ;
#52401=FACE_OUTER_BOUND ( 'NONE', #99487, .T. ) ;
#52407=CARTESIAN_POINT ( 'NONE',  ( 3.794707603699265519E-15, -5.876774720514426953, 17.50000000000000000 ) ) ;
#52410=CARTESIAN_POINT ( 'NONE',  ( 22.02124265030973760, 7.743225279485574042, 16.20402280011862217 ) ) ;
#52416=AXIS2_PLACEMENT_3D ( 'NONE', #58664, #35827, #34334 ) ;
#52424=CARTESIAN_POINT ( 'NONE',  ( -13.36367879947601445, -6.376774720514426953, 20.00000000000000355 ) ) ;
#52434=CARTESIAN_POINT ( 'NONE',  ( -0.3982818654701407723, -6.376774720514410077, 19.46306892155547530 ) ) ;
#52438=VERTEX_POINT ( 'NONE', #51089 ) ;
#52440=DIRECTION ( 'NONE',  ( 0.000000000000000000, 0.000000000000000000, 1.000000000000000000 ) ) ;
#52462=FACE_OUTER_BOUND ( 'NONE', #1193, .T. ) ;
#52469=CARTESIAN_POINT ( 'NONE',  ( -10.11875734969026297, -3.316774720514426456, 30.51402280011862089 ) ) ;
#52476=CARTESIAN_POINT ( 'NONE',  ( -0.02075734969026423599, 5.965225279485572685, -0.08597719988137648983 ) ) ;
#52478=CARTESIAN_POINT ( 'NONE',  ( 30.60111574538730039, -4.387371784078713866, 26.76015704162893627 ) ) ;
#52489=AXIS2_PLACEMENT_3D ( 'NONE', #68633, #99551, #84845 ) ;
#52491=CARTESIAN_POINT ( 'NONE',  ( 3.398951772795901771, -6.376774720514402972, 18.23562605320997676 ) ) ;
#52506=PLANE ( 'NONE',  #41817 ) ;
#52509=DIRECTION ( 'NONE',  ( 0.000000000000000000, 0.000000000000000000, 1.000000000000000000 ) ) ;
#52519=CARTESIAN_POINT ( 'NONE',  ( -1.653359744423585465, -6.376774720514413630, 19.34586827028017098 ) ) ;
#52534=CARTESIAN_POINT ( 'NONE',  ( 0.3180806761505774460, -5.876774720514415407, 20.02963804100705403 ) ) ;
#52546=VECTOR ( 'NONE', #90707, 1000.000000000000000 ) ;
#52547=FACE_OUTER_BOUND ( 'NONE', #30699, .T. ) ;
#52549=EDGE_LOOP ( 'NONE', ( #81625, #21827, #32100, #78502 ) ) ;
#52550=CARTESIAN_POINT ( 'NONE',  ( 3.960454120839856706, -6.376774720514402972, 18.17119035270509997 ) ) ;
#52556=ORIENTED_EDGE ( 'NONE', *, *, #3697, .T. ) ;
#52565=CARTESIAN_POINT ( 'NONE',  ( -3.108787716482549701, -6.376774720514417183, 20.32624910079993086 ) ) ;
#52573=ORIENTED_EDGE ( 'NONE', *, *, #41531, .F. ) ;
#52574=CARTESIAN_POINT ( 'NONE',  ( 4.653515142448186204, -6.376774720514413630, 19.86181745814487343 ) ) ;
#52581=CARTESIAN_POINT ( 'NONE',  ( 22.02124265030973760, -5.356774720514425603, 12.85402280011862430 ) ) ;
#52588=ORIENTED_EDGE ( 'NONE', *, *, #1246, .T. ) ;
#52593=DIRECTION ( 'NONE',  ( -0.9952638024365005887, 0.000000000000000000, -0.09721092304694052555 ) ) ;
#52604=CARTESIAN_POINT ( 'NONE',  ( 9.940598223437573822, -5.876774720514426953, 18.21871304725684837 ) ) ;
#52627=CARTESIAN_POINT ( 'NONE',  ( 10.73203334292264088, -3.902996417034998000, -26.95265065337511601 ) ) ;
#52628=VECTOR ( 'NONE', #85246, 1000.000000000000114 ) ;
#52638=CARTESIAN_POINT ( 'NONE',  ( 3.632573734185411851, -5.876774720514429617, 21.82795992345630509 ) ) ;
#52644=CARTESIAN_POINT ( 'NONE',  ( 27.53860345374808105, -4.772774720514425972, -6.982392034746241372 ) ) ;
#52656=VECTOR ( 'NONE', #3238, 1000.000000000000000 ) ;
#52661=CARTESIAN_POINT ( 'NONE',  ( 3.176458874063931681, -0.3587747205143967943, -28.85257003503889806 ) ) ;
#52674=ORIENTED_EDGE ( 'NONE', *, *, #69988, .F. ) ;
#52697=CARTESIAN_POINT ( 'NONE',  ( 3.797776442307698286, -6.376774720514401196, 18.16025641025640525 ) ) ;
#52709=CARTESIAN_POINT ( 'NONE',  ( 6.403846153846157740, -6.376774720514426065, 21.48076923076922995 ) ) ;
#52718=ORIENTED_EDGE ( 'NONE', *, *, #13328, .F. ) ;
#52730=CARTESIAN_POINT ( 'NONE',  ( 14.76093561896379214, 5.965225279485572685, -26.55548769130089681 ) ) ;
#52740=EDGE_CURVE ( 'NONE', #20076, #83403, #36645, .T. ) ;
#52747=ORIENTED_EDGE ( 'NONE', *, *, #78299, .T. ) ;
#52760=EDGE_CURVE ( 'NONE', #79973, #35655, #62482, .T. ) ;
#52763=AXIS2_PLACEMENT_3D ( 'NONE', #60134, #21532, #52509 ) ;
#52765=CARTESIAN_POINT ( 'NONE',  ( 33.54680291763921929, -3.871631182425088191, -11.45966867074879580 ) ) ;
#52769=CARTESIAN_POINT ( 'NONE',  ( -27.86046284349297864, 5.965225279485572685, -8.091963836038754465 ) ) ;
#52774=EDGE_CURVE ( 'NONE', #30745, #63171, #39340, .T. ) ;
#52777=CARTESIAN_POINT ( 'NONE',  ( 29.73860345376319003, -1.682774720514426114, -8.849814207987163783 ) ) ;
#52779=LINE ( 'NONE', #23302, #28501 ) ;
#52785=CARTESIAN_POINT ( 'NONE',  ( 5.671135738765417322, -5.876774720514422512, 20.99074880795119924 ) ) ;
#52786=EDGE_CURVE ( 'NONE', #34762, #56620, #38841, .T. ) ;
#52788=CARTESIAN_POINT ( 'NONE',  ( 0.000000000000000000, -4.056774720514426669, 0.000000000000000000 ) ) ;
#52799=EDGE_CURVE ( 'NONE', #68647, #57214, #26772, .T. ) ;
#52809=CARTESIAN_POINT ( 'NONE',  ( 6.480733632922428988, -6.376774720514426065, 21.47849199606610782 ) ) ;
#52832=CARTESIAN_POINT ( 'NONE',  ( -5.926585084595196840, -5.876774720514416295, 20.19722303762275573 ) ) ;
#52866=EDGE_CURVE ( 'NONE', #52968, #14119, #14894, .T. ) ;
#52868=CARTESIAN_POINT ( 'NONE',  ( -3.826923076923078426, -6.376774720514408301, 19.19230769230769695 ) ) ;
#52869=DIRECTION ( 'NONE',  ( 0.000000000000000000, 1.000000000000000000, 0.000000000000000000 ) ) ;
#52871=EDGE_CURVE ( 'NONE', #67215, #94249, #78391, .T. ) ;
#52873=EDGE_CURVE ( 'NONE', #50095, #58927, #96140, .T. ) ;
#52877=PLANE ( 'NONE',  #99814 ) ;
#52885=DIRECTION ( 'NONE',  ( -0.2488812114211667037, 0.000000000000000000, -0.9685340172660599212 ) ) ;
#52888=EDGE_CURVE ( 'NONE', #29990, #45914, #11396, .T. ) ;
#52893=AXIS2_PLACEMENT_3D ( 'NONE', #51760, #98408, #12681 ) ;
#52897=CARTESIAN_POINT ( 'NONE',  ( 6.184520403203631389, -5.356774720514425603, -25.32021290018218451 ) ) ;
#52902=FACE_OUTER_BOUND ( 'NONE', #26244, .T. ) ;
#52904=DIRECTION ( 'NONE',  ( -0.000000000000000000, 1.000000000000000000, -0.000000000000000000 ) ) ;
#52911=CARTESIAN_POINT ( 'NONE',  ( 3.180076745125948179, 5.965225279485592225, -28.87659520466657526 ) ) ;
#52916=EDGE_LOOP ( 'NONE', ( #17080, #26297, #22130, #15215 ) ) ;
#52943=LINE ( 'NONE', #60564, #35094 ) ;
#52946=CARTESIAN_POINT ( 'NONE',  ( 0.7051282051282083962, -5.876774720514426953, 21.75000000000000000 ) ) ;
#52947=EDGE_LOOP ( 'NONE', ( #73534, #86420, #35355, #25995 ) ) ;
#52958=ORIENTED_EDGE ( 'NONE', *, *, #49029, .F. ) ;
#52959=CARTESIAN_POINT ( 'NONE',  ( 29.73860345376319003, -1.682774720514426114, -1.272392034746785860 ) ) ;
#52962=CARTESIAN_POINT ( 'NONE',  ( -19.80875734969026425, 5.965225279485572685, 31.02402280011862246 ) ) ;
#52968=VERTEX_POINT ( 'NONE', #72804 ) ;
#52972=ORIENTED_EDGE ( 'NONE', *, *, #26043, .F. ) ;
#52974=ORIENTED_EDGE ( 'NONE', *, *, #63314, .T. ) ;
#52982=CARTESIAN_POINT ( 'NONE',  ( 5.541369867593821219, -5.876774720514426065, 21.42815349816763160 ) ) ;
#52993=CARTESIAN_POINT ( 'NONE',  ( 3.248328688408994580, -5.876774720514406525, 18.75910638930973917 ) ) ;
#52995=CARTESIAN_POINT ( 'NONE',  ( 3.769940963823357638, -5.876774720514403860, 18.16074422543206879 ) ) ;
#53006=EDGE_CURVE ( 'NONE', #71460, #59162, #19000, .T. ) ;
#53008=LINE ( 'NONE', #84932, #66958 ) ;
#53016=DIRECTION ( 'NONE',  ( -0.000000000000000000, 1.000000000000000000, -0.000000000000000000 ) ) ;
#53018=DIRECTION ( 'NONE',  ( 0.000000000000000000, -1.000000000000000000, 0.000000000000000000 ) ) ;
#53026=CARTESIAN_POINT ( 'NONE',  ( -1.044792363895550302, -6.376774720514417183, 20.41272575174754422 ) ) ;
#53027=CARTESIAN_POINT ( 'NONE',  ( -1.345681049247692940, -6.376774720514410077, 19.69174559449348294 ) ) ;
#53036=LINE ( 'NONE', #62643, #16013 ) ;
#53042=ORIENTED_EDGE ( 'NONE', *, *, #22042, .T. ) ;
#53043=CARTESIAN_POINT ( 'NONE',  ( -0.2112149364088803105, -6.376774720514410077, 19.49357334786886398 ) ) ;
#53048=CARTESIAN_POINT ( 'NONE',  ( -10.24059822343757808, -6.376774720514426953, 22.08128695274315945 ) ) ;
#53050=VERTEX_POINT ( 'NONE', #97621 ) ;
#53057=ORIENTED_EDGE ( 'NONE', *, *, #39252, .T. ) ;
#53072=CARTESIAN_POINT ( 'NONE',  ( -3.004714864173751998, -5.876774720514410966, 19.63296556618507083 ) ) ;
#53084=CARTESIAN_POINT ( 'NONE',  ( 4.613443512364428400, -6.376774720514411854, 19.38647409819875733 ) ) ;
#53085=VERTEX_POINT ( 'NONE', #10392 ) ;
#53089=CARTESIAN_POINT ( 'NONE',  ( 31.62300803125484094, -5.234178280976530928, -3.660617518925037395 ) ) ;
#53104=ORIENTED_EDGE ( 'NONE', *, *, #80833, .T. ) ;
#53108=CARTESIAN_POINT ( 'NONE',  ( 32.66876533700883556, 5.965225279485572685, -12.58926540598386445 ) ) ;
#53125=CARTESIAN_POINT ( 'NONE',  ( -2.532641601674031850, -6.376774720514410077, 19.55266968305501507 ) ) ;
#53135=PLANE ( 'NONE',  #20889 ) ;
#53140=EDGE_CURVE ( 'NONE', #60724, #100069, #61074, .T. ) ;
#53142=CARTESIAN_POINT ( 'NONE',  ( 14.76093561896378326, -3.316774720514426456, -26.55548769130088260 ) ) ;
#53146=DIRECTION ( 'NONE',  ( 0.000000000000000000, 0.000000000000000000, -1.000000000000000000 ) ) ;
#53149=DIRECTION ( 'NONE',  ( -0.000000000000000000, 1.000000000000000000, -0.000000000000000000 ) ) ;
#53150=CARTESIAN_POINT ( 'NONE',  ( 3.323502641304225236, -5.876774720514426065, 21.72931788002195219 ) ) ;
#53157=CARTESIAN_POINT ( 'NONE',  ( 22.02124265030973760, -7.835183881457444599, 14.80402280011862359 ) ) ;
#53160=CARTESIAN_POINT ( 'NONE',  ( 22.81105451610979173, 8.475225279485572472, -17.31691820600746823 ) ) ;
#53161=AXIS2_PLACEMENT_3D ( 'NONE', #82538, #50601, #81555 ) ;
#53162=EDGE_CURVE ( 'NONE', #65082, #11869, #6764, .T. ) ;
#53165=DIRECTION ( 'NONE',  ( 0.000000000000000000, 0.000000000000000000, 1.000000000000000000 ) ) ;
#53166=B_SPLINE_SURFACE_WITH_KNOTS ( 'NONE', 3, 1, ( 
 ( #74450, #10554 ),
 ( #43513, #28273 ),
 ( #88189, #3953 ),
 ( #26281, #97780 ),
 ( #18659, #49634 ),
 ( #72467, #4454 ),
 ( #11547, #42523 ),
 ( #35406, #4942 ),
 ( #73460, #19654 ),
 ( #66858, #59231 ),
 ( #80564, #2961 ),
 ( #11059, #43015 ),
 ( #66363, #33894 ),
 ( #96295, #58241 ),
 ( #50127, #57259 ) ),
 .UNSPECIFIED., .F., .F., .F.,
 ( 4, 1, 1, 1, 1, 1, 1, 1, 1, 1, 1, 1, 4 ),
 ( 2, 2 ),
 ( 0.000000000000000000, 0.1041667992898099859, 0.1978560952899031111, 0.2832345117281489522, 0.3600126653135322652, 0.4338442080180774374, 0.5095057223304355620, 0.5870428909783852456, 0.6687538545127398315, 0.7511636688534701900, 0.8334676797015420080, 0.9158479811556836658, 1.000000000000000000 ),
 ( 0.000000000000000000, 1.000000000000000000 ),
 .UNSPECIFIED. ) ;
#53167=CARTESIAN_POINT ( 'NONE',  ( -5.799455386767018439, -6.376774720514413630, 19.66076420632890276 ) ) ;
#53168=DIRECTION ( 'NONE',  ( -0.000000000000000000, 1.000000000000000000, -0.000000000000000000 ) ) ;
#53174=CARTESIAN_POINT ( 'NONE',  ( -17.64648606763744354, 5.965225279485594001, -23.04404205923972526 ) ) ;
#53177=DIRECTION ( 'NONE',  ( 0.000000000000000000, 1.000000000000000000, 0.000000000000000000 ) ) ;
#53198=ORIENTED_EDGE ( 'NONE', *, *, #8486, .T. ) ;
#53200=CIRCLE ( 'NONE', #9430, 129.7684398600581517 ) ;
#53202=CARTESIAN_POINT ( 'NONE',  ( -11.64875734969026233, 5.965225279485572685, 30.51402280011862089 ) ) ;
#53205=ORIENTED_EDGE ( 'NONE', *, *, #32528, .T. ) ;
#53206=CARTESIAN_POINT ( 'NONE',  ( 4.886128916861816052, -5.876774720514410077, 19.14085035285361514 ) ) ;
#53207=AXIS2_PLACEMENT_3D ( 'NONE', #40905, #57154, #88093 ) ;
#53219=EDGE_LOOP ( 'NONE', ( #40976, #54222, #81918, #32077 ) ) ;
#53228=DIRECTION ( 'NONE',  ( 0.000000000000000000, 1.000000000000000000, -8.673617379884035472E-16 ) ) ;
#53236=DIRECTION ( 'NONE',  ( 0.000000000000000000, 0.000000000000000000, 1.000000000000000000 ) ) ;
#53250=DIRECTION ( 'NONE',  ( 0.000000000000000000, 0.000000000000000000, 1.000000000000000000 ) ) ;
#53255=EDGE_CURVE ( 'NONE', #33670, #52199, #31100, .T. ) ;
#53256=CARTESIAN_POINT ( 'NONE',  ( -5.895658455092926076, -5.876774720514418071, 20.50445910983877340 ) ) ;
#53268=CARTESIAN_POINT ( 'NONE',  ( 33.29716795723528833, -4.396921096972350007, -11.57973373708315989 ) ) ;
#53288=AXIS2_PLACEMENT_3D ( 'NONE', #10950, #3848, #50025 ) ;
#53290=DIRECTION ( 'NONE',  ( -1.333806637208504346E-15, 6.669033186042521139E-15, -1.000000000000000000 ) ) ;
#53296=ORIENTED_EDGE ( 'NONE', *, *, #14202, .T. ) ;
#53297=DIRECTION ( 'NONE',  ( 0.5630016722799275897, 7.885106708985486076E-16, -0.8264557562326038109 ) ) ;
#53310=B_SPLINE_CURVE_WITH_KNOTS ( 'NONE', 3,
 ( #81956, #74345, #75827, #21534, #6327, #89573, #27678, #5328, #28669, #60137, #66261, #91060, #20056, #67747, #36289, #37282, #4836, #12930, #59631 ),
 .UNSPECIFIED., .F., .F.,
 ( 4, 1, 1, 1, 1, 1, 1, 1, 1, 1, 1, 1, 1, 1, 1, 1, 4 ),
 ( 0.000000000000000000, 0.06867706841303471144, 0.1368709585090958913, 0.2061143571452998258, 0.2775381819697287922, 0.3497719775548993604, 0.4212508361555678538, 0.4929107569233706077, 0.5670265889927378344, 0.6066141532413346082, 0.6497039535189880199, 0.6973031504846840534, 0.7490856597091360980, 0.8048806474593088733, 0.8654850057023349974, 0.9302371271531362229, 1.000000000000000000 ),
 .UNSPECIFIED. ) ;
#53312=VERTEX_POINT ( 'NONE', #15874 ) ;
#53329=CARTESIAN_POINT ( 'NONE',  ( -10.58858228176428717, 5.965225279485594001, -27.03148018517017093 ) ) ;
#53330=VERTEX_POINT ( 'NONE', #41742 ) ;
#53338=EDGE_LOOP ( 'NONE', ( #70668, #88876, #77440, #55684 ) ) ;
#53343=VECTOR ( 'NONE', #95842, 1000.000000000000000 ) ;
#53370=ORIENTED_EDGE ( 'NONE', *, *, #95374, .F. ) ;
#53371=EDGE_CURVE ( 'NONE', #81742, #96474, #38124, .T. ) ;
#53375=DIRECTION ( 'NONE',  ( -0.000000000000000000, 1.000000000000000000, -0.000000000000000000 ) ) ;
#53378=EDGE_CURVE ( 'NONE', #7123, #24236, #80179, .T. ) ;
#53388=CARTESIAN_POINT ( 'NONE',  ( -1.540913562699879114, -5.876774720514410966, 19.44316438561912008 ) ) ;
#53389=VECTOR ( 'NONE', #29192, 1000.000000000000000 ) ;
#53399=AXIS2_PLACEMENT_3D ( 'NONE', #45185, #30449, #98446 ) ;
#53400=CARTESIAN_POINT ( 'NONE',  ( 7.395977348698951737, -5.299853574627441333, -25.64291752716363249 ) ) ;
#53401=CARTESIAN_POINT ( 'NONE',  ( -65.05438548721848235, -5.356774720514425603, 27.45402280011862572 ) ) ;
#53405=CARTESIAN_POINT ( 'NONE',  ( -1.371775545366004545, -6.376774720514413630, 20.39230070883894186 ) ) ;
#53416=CARTESIAN_POINT ( 'NONE',  ( -7.326845193947049140, -5.876774720514418071, 20.33046051580616265 ) ) ;
#53429=CARTESIAN_POINT ( 'NONE',  ( -5.837039262820512775, -6.376774720514413630, 19.76512419871795245 ) ) ;
#53437=CARTESIAN_POINT ( 'NONE',  ( 0.3908843598833069422, -6.376774720514420736, 20.63520656483649773 ) ) ;
#53448=DIRECTION ( 'NONE',  ( 0.000000000000000000, 0.000000000000000000, 1.000000000000000000 ) ) ;
#53450=CARTESIAN_POINT ( 'NONE',  ( 32.90449424769446551, -3.618459821963367240, -13.06102137676440300 ) ) ;
#53458=ORIENTED_EDGE ( 'NONE', *, *, #47821, .F. ) ;
#53469=CARTESIAN_POINT ( 'NONE',  ( 7.479587785762670471, -6.376774720514417183, 20.73799387832858088 ) ) ;
#53474=DIRECTION ( 'NONE',  ( 2.216313064514630211E-15, -7.253388211138789781E-15, 1.000000000000000000 ) ) ;
#53476=ADVANCED_FACE ( 'NONE', ( #52337 ), #37101, .F. ) ;
#53477=CARTESIAN_POINT ( 'NONE',  ( 30.55234109742892912, -6.376774720514427841, 1.942002712049490487 ) ) ;
#53480=ADVANCED_FACE ( 'NONE', ( #13256 ), #5158, .F. ) ;
#53484=B_SPLINE_CURVE_WITH_KNOTS ( 'NONE', 3,
 ( #15239, #46196, #91864, #36575, #68044, #14733, #98464, #98969 ),
 .UNSPECIFIED., .F., .F.,
 ( 4, 2, 2, 4 ),
 ( 0.007591603542867194493, 0.008652426217380708440, 0.009713248891894220652, 0.01183489424092124681 ),
 .UNSPECIFIED. ) ;
#53485=CARTESIAN_POINT ( 'NONE',  ( -4.141025641025640525, -5.876774720514418959, 20.67377804487179915 ) ) ;
#53489=EDGE_CURVE ( 'NONE', #42575, #35496, #81961, .T. ) ;
#53497=DIRECTION ( 'NONE',  ( 0.000000000000000000, -1.000000000000000000, 0.000000000000000000 ) ) ;
#53499=CARTESIAN_POINT ( 'NONE',  ( 2.884397429187188333, -5.876774720514407413, 18.67943752795919110 ) ) ;
#53501=CARTESIAN_POINT ( 'NONE',  ( 26.73860345374794889, -5.356774720514430044, -3.777353070936031898 ) ) ;
#53511=EDGE_CURVE ( 'NONE', #69928, #49051, #91382, .T. ) ;
#53521=CARTESIAN_POINT ( 'NONE',  ( 0.3910256410256383042, -6.376774720514408301, 19.19230769230768985 ) ) ;
#53536=CARTESIAN_POINT ( 'NONE',  ( 19.75748517575715368, 5.965225279485572685, 28.87153971905864580 ) ) ;
#53538=DIRECTION ( 'NONE',  ( -0.6392559695863496705, 6.845827386180411947E-16, -0.7689940216596069522 ) ) ;
#53541=VERTEX_POINT ( 'NONE', #57303 ) ;
#53542=CARTESIAN_POINT ( 'NONE',  ( 0.2885822020289898759, -6.376774720514415407, 19.94806476610988710 ) ) ;
#53545=VECTOR ( 'NONE', #89788, 1000.000000000000114 ) ;
#53551=VECTOR ( 'NONE', #12835, 1000.000000000000000 ) ;
#53556=CARTESIAN_POINT ( 'NONE',  ( 32.53135143123563466, 5.965225279485572685, 6.926385399448451885 ) ) ;
#53566=EDGE_CURVE ( 'NONE', #75580, #54291, #66414, .T. ) ;
#53570=CARTESIAN_POINT ( 'NONE',  ( -4.141439336867657417, -6.376774720514418959, 20.56083401959468304 ) ) ;
#53573=ORIENTED_EDGE ( 'NONE', *, *, #91098, .F. ) ;
#53574=CARTESIAN_POINT ( 'NONE',  ( -3.054691362729579751, -5.876774720514412742, 19.78730719034165375 ) ) ;
#53576=CARTESIAN_POINT ( 'NONE',  ( 9.150000000000000355, -5.876774720514426953, -15.70000000000000284 ) ) ;
#53578=ADVANCED_FACE ( 'NONE', ( #82110 ), #73013, .F. ) ;
#53581=EDGE_LOOP ( 'NONE', ( #33630, #43604, #17542, #50799, #86134, #4489, #47075, #27645 ) ) ;
#53591=EDGE_LOOP ( 'NONE', ( #85147, #32755, #51475, #98685 ) ) ;
#53612=DIRECTION ( 'NONE',  ( 0.03244919754393515293, 0.000000000000000000, -0.9994733861282923959 ) ) ;
#53633=FACE_OUTER_BOUND ( 'NONE', #84512, .T. ) ;
#53638=DIRECTION ( 'NONE',  ( 0.000000000000000000, 0.000000000000000000, 1.000000000000000000 ) ) ;
#53640=EDGE_LOOP ( 'NONE', ( #81563, #12979, #67378, #24912 ) ) ;
#53642=CARTESIAN_POINT ( 'NONE',  ( -26.91814428177455909, 5.965225279485572685, 29.98490496616818746 ) ) ;
#53650=CARTESIAN_POINT ( 'NONE',  ( 3.323502641304225236, -6.376774720514426065, 21.72931788002195219 ) ) ;
#53653=DIRECTION ( 'NONE',  ( 0.000000000000000000, 0.000000000000000000, 1.000000000000000000 ) ) ;
#53665=CARTESIAN_POINT ( 'NONE',  ( 4.518205171808153509, -5.876774720514407413, 19.05004583296150500 ) ) ;
#53666=LINE ( 'NONE', #29810, #59352 ) ;
#53670=LINE ( 'NONE', #24200, #28711 ) ;
#53673=CARTESIAN_POINT ( 'NONE',  ( -5.596556251055551101, -6.376774720514413630, 19.35667676486397681 ) ) ;
#53674=DIRECTION ( 'NONE',  ( -0.7689940216596069522, -5.365801633547210331E-16, 0.6392559695863496705 ) ) ;
#53675=LINE ( 'NONE', #68392, #35738 ) ;
#53697=EDGE_LOOP ( 'NONE', ( #66522, #97035, #13207, #6270 ) ) ;
#53709=VERTEX_POINT ( 'NONE', #37435 ) ;
#53710=CARTESIAN_POINT ( 'NONE',  ( 4.468667172983064262, -5.876774720514399419, 18.40700896291420463 ) ) ;
#53718=CARTESIAN_POINT ( 'NONE',  ( 5.920986267150416538, -6.376774720514422512, 21.32549308339960348 ) ) ;
#53724=DIRECTION ( 'NONE',  ( 0.000000000000000000, -1.000000000000000000, 0.000000000000000000 ) ) ;
#53727=CARTESIAN_POINT ( 'NONE',  ( 33.69795529655567634, -0.6647747205144264315, 20.86760796525322093 ) ) ;
#53763=CARTESIAN_POINT ( 'NONE',  ( -7.999999999999996447, -5.876774720514426953, 17.50000000000000000 ) ) ;
#53764=CARTESIAN_POINT ( 'NONE',  ( 30.93860345374796594, -0.6647747205144264315, 19.84760796525321780 ) ) ;
#53772=CARTESIAN_POINT ( 'NONE',  ( 33.63305001869471056, -3.481148584080995700, -11.52139411009015291 ) ) ;
#53776=DIRECTION ( 'NONE',  ( -0.000000000000000000, 1.000000000000000000, -0.000000000000000000 ) ) ;
#53778=FACE_OUTER_BOUND ( 'NONE', #49354, .T. ) ;
#53802=CARTESIAN_POINT ( 'NONE',  ( -20.27875734969026311, -7.835183881457444599, 24.00402280011862288 ) ) ;
#53808=AXIS2_PLACEMENT_3D ( 'NONE', #13689, #36534, #98423 ) ;
#53811=EDGE_LOOP ( 'NONE', ( #58376, #38653, #58234, #15621 ) ) ;
#53814=CARTESIAN_POINT ( 'NONE',  ( 3.323502641304225236, -5.876774720514426065, 21.72931788002195219 ) ) ;
#53830=LINE ( 'NONE', #14744, #98725 ) ;
#53831=AXIS2_PLACEMENT_3D ( 'NONE', #3980, #35429, #97807 ) ;
#53843=LINE ( 'NONE', #21368, #80601 ) ;
#53850=CARTESIAN_POINT ( 'NONE',  ( 31.69086887328960245, -3.760767191028114631, 29.45064099519496992 ) ) ;
#53863=ORIENTED_EDGE ( 'NONE', *, *, #75191, .T. ) ;
#53877=EDGE_CURVE ( 'NONE', #53050, #36610, #32003, .T. ) ;
#53878=ADVANCED_FACE ( 'NONE', ( #32507 ), #6991, .T. ) ;
#53904=VECTOR ( 'NONE', #22637, 1000.000000000000000 ) ;
#53917=LINE ( 'NONE', #47690, #27118 ) ;
#53927=EDGE_CURVE ( 'NONE', #20446, #80744, #7051, .T. ) ;
#53930=ORIENTED_EDGE ( 'NONE', *, *, #50523, .F. ) ;
#53937=EDGE_CURVE ( 'NONE', #65105, #35590, #91774, .T. ) ;
#53944=ADVANCED_FACE ( 'NONE', ( #38002 ), #60361, .F. ) ;
#53947=ORIENTED_EDGE ( 'NONE', *, *, #58868, .F. ) ;
#53953=ORIENTED_EDGE ( 'NONE', *, *, #4906, .T. ) ;
#53960=CARTESIAN_POINT ( 'NONE',  ( 31.27206728860909024, -4.132774720514318822, -3.930752063305056332 ) ) ;
#53967=ORIENTED_EDGE ( 'NONE', *, *, #79106, .F. ) ;
#53970=CARTESIAN_POINT ( 'NONE',  ( 32.65112488154859705, -3.727967435732443047, -2.714891177973568492 ) ) ;
#53973=VECTOR ( 'NONE', #56770, 1000.000000000000000 ) ;
#53982=CARTESIAN_POINT ( 'NONE',  ( 6.420673076923079314, -5.876774720514427841, 21.83974358974358765 ) ) ;
#54008=CARTESIAN_POINT ( 'NONE',  ( 4.016587897052070311, -6.376774720514426065, 21.44459449800855921 ) ) ;
#54011=FACE_OUTER_BOUND ( 'NONE', #90006, .T. ) ;
#54012=LINE ( 'NONE', #92552, #32645 ) ;
#54028=CARTESIAN_POINT ( 'NONE',  ( -7.627782137226129855, -6.376774720514413630, 20.04377961306771994 ) ) ;
#54031=VERTEX_POINT ( 'NONE', #67462 ) ;
#54040=AXIS2_PLACEMENT_3D ( 'NONE', #78283, #70687, #9277 ) ;
#54049=EDGE_LOOP ( 'NONE', ( #69161, #63734, #8496, #93242, #9988, #63423, #61752, #14095, #66281, #37407, #26249, #4003, #2205, #29724, #32562 ) ) ;
#54052=EDGE_CURVE ( 'NONE', #8388, #74863, #22756, .T. ) ;
#54057=CARTESIAN_POINT ( 'NONE',  ( 4.912344403463128728, -6.376774720514408301, 19.26008510998990886 ) ) ;
#54059=VERTEX_POINT ( 'NONE', #47126 ) ;
#54063=VERTEX_POINT ( 'NONE', #23767 ) ;
#54065=DIRECTION ( 'NONE',  ( 0.000000000000000000, -3.740001113483016365E-15, -1.000000000000000000 ) ) ;
#54066=CARTESIAN_POINT ( 'NONE',  ( -4.440151687742864617, -5.876774720514411854, 19.67013632031035897 ) ) ;
#54072=CARTESIAN_POINT ( 'NONE',  ( -29.49875734969026198, -0.3587747205144265483, 10.11402280011862587 ) ) ;
#54075=CARTESIAN_POINT ( 'NONE',  ( -4.147110899021980934, -6.376774720514418959, 20.45311193189268906 ) ) ;
#54078=ADVANCED_FACE ( 'NONE', ( #77048 ), #86172, .F. ) ;
#54079=PLANE ( 'NONE',  #40363 ) ;
#54082=EDGE_LOOP ( 'NONE', ( #95883, #29395 ) ) ;
#54083=CARTESIAN_POINT ( 'NONE',  ( 4.372949846226492632, -6.376774720514404748, 18.80635842184136308 ) ) ;
#54091=CARTESIAN_POINT ( 'NONE',  ( 5.659515148826130826, -3.316774720513238517, -27.47062408975114067 ) ) ;
#54094=DIRECTION ( 'NONE',  ( -0.000000000000000000, 0.000000000000000000, -1.000000000000000000 ) ) ;
#54099=VECTOR ( 'NONE', #68927, 1000.000000000000114 ) ;
#54104=VECTOR ( 'NONE', #64871, 1000.000000000000000 ) ;
#54115=VERTEX_POINT ( 'NONE', #100373 ) ;
#54126=FACE_BOUND ( 'NONE', #54049, .T. ) ;
#54131=DIRECTION ( 'NONE',  ( 0.9921023176230513441, 0.000000000000000000, -0.1254312216594016538 ) ) ;
#54153=CARTESIAN_POINT ( 'NONE',  ( 2.989331223418256744, -6.376774720514424288, 21.46569930292093886 ) ) ;
#54156=DIRECTION ( 'NONE',  ( 1.000000000000000000, 0.000000000000000000, 0.000000000000000000 ) ) ;
#54159=DIRECTION ( 'NONE',  ( 0.000000000000000000, -1.000000000000000000, 0.000000000000000000 ) ) ;
#54160=LINE ( 'NONE', #46533, #54916 ) ;
#54161=CARTESIAN_POINT ( 'NONE',  ( 15.10689886641524105, -3.536627728863115827, -27.28884555219614327 ) ) ;
#54170=CARTESIAN_POINT ( 'NONE',  ( 4.328803674008796065, -5.876774720514407413, 18.75671216747623049 ) ) ;
#54171=VECTOR ( 'NONE', #93585, 1000.000000000000000 ) ;
#54179=CARTESIAN_POINT ( 'NONE',  ( -5.706951327759631099, -6.376774720514413630, 19.48569229636961353 ) ) ;
#54193=EDGE_LOOP ( 'NONE', ( #65566, #6028, #26113, #68755 ) ) ;
#54213=CARTESIAN_POINT ( 'NONE',  ( 4.856316114246853388, -5.876774720514406525, 19.03119074624055074 ) ) ;
#54222=ORIENTED_EDGE ( 'NONE', *, *, #20805, .F. ) ;
#54223=VERTEX_POINT ( 'NONE', #11054 ) ;
#54237=AXIS2_PLACEMENT_3D ( 'NONE', #26730, #51071, #33839 ) ;
#54238=VERTEX_POINT ( 'NONE', #41507 ) ;
#54246=DIRECTION ( 'NONE',  ( -0.1875268396392987258, 0.000000000000000000, -0.9822594791677485837 ) ) ;
#54248=CARTESIAN_POINT ( 'NONE',  ( -7.641025641025638748, -5.876774720514426953, 21.75000000000001066 ) ) ;
#54265=EDGE_CURVE ( 'NONE', #17321, #26032, #1953, .T. ) ;
#54276=ORIENTED_EDGE ( 'NONE', *, *, #4027, .F. ) ;
#54282=CARTESIAN_POINT ( 'NONE',  ( -0.6227173540047638012, -6.376774720514413630, 19.48351902941045211 ) ) ;
#54291=VERTEX_POINT ( 'NONE', #12041 ) ;
#54305=ORIENTED_EDGE ( 'NONE', *, *, #55124, .F. ) ;
#54315=ORIENTED_EDGE ( 'NONE', *, *, #13513, .F. ) ;
#54318=EDGE_CURVE ( 'NONE', #50083, #27752, #97774, .T. ) ;
#54332=FACE_OUTER_BOUND ( 'NONE', #87742, .T. ) ;
#54333=CARTESIAN_POINT ( 'NONE',  ( 4.585161930874343206, -5.876774720514427841, 21.47592444013076118 ) ) ;
#54335=VERTEX_POINT ( 'NONE', #31129 ) ;
#54352=CARTESIAN_POINT ( 'NONE',  ( 9.278253834636473130, -5.876774720514426953, 18.21871304725684482 ) ) ;
#54359=CARTESIAN_POINT ( 'NONE',  ( 15.97264540888995299, -3.316774720514426456, -27.93485543958162864 ) ) ;
#54360=CARTESIAN_POINT ( 'NONE',  ( -5.486124437288584232, -5.876774720514417183, 19.74568812963598319 ) ) ;
#54367=DIRECTION ( 'NONE',  ( -1.000000000000000000, 0.000000000000000000, 1.257682986112628908E-16 ) ) ;
#54368=DIRECTION ( 'NONE',  ( 0.000000000000000000, -1.000000000000000000, 0.000000000000000000 ) ) ;
#54376=VERTEX_POINT ( 'NONE', #43993 ) ;
#54394=PLANE ( 'NONE',  #71292 ) ;
#54415=VECTOR ( 'NONE', #95855, 1000.000000000000000 ) ;
#54417=EDGE_LOOP ( 'NONE', ( #22471, #35589, #96005, #21719, #75114, #54528, #65589, #24917, #30217 ) ) ;
#54420=DIRECTION ( 'NONE',  ( -8.334928612639484546E-17, 1.000000000000000000, -7.321843366904296032E-17 ) ) ;
#54423=VECTOR ( 'NONE', #75908, 1000.000000000000114 ) ;
#54434=CARTESIAN_POINT ( 'NONE',  ( -0.4909855769230799249, -5.876774720514410077, 19.14743589743590491 ) ) ;
#54439=LINE ( 'NONE', #23455, #96721 ) ;
#54440=VERTEX_POINT ( 'NONE', #58723 ) ;
#54442=DIRECTION ( 'NONE',  ( 0.000000000000000000, -1.000000000000000000, 0.000000000000000000 ) ) ;
#54460=CARTESIAN_POINT ( 'NONE',  ( 7.311104923646705167, -5.876774720514416295, 20.13320233724603980 ) ) ;
#54462=VERTEX_POINT ( 'NONE', #2704 ) ;
#54465=ORIENTED_EDGE ( 'NONE', *, *, #2514, .T. ) ;
#54482=CARTESIAN_POINT ( 'NONE',  ( 3.552794897967157528, -6.376774720514401196, 18.18650940196788568 ) ) ;
#54485=DIRECTION ( 'NONE',  ( -0.000000000000000000, 0.000000000000000000, -1.000000000000000000 ) ) ;
#54491=DIRECTION ( 'NONE',  ( 0.000000000000000000, -1.000000000000000000, 0.000000000000000000 ) ) ;
#54500=FACE_OUTER_BOUND ( 'NONE', #83603, .T. ) ;
#54511=CARTESIAN_POINT ( 'NONE',  ( 0.3910256410256418569, -5.876774720514419847, 20.67377804487180271 ) ) ;
#54516=CARTESIAN_POINT ( 'NONE',  ( -7.641025641025641413, -6.376774720514418959, 20.36458333333334636 ) ) ;
#54517=B_SPLINE_CURVE_WITH_KNOTS ( 'NONE', 3,
 ( #77193, #8711, #91933, #92429, #22896, #7699, #53388, #45765, #47273, #84317, #91, #86328, #15806, #69608, #23400 ),
 .UNSPECIFIED., .F., .F.,
 ( 4, 1, 1, 1, 1, 1, 1, 1, 1, 1, 1, 1, 4 ),
 ( 0.000000000000000000, 0.07176606415833945707, 0.1412255357663688426, 0.2091158524974623678, 0.2748396534685264014, 0.3394829303752206484, 0.4024762667353993240, 0.4649418891713267277, 0.5268326406463827993, 0.6474148160608228508, 0.7655615117859491114, 0.8816150870393308914, 1.000000000000000000 ),
 .UNSPECIFIED. ) ;
#54527=EDGE_LOOP ( 'NONE', ( #100097, #48466, #42046, #5800 ) ) ;
#54528=ORIENTED_EDGE ( 'NONE', *, *, #98736, .F. ) ;
#54529=CARTESIAN_POINT ( 'NONE',  ( -0.1037292527911751056, -6.376774720514413630, 19.53657742262743824 ) ) ;
#54538=CARTESIAN_POINT ( 'NONE',  ( -4.141025641025641413, -5.876774720514419847, 20.67377804487180271 ) ) ;
#54541=VERTEX_POINT ( 'NONE', #71208 ) ;
#54545=DIRECTION ( 'NONE',  ( -0.000000000000000000, -1.000000000000000000, -0.000000000000000000 ) ) ;
#54546=ORIENTED_EDGE ( 'NONE', *, *, #80065, .T. ) ;
#54549=LINE ( 'NONE', #7362, #68080 ) ;
#54550=CARTESIAN_POINT ( 'NONE',  ( -4.213970605900704491, -5.876774720514415407, 20.02963804100705758 ) ) ;
#54555=DIRECTION ( 'NONE',  ( -0.06486421869277853025, 0.000000000000000000, 0.9978940991575085961 ) ) ;
#54559=CARTESIAN_POINT ( 'NONE',  ( -1.568769572606061535, -5.876774720514415407, 19.76359802465961835 ) ) ;
#54560=ORIENTED_EDGE ( 'NONE', *, *, #26105, .T. ) ;
#54561=CARTESIAN_POINT ( 'NONE',  ( 0.000000000000000000, -4.056774720514426669, 0.000000000000000000 ) ) ;
#54564=ORIENTED_EDGE ( 'NONE', *, *, #90843, .F. ) ;
#54567=VECTOR ( 'NONE', #94925, 1000.000000000000000 ) ;
#54575=CARTESIAN_POINT ( 'NONE',  ( 282.9764569301858046, 5.965225279485572685, 20.79159422840526616 ) ) ;
#54577=CARTESIAN_POINT ( 'NONE',  ( 9.214646252596866205, -5.356774720515496746, -27.04520690447069597 ) ) ;
#54583=ORIENTED_EDGE ( 'NONE', *, *, #24326, .T. ) ;
#54593=ORIENTED_EDGE ( 'NONE', *, *, #91820, .T. ) ;
#54595=CARTESIAN_POINT ( 'NONE',  ( 14.76093561896379214, -3.316774720514426456, -26.55548769130089681 ) ) ;
#54597=CARTESIAN_POINT ( 'NONE',  ( -6.775140224358976226, -5.876774720514409189, 19.14743589743590846 ) ) ;
#54602=ORIENTED_EDGE ( 'NONE', *, *, #100148, .F. ) ;
#54606=CARTESIAN_POINT ( 'NONE',  ( -1.044871794871790938, -5.876774720514426953, 21.75000000000000355 ) ) ;
#54613=VECTOR ( 'NONE', #32623, 1000.000000000000000 ) ;
#54617=CARTESIAN_POINT ( 'NONE',  ( 32.84232313084847732, -4.840274619473232676, -11.71291885348859196 ) ) ;
#54623=DIRECTION ( 'NONE',  ( -0.000000000000000000, 1.000000000000000000, -0.000000000000000000 ) ) ;
#54627=PLANE ( 'NONE',  #74357 ) ;
#54642=LINE ( 'NONE', #39407, #28912 ) ;
#54643=DIRECTION ( 'NONE',  ( 0.5473879298857849962, 0.000000000000000000, 0.8368789961609472972 ) ) ;
#54646=VECTOR ( 'NONE', #23192, 1000.000000000000000 ) ;
#54648=EDGE_CURVE ( 'NONE', #16838, #95239, #35148, .T. ) ;
#54651=PLANE ( 'NONE',  #55893 ) ;
#54661=CARTESIAN_POINT ( 'NONE',  ( 4.413617546364139166, -5.876774720514407413, 18.86076033669171181 ) ) ;
#54666=ORIENTED_EDGE ( 'NONE', *, *, #79456, .T. ) ;
#54670=CARTESIAN_POINT ( 'NONE',  ( -5.053929855541893446, -6.376774720514410077, 19.14848118821636547 ) ) ;
#54672=CARTESIAN_POINT ( 'NONE',  ( -0.02075734969026423599, 6.475225279485573360, -0.08597719988137648983 ) ) ;
#54676=ORIENTED_EDGE ( 'NONE', *, *, #78411, .F. ) ;
#54686=CIRCLE ( 'NONE', #74157, 2.500000000000000444 ) ;
#54690=CARTESIAN_POINT ( 'NONE',  ( 4.653733606810938284, -5.876774720514412742, 19.95301661664751336 ) ) ;
#54692=EDGE_LOOP ( 'NONE', ( #64082, #75565, #70249, #92832 ) ) ;
#54695=ORIENTED_EDGE ( 'NONE', *, *, #65787, .T. ) ;
#54696=AXIS2_PLACEMENT_3D ( 'NONE', #38244, #46872, #100119 ) ;
#54701=B_SPLINE_CURVE_WITH_KNOTS ( 'NONE', 3,
 ( #29109, #62073, #93496, #68681, #23986, #92005, #657, #7770, #39715, #7262, #84891, #160, #54958, #76762, #30104, #70674, #69679, #94002, #6767 ),
 .UNSPECIFIED., .F., .F.,
 ( 4, 1, 1, 1, 1, 1, 1, 1, 1, 1, 1, 1, 1, 1, 1, 1, 4 ),
 ( 0.000000000000000000, 0.07560433049574560860, 0.1479650154827357456, 0.2187969985237000203, 0.2894704453213765016, 0.3597242180874995476, 0.4297077387530455206, 0.5004965198485865630, 0.5744290198679483650, 0.6139472962286703916, 0.6571552698261112768, 0.7039727697209375856, 0.7549389848168005512, 0.8097066112894875101, 0.8688329536985499590, 0.9323854739325975194, 1.000000000000000000 ),
 .UNSPECIFIED. ) ;
#54720=VERTEX_POINT ( 'NONE', #29015 ) ;
#54722=EDGE_CURVE ( 'NONE', #27752, #35590, #22036, .T. ) ;
#54723=DIRECTION ( 'NONE',  ( -0.000000000000000000, 1.000000000000000000, -0.000000000000000000 ) ) ;
#54754=LINE ( 'NONE', #1966, #75108 ) ;
#54773=CARTESIAN_POINT ( 'NONE',  ( 10.24059822343757986, -5.876774720514426953, 22.82308057603840368 ) ) ;
#54802=EDGE_LOOP ( 'NONE', ( #41890, #47122, #2580, #87495, #57601 ) ) ;
#54808=VERTEX_POINT ( 'NONE', #30515 ) ;
#54809=ORIENTED_EDGE ( 'NONE', *, *, #91943, .T. ) ;
#54816=ADVANCED_FACE ( 'NONE', ( #91407 ), #21884, .T. ) ;
#54818=ORIENTED_EDGE ( 'NONE', *, *, #91243, .T. ) ;
#54831=EDGE_CURVE ( 'NONE', #1282, #60109, #43148, .T. ) ;
#54834=CARTESIAN_POINT ( 'NONE',  ( -32.30247028140506416, 6.475225279485573360, 27.60502002861223048 ) ) ;
#54836=ORIENTED_EDGE ( 'NONE', *, *, #19409, .F. ) ;
#54838=ORIENTED_EDGE ( 'NONE', *, *, #67321, .T. ) ;
#54848=ORIENTED_EDGE ( 'NONE', *, *, #74195, .T. ) ;
#54850=B_SPLINE_CURVE_WITH_KNOTS ( 'NONE', 3,
 ( #40083, #63441, #94361, #24847, #2034, #2737, #88966 ),
 .UNSPECIFIED., .F., .F.,
 ( 4, 1, 1, 1, 4 ),
 ( 0.000000000000000000, 0.2835948081386937547, 0.5433948405759735367, 0.7806456291745620391, 1.000000000000000000 ),
 .UNSPECIFIED. ) ;
#54855=CARTESIAN_POINT ( 'NONE',  ( 29.58524742607616176, -4.112217781777255610, 29.11978736867098760 ) ) ;
#54856=CARTESIAN_POINT ( 'NONE',  ( -5.576923076923076650, -5.876774720514418071, 20.44941907051282470 ) ) ;
#54862=CARTESIAN_POINT ( 'NONE',  ( -5.554587162835583847, -5.876774720514417183, 19.99258394656885329 ) ) ;
#54867=CARTESIAN_POINT ( 'NONE',  ( 2.993365552154886089, -5.876774720514413630, 19.24059921568563425 ) ) ;
#54871=CARTESIAN_POINT ( 'NONE',  ( 14.83405752585509596, -4.881907540129173384, -27.54622755360215791 ) ) ;
#54874=CARTESIAN_POINT ( 'NONE',  ( -65.05438548721848235, 6.475225279485573360, 0.7300228001186309656 ) ) ;
#54875=FACE_OUTER_BOUND ( 'NONE', #60804, .T. ) ;
#54878=AXIS2_PLACEMENT_3D ( 'NONE', #73733, #66153, #74233 ) ;
#54889=CARTESIAN_POINT ( 'NONE',  ( 5.464387484610083057, -6.376774720514420736, 21.31215092858952431 ) ) ;
#54891=CARTESIAN_POINT ( 'NONE',  ( -4.141025641025642301, -5.876774720514409189, 19.19230769230769695 ) ) ;
#54896=ORIENTED_EDGE ( 'NONE', *, *, #48658, .T. ) ;
#54902=FACE_OUTER_BOUND ( 'NONE', #33717, .T. ) ;
#54905=ORIENTED_EDGE ( 'NONE', *, *, #99060, .F. ) ;
#54913=CARTESIAN_POINT ( 'NONE',  ( 31.59245846751552378, -5.049734226592146769, -4.287355462049295518 ) ) ;
#54916=VECTOR ( 'NONE', #1369, 1000.000000000000000 ) ;
#54928=AXIS2_PLACEMENT_3D ( 'NONE', #30826, #92218, #98322 ) ;
#54929=ORIENTED_EDGE ( 'NONE', *, *, #86679, .T. ) ;
#54940=EDGE_CURVE ( 'NONE', #100313, #9886, #41170, .T. ) ;
#54945=CARTESIAN_POINT ( 'NONE',  ( 33.07248226229787491, -4.977706540348799891, -12.91345179487514905 ) ) ;
#54949=ADVANCED_FACE ( 'NONE', ( #47253 ), #85299, .F. ) ;
#54950=EDGE_LOOP ( 'NONE', ( #63933, #15523, #21113, #56095 ) ) ;
#54958=CARTESIAN_POINT ( 'NONE',  ( -7.603582339867426043, -6.376774720514417183, 19.86545874326176175 ) ) ;
#54998=CIRCLE ( 'NONE', #74472, 28.96799999999999642 ) ;
#55008=CARTESIAN_POINT ( 'NONE',  ( 6.365284455128204399, -6.376774720514413630, 19.73076923076922640 ) ) ;
#55016=CARTESIAN_POINT ( 'NONE',  ( -10.75273025779354796, -6.376774720514426953, 23.03521261039436752 ) ) ;
#55020=PLANE ( 'NONE',  #64610 ) ;
#55035=CARTESIAN_POINT ( 'NONE',  ( -5.023036858974361252, -6.376774720514410077, 19.14743589743590846 ) ) ;
#55041=VERTEX_POINT ( 'NONE', #48766 ) ;
#55045=VECTOR ( 'NONE', #10920, 1000.000000000000000 ) ;
#55055=EDGE_CURVE ( 'NONE', #54440, #69030, #31014, .T. ) ;
#55057=DIRECTION ( 'NONE',  ( -0.000000000000000000, 1.000000000000000000, -0.000000000000000000 ) ) ;
#55058=CARTESIAN_POINT ( 'NONE',  ( -4.213970605900704491, -6.376774720514415407, 20.02963804100705758 ) ) ;
#55060=EDGE_LOOP ( 'NONE', ( #91851, #9797, #13613, #3177 ) ) ;
#55069=AXIS2_PLACEMENT_3D ( 'NONE', #23224, #39966, #61818 ) ;
#55083=CARTESIAN_POINT ( 'NONE',  ( 6.184520403203634942, -6.376774720514426953, -25.32021290018218451 ) ) ;
#55085=CARTESIAN_POINT ( 'NONE',  ( 7.732492002959944877, -5.356774720515376842, -27.16032169580908473 ) ) ;
#55096=CARTESIAN_POINT ( 'NONE',  ( -6.680782769985652791, -6.376774720514411854, 19.46295461892502132 ) ) ;
#55124=EDGE_CURVE ( 'NONE', #71450, #63790, #7491, .T. ) ;
#55128=DIRECTION ( 'NONE',  ( 0.000000000000000000, 0.000000000000000000, 1.000000000000000000 ) ) ;
#55129=CARTESIAN_POINT ( 'NONE',  ( -2.599001758237162285, -5.876774720514414518, 19.60308799987317485 ) ) ;
#55133=VECTOR ( 'NONE', #97597, 1000.000000000000000 ) ;
#55134=CARTESIAN_POINT ( 'NONE',  ( 4.403244164709623654, -5.876774720514404748, 18.35516266052912826 ) ) ;
#55136=ORIENTED_EDGE ( 'NONE', *, *, #34116, .F. ) ;
#55145=CARTESIAN_POINT ( 'NONE',  ( 32.60294298177590377, -2.682774720514426559, -11.48871326860665931 ) ) ;
#55154=CIRCLE ( 'NONE', #95632, 2.040000000000000036 ) ;
#55159=CARTESIAN_POINT ( 'NONE',  ( 25.61870917940689196, 5.965225279485572685, 29.49402280011862487 ) ) ;
#55161=CYLINDRICAL_SURFACE ( 'NONE', #74256, 1.700000000000000178 ) ;
#55164=CARTESIAN_POINT ( 'NONE',  ( -2.750773227259631692, -6.376774720514413630, 19.84584863393302001 ) ) ;
#55187=ORIENTED_EDGE ( 'NONE', *, *, #72679, .T. ) ;
#55189=VERTEX_POINT ( 'NONE', #92297 ) ;
#55194=VERTEX_POINT ( 'NONE', #36511 ) ;
#55198=CARTESIAN_POINT ( 'NONE',  ( 4.613443512364428400, -5.876774720514412742, 19.38647409819875733 ) ) ;
#55200=ORIENTED_EDGE ( 'NONE', *, *, #94861, .T. ) ;
#55207=ORIENTED_EDGE ( 'NONE', *, *, #53255, .F. ) ;
#55215=CARTESIAN_POINT ( 'NONE',  ( -6.499903988472228278, -5.876774720514408301, 19.18381548539529646 ) ) ;
#55224=DIRECTION ( 'NONE',  ( -0.7640209514960704107, 0.000000000000000000, 0.6451914333552789538 ) ) ;
#55226=ORIENTED_EDGE ( 'NONE', *, *, #29816, .F. ) ;
#55235=CYLINDRICAL_SURFACE ( 'NONE', #88699, 2.499999999999996891 ) ;
#55237=CARTESIAN_POINT ( 'NONE',  ( 0.000000000000000000, -6.376774720514426953, 0.000000000000000000 ) ) ;
#55239=LINE ( 'NONE', #70954, #42192 ) ;
#55242=ORIENTED_EDGE ( 'NONE', *, *, #82704, .T. ) ;
#55269=ORIENTED_EDGE ( 'NONE', *, *, #72938, .F. ) ;
#55272=AXIS2_PLACEMENT_3D ( 'NONE', #61733, #16027, #63232 ) ;
#55281=CARTESIAN_POINT ( 'NONE',  ( -0.4686347352592966087, -5.876774720514411854, 19.46274624311237034 ) ) ;
#55286=FACE_OUTER_BOUND ( 'NONE', #52173, .T. ) ;
#55287=ADVANCED_FACE ( 'NONE', ( #37018 ), #14672, .T. ) ;
#55301=ORIENTED_EDGE ( 'NONE', *, *, #47825, .F. ) ;
#55306=CARTESIAN_POINT ( 'NONE',  ( -1.595974963000059477, -5.876774720514407413, 19.39236848396478408 ) ) ;
#55307=VERTEX_POINT ( 'NONE', #83179 ) ;
#55323=VERTEX_POINT ( 'NONE', #86687 ) ;
#55330=CARTESIAN_POINT ( 'NONE',  ( 5.085443162053245203, -3.316774720514426456, -27.56355752155217331 ) ) ;
#55339=ORIENTED_EDGE ( 'NONE', *, *, #86548, .F. ) ;
#55344=ORIENTED_EDGE ( 'NONE', *, *, #13513, .T. ) ;
#55356=CARTESIAN_POINT ( 'NONE',  ( 31.60706529141451426, -4.540774720514427543, 26.12024523944107202 ) ) ;
#55388=LINE ( 'NONE', #3607, #73625 ) ;
#55389=CARTESIAN_POINT ( 'NONE',  ( 6.420673076923079314, -6.376774720514427841, 21.83974358974358765 ) ) ;
#55393=DIRECTION ( 'NONE',  ( -0.7512896232465786639, -0.000000000000000000, -0.6599726524652470561 ) ) ;
#55400=ADVANCED_FACE ( 'NONE', ( #94798 ), #93290, .F. ) ;
#55428=FACE_OUTER_BOUND ( 'NONE', #13865, .T. ) ;
#55430=ORIENTED_EDGE ( 'NONE', *, *, #42201, .T. ) ;
#55435=CARTESIAN_POINT ( 'NONE',  ( 0.2885822020289898759, -6.376774720514415407, 19.94806476610988710 ) ) ;
#55440=DIRECTION ( 'NONE',  ( -0.000000000000000000, 1.000000000000000000, -0.000000000000000000 ) ) ;
#55462=DIRECTION ( 'NONE',  ( 1.000000000000000000, 0.000000000000000000, 0.000000000000000000 ) ) ;
#55464=CARTESIAN_POINT ( 'NONE',  ( -1.304987980769231948, -6.376774720514413630, 19.76512419871795245 ) ) ;
#55472=AXIS2_PLACEMENT_3D ( 'NONE', #38031, #90822, #90322 ) ;
#55476=AXIS2_PLACEMENT_3D ( 'NONE', #2486, #11088, #73002 ) ;
#55485=FACE_OUTER_BOUND ( 'NONE', #64006, .T. ) ;
#55495=ORIENTED_EDGE ( 'NONE', *, *, #72984, .F. ) ;
#55499=CARTESIAN_POINT ( 'NONE',  ( -0.02075734969026423599, -3.316774720514426456, -0.08597719988137648983 ) ) ;
#55504=CARTESIAN_POINT ( 'NONE',  ( 3.362030615038681169, -6.376774720514424288, 21.34376340489846413 ) ) ;
#55507=DIRECTION ( 'NONE',  ( -0.000000000000000000, -1.000000000000000000, -0.000000000000000000 ) ) ;
#55525=DIRECTION ( 'NONE',  ( -1.000000000000000000, 0.000000000000000000, 2.338552693767719605E-15 ) ) ;
#55533=DIRECTION ( 'NONE',  ( 0.000000000000000000, 0.000000000000000000, 1.000000000000000000 ) ) ;
#55536=EDGE_CURVE ( 'NONE', #36349, #93143, #10067, .T. ) ;
#55538=CYLINDRICAL_SURFACE ( 'NONE', #60966, 2.500000000000000444 ) ;
#55544=DIRECTION ( 'NONE',  ( -0.000000000000000000, 1.000000000000000000, -0.000000000000000000 ) ) ;
#55560=CARTESIAN_POINT ( 'NONE',  ( -4.152941208099351300, -6.376774720514415407, 20.35309744218305639 ) ) ;
#55566=PLANE ( 'NONE',  #36968 ) ;
#55582=CARTESIAN_POINT ( 'NONE',  ( 10.24059822343757808, -6.376774720514426953, 17.17691942396160698 ) ) ;
#55588=CARTESIAN_POINT ( 'NONE',  ( 8.720390671794367776, -5.356774720513354460, -27.07197491334870065 ) ) ;
#55594=ORIENTED_EDGE ( 'NONE', *, *, #24222, .T. ) ;
#55602=ORIENTED_EDGE ( 'NONE', *, *, #7194, .F. ) ;
#55614=DIRECTION ( 'NONE',  ( -0.000000000000000000, 0.000000000000000000, -1.000000000000000000 ) ) ;
#55615=AXIS2_PLACEMENT_3D ( 'NONE', #33847, #78504, #32851 ) ;
#55623=CARTESIAN_POINT ( 'NONE',  ( -5.596556251055551101, -5.876774720514411854, 19.35667676486397681 ) ) ;
#55624=ORIENTED_EDGE ( 'NONE', *, *, #73786, .F. ) ;
#55637=CARTESIAN_POINT ( 'NONE',  ( 4.967620699791259753, -5.876774720514416295, 19.94530485585548973 ) ) ;
#55640=DIRECTION ( 'NONE',  ( 0.000000000000000000, 0.000000000000000000, 1.000000000000000000 ) ) ;
#55652=CARTESIAN_POINT ( 'NONE',  ( 4.547994309883463870, -5.876774720514421624, 20.87593061325451416 ) ) ;
#55654=FACE_OUTER_BOUND ( 'NONE', #80430, .T. ) ;
#55655=VECTOR ( 'NONE', #25647, 1000.000000000000000 ) ;
#55657=ORIENTED_EDGE ( 'NONE', *, *, #26438, .F. ) ;
#55663=VECTOR ( 'NONE', #77168, 1000.000000000000114 ) ;
#55684=ORIENTED_EDGE ( 'NONE', *, *, #62396, .T. ) ;
#55694=CIRCLE ( 'NONE', #81605, 1.530000000000000249 ) ;
#55695=VERTEX_POINT ( 'NONE', #12559 ) ;
#55700=CARTESIAN_POINT ( 'NONE',  ( 4.328803674008796065, -5.876774720514407413, 18.75671216747623049 ) ) ;
#55705=AXIS2_PLACEMENT_3D ( 'NONE', #82489, #50552, #81507 ) ;
#55711=ORIENTED_EDGE ( 'NONE', *, *, #8811, .F. ) ;
#55714=ORIENTED_EDGE ( 'NONE', *, *, #92711, .F. ) ;
#55742=ORIENTED_EDGE ( 'NONE', *, *, #53006, .F. ) ;
#55746=EDGE_CURVE ( 'NONE', #97499, #69556, #10121, .T. ) ;
#55761=DIRECTION ( 'NONE',  ( -0.6392559695863496705, 6.845827386180411947E-16, -0.7689940216596069522 ) ) ;
#55765=CARTESIAN_POINT ( 'NONE',  ( -6.487934372591614540, -5.876774720514411854, 19.49432735726520605 ) ) ;
#55776=EDGE_CURVE ( 'NONE', #35863, #45042, #30781, .T. ) ;
#55778=EDGE_CURVE ( 'NONE', #63083, #40447, #26717, .T. ) ;
#55789=EDGE_LOOP ( 'NONE', ( #24735, #46426, #83118, #74014 ) ) ;
#55794=ORIENTED_EDGE ( 'NONE', *, *, #53489, .F. ) ;
#55802=LINE ( 'NONE', #32952, #16084 ) ;
#55808=CARTESIAN_POINT ( 'NONE',  ( -6.989144439031651501, -5.876774720514410966, 19.51167604195716621 ) ) ;
#55812=CARTESIAN_POINT ( 'NONE',  ( -19.80875734969026425, -0.3587747205144265483, 31.02402280011862246 ) ) ;
#55815=VERTEX_POINT ( 'NONE', #77933 ) ;
#55820=ORIENTED_EDGE ( 'NONE', *, *, #86622, .T. ) ;
#55822=CARTESIAN_POINT ( 'NONE',  ( -5.837039262820512775, -6.376774720514413630, 19.76512419871795245 ) ) ;
#55832=CARTESIAN_POINT ( 'NONE',  ( 25.40723128797996822, -4.683802162961660187, -10.80818206156904537 ) ) ;
#55838=VERTEX_POINT ( 'NONE', #831 ) ;
#55847=CARTESIAN_POINT ( 'NONE',  ( 32.70752563734568952, -3.536205085657706082, -3.307643893017725212 ) ) ;
#55853=LINE ( 'NONE', #93382, #11004 ) ;
#55859=DIRECTION ( 'NONE',  ( -0.000000000000000000, 1.000000000000000000, -0.000000000000000000 ) ) ;
#55863=CARTESIAN_POINT ( 'NONE',  ( 29.58897068672300179, -4.307329379639823763, 29.06043472499518643 ) ) ;
#55885=LINE ( 'NONE', #33529, #54567 ) ;
#55892=CARTESIAN_POINT ( 'NONE',  ( 5.654871928786437074, -5.876774720514420736, 20.64717925217163952 ) ) ;
#55893=AXIS2_PLACEMENT_3D ( 'NONE', #55159, #56159, #81351 ) ;
#55895=EDGE_LOOP ( 'NONE', ( #43466, #41470, #42700, #8928, #84198, #47840, #20329, #4046 ) ) ;
#55899=DIRECTION ( 'NONE',  ( 0.000000000000000000, -1.000000000000000000, 0.000000000000000000 ) ) ;
#55930=CARTESIAN_POINT ( 'NONE',  ( 16.89397143409390623, -6.376774720514426953, 16.89397143409405899 ) ) ;
#55937=ORIENTED_EDGE ( 'NONE', *, *, #67515, .T. ) ;
#55938=ORIENTED_EDGE ( 'NONE', *, *, #6852, .F. ) ;
#55941=CARTESIAN_POINT ( 'NONE',  ( 5.367993895751241418, -5.876774720514418071, 20.45854982692612722 ) ) ;
#55944=ORIENTED_EDGE ( 'NONE', *, *, #87000, .T. ) ;
#55946=CARTESIAN_POINT ( 'NONE',  ( 2.591645189881369493, -5.876774720514412742, 19.84288601127407148 ) ) ;
#55950=ORIENTED_EDGE ( 'NONE', *, *, #97273, .T. ) ;
#55955=CIRCLE ( 'NONE', #47835, 11.85241003308276042 ) ;
#55971=DIRECTION ( 'NONE',  ( 0.1489078231574191002, 6.845827386180410961E-16, -0.9888510809027407644 ) ) ;
#55979=AXIS2_PLACEMENT_3D ( 'NONE', #46428, #77359, #48439 ) ;
#55982=ORIENTED_EDGE ( 'NONE', *, *, #56096, .T. ) ;
#55983=CARTESIAN_POINT ( 'NONE',  ( 29.73860345376319358, -5.356774720496559894, 1.647607965253213846 ) ) ;
#55984=EDGE_CURVE ( 'NONE', #82993, #67077, #13431, .T. ) ;
#55995=CARTESIAN_POINT ( 'NONE',  ( 31.62974406627585466, -4.069828902950619387, 27.10097837741100335 ) ) ;
#55999=CARTESIAN_POINT ( 'NONE',  ( 4.736659488006659480, -6.376774720514420736, 21.25082490164487581 ) ) ;
#56000=FACE_OUTER_BOUND ( 'NONE', #95729, .T. ) ;
#56011=CARTESIAN_POINT ( 'NONE',  ( 3.825768195983636044, -6.376774720514424288, 21.47884071039599618 ) ) ;
#56013=CYLINDRICAL_SURFACE ( 'NONE', #98525, 11.85241003308275864 ) ;
#56014=CARTESIAN_POINT ( 'NONE',  ( 5.981014360695730225, -5.876774720514425177, 21.36744920115099333 ) ) ;
#56020=ORIENTED_EDGE ( 'NONE', *, *, #12908, .T. ) ;
#56022=EDGE_CURVE ( 'NONE', #91581, #23237, #53310, .T. ) ;
#56035=ORIENTED_EDGE ( 'NONE', *, *, #7420, .T. ) ;
#56036=VECTOR ( 'NONE', #36005, 1000.000000000000000 ) ;
#56039=VECTOR ( 'NONE', #26329, 1000.000000000000000 ) ;
#56041=VECTOR ( 'NONE', #75133, 1000.000000000000000 ) ;
#56051=CARTESIAN_POINT ( 'NONE',  ( -8.978253834636468866, -5.876774720514426953, 0.000000000000000000 ) ) ;
#56057=CARTESIAN_POINT ( 'NONE',  ( 2.598318274922708060, -6.376774720514413630, 19.68966562063331693 ) ) ;
#56066=CARTESIAN_POINT ( 'NONE',  ( 6.792576760808763936, -5.876774720514415407, 20.16775508794004779 ) ) ;
#56071=ORIENTED_EDGE ( 'NONE', *, *, #95620, .T. ) ;
#56075=ORIENTED_EDGE ( 'NONE', *, *, #26355, .F. ) ;
#56077=ORIENTED_EDGE ( 'NONE', *, *, #51159, .T. ) ;
#56083=CARTESIAN_POINT ( 'NONE',  ( 22.02124265030973760, -6.376774720514428729, 13.20402280011862395 ) ) ;
#56084=FACE_OUTER_BOUND ( 'NONE', #77290, .T. ) ;
#56090=PLANE ( 'NONE',  #15736 ) ;
#56094=DIRECTION ( 'NONE',  ( -1.000000000000000000, 0.000000000000000000, -1.226388327005079762E-16 ) ) ;
#56095=ORIENTED_EDGE ( 'NONE', *, *, #71207, .T. ) ;
#56096=EDGE_CURVE ( 'NONE', #17609, #26067, #43899, .T. ) ;
#56098=EDGE_CURVE ( 'NONE', #23800, #77005, #37776, .T. ) ;
#56101=ORIENTED_EDGE ( 'NONE', *, *, #46286, .F. ) ;
#56103=EDGE_LOOP ( 'NONE', ( #64339, #46582, #40735, #76638 ) ) ;
#56109=ORIENTED_EDGE ( 'NONE', *, *, #48770, .T. ) ;
#56111=DIRECTION ( 'NONE',  ( 0.000000000000000000, -1.000000000000000000, 0.000000000000000000 ) ) ;
#56119=CARTESIAN_POINT ( 'NONE',  ( -4.465079497292244959, -5.876774720514410077, 19.29815762497054976 ) ) ;
#56122=AXIS2_PLACEMENT_3D ( 'NONE', #48042, #86092, #2370 ) ;
#56131=CARTESIAN_POINT ( 'NONE',  ( -13.89275734969026388, 5.965225279485572685, 30.51402280011862089 ) ) ;
#56136=CARTESIAN_POINT ( 'NONE',  ( -11.64875734969026233, 5.965225279485572685, 31.02402280011862246 ) ) ;
#56150=DIRECTION ( 'NONE',  ( -0.000000000000000000, 1.000000000000000000, -0.000000000000000000 ) ) ;
#56153=ADVANCED_FACE ( 'NONE', ( #54011 ), #74975, .T. ) ;
#56159=DIRECTION ( 'NONE',  ( 1.000000000000000000, 0.000000000000000000, 0.000000000000000000 ) ) ;
#56170=LINE ( 'NONE', #63286, #49594 ) ;
#56173=EDGE_LOOP ( 'NONE', ( #19328, #51082, #2026, #56101 ) ) ;
#56182=ORIENTED_EDGE ( 'NONE', *, *, #48073, .F. ) ;
#56185=ORIENTED_EDGE ( 'NONE', *, *, #31794, .F. ) ;
#56189=TOROIDAL_SURFACE ( 'NONE', #48066, 132.8284398600581540, 3.060000000000000053 ) ;
#56190=ORIENTED_EDGE ( 'NONE', *, *, #43272, .F. ) ;
#56199=CIRCLE ( 'NONE', #17279, 0.3000000000000016542 ) ;
#56201=CARTESIAN_POINT ( 'NONE',  ( 3.825970207471427020, -5.876774720514403860, 18.52126221587801780 ) ) ;
#56211=CARTESIAN_POINT ( 'NONE',  ( -4.993225604111834137, -0.3587747205143964613, -29.11654937215279304 ) ) ;
#56214=ORIENTED_EDGE ( 'NONE', *, *, #45266, .F. ) ;
#56215=CARTESIAN_POINT ( 'NONE',  ( -5.877732331298974877, -5.876774720514411854, 19.69174559449349005 ) ) ;
#56231=VECTOR ( 'NONE', #69185, 1000.000000000000000 ) ;
#56240=CARTESIAN_POINT ( 'NONE',  ( -7.234140626586239797, -6.376774720514411854, 19.72789237585158162 ) ) ;
#56241=CARTESIAN_POINT ( 'NONE',  ( -23.62875734969026453, 6.143225279485574397, 23.50402280011862288 ) ) ;
#56247=CARTESIAN_POINT ( 'NONE',  ( -28.98875734969026041, 5.965225279485572685, 23.37402280011862743 ) ) ;
#56254=DIRECTION ( 'NONE',  ( 0.000000000000000000, -1.000000000000000000, 0.000000000000000000 ) ) ;
#56259=AXIS2_PLACEMENT_3D ( 'NONE', #35064, #96954, #89349 ) ;
#56262=CYLINDRICAL_SURFACE ( 'NONE', #31369, 1.836000000000000743 ) ;
#56271=CARTESIAN_POINT ( 'NONE',  ( -5.926585084595196840, -6.376774720514415407, 20.19722303762275573 ) ) ;
#56284=DIRECTION ( 'NONE',  ( 1.000000000000000000, 0.000000000000000000, 0.000000000000000000 ) ) ;
#56293=AXIS2_PLACEMENT_3D ( 'NONE', #31233, #38845, #69803 ) ;
#56297=CARTESIAN_POINT ( 'NONE',  ( 4.910384361841649614, -6.376774720514420736, 20.73924463800384643 ) ) ;
#56298=B_SPLINE_SURFACE_WITH_KNOTS ( 'NONE', 3, 1, ( 
 ( #52697, #61324 ),
 ( #84638, #15624 ),
 ( #83636, #13616 ),
 ( #100339, #7514 ),
 ( #92249, #52200 ),
 ( #23227, #38965 ),
 ( #30855, #67934 ),
 ( #98856, #6521 ),
 ( #37966, #44586 ),
 ( #14118, #91250 ),
 ( #76017, #53710 ),
 ( #68423, #68917 ),
 ( #405, #29351 ),
 ( #45592, #85137 ),
 ( #75514, #22720 ),
 ( #29852, #15128 ),
 ( #93248, #99356 ),
 ( #60324, #37473 ),
 ( #21723, #54213 ),
 ( #8016, #53206 ),
 ( #45093, #60823 ),
 ( #83128, #46091 ),
 ( #84135, #7017 ),
 ( #6013, #69420 ),
 ( #14624, #69920 ),
 ( #31356, #91743 ),
 ( #61821, #22225 ) ),
 .UNSPECIFIED., .F., .F., .F.,
 ( 4, 1, 1, 1, 1, 1, 1, 1, 1, 1, 1, 1, 1, 1, 1, 1, 1, 1, 1, 1, 1, 1, 1, 1, 4 ),
 ( 2, 2 ),
 ( 0.000000000000000000, 0.03374242470187671650, 0.06653347536929221651, 0.09915346175681749585, 0.1315397542107091811, 0.1640870483339715857, 0.1965627449807513250, 0.2297068306392113790, 0.2633146464865417924, 0.2975043287136188708, 0.3316856488303484563, 0.3664815111438048945, 0.4020997606356003784, 0.4389576272716395611, 0.4767476992267967173, 0.5159851313836553155, 0.5565892450615084197, 0.5995194112260104902, 0.6457650933466750898, 0.6954865607436527819, 0.7487207768830330679, 0.8056874135317430019, 0.8667539575566982624, 0.9314053777412569790, 1.000000000000000000 ),
 ( 0.000000000000000000, 1.000000000000000000 ),
 .UNSPECIFIED. ) ;
#56308=EDGE_LOOP ( 'NONE', ( #17121, #74630, #58301, #83232, #41145 ) ) ;
#56314=CARTESIAN_POINT ( 'NONE',  ( -1.318699232124953324, -6.376774720514411854, 19.74039977944280722 ) ) ;
#56315=ADVANCED_FACE ( 'NONE', ( #91812 ), #13182, .F. ) ;
#56323=ORIENTED_EDGE ( 'NONE', *, *, #2603, .T. ) ;
#56337=ADVANCED_FACE ( 'NONE', ( #44152 ), #45651, .F. ) ;
#56344=CARTESIAN_POINT ( 'NONE',  ( 4.115044103975469270, -5.876774720514427841, 21.79213183355573946 ) ) ;
#56349=ADVANCED_FACE ( 'NONE', ( #59890 ), #44635, .T. ) ;
#56376=CARTESIAN_POINT ( 'NONE',  ( -5.574014511416001127, -5.876774720514415407, 20.24089781925592391 ) ) ;
#56390=CARTESIAN_POINT ( 'NONE',  ( 17.51792015816173986, -0.3587747205144265483, 29.01255224319336889 ) ) ;
#56395=ORIENTED_EDGE ( 'NONE', *, *, #86690, .F. ) ;
#56400=EDGE_CURVE ( 'NONE', #57117, #27752, #11959, .T. ) ;
#56405=DIRECTION ( 'NONE',  ( -0.000000000000000000, 1.000000000000000000, -0.000000000000000000 ) ) ;
#56407=CARTESIAN_POINT ( 'NONE',  ( 9.402885806365684829, -0.3587747205144265483, 29.04108526060719342 ) ) ;
#56427=EDGE_CURVE ( 'NONE', #24488, #70415, #31926, .T. ) ;
#56430=CARTESIAN_POINT ( 'NONE',  ( 31.44923352942285177, -5.094381739198088788, -4.378347922178638107 ) ) ;
#56433=EDGE_CURVE ( 'NONE', #15795, #76129, #61886, .T. ) ;
#56440=DIRECTION ( 'NONE',  ( 0.000000000000000000, 0.000000000000000000, 1.000000000000000000 ) ) ;
#56457=ORIENTED_EDGE ( 'NONE', *, *, #67198, .F. ) ;
#56485=EDGE_CURVE ( 'NONE', #94122, #79731, #32925, .T. ) ;
#56499=CARTESIAN_POINT ( 'NONE',  ( -5.000686017310577824, -6.376774720514411854, 19.46274624311237034 ) ) ;
#56502=CARTESIAN_POINT ( 'NONE',  ( 4.638796026491669444, -6.376774720514424288, 21.40644651702305268 ) ) ;
#56503=DIRECTION ( 'NONE',  ( 0.000000000000000000, 0.000000000000000000, -1.000000000000000000 ) ) ;
#56505=CYLINDRICAL_SURFACE ( 'NONE', #80185, 1.325999999999943446 ) ;
#56512=DIRECTION ( 'NONE',  ( -1.000000000000000000, 0.000000000000000000, 5.238131417152343399E-15 ) ) ;
#56518=DIRECTION ( 'NONE',  ( -1.257682986112628661E-16, 0.000000000000000000, -1.000000000000000000 ) ) ;
#56523=VERTEX_POINT ( 'NONE', #79083 ) ;
#56529=CARTESIAN_POINT ( 'NONE',  ( -6.818021687177533430, -5.876774720514408301, 19.14905311829361167 ) ) ;
#56530=AXIS2_PLACEMENT_3D ( 'NONE', #56659, #32806, #63784 ) ;
#56537=ORIENTED_EDGE ( 'NONE', *, *, #60097, .F. ) ;
#56540=CARTESIAN_POINT ( 'NONE',  ( 7.403636664866980688, -5.876774720514424288, 21.18544102487025782 ) ) ;
#56541=CARTESIAN_POINT ( 'NONE',  ( -10.24059822343757808, -5.876774720514426953, 22.08128695274315945 ) ) ;
#56543=EDGE_CURVE ( 'NONE', #77715, #40322, #17695, .T. ) ;
#56548=LINE ( 'NONE', #49434, #66540 ) ;
#56550=CARTESIAN_POINT ( 'NONE',  ( 31.41423154468143153, -2.682774720514426559, -0.3119954678742140053 ) ) ;
#56556=LINE ( 'NONE', #71769, #36528 ) ;
#56559=CARTESIAN_POINT ( 'NONE',  ( -25.92875734969026524, -5.356774720514425603, 0.7300228001186309656 ) ) ;
#56577=ADVANCED_FACE ( 'NONE', ( #73482 ), #72495, .F. ) ;
#56578=ORIENTED_EDGE ( 'NONE', *, *, #66991, .T. ) ;
#56584=DIRECTION ( 'NONE',  ( 0.000000000000000000, 0.000000000000000000, 1.000000000000000000 ) ) ;
#56587=ORIENTED_EDGE ( 'NONE', *, *, #66535, .F. ) ;
#56592=CIRCLE ( 'NONE', #12803, 2.040000000000000036 ) ;
#56601=VERTEX_POINT ( 'NONE', #18684 ) ;
#56603=FACE_OUTER_BOUND ( 'NONE', #45225, .T. ) ;
#56607=CARTESIAN_POINT ( 'NONE',  ( -5.960145391809922089, -6.376774720514415407, 20.04104409779160534 ) ) ;
#56611=CARTESIAN_POINT ( 'NONE',  ( 31.60906425211781823, -3.844812497472038793, -2.545713913898462799 ) ) ;
#56614=CARTESIAN_POINT ( 'NONE',  ( -28.47875734969026240, 5.965225279485572685, 26.43402280011862615 ) ) ;
#56620=VERTEX_POINT ( 'NONE', #95815 ) ;
#56621=DIRECTION ( 'NONE',  ( -1.000000000000000000, -0.000000000000000000, 0.000000000000000000 ) ) ;
#56630=DIRECTION ( 'NONE',  ( 0.000000000000000000, 1.000000000000000000, 0.000000000000000000 ) ) ;
#56637=CARTESIAN_POINT ( 'NONE',  ( -2.457093156980370452, -5.876774720514412742, 19.51167604195716976 ) ) ;
#56654=FACE_OUTER_BOUND ( 'NONE', #7110, .T. ) ;
#56659=CARTESIAN_POINT ( 'NONE',  ( 9.402885806365684829, 5.965225279485572685, 29.04108526060719342 ) ) ;
#56663=ADVANCED_FACE ( 'NONE', ( #80592 ), #42053, .T. ) ;
#56664=CARTESIAN_POINT ( 'NONE',  ( 282.9764569301858046, -6.376774720514426953, 20.79159422840526616 ) ) ;
#56666=CARTESIAN_POINT ( 'NONE',  ( -2.794793911895765870, -6.376774720514417183, 20.33046051580616265 ) ) ;
#56673=CIRCLE ( 'NONE', #67968, 25.90800000000000125 ) ;
#56677=ORIENTED_EDGE ( 'NONE', *, *, #62081, .T. ) ;
#56678=AXIS2_PLACEMENT_3D ( 'NONE', #52788, #60908, #490 ) ;
#56679=DIRECTION ( 'NONE',  ( 0.000000000000000000, 1.000000000000000000, 0.000000000000000000 ) ) ;
#56686=EDGE_LOOP ( 'NONE', ( #19883, #14727, #50536, #71806 ) ) ;
#56694=VERTEX_POINT ( 'NONE', #26810 ) ;
#56697=CARTESIAN_POINT ( 'NONE',  ( -28.32169924589829080, 5.965225279485592225, -8.244178532169447848 ) ) ;
#56702=DIRECTION ( 'NONE',  ( 0.000000000000000000, 0.000000000000000000, 1.000000000000000000 ) ) ;
#56705=CARTESIAN_POINT ( 'NONE',  ( 4.214857194124448370, -6.376774720514402972, 18.65898740197609840 ) ) ;
#56714=LINE ( 'NONE', #40974, #1731 ) ;
#56718=DIRECTION ( 'NONE',  ( 0.000000000000000000, 0.000000000000000000, 1.000000000000000000 ) ) ;
#56738=VECTOR ( 'NONE', #31072, 1000.000000000000000 ) ;
#56739=CARTESIAN_POINT ( 'NONE',  ( -7.234140626586239797, -5.876774720514411854, 19.72789237585158162 ) ) ;
#56746=CARTESIAN_POINT ( 'NONE',  ( -7.326923076923074873, -5.876774720514426953, 21.75000000000001066 ) ) ;
#56748=VECTOR ( 'NONE', #18394, 1000.000000000000000 ) ;
#56760=VECTOR ( 'NONE', #22993, 1000.000000000000000 ) ;
#56770=DIRECTION ( 'NONE',  ( 0.000000000000000000, -1.000000000000000000, 0.000000000000000000 ) ) ;
#56776=CYLINDRICAL_SURFACE ( 'NONE', #2998, 2.040000000000000036 ) ;
#56789=EDGE_CURVE ( 'NONE', #76914, #71823, #61269, .T. ) ;
#56795=CARTESIAN_POINT ( 'NONE',  ( 4.819673832743241348, -6.376774720514422512, 21.07066438048017076 ) ) ;
#56797=LINE ( 'NONE', #18213, #25302 ) ;
#56799=ADVANCED_FACE ( 'NONE', ( #84078 ), #28801, .F. ) ;
#56805=DIRECTION ( 'NONE',  ( 1.000000000000000000, -0.000000000000000000, 2.417950247244706201E-16 ) ) ;
#56828=CARTESIAN_POINT ( 'NONE',  ( -5.970505764849975527, -6.376774720514411854, 19.55848054040323802 ) ) ;
#56829=CARTESIAN_POINT ( 'NONE',  ( 2.932009311892267434, -5.876774720514410077, 19.53174284846577891 ) ) ;
#56833=CARTESIAN_POINT ( 'NONE',  ( 12.99736557111424595, -3.316774720514426900, -27.13536621820933448 ) ) ;
#56847=VERTEX_POINT ( 'NONE', #99304 ) ;
#56850=VERTEX_POINT ( 'NONE', #13065 ) ;
#56874=CIRCLE ( 'NONE', #92456, 2.249999999999998668 ) ;
#56875=DIRECTION ( 'NONE',  ( -0.000000000000000000, 1.000000000000000000, -0.000000000000000000 ) ) ;
#56881=CARTESIAN_POINT ( 'NONE',  ( 4.415069475862049231, -5.876774720514424288, 21.13806644168711557 ) ) ;
#56886=VERTEX_POINT ( 'NONE', #37914 ) ;
#56890=CARTESIAN_POINT ( 'NONE',  ( -9.149999999999996803, -6.376774720514426953, 11.88602120139452012 ) ) ;
#56908=EDGE_CURVE ( 'NONE', #15238, #90130, #28651, .T. ) ;
#56911=FACE_OUTER_BOUND ( 'NONE', #25988, .T. ) ;
#56924=ADVANCED_FACE ( 'NONE', ( #55654 ), #32799, .F. ) ;
#56937=EDGE_LOOP ( 'NONE', ( #31027, #98099, #96156, #19213 ) ) ;
#56940=ORIENTED_EDGE ( 'NONE', *, *, #1223, .T. ) ;
#56943=EDGE_LOOP ( 'NONE', ( #38866, #54836, #67814, #80715 ) ) ;
#56945=CARTESIAN_POINT ( 'NONE',  ( 6.963174204274080736, -6.376774720514415407, 20.29202897614545975 ) ) ;
#56946=CARTESIAN_POINT ( 'NONE',  ( 5.873458226074941280, -6.376774720514413630, 19.84669099281175164 ) ) ;
#56950=CARTESIAN_POINT ( 'NONE',  ( 19.75748517575715368, 5.965225279485572685, 28.87153971905864580 ) ) ;
#56957=LINE ( 'NONE', #26497, #33914 ) ;
#56958=VECTOR ( 'NONE', #92048, 1000.000000000000000 ) ;
#56981=DIRECTION ( 'NONE',  ( 0.000000000000000000, -1.000000000000000000, 0.000000000000000000 ) ) ;
#56991=CARTESIAN_POINT ( 'NONE',  ( -28.47875734969026240, 5.965225279485572685, 26.43402280011862615 ) ) ;
#57002=CYLINDRICAL_SURFACE ( 'NONE', #34262, 130.7884398600581335 ) ;
#57005=EDGE_CURVE ( 'NONE', #98963, #27719, #56199, .T. ) ;
#57007=AXIS2_PLACEMENT_3D ( 'NONE', #6449, #67861, #37406 ) ;
#57013=CARTESIAN_POINT ( 'NONE',  ( -2.188401442307694289, -6.376774720514411854, 19.46153846153846700 ) ) ;
#57029=CARTESIAN_POINT ( 'NONE',  ( 12.48433401490028949, -6.376774720514426953, -25.05541855807676299 ) ) ;
#57031=CARTESIAN_POINT ( 'NONE',  ( -7.243541020599075786, -5.876774720514408301, 19.27798293355755632 ) ) ;
#57036=FACE_OUTER_BOUND ( 'NONE', #81712, .T. ) ;
#57042=EDGE_CURVE ( 'NONE', #48508, #42578, #95069, .T. ) ;
#57044=CARTESIAN_POINT ( 'NONE',  ( 5.949073730962466833, 6.475225279485573360, -27.94053387008862188 ) ) ;
#57058=VECTOR ( 'NONE', #21625, 1000.000000000000000 ) ;
#57063=CARTESIAN_POINT ( 'NONE',  ( 2.591645189881369493, -6.376774720514411854, 19.84288601127407148 ) ) ;
#57065=EDGE_LOOP ( 'NONE', ( #71391, #29299, #27233, #51368 ) ) ;
#57066=DIRECTION ( 'NONE',  ( 0.000000000000000000, -1.000000000000000000, 0.000000000000000000 ) ) ;
#57075=CARTESIAN_POINT ( 'NONE',  ( 32.76111974776238611, -3.316774720514426900, -3.850861272813261849 ) ) ;
#57081=AXIS2_PLACEMENT_3D ( 'NONE', #45636, #28397, #59361 ) ;
#57100=ORIENTED_EDGE ( 'NONE', *, *, #62876, .F. ) ;
#57106=ORIENTED_EDGE ( 'NONE', *, *, #59623, .F. ) ;
#57117=VERTEX_POINT ( 'NONE', #72375 ) ;
#57122=EDGE_CURVE ( 'NONE', #11758, #83886, #3866, .T. ) ;
#57124=EDGE_CURVE ( 'NONE', #98244, #64840, #2361, .T. ) ;
#57129=ORIENTED_EDGE ( 'NONE', *, *, #90952, .T. ) ;
#57132=CARTESIAN_POINT ( 'NONE',  ( 15.99960863614631101, -3.577630190450212577, -27.91116951066581819 ) ) ;
#57135=LINE ( 'NONE', #88070, #5078 ) ;
#57154=DIRECTION ( 'NONE',  ( 0.000000000000000000, 1.000000000000000000, 0.000000000000000000 ) ) ;
#57189=CARTESIAN_POINT ( 'NONE',  ( -11.64875734969026233, 5.965225279485572685, 31.02402280011862246 ) ) ;
#57198=CARTESIAN_POINT ( 'NONE',  ( 2.911360383046243783, -6.376774720514417183, 20.24673073119071276 ) ) ;
#57208=ORIENTED_EDGE ( 'NONE', *, *, #99918, .T. ) ;
#57212=VERTEX_POINT ( 'NONE', #22049 ) ;
#57214=VERTEX_POINT ( 'NONE', #82465 ) ;
#57216=ORIENTED_EDGE ( 'NONE', *, *, #8811, .T. ) ;
#57224=DIRECTION ( 'NONE',  ( 0.000000000000000000, -0.7071067811865513475, -0.7071067811865436870 ) ) ;
#57227=ORIENTED_EDGE ( 'NONE', *, *, #8788, .F. ) ;
#57237=EDGE_LOOP ( 'NONE', ( #16591, #88400, #74912, #88256 ) ) ;
#57240=CARTESIAN_POINT ( 'NONE',  ( 30.58729439590573307, -4.540774720514427543, 26.14186284044631492 ) ) ;
#57243=EDGE_CURVE ( 'NONE', #11758, #81218, #36798, .T. ) ;
#57248=CARTESIAN_POINT ( 'NONE',  ( 6.437068816671457583, -3.316774720514427344, -28.37834077173919667 ) ) ;
#57249=LINE ( 'NONE', #3455, #80020 ) ;
#57253=LINE ( 'NONE', #11544, #48618 ) ;
#57254=VECTOR ( 'NONE', #87700, 1000.000000000000000 ) ;
#57258=CARTESIAN_POINT ( 'NONE',  ( 9.150000000000000355, -6.376774720514426953, -15.70000000000000284 ) ) ;
#57259=CARTESIAN_POINT ( 'NONE',  ( -0.4909855769230798139, -5.876774720514408301, 19.14743589743590135 ) ) ;
#57273=CARTESIAN_POINT ( 'NONE',  ( -7.326923076923076650, -6.376774720514417183, 20.36318108974359831 ) ) ;
#57280=EDGE_CURVE ( 'NONE', #59933, #48082, #41755, .T. ) ;
#57287=VERTEX_POINT ( 'NONE', #49368 ) ;
#57290=CARTESIAN_POINT ( 'NONE',  ( 7.480769230769231726, -6.376774720514420736, 20.77403846153845635 ) ) ;
#57295=CARTESIAN_POINT ( 'NONE',  ( -5.265981236333618470E-16, -4.056774720514426669, -4.299999999999999822 ) ) ;
#57300=VECTOR ( 'NONE', #78824, 1000.000000000000000 ) ;
#57303=CARTESIAN_POINT ( 'NONE',  ( 6.403846153846157740, -5.876774720514425177, 21.48076923076922995 ) ) ;
#57311=ORIENTED_EDGE ( 'NONE', *, *, #25063, .F. ) ;
#57325=EDGE_LOOP ( 'NONE', ( #74093, #58670, #7776, #94865 ) ) ;
#57331=CARTESIAN_POINT ( 'NONE',  ( -6.728471858368818559, -6.376774720514408301, 19.14926908420045137 ) ) ;
#57337=CARTESIAN_POINT ( 'NONE',  ( 11.80640562518893866, -3.316774720514426011, -27.06722565682295567 ) ) ;
#57340=CARTESIAN_POINT ( 'NONE',  ( 30.09341516180546350, -2.682774720514426559, -11.39311774897855933 ) ) ;
#57348=ORIENTED_EDGE ( 'NONE', *, *, #74397, .F. ) ;
#57351=ORIENTED_EDGE ( 'NONE', *, *, #52799, .T. ) ;
#57359=CARTESIAN_POINT ( 'NONE',  ( 3.552327343495968570, -6.376774720514427841, 21.81288606793570395 ) ) ;
#57374=CARTESIAN_POINT ( 'NONE',  ( -1.044871794871790938, -5.876774720514426953, 21.75000000000000355 ) ) ;
#57375=DIRECTION ( 'NONE',  ( 0.000000000000000000, 0.000000000000000000, -1.000000000000000000 ) ) ;
#57378=EDGE_CURVE ( 'NONE', #49156, #14292, #41243, .T. ) ;
#57385=CARTESIAN_POINT ( 'NONE',  ( 4.639188450898540594, -5.876774720514418959, 20.39229233339611014 ) ) ;
#57396=DIRECTION ( 'NONE',  ( -0.000000000000000000, -1.000000000000000000, -0.000000000000000000 ) ) ;
#57403=CARTESIAN_POINT ( 'NONE',  ( -7.567681410454951241, -5.876774720514412742, 19.71630089903357330 ) ) ;
#57424=ORIENTED_EDGE ( 'NONE', *, *, #6284, .F. ) ;
#57429=VECTOR ( 'NONE', #64936, 1000.000000000000000 ) ;
#57445=ORIENTED_EDGE ( 'NONE', *, *, #24621, .T. ) ;
#57446=VERTEX_POINT ( 'NONE', #20881 ) ;
#57448=DIRECTION ( 'NONE',  ( 0.9822594791677485837, 0.000000000000000000, -0.1875268396392987258 ) ) ;
#57455=CARTESIAN_POINT ( 'NONE',  ( 2.650685085285006348, -5.876774720514410077, 19.28073557658628445 ) ) ;
#57463=ORIENTED_EDGE ( 'NONE', *, *, #40039, .T. ) ;
#57474=LINE ( 'NONE', #50349, #79320 ) ;
#57477=DIRECTION ( 'NONE',  ( -0.000000000000000000, 1.000000000000000000, -0.000000000000000000 ) ) ;
#57492=DIRECTION ( 'NONE',  ( -0.000000000000000000, 1.000000000000000000, -0.000000000000000000 ) ) ;
#57498=CARTESIAN_POINT ( 'NONE',  ( 31.61406883670153789, -4.508386143373845023, 26.44289287685778334 ) ) ;
#57501=ORIENTED_EDGE ( 'NONE', *, *, #86875, .T. ) ;
#57505=DIRECTION ( 'NONE',  ( 0.000000000000000000, 0.000000000000000000, 1.000000000000000000 ) ) ;
#57514=CARTESIAN_POINT ( 'NONE',  ( 3.362030615038681169, -5.876774720514423400, 21.34376340489846413 ) ) ;
#57515=CARTESIAN_POINT ( 'NONE',  ( -1.501937386944296460, -6.376774720514415407, 19.86422795159478483 ) ) ;
#57516=LINE ( 'NONE', #65635, #5358 ) ;
#57518=LINE ( 'NONE', #18926, #33727 ) ;
#57519=DIRECTION ( 'NONE',  ( 0.000000000000000000, 0.000000000000000000, -1.000000000000000000 ) ) ;
#57529=CIRCLE ( 'NONE', #99636, 252.4458649670781085 ) ;
#57530=CARTESIAN_POINT ( 'NONE',  ( 12.30588647389939538, -3.316774720514762187, -28.11066263608955751 ) ) ;
#57532=CARTESIAN_POINT ( 'NONE',  ( -7.567681410454951241, -5.876774720514411854, 19.71630089903357330 ) ) ;
#57535=B_SPLINE_CURVE_WITH_KNOTS ( 'NONE', 3,
 ( #36730, #12876, #3799, #81907, #49981 ),
 .UNSPECIFIED., .F., .F.,
 ( 4, 1, 4 ),
 ( 0.000000000000000000, 0.5126593363417801807, 0.9999999999999998890 ),
 .UNSPECIFIED. ) ;
#57538=CARTESIAN_POINT ( 'NONE',  ( -0.02075734969026423599, -6.376774720514426953, -29.05397719988137339 ) ) ;
#57542=CARTESIAN_POINT ( 'NONE',  ( 6.955725288069978696, -5.876774720514426065, 21.70430095680336890 ) ) ;
#57544=DIRECTION ( 'NONE',  ( -0.000000000000000000, 1.000000000000000000, -0.000000000000000000 ) ) ;
#57557=DIRECTION ( 'NONE',  ( 0.000000000000000000, 0.000000000000000000, -1.000000000000000000 ) ) ;
#57561=ORIENTED_EDGE ( 'NONE', *, *, #87635, .F. ) ;
#57562=ORIENTED_EDGE ( 'NONE', *, *, #52888, .F. ) ;
#57563=DIRECTION ( 'NONE',  ( -1.000000000000000000, 0.000000000000000000, 0.000000000000000000 ) ) ;
#57568=VERTEX_POINT ( 'NONE', #35506 ) ;
#57570=EDGE_CURVE ( 'NONE', #54376, #69295, #23548, .T. ) ;
#57575=DIRECTION ( 'NONE',  ( 0.000000000000000000, -1.000000000000000000, 0.000000000000000000 ) ) ;
#57576=CARTESIAN_POINT ( 'NONE',  ( 13.91401389203221406, -6.376774720514426953, 27.24920385068457662 ) ) ;
#57579=CARTESIAN_POINT ( 'NONE',  ( 3.128267882468583228, -5.876774720514423400, 21.08409277973916218 ) ) ;
#57601=ORIENTED_EDGE ( 'NONE', *, *, #43090, .T. ) ;
#57607=EDGE_CURVE ( 'NONE', #53312, #10530, #81169, .T. ) ;
#57609=LINE ( 'NONE', #87544, #23037 ) ;
#57614=EDGE_CURVE ( 'NONE', #63282, #67539, #19141, .T. ) ;
#57615=VERTEX_POINT ( 'NONE', #82166 ) ;
#57623=VERTEX_POINT ( 'NONE', #74555 ) ;
#57625=CARTESIAN_POINT ( 'NONE',  ( 5.395440699609681090, -0.3587747205144061202, -28.51842087987364849 ) ) ;
#57649=CARTESIAN_POINT ( 'NONE',  ( 3.362850247043494001, -6.376774720514404748, 18.65880685207958223 ) ) ;
#57652=DIRECTION ( 'NONE',  ( 0.000000000000000000, 0.000000000000000000, -1.000000000000000000 ) ) ;
#57654=EDGE_CURVE ( 'NONE', #71712, #46766, #57856, .T. ) ;
#57659=DIRECTION ( 'NONE',  ( -0.000000000000000000, -1.000000000000000000, -0.000000000000000000 ) ) ;
#57661=ORIENTED_EDGE ( 'NONE', *, *, #68237, .T. ) ;
#57673=FACE_OUTER_BOUND ( 'NONE', #95257, .T. ) ;
#57685=CARTESIAN_POINT ( 'NONE',  ( 2.905029696106983916, -6.376774720514415407, 20.12486936895525957 ) ) ;
#57695=CARTESIAN_POINT ( 'NONE',  ( -19.80875734969026425, -0.3587747205144265483, 30.51402280011862089 ) ) ;
#57696=VERTEX_POINT ( 'NONE', #99865 ) ;
#57708=ORIENTED_EDGE ( 'NONE', *, *, #23778, .T. ) ;
#57729=FACE_OUTER_BOUND ( 'NONE', #48314, .T. ) ;
#57740=VECTOR ( 'NONE', #14504, 1000.000000000000000 ) ;
#57759=DIRECTION ( 'NONE',  ( -0.000000000000000000, -1.000000000000000000, -0.000000000000000000 ) ) ;
#57764=VECTOR ( 'NONE', #91560, 1000.000000000000000 ) ;
#57770=DIRECTION ( 'NONE',  ( -0.000000000000000000, -1.000000000000000000, -0.000000000000000000 ) ) ;
#57771=AXIS2_PLACEMENT_3D ( 'NONE', #32022, #62998, #87310 ) ;
#57775=LINE ( 'NONE', #74965, #52546 ) ;
#57776=VECTOR ( 'NONE', #72647, 1000.000000000000000 ) ;
#57777=DIRECTION ( 'NONE',  ( 0.000000000000000000, 0.000000000000000000, 1.000000000000000000 ) ) ;
#57795=LINE ( 'NONE', #43063, #53343 ) ;
#57809=CIRCLE ( 'NONE', #74021, 0.8160000000000007248 ) ;
#57811=ADVANCED_FACE ( 'NONE', ( #25766 ), #61527, .F. ) ;
#57812=DIRECTION ( 'NONE',  ( 0.000000000000000000, 0.000000000000000000, 1.000000000000000000 ) ) ;
#57828=ORIENTED_EDGE ( 'NONE', *, *, #87484, .T. ) ;
#57829=CARTESIAN_POINT ( 'NONE',  ( 10.62437663934349530, 6.475225279485576024, -27.03002426119959978 ) ) ;
#57831=EDGE_CURVE ( 'NONE', #42771, #94651, #34949, .T. ) ;
#57847=EDGE_LOOP ( 'NONE', ( #46978, #62517, #74237, #84800 ) ) ;
#57852=CARTESIAN_POINT ( 'NONE',  ( 0.3910256410256394144, -5.876774720514411854, 19.63681891025641235 ) ) ;
#57856=LINE ( 'NONE', #3557, #39784 ) ;
#57869=DIRECTION ( 'NONE',  ( 0.000000000000000000, -1.000000000000000000, 0.000000000000000000 ) ) ;
#57873=EDGE_CURVE ( 'NONE', #40969, #34853, #33128, .T. ) ;
#57879=CARTESIAN_POINT ( 'NONE',  ( 4.547994309883463870, -5.876774720514421624, 20.87593061325451416 ) ) ;
#57883=DIRECTION ( 'NONE',  ( 0.000000000000000000, 0.000000000000000000, -1.000000000000000000 ) ) ;
#57892=DIRECTION ( 'NONE',  ( 0.000000000000000000, -1.000000000000000000, 0.000000000000000000 ) ) ;
#57897=VECTOR ( 'NONE', #87553, 1000.000000000000000 ) ;
#57910=FACE_OUTER_BOUND ( 'NONE', #23835, .T. ) ;
#57915=VECTOR ( 'NONE', #72417, 1000.000000000000000 ) ;
#57932=CARTESIAN_POINT ( 'NONE',  ( 29.73860345376319003, 1.477225279485574028, 19.84760796525321425 ) ) ;
#57939=EDGE_LOOP ( 'NONE', ( #98754, #6459, #62474, #32217 ) ) ;
#57940=DIRECTION ( 'NONE',  ( -0.06916465693916194757, -0.000000000000000000, 0.9976052577199501226 ) ) ;
#57943=ORIENTED_EDGE ( 'NONE', *, *, #34101, .F. ) ;
#57957=ORIENTED_EDGE ( 'NONE', *, *, #32240, .T. ) ;
#57959=CARTESIAN_POINT ( 'NONE',  ( 12.36220485508518685, -4.378682769551595300, -27.78718873729292582 ) ) ;
#57963=ORIENTED_EDGE ( 'NONE', *, *, #66977, .F. ) ;
#57977=LINE ( 'NONE', #17392, #43759 ) ;
#57979=EDGE_CURVE ( 'NONE', #95847, #60537, #73845, .T. ) ;
#57987=CARTESIAN_POINT ( 'NONE',  ( -28.49194798280534968, -6.376774720514426953, 28.38521343323375490 ) ) ;
#57991=AXIS2_PLACEMENT_3D ( 'NONE', #100070, #30586, #47822 ) ;
#57993=ADVANCED_FACE ( 'NONE', ( #11293 ), #74196, .F. ) ;
#57997=CARTESIAN_POINT ( 'NONE',  ( -5.544977400725785266, -6.376774720514411854, 19.92818918856636401 ) ) ;
#58010=LINE ( 'NONE', #88942, #26912 ) ;
#58014=FACE_OUTER_BOUND ( 'NONE', #7844, .T. ) ;
#58017=LINE ( 'NONE', #27557, #17496 ) ;
#58018=CARTESIAN_POINT ( 'NONE',  ( 32.98733314340959311, 5.965225279485572685, 2.074222136288530027 ) ) ;
#58024=VECTOR ( 'NONE', #93636, 1000.000000000000000 ) ;
#58028=CARTESIAN_POINT ( 'NONE',  ( 5.548031177074126852, -6.376774720514426953, -25.42222224686167920 ) ) ;
#58030=CARTESIAN_POINT ( 'NONE',  ( -7.491187506528125262, -6.376774720514410077, 19.53857357749109980 ) ) ;
#58035=B_SPLINE_SURFACE_WITH_KNOTS ( 'NONE', 3, 1, ( 
 ( #68620, #20935 ),
 ( #60025, #82836 ),
 ( #45290, #38155 ),
 ( #14315, #14815 ),
 ( #53405, #6212 ),
 ( #7205, #21425 ),
 ( #37171, #44296 ),
 ( #69108, #20430 ),
 ( #67146, #68128 ),
 ( #29549, #67633 ),
 ( #44792, #28550 ),
 ( #99050, #74721 ),
 ( #100037, #61521 ),
 ( #36178, #30041 ),
 ( #60527, #91440 ),
 ( #13317, #84329 ),
 ( #51403, #99543 ),
 ( #75225, #52399 ),
 ( #21923, #76215 ) ),
 .UNSPECIFIED., .F., .F., .F.,
 ( 4, 1, 1, 1, 1, 1, 1, 1, 1, 1, 1, 1, 1, 1, 1, 1, 4 ),
 ( 2, 2 ),
 ( 0.000000000000000000, 0.07563486594245749650, 0.1456749912579856643, 0.2101933844674982454, 0.2691971886348943910, 0.3228467966362091879, 0.3711350468222357479, 0.4143602045761037855, 0.4526539356929054625, 0.5231868047418553047, 0.5919172609462786117, 0.6599757056395090249, 0.7292117337225374474, 0.7981350023964016716, 0.8652933977976429158, 0.9318417558440025283, 1.000000000000000000 ),
 ( 0.000000000000000000, 1.000000000000000000 ),
 .UNSPECIFIED. ) ;
#58036=CARTESIAN_POINT ( 'NONE',  ( -29.49875734969025842, 5.965225279485572685, 15.62202280011862321 ) ) ;
#58041=CARTESIAN_POINT ( 'NONE',  ( 6.698292889820671725, -6.376774720514424288, 21.80822233811499444 ) ) ;
#58046=EDGE_LOOP ( 'NONE', ( #88041, #11957, #77338, #36245, #17691, #53967, #8637 ) ) ;
#58048=CARTESIAN_POINT ( 'NONE',  ( 0.3910256410256441884, -6.376774720514427841, 21.75000000000000000 ) ) ;
#58059=DIRECTION ( 'NONE',  ( -0.000000000000000000, -1.000000000000000000, -0.000000000000000000 ) ) ;
#58068=EDGE_CURVE ( 'NONE', #71712, #39562, #31918, .T. ) ;
#58073=CARTESIAN_POINT ( 'NONE',  ( 7.164391295225654765, -5.876774720514420736, 20.71606273170883838 ) ) ;
#58076=LINE ( 'NONE', #74278, #49699 ) ;
#58079=DIRECTION ( 'NONE',  ( 1.000000000000000000, 0.000000000000000000, 0.000000000000000000 ) ) ;
#58084=CARTESIAN_POINT ( 'NONE',  ( 14.85834502026402681, -3.582999323269832725, -27.37203305628894867 ) ) ;
#58090=CARTESIAN_POINT ( 'NONE',  ( -28.98875734969026041, -3.316774720514426456, -0.08597719988137648983 ) ) ;
#58091=DIRECTION ( 'NONE',  ( 0.9685340172660600322, 0.000000000000000000, -0.2488812114211667037 ) ) ;
#58094=DIRECTION ( 'NONE',  ( 0.000000000000000000, -1.000000000000000000, 0.000000000000000000 ) ) ;
#58098=VERTEX_POINT ( 'NONE', #37119 ) ;
#58100=CARTESIAN_POINT ( 'NONE',  ( 7.164391295225654765, -6.376774720514420736, 20.71606273170883838 ) ) ;
#58112=EDGE_CURVE ( 'NONE', #67290, #16727, #45243, .T. ) ;
#58114=VERTEX_POINT ( 'NONE', #49262 ) ;
#58127=CARTESIAN_POINT ( 'NONE',  ( 15.97264540888995299, -3.316774720514426456, -27.93485543958162154 ) ) ;
#58134=CARTESIAN_POINT ( 'NONE',  ( -0.02075734969026423599, -3.316774720514426456, -0.08597719988137648983 ) ) ;
#58137=CARTESIAN_POINT ( 'NONE',  ( 22.81105451610979173, -4.772774720514425972, -18.46691820600746681 ) ) ;
#58145=FACE_OUTER_BOUND ( 'NONE', #15516, .T. ) ;
#58157=LINE ( 'NONE', #66278, #4243 ) ;
#58165=DIRECTION ( 'NONE',  ( 0.000000000000000000, 0.000000000000000000, -1.000000000000000000 ) ) ;
#58173=CARTESIAN_POINT ( 'NONE',  ( -4.141025641025638748, -5.876774720514426953, 21.75000000000000355 ) ) ;
#58180=AXIS2_PLACEMENT_3D ( 'NONE', #78855, #17977, #57557 ) ;
#58185=CARTESIAN_POINT ( 'NONE',  ( 0.03625801282051022839, -5.876774720514410077, 19.27714342948718240 ) ) ;
#58194=EDGE_LOOP ( 'NONE', ( #75790, #55711, #39, #81250 ) ) ;
#58204=CYLINDRICAL_SURFACE ( 'NONE', #71365, 27.94799999999999685 ) ;
#58218=ORIENTED_EDGE ( 'NONE', *, *, #987, .T. ) ;
#58221=CARTESIAN_POINT ( 'NONE',  ( 33.74607884027702909, -0.3587747205144265483, -4.999864028243830916 ) ) ;
#58228=ORIENTED_EDGE ( 'NONE', *, *, #34081, .F. ) ;
#58234=ORIENTED_EDGE ( 'NONE', *, *, #25901, .F. ) ;
#58241=CARTESIAN_POINT ( 'NONE',  ( -0.5218785734906133955, -5.876774720514408301, 19.14848118821636547 ) ) ;
#58252=CARTESIAN_POINT ( 'NONE',  ( 16.26279755680690542, 6.475225279485573360, -27.67997040356620531 ) ) ;
#58256=LINE ( 'NONE', #10071, #57254 ) ;
#58260=AXIS2_PLACEMENT_3D ( 'NONE', #35610, #58454, #12244 ) ;
#58274=DIRECTION ( 'NONE',  ( -1.000000000000000000, -0.000000000000000000, 0.000000000000000000 ) ) ;
#58276=CARTESIAN_POINT ( 'NONE',  ( 31.44230187582509117, -4.132774720514425404, -3.488634554324458570 ) ) ;
#58280=ORIENTED_EDGE ( 'NONE', *, *, #98096, .F. ) ;
#58284=CARTESIAN_POINT ( 'NONE',  ( 4.931367317174526477, -6.376774720514420736, 20.61012727089847019 ) ) ;
#58290=EDGE_CURVE ( 'NONE', #12603, #12714, #88307, .T. ) ;
#58301=ORIENTED_EDGE ( 'NONE', *, *, #58936, .F. ) ;
#58309=EDGE_CURVE ( 'NONE', #4364, #95881, #43629, .T. ) ;
#58318=VECTOR ( 'NONE', #44451, 1000.000000000000000 ) ;
#58320=CARTESIAN_POINT ( 'NONE',  ( 3.559170184186323915, -5.876774720514403860, 18.55412939673608719 ) ) ;
#58324=ORIENTED_EDGE ( 'NONE', *, *, #63219, .F. ) ;
#58325=CARTESIAN_POINT ( 'NONE',  ( 6.620851319379956301, -3.316774720514426011, -27.30756699305372592 ) ) ;
#58333=LINE ( 'NONE', #81660, #15595 ) ;
#58335=PLANE ( 'NONE',  #21538 ) ;
#58343=VERTEX_POINT ( 'NONE', #77054 ) ;
#58346=DIRECTION ( 'NONE',  ( 0.000000000000000000, 0.000000000000000000, -1.000000000000000000 ) ) ;
#58347=ORIENTED_EDGE ( 'NONE', *, *, #72539, .T. ) ;
#58349=DIRECTION ( 'NONE',  ( -0.000000000000000000, -1.000000000000000000, -0.000000000000000000 ) ) ;
#58353=PLANE ( 'NONE',  #98869 ) ;
#58370=ORIENTED_EDGE ( 'NONE', *, *, #57654, .T. ) ;
#58376=ORIENTED_EDGE ( 'NONE', *, *, #78157, .F. ) ;
#58383=CARTESIAN_POINT ( 'NONE',  ( -10.75273025779354796, -5.876774720514426953, 23.03521261039436752 ) ) ;
#58414=AXIS2_PLACEMENT_3D ( 'NONE', #59232, #90177, #51623 ) ;
#58416=VECTOR ( 'NONE', #87617, 1000.000000000000000 ) ;
#58422=EDGE_CURVE ( 'NONE', #71923, #30845, #76547, .T. ) ;
#58424=ORIENTED_EDGE ( 'NONE', *, *, #66541, .T. ) ;
#58435=CARTESIAN_POINT ( 'NONE',  ( 6.887358010905132666, -6.376774720514426065, 21.32574817943157086 ) ) ;
#58442=CARTESIAN_POINT ( 'NONE',  ( 14.97568007496990816, -3.504021928054934509, -28.39450375387878722 ) ) ;
#58454=DIRECTION ( 'NONE',  ( -2.464095846557964090E-17, 1.000000000000000000, 0.000000000000000000 ) ) ;
#58456=ORIENTED_EDGE ( 'NONE', *, *, #84462, .T. ) ;
#58467=LINE ( 'NONE', #96015, #27475 ) ;
#58468=CARTESIAN_POINT ( 'NONE',  ( 5.495499487697820484, -5.876774720514418071, 20.18701882043406926 ) ) ;
#58470=CARTESIAN_POINT ( 'NONE',  ( 7.041152093163508319, -6.376774720514424288, 21.17127001373575368 ) ) ;
#58472=CARTESIAN_POINT ( 'NONE',  ( -13.89275734969026388, 5.965225279485572685, 31.02402280011862246 ) ) ;
#58474=VERTEX_POINT ( 'NONE', #99880 ) ;
#58478=CARTESIAN_POINT ( 'NONE',  ( -7.326923076923074873, -6.376774720514427841, 21.75000000000001066 ) ) ;
#58487=ORIENTED_EDGE ( 'NONE', *, *, #65951, .F. ) ;
#58495=CARTESIAN_POINT ( 'NONE',  ( 4.261846905714947731, -6.376774720514427841, 21.73176331363731251 ) ) ;
#58497=ADVANCED_FACE ( 'NONE', ( #22760 ), #21762, .T. ) ;
#58507=CARTESIAN_POINT ( 'NONE',  ( -8.978253834636468866, -6.376774720514426953, 18.51871304725684553 ) ) ;
#58508=PLANE ( 'NONE',  #29594 ) ;
#58511=CARTESIAN_POINT ( 'NONE',  ( 5.331146515430939203, -6.376774720514420736, 20.91308853528358469 ) ) ;
#58512=DIRECTION ( 'NONE',  ( 0.000000000000000000, 0.000000000000000000, 1.000000000000000000 ) ) ;
#58513=DIRECTION ( 'NONE',  ( 0.000000000000000000, 1.000000000000000000, 0.000000000000000000 ) ) ;
#58519=CARTESIAN_POINT ( 'NONE',  ( 4.215004826710222474, -6.376774720514427841, 21.34072927444733381 ) ) ;
#58521=CARTESIAN_POINT ( 'NONE',  ( 11.32485880260453293, -6.376774720514427841, -25.00877359051251148 ) ) ;
#58523=DIRECTION ( 'NONE',  ( -0.7071067811865442421, 0.000000000000000000, 0.7071067811865507924 ) ) ;
#58525=ORIENTED_EDGE ( 'NONE', *, *, #54265, .F. ) ;
#58526=CARTESIAN_POINT ( 'NONE',  ( 30.53060340732036693, -4.132774720514426292, -5.153186819891554471 ) ) ;
#58532=DIRECTION ( 'NONE',  ( -1.000000000000000000, -0.000000000000000000, -7.994117400814786717E-16 ) ) ;
#58536=CARTESIAN_POINT ( 'NONE',  ( -1.967852706420949005, -5.876774720514407413, 19.18381548539530357 ) ) ;
#58547=EDGE_LOOP ( 'NONE', ( #18874, #44843, #75913, #95712 ) ) ;
#58552=FACE_OUTER_BOUND ( 'NONE', #71843, .T. ) ;
#58554=FACE_OUTER_BOUND ( 'NONE', #93258, .T. ) ;
#58560=CARTESIAN_POINT ( 'NONE',  ( -4.169309590939843879, -6.376774720514411854, 19.59793130852656518 ) ) ;
#58564=ORIENTED_EDGE ( 'NONE', *, *, #2477, .T. ) ;
#58585=DIRECTION ( 'NONE',  ( -0.000000000000000000, -1.000000000000000000, -0.000000000000000000 ) ) ;
#58586=DIRECTION ( 'NONE',  ( 0.000000000000000000, 0.000000000000000000, -1.000000000000000000 ) ) ;
#58592=LINE ( 'NONE', #17148, #69271 ) ;
#58596=ORIENTED_EDGE ( 'NONE', *, *, #96217, .F. ) ;
#58603=ADVANCED_FACE ( 'NONE', ( #81070 ), #53166, .T. ) ;
#58613=VERTEX_POINT ( 'NONE', #76426 ) ;
#58616=ADVANCED_FACE ( 'NONE', ( #15036 ), #19861, .T. ) ;
#58641=VECTOR ( 'NONE', #29368, 1000.000000000000000 ) ;
#58648=ORIENTED_EDGE ( 'NONE', *, *, #39155, .T. ) ;
#58659=AXIS2_PLACEMENT_3D ( 'NONE', #81337, #12305, #42304 ) ;
#58664=CARTESIAN_POINT ( 'NONE',  ( 10.86264265030973952, 5.965225279485574461, -27.62597719988137612 ) ) ;
#58670=ORIENTED_EDGE ( 'NONE', *, *, #62735, .F. ) ;
#58673=CARTESIAN_POINT ( 'NONE',  ( 32.98733314340959311, 5.965225279485572685, 2.074222136288530027 ) ) ;
#58678=DIRECTION ( 'NONE',  ( 0.000000000000000000, -1.000000000000000000, 0.000000000000000000 ) ) ;
#58679=LINE ( 'NONE', #3908, #57915 ) ;
#58680=CIRCLE ( 'NONE', #34417, 1.149999999999998135 ) ;
#58689=ORIENTED_EDGE ( 'NONE', *, *, #13718, .F. ) ;
#58691=CARTESIAN_POINT ( 'NONE',  ( 11.62916340711181284, 5.965225279485572685, 28.75961759920349792 ) ) ;
#58693=CARTESIAN_POINT ( 'NONE',  ( 22.81105451610979173, 6.475225279485573360, -18.46691820600746681 ) ) ;
#58699=DIRECTION ( 'NONE',  ( 0.000000000000000000, 0.000000000000000000, -1.000000000000000000 ) ) ;
#58706=ORIENTED_EDGE ( 'NONE', *, *, #46492, .F. ) ;
#58709=CARTESIAN_POINT ( 'NONE',  ( -10.32858501761201353, -6.295917116278983983, 28.25808420984930791 ) ) ;
#58710=CIRCLE ( 'NONE', #60318, 2.249999999999998668 ) ;
#58716=CARTESIAN_POINT ( 'NONE',  ( 30.53060340732035982, 6.475225279485573360, 20.86760796525322093 ) ) ;
#58718=DIRECTION ( 'NONE',  ( -0.000000000000000000, 1.000000000000000000, -0.000000000000000000 ) ) ;
#58723=CARTESIAN_POINT ( 'NONE',  ( -4.568292318365942073, 5.965225279485572685, 30.06720597538392425 ) ) ;
#58724=DIRECTION ( 'NONE',  ( -2.417950247244706201E-16, 0.000000000000000000, 1.000000000000000000 ) ) ;
#58749=DIRECTION ( 'NONE',  ( 0.000000000000000000, 0.000000000000000000, -1.000000000000000000 ) ) ;
#58750=VECTOR ( 'NONE', #87552, 1000.000000000000227 ) ;
#58779=DIRECTION ( 'NONE',  ( -0.7071067811865507924, -0.000000000000000000, -0.7071067811865442421 ) ) ;
#58783=PLANE ( 'NONE',  #4737 ) ;
#58797=LINE ( 'NONE', #34959, #10965 ) ;
#58803=AXIS2_PLACEMENT_3D ( 'NONE', #63511, #24421, #77190 ) ;
#58807=EDGE_CURVE ( 'NONE', #14292, #39331, #50015, .T. ) ;
#58810=CARTESIAN_POINT ( 'NONE',  ( 3.787259615384621636, -5.876774720514405637, 18.51923076923076650 ) ) ;
#58819=EDGE_CURVE ( 'NONE', #89693, #55307, #26158, .T. ) ;
#58822=LINE ( 'NONE', #15498, #70832 ) ;
#58823=CARTESIAN_POINT ( 'NONE',  ( 5.654871928786437074, -5.876774720514419847, 20.64717925217163952 ) ) ;
#58825=CIRCLE ( 'NONE', #86337, 0.8160000000000007248 ) ;
#58838=CARTESIAN_POINT ( 'NONE',  ( 3.181132013147180970, -6.376774720514426065, 21.64201922499777808 ) ) ;
#58841=CARTESIAN_POINT ( 'NONE',  ( 16.26279755680690542, -1.684774720514426560, -27.67997040356620531 ) ) ;
#58846=ADVANCED_FACE ( 'NONE', ( #19041 ), #50500, .F. ) ;
#58859=VERTEX_POINT ( 'NONE', #81455 ) ;
#58860=CARTESIAN_POINT ( 'NONE',  ( 3.825768195983636044, -5.876774720514424288, 21.47884071039599618 ) ) ;
#58868=EDGE_CURVE ( 'NONE', #42081, #86899, #41785, .T. ) ;
#58875=DIRECTION ( 'NONE',  ( 0.000000000000000000, 0.000000000000000000, 1.000000000000000000 ) ) ;
#58884=CARTESIAN_POINT ( 'NONE',  ( 5.696197030082937651, -6.376774720514422512, 21.05387829558662816 ) ) ;
#58885=EDGE_LOOP ( 'NONE', ( #16003, #75098, #73830, #63596 ) ) ;
#58887=CARTESIAN_POINT ( 'NONE',  ( 12.88745205057041510, -5.152774720521900775, -28.14312002385437239 ) ) ;
#58904=ORIENTED_EDGE ( 'NONE', *, *, #70784, .T. ) ;
#58916=VERTEX_POINT ( 'NONE', #89559 ) ;
#58917=ORIENTED_EDGE ( 'NONE', *, *, #45327, .T. ) ;
#58921=EDGE_LOOP ( 'NONE', ( #91855, #98845, #29134, #25614, #85463, #51795 ) ) ;
#58927=VERTEX_POINT ( 'NONE', #65255 ) ;
#58930=LINE ( 'NONE', #89872, #64944 ) ;
#58934=CIRCLE ( 'NONE', #33010, 4.299999999999999822 ) ;
#58936=EDGE_CURVE ( 'NONE', #41375, #48360, #96180, .T. ) ;
#58937=DIRECTION ( 'NONE',  ( 0.000000000000000000, -1.000000000000000000, 0.000000000000000000 ) ) ;
#58938=DIRECTION ( 'NONE',  ( 0.000000000000000000, 1.000000000000000000, -0.000000000000000000 ) ) ;
#58946=CARTESIAN_POINT ( 'NONE',  ( 12.09245314707524876, -4.658029312750951334, -27.52981586573924488 ) ) ;
#58949=EDGE_CURVE ( 'NONE', #40969, #7626, #13916, .T. ) ;
#58955=ORIENTED_EDGE ( 'NONE', *, *, #35892, .T. ) ;
#58991=CARTESIAN_POINT ( 'NONE',  ( 3.797776442307698286, -6.376774720514427841, 21.83974358974358410 ) ) ;
#58997=EDGE_CURVE ( 'NONE', #6989, #77894, #2101, .T. ) ;
#58998=ORIENTED_EDGE ( 'NONE', *, *, #15633, .T. ) ;
#59009=CARTESIAN_POINT ( 'NONE',  ( -7.312991930324885814, -6.376774720514413630, 20.02088365235844947 ) ) ;
#59011=DIRECTION ( 'NONE',  ( -0.000000000000000000, -1.000000000000000000, -0.000000000000000000 ) ) ;
#59021=CARTESIAN_POINT ( 'NONE',  ( 9.002841642506252740, -6.376774720514426065, -25.01329513651794656 ) ) ;
#59036=CARTESIAN_POINT ( 'NONE',  ( -24.90875734969025501, -5.356774720514425603, 26.43402280011862615 ) ) ;
#59039=PLANE ( 'NONE',  #32394 ) ;
#59044=DIRECTION ( 'NONE',  ( -0.000000000000000000, 1.000000000000000000, -0.000000000000000000 ) ) ;
#59055=CARTESIAN_POINT ( 'NONE',  ( 13.91401389203221406, 6.475225279485573360, 158.0376437107427137 ) ) ;
#59075=CIRCLE ( 'NONE', #13631, 2.249999999999998668 ) ;
#59076=CARTESIAN_POINT ( 'NONE',  ( 32.53346577320679245, -2.682774720514426559, -11.93731717363830747 ) ) ;
#59092=DIRECTION ( 'NONE',  ( 0.000000000000000000, -1.000000000000000000, 0.000000000000000000 ) ) ;
#59099=ORIENTED_EDGE ( 'NONE', *, *, #48669, .T. ) ;
#59104=LINE ( 'NONE', #42879, #19423 ) ;
#59115=EDGE_CURVE ( 'NONE', #97841, #77005, #75488, .T. ) ;
#59128=CARTESIAN_POINT ( 'NONE',  ( -4.568292318365942073, -0.3587747205144265483, 30.06720597538392425 ) ) ;
#59131=DIRECTION ( 'NONE',  ( 0.000000000000000000, 0.000000000000000000, 1.000000000000000000 ) ) ;
#59133=DIRECTION ( 'NONE',  ( -1.000000000000000000, 0.000000000000000000, 0.000000000000000000 ) ) ;
#59148=CARTESIAN_POINT ( 'NONE',  ( -1.044639546681034536, -6.376774720514417183, 20.34213149456667580 ) ) ;
#59155=DIRECTION ( 'NONE',  ( -1.000000000000000000, -0.000000000000000000, -7.994117400814786717E-16 ) ) ;
#59162=VERTEX_POINT ( 'NONE', #100128 ) ;
#59176=CARTESIAN_POINT ( 'NONE',  ( -10.59832330691884117, -0.3587747205144061757, -27.05373799718300987 ) ) ;
#59181=ADVANCED_FACE ( 'NONE', ( #3595 ), #4088, .T. ) ;
#59199=CARTESIAN_POINT ( 'NONE',  ( 13.91401389203221406, -0.3587747205144265483, 158.0376437107427137 ) ) ;
#59202=VERTEX_POINT ( 'NONE', #27426 ) ;
#59205=CARTESIAN_POINT ( 'NONE',  ( 9.150000000000000355, -5.876774720514426953, -15.70000000000000284 ) ) ;
#59214=CARTESIAN_POINT ( 'NONE',  ( -10.12061615367207601, -3.718318319926830373, 30.49412484105965859 ) ) ;
#59225=CARTESIAN_POINT ( 'NONE',  ( -28.98875734969026396, 5.965225279485572685, 7.870022800118628759 ) ) ;
#59231=CARTESIAN_POINT ( 'NONE',  ( -0.8460708837923186509, -5.876774720514410077, 19.21968329462762526 ) ) ;
#59232=CARTESIAN_POINT ( 'NONE',  ( 22.02124265030973760, -7.835183881457444599, 16.20402280011862217 ) ) ;
#59264=CARTESIAN_POINT ( 'NONE',  ( -20.27875734969026311, 7.743225279485574042, 24.00402280011862288 ) ) ;
#59267=CARTESIAN_POINT ( 'NONE',  ( 5.641025641025643189, -6.376774720514420736, 20.78665865384615330 ) ) ;
#59270=CARTESIAN_POINT ( 'NONE',  ( -10.11875734969026297, 5.965225279485572685, 30.51402280011862089 ) ) ;
#59286=CIRCLE ( 'NONE', #83607, 4.299999999999999822 ) ;
#59288=ORIENTED_EDGE ( 'NONE', *, *, #98913, .F. ) ;
#59298=VECTOR ( 'NONE', #87872, 1000.000000000000227 ) ;
#59303=ORIENTED_EDGE ( 'NONE', *, *, #12334, .F. ) ;
#59308=EDGE_CURVE ( 'NONE', #34190, #53709, #46637, .T. ) ;
#59316=EDGE_CURVE ( 'NONE', #34477, #46605, #16413, .T. ) ;
#59321=CARTESIAN_POINT ( 'NONE',  ( 6.273728352332436309, -5.876774720514415407, 20.10092598260902008 ) ) ;
#59323=CARTESIAN_POINT ( 'NONE',  ( 5.766314450391940127, -6.376774720514424288, 21.17177008079512035 ) ) ;
#59341=VECTOR ( 'NONE', #75447, 1000.000000000000000 ) ;
#59343=CARTESIAN_POINT ( 'NONE',  ( -12.64432969575899968, -0.3587747205143967943, -26.13179214487285407 ) ) ;
#59352=VECTOR ( 'NONE', #6978, 1000.000000000000000 ) ;
#59353=ORIENTED_EDGE ( 'NONE', *, *, #5909, .F. ) ;
#59354=VECTOR ( 'NONE', #23086, 1000.000000000000227 ) ;
#59359=DIRECTION ( 'NONE',  ( -0.000000000000000000, 1.000000000000000000, -0.000000000000000000 ) ) ;
#59361=DIRECTION ( 'NONE',  ( 0.9822594791677485837, 0.000000000000000000, -0.1875268396392986980 ) ) ;
#59364=AXIS2_PLACEMENT_3D ( 'NONE', #90919, #28516, #30009 ) ;
#59370=AXIS2_PLACEMENT_3D ( 'NONE', #96328, #65908, #96823 ) ;
#59381=ORIENTED_EDGE ( 'NONE', *, *, #40048, .T. ) ;
#59398=ORIENTED_EDGE ( 'NONE', *, *, #71139, .F. ) ;
#59424=CIRCLE ( 'NONE', #15675, 130.7884398600581335 ) ;
#59425=ORIENTED_EDGE ( 'NONE', *, *, #23529, .F. ) ;
#59447=ORIENTED_EDGE ( 'NONE', *, *, #67524, .F. ) ;
#59450=DIRECTION ( 'NONE',  ( -1.000000000000000000, 0.000000000000000000, -0.000000000000000000 ) ) ;
#59460=EDGE_CURVE ( 'NONE', #23749, #94938, #58010, .T. ) ;
#59466=CIRCLE ( 'NONE', #51354, 0.3000000000000016542 ) ;
#59470=CARTESIAN_POINT ( 'NONE',  ( -32.30247028140506416, -1.684774720514426560, 27.60502002861223048 ) ) ;
#59500=EDGE_CURVE ( 'NONE', #1528, #5079, #59286, .T. ) ;
#59501=VECTOR ( 'NONE', #36253, 1000.000000000000000 ) ;
#59502=CARTESIAN_POINT ( 'NONE',  ( -6.741682653110981249, 5.965225279485572685, 30.62569541381301619 ) ) ;
#59508=EDGE_LOOP ( 'NONE', ( #58917, #79155, #99768, #91498 ) ) ;
#59509=ADVANCED_FACE ( 'NONE', ( #52375 ), #52877, .T. ) ;
#59510=CARTESIAN_POINT ( 'NONE',  ( -2.768609665556983845, 5.965225279485594001, -29.41086200512614823 ) ) ;
#59511=CARTESIAN_POINT ( 'NONE',  ( 4.653846153846159517, -5.876774720514415407, 19.99999999999999289 ) ) ;
#59521=CARTESIAN_POINT ( 'NONE',  ( -2.285970405126252825, -5.876774720514409189, 19.14905311829361167 ) ) ;
#59526=CARTESIAN_POINT ( 'NONE',  ( 6.467769777575680834, -5.876774720514427841, 21.83821538399986650 ) ) ;
#59528=AXIS2_PLACEMENT_3D ( 'NONE', #53329, #90379, #14239 ) ;
#59547=FACE_OUTER_BOUND ( 'NONE', #20404, .T. ) ;
#59557=ORIENTED_EDGE ( 'NONE', *, *, #42798, .F. ) ;
#59569=CARTESIAN_POINT ( 'NONE',  ( 3.448102555317568374, -5.876774720514424288, 21.39871091031772110 ) ) ;
#59574=EDGE_LOOP ( 'NONE', ( #25794, #1469, #26650, #51953, #36899 ) ) ;
#59579=ORIENTED_EDGE ( 'NONE', *, *, #89298, .F. ) ;
#59582=CARTESIAN_POINT ( 'NONE',  ( -25.92875734969026169, -3.316774720514426456, 26.43402280011862615 ) ) ;
#59583=VECTOR ( 'NONE', #54246, 1000.000000000000000 ) ;
#59589=ORIENTED_EDGE ( 'NONE', *, *, #78158, .F. ) ;
#59591=CARTESIAN_POINT ( 'NONE',  ( 7.010993867624484288, -6.376774720514417183, 20.34381700913260715 ) ) ;
#59597=DIRECTION ( 'NONE',  ( 0.000000000000000000, -1.000000000000000000, 0.000000000000000000 ) ) ;
#59607=CARTESIAN_POINT ( 'NONE',  ( 2.968164339864655332, -6.376774720514408301, 19.33154224050496595 ) ) ;
#59609=VECTOR ( 'NONE', #90895, 1000.000000000000114 ) ;
#59623=EDGE_CURVE ( 'NONE', #57615, #17980, #58333, .T. ) ;
#59631=CARTESIAN_POINT ( 'NONE',  ( -4.141025641025641413, -5.876774720514419847, 20.67377804487180271 ) ) ;
#59642=EDGE_CURVE ( 'NONE', #99983, #96134, #97381, .T. ) ;
#59657=DIRECTION ( 'NONE',  ( 0.000000000000000000, 0.000000000000000000, -1.000000000000000000 ) ) ;
#59658=ORIENTED_EDGE ( 'NONE', *, *, #47764, .T. ) ;
#59659=VERTEX_POINT ( 'NONE', #83137 ) ;
#59666=DIRECTION ( 'NONE',  ( -0.000000000000000000, 1.000000000000000000, -0.000000000000000000 ) ) ;
#59667=CARTESIAN_POINT ( 'NONE',  ( 0.000000000000000000, -2.682774720514426559, 0.000000000000000000 ) ) ;
#59672=ADVANCED_FACE ( 'NONE', ( #34983 ), #36100, .T. ) ;
#59681=ORIENTED_EDGE ( 'NONE', *, *, #35893, .F. ) ;
#59688=CARTESIAN_POINT ( 'NONE',  ( -3.054691362729579751, -6.376774720514413630, 19.78730719034165375 ) ) ;
#59699=CARTESIAN_POINT ( 'NONE',  ( 25.83488407601165093, -3.407774720514426647, -11.31196583263649558 ) ) ;
#59702=DIRECTION ( 'NONE',  ( 0.000000000000000000, 1.000000000000000000, 0.000000000000000000 ) ) ;
#59706=CARTESIAN_POINT ( 'NONE',  ( 31.74473449900405697, -4.976825198871215328, -4.259190951192157293 ) ) ;
#59716=B_SPLINE_CURVE_WITH_KNOTS ( 'NONE', 3,
 ( #28679, #91070, #53027, #44416, #5343, #84453, #21546, #37789, #52519, #37296, #75339, #29673, #68741, #91564, #36299 ),
 .UNSPECIFIED., .F., .F.,
 ( 4, 1, 1, 1, 1, 1, 1, 1, 1, 1, 1, 1, 4 ),
 ( 0.000000000000000000, 0.07176606415833945707, 0.1412255357663688426, 0.2091158524974623678, 0.2748396534685264014, 0.3394829303752206484, 0.4024762667353993240, 0.4649418891713267277, 0.5268326406463827993, 0.6474148160608228508, 0.7655615117859491114, 0.8816150870393308914, 1.000000000000000000 ),
 .UNSPECIFIED. ) ;
#59724=EDGE_LOOP ( 'NONE', ( #43121, #94627, #81928, #100349 ) ) ;
#59730=CARTESIAN_POINT ( 'NONE',  ( -29.49875734969025842, -0.3587747205144265483, 25.61802280011862720 ) ) ;
#59738=CARTESIAN_POINT ( 'NONE',  ( -2.780940648273603433, -5.876774720514411854, 20.02088365235843881 ) ) ;
#59752=ORIENTED_EDGE ( 'NONE', *, *, #5960, .F. ) ;
#59757=CYLINDRICAL_SURFACE ( 'NONE', #26956, 27.94799999999999685 ) ;
#59759=EDGE_CURVE ( 'NONE', #58114, #48360, #22230, .T. ) ;
#59782=CARTESIAN_POINT ( 'NONE',  ( 3.036358173076929123, -6.376774720514420736, 20.87990785256409865 ) ) ;
#59783=CARTESIAN_POINT ( 'NONE',  ( 33.74607884027702909, -0.3587747205144265483, -4.999864028243830916 ) ) ;
#59790=CARTESIAN_POINT ( 'NONE',  ( 6.955725288069978696, -5.876774720514425177, 21.70430095680336890 ) ) ;
#59800=ORIENTED_EDGE ( 'NONE', *, *, #41708, .F. ) ;
#59802=ORIENTED_EDGE ( 'NONE', *, *, #61338, .T. ) ;
#59813=ORIENTED_EDGE ( 'NONE', *, *, #25363, .T. ) ;
#59820=DIRECTION ( 'NONE',  ( 0.000000000000000000, 1.478457507934778393E-16, -1.000000000000000000 ) ) ;
#59822=CARTESIAN_POINT ( 'NONE',  ( -3.108974358974359475, -5.876774720514418071, 20.36458333333334281 ) ) ;
#59829=CARTESIAN_POINT ( 'NONE',  ( 5.642655980204820843, -6.376774720514418959, 20.71586687040766961 ) ) ;
#59833=ORIENTED_EDGE ( 'NONE', *, *, #9226, .F. ) ;
#59847=CARTESIAN_POINT ( 'NONE',  ( -0.9257915630711897048, -5.876774720514409189, 19.25892998154168012 ) ) ;
#59851=CARTESIAN_POINT ( 'NONE',  ( -3.108787716482549701, -6.376774720514417183, 20.32624910079993086 ) ) ;
#59856=AXIS2_PLACEMENT_3D ( 'NONE', #52407, #61530, #83343 ) ;
#59867=CARTESIAN_POINT ( 'NONE',  ( 4.016587897052070311, -5.876774720514425177, 21.44459449800855921 ) ) ;
#59873=ORIENTED_EDGE ( 'NONE', *, *, #38191, .F. ) ;
#59881=ADVANCED_FACE ( 'NONE', ( #21733 ), #83644, .F. ) ;
#59886=EDGE_CURVE ( 'NONE', #86736, #3834, #9153, .T. ) ;
#59890=FACE_OUTER_BOUND ( 'NONE', #17070, .T. ) ;
#59894=CARTESIAN_POINT ( 'NONE',  ( 11.86515846156731335, -5.152774720514426754, -28.09350142571734921 ) ) ;
#59896=CARTESIAN_POINT ( 'NONE',  ( 14.76093561896379214, 5.965225279485572685, -26.55548769130089681 ) ) ;
#59897=CARTESIAN_POINT ( 'NONE',  ( 32.98733314340959311, -0.3587747205144265483, 2.074222136288530027 ) ) ;
#59901=ORIENTED_EDGE ( 'NONE', *, *, #40383, .T. ) ;
#59907=DIRECTION ( 'NONE',  ( 0.000000000000000000, -1.000000000000000000, -8.393823270855521221E-16 ) ) ;
#59912=AXIS2_PLACEMENT_3D ( 'NONE', #98449, #36558, #69015 ) ;
#59918=ORIENTED_EDGE ( 'NONE', *, *, #43030, .T. ) ;
#59921=DIRECTION ( 'NONE',  ( 0.000000000000000000, 0.000000000000000000, -1.000000000000000000 ) ) ;
#59922=EDGE_CURVE ( 'NONE', #74381, #39047, #26972, .T. ) ;
#59923=VECTOR ( 'NONE', #64453, 1000.000000000000000 ) ;
#59933=VERTEX_POINT ( 'NONE', #48452 ) ;
#59935=ADVANCED_FACE ( 'NONE', ( #65692 ), #10881, .T. ) ;
#59937=VERTEX_POINT ( 'NONE', #94612 ) ;
#59941=CARTESIAN_POINT ( 'NONE',  ( 14.47435193673551090, -3.621805754661552523, -28.36943713414519763 ) ) ;
#59950=ORIENTED_EDGE ( 'NONE', *, *, #67369, .F. ) ;
#59965=CARTESIAN_POINT ( 'NONE',  ( 5.109298100548420152, -3.316774720514426456, -27.55941679637948383 ) ) ;
#59968=ORIENTED_EDGE ( 'NONE', *, *, #29489, .T. ) ;
#59969=CARTESIAN_POINT ( 'NONE',  ( 29.68604458549361169, -6.066877414785177614, 27.51520267613161153 ) ) ;
#59977=VECTOR ( 'NONE', #94099, 1000.000000000000000 ) ;
#60016=CARTESIAN_POINT ( 'NONE',  ( 30.93860345374796239, 5.965225279485572685, 28.07639619989137003 ) ) ;
#60025=CARTESIAN_POINT ( 'NONE',  ( -1.359251851468251449, -6.376774720514420736, 20.71116975788854120 ) ) ;
#60026=ORIENTED_EDGE ( 'NONE', *, *, #9801, .T. ) ;
#60032=CARTESIAN_POINT ( 'NONE',  ( 6.420673076923079314, -5.876774720514427841, 21.83974358974358765 ) ) ;
#60044=VECTOR ( 'NONE', #22102, 1000.000000000000000 ) ;
#60051=EDGE_LOOP ( 'NONE', ( #55269, #79138 ) ) ;
#60054=ORIENTED_EDGE ( 'NONE', *, *, #12289, .T. ) ;
#60055=ORIENTED_EDGE ( 'NONE', *, *, #44106, .F. ) ;
#60069=AXIS2_PLACEMENT_3D ( 'NONE', #62595, #53497, #68709 ) ;
#60071=VECTOR ( 'NONE', #85115, 1000.000000000000000 ) ;
#60073=ORIENTED_EDGE ( 'NONE', *, *, #72679, .F. ) ;
#60076=ORIENTED_EDGE ( 'NONE', *, *, #92289, .T. ) ;
#60081=ORIENTED_EDGE ( 'NONE', *, *, #77380, .F. ) ;
#60086=DIRECTION ( 'NONE',  ( -1.257682986112628908E-16, -0.000000000000000000, -1.000000000000000000 ) ) ;
#60093=FACE_OUTER_BOUND ( 'NONE', #48693, .T. ) ;
#60097=EDGE_CURVE ( 'NONE', #90882, #41242, #7790, .T. ) ;
#60098=ADVANCED_FACE ( 'NONE', ( #73773 ), #56189, .T. ) ;
#60099=VERTEX_POINT ( 'NONE', #50950 ) ;
#60105=CARTESIAN_POINT ( 'NONE',  ( 29.75292639967170771, -5.303223407918566501, 26.69524796275325684 ) ) ;
#60109=VERTEX_POINT ( 'NONE', #51942 ) ;
#60113=ORIENTED_EDGE ( 'NONE', *, *, #98310, .T. ) ;
#60114=CARTESIAN_POINT ( 'NONE',  ( 3.450324536843889067, -6.376774720514404748, 18.60429515659643229 ) ) ;
#60115=CARTESIAN_POINT ( 'NONE',  ( 3.183477995988301945, -5.876774720514405637, 18.35601591497023577 ) ) ;
#60134=CARTESIAN_POINT ( 'NONE',  ( -13.36367879947601445, -5.876774720514426953, 20.00000000000000355 ) ) ;
#60137=CARTESIAN_POINT ( 'NONE',  ( -4.243469080022288509, -5.876774720514412742, 19.94806476610987644 ) ) ;
#60142=DIRECTION ( 'NONE',  ( -0.6392559695863496705, 6.845827386180411947E-16, -0.7689940216596069522 ) ) ;
#60162=VERTEX_POINT ( 'NONE', #11872 ) ;
#60163=EDGE_CURVE ( 'NONE', #92445, #71754, #86942, .T. ) ;
#60174=FACE_BOUND ( 'NONE', #54082, .T. ) ;
#60181=DIRECTION ( 'NONE',  ( 0.000000000000000000, 0.000000000000000000, -1.000000000000000000 ) ) ;
#60184=LINE ( 'NONE', #50559, #69609 ) ;
#60189=CARTESIAN_POINT ( 'NONE',  ( -2.285970405126252825, -6.376774720514408301, 19.14905311829361167 ) ) ;
#60194=CARTESIAN_POINT ( 'NONE',  ( 30.53060340732036337, -2.682774720514426559, 3.744237563515920634E-15 ) ) ;
#60201=ADVANCED_FACE ( 'NONE', ( #4273 ), #35222, .F. ) ;
#60204=ORIENTED_EDGE ( 'NONE', *, *, #8404, .F. ) ;
#60223=CARTESIAN_POINT ( 'NONE',  ( -10.22992732494356005, -5.749436596009021017, 29.32115093811272288 ) ) ;
#60225=DIRECTION ( 'NONE',  ( -0.000000000000000000, 1.000000000000000000, -0.000000000000000000 ) ) ;
#60226=ORIENTED_EDGE ( 'NONE', *, *, #48770, .F. ) ;
#60245=EDGE_CURVE ( 'NONE', #7198, #8989, #52943, .T. ) ;
#60267=CARTESIAN_POINT ( 'NONE',  ( 3.398286024651508530, -5.876774720514429617, 21.76255057507181334 ) ) ;
#60271=CARTESIAN_POINT ( 'NONE',  ( -5.891025641025639636, -6.376774720514420736, 20.75510817307693046 ) ) ;
#60280=VECTOR ( 'NONE', #45040, 1000.000000000000000 ) ;
#60285=DIRECTION ( 'NONE',  ( 0.000000000000000000, 0.000000000000000000, 1.000000000000000000 ) ) ;
#60298=ORIENTED_EDGE ( 'NONE', *, *, #39092, .F. ) ;
#60305=ORIENTED_EDGE ( 'NONE', *, *, #84462, .F. ) ;
#60316=DIRECTION ( 'NONE',  ( -0.000000000000000000, -1.000000000000000000, -0.000000000000000000 ) ) ;
#60318=AXIS2_PLACEMENT_3D ( 'NONE', #16140, #62848, #24749 ) ;
#60323=EDGE_CURVE ( 'NONE', #40447, #42731, #2765, .T. ) ;
#60324=CARTESIAN_POINT ( 'NONE',  ( 4.821763668436347849, -6.376774720514406525, 18.93074869776452829 ) ) ;
#60330=EDGE_CURVE ( 'NONE', #78100, #91151, #24972, .T. ) ;
#60361=PLANE ( 'NONE',  #90075 ) ;
#60368=LINE ( 'NONE', #20764, #2876 ) ;
#60375=DIRECTION ( 'NONE',  ( 0.000000000000000000, -1.000000000000000000, 0.000000000000000000 ) ) ;
#60389=EDGE_CURVE ( 'NONE', #5644, #87540, #71664, .T. ) ;
#60394=EDGE_CURVE ( 'NONE', #90882, #67798, #24474, .T. ) ;
#60395=CARTESIAN_POINT ( 'NONE',  ( 33.61456970919608978, -3.316774720514426900, -11.35828564741660962 ) ) ;
#60412=CARTESIAN_POINT ( 'NONE',  ( 5.811591729264017125, -5.876774720514422512, 21.22699980322195046 ) ) ;
#60436=CARTESIAN_POINT ( 'NONE',  ( 2.677468215678941110, -5.876774720514418959, 20.83735685176740304 ) ) ;
#60455=B_SPLINE_SURFACE_WITH_KNOTS ( 'NONE', 3, 1, ( 
 ( #11350, #80359 ),
 ( #27581, #5230 ),
 ( #10852, #36186 ),
 ( #97081, #73255 ),
 ( #72763, #42324 ),
 ( #26071, #57044 ),
 ( #50917, #87979 ) ),
 .UNSPECIFIED., .F., .F., .F.,
 ( 4, 1, 1, 1, 4 ),
 ( 2, 2 ),
 ( 0.000000000000000000, 0.1496899112665939224, 0.2993798225331877338, 0.4490697337997815453, 0.5987596450663754677 ),
 ( 0.000000000000000000, 1.000000000000000000 ),
 .UNSPECIFIED. ) ;
#60458=EDGE_CURVE ( 'NONE', #26531, #63950, #80504, .T. ) ;
#60476=AXIS2_PLACEMENT_3D ( 'NONE', #79337, #24550, #40287 ) ;
#60482=CARTESIAN_POINT ( 'NONE',  ( 15.34241074214975065, -3.824162593742471028, -28.48848699765728654 ) ) ;
#60483=CARTESIAN_POINT ( 'NONE',  ( 33.96422015159436114, 5.965225279485572685, -7.233236000911337449 ) ) ;
#60503=VECTOR ( 'NONE', #39272, 1000.000000000000000 ) ;
#60519=CARTESIAN_POINT ( 'NONE',  ( -24.90875734969025501, 5.965225279485572685, 30.00402280011862288 ) ) ;
#60527=CARTESIAN_POINT ( 'NONE',  ( -1.845912073933368536, -6.376774720514408301, 19.53740760792477360 ) ) ;
#60528=B_SPLINE_SURFACE_WITH_KNOTS ( 'NONE', 3, 1, ( 
 ( #37708, #92984 ),
 ( #83880, #45337 ),
 ( #68169, #6754 ),
 ( #68668, #29095 ),
 ( #99586, #7248 ) ),
 .UNSPECIFIED., .F., .F., .F.,
 ( 4, 1, 4 ),
 ( 2, 2 ),
 ( 0.000000000000000000, 0.4873406636582197082, 0.9999999999999998890 ),
 ( 0.000000000000000000, 1.000000000000000000 ),
 .UNSPECIFIED. ) ;
#60529=DIRECTION ( 'NONE',  ( 0.000000000000000000, -1.000000000000000000, 0.000000000000000000 ) ) ;
#60535=AXIS2_PLACEMENT_3D ( 'NONE', #88783, #80160, #51212 ) ;
#60536=DIRECTION ( 'NONE',  ( -0.000000000000000000, 1.000000000000000000, -0.000000000000000000 ) ) ;
#60537=VERTEX_POINT ( 'NONE', #97489 ) ;
#60548=DIRECTION ( 'NONE',  ( 0.000000000000000000, 0.000000000000000000, 1.000000000000000000 ) ) ;
#60552=ORIENTED_EDGE ( 'NONE', *, *, #44419, .T. ) ;
#60554=CARTESIAN_POINT ( 'NONE',  ( 10.24059822343757986, -6.376774720514426953, 22.82308057603840368 ) ) ;
#60564=CARTESIAN_POINT ( 'NONE',  ( 31.63608488009065667, -6.376774720514426953, 27.34773273846995068 ) ) ;
#60586=CIRCLE ( 'NONE', #10155, 251.4258649670780699 ) ;
#60587=PLANE ( 'NONE',  #45292 ) ;
#60603=DIRECTION ( 'NONE',  ( -1.000000000000000000, 0.000000000000000000, 0.000000000000000000 ) ) ;
#60605=CARTESIAN_POINT ( 'NONE',  ( 5.994920710892026605, -5.876774720514429617, 21.76186867112717138 ) ) ;
#60608=EDGE_LOOP ( 'NONE', ( #6642, #40319, #59099, #85006 ) ) ;
#60614=CARTESIAN_POINT ( 'NONE',  ( 2.747717285871495108, -6.376774720514404748, 18.94713297040818034 ) ) ;
#60621=VERTEX_POINT ( 'NONE', #24737 ) ;
#60631=CARTESIAN_POINT ( 'NONE',  ( 29.77147767949874790, -5.356774720514425603, 26.15915692125051706 ) ) ;
#60639=CARTESIAN_POINT ( 'NONE',  ( -28.98875734969026396, -0.3587747205144265483, 10.11402280011862587 ) ) ;
#60659=ORIENTED_EDGE ( 'NONE', *, *, #19174, .F. ) ;
#60660=CARTESIAN_POINT ( 'NONE',  ( 0.3670296583442628213, -6.376774720514417183, 20.26087634804755311 ) ) ;
#60665=LINE ( 'NONE', #68761, #33904 ) ;
#60674=DIRECTION ( 'NONE',  ( 0.000000000000000000, -1.000000000000000000, 0.000000000000000000 ) ) ;
#60676=EDGE_LOOP ( 'NONE', ( #68301, #40649, #58904, #1819 ) ) ;
#60677=PLANE ( 'NONE',  #1612 ) ;
#60678=ORIENTED_EDGE ( 'NONE', *, *, #429, .T. ) ;
#60683=CARTESIAN_POINT ( 'NONE',  ( -27.25988310792305214, 5.965225279485572685, 30.32664379231667695 ) ) ;
#60686=ORIENTED_EDGE ( 'NONE', *, *, #58112, .F. ) ;
#60687=CARTESIAN_POINT ( 'NONE',  ( -0.7067007548136460260, -5.876774720514410966, 19.51517878119693350 ) ) ;
#60696=EDGE_CURVE ( 'NONE', #55815, #2790, #96726, .T. ) ;
#60700=DIRECTION ( 'NONE',  ( -0.000000000000000000, 1.000000000000000000, -0.000000000000000000 ) ) ;
#60709=DIRECTION ( 'NONE',  ( -2.246662546894773332E-15, 7.121496375062676691E-15, -1.000000000000000000 ) ) ;
#60719=AXIS2_PLACEMENT_3D ( 'NONE', #691, #54485, #93029 ) ;
#60720=CARTESIAN_POINT ( 'NONE',  ( -10.54059822343757702, -6.376774720514426953, 17.17691942396159988 ) ) ;
#60724=VERTEX_POINT ( 'NONE', #35370 ) ;
#60728=ORIENTED_EDGE ( 'NONE', *, *, #80950, .T. ) ;
#60737=CARTESIAN_POINT ( 'NONE',  ( -2.762050907158362989, -5.876774720514413630, 19.89644244529369033 ) ) ;
#60739=CARTESIAN_POINT ( 'NONE',  ( 26.25551457520355214, -500000.0000000000582, -10.59759736550658360 ) ) ;
#60741=CIRCLE ( 'NONE', #4025, 0.3000000000000016542 ) ;
#60747=FACE_OUTER_BOUND ( 'NONE', #13014, .T. ) ;
#60752=DIRECTION ( 'NONE',  ( -0.6451914333552656311, 0.000000000000000000, -0.7640209514960816239 ) ) ;
#60753=AXIS2_PLACEMENT_3D ( 'NONE', #44086, #19238, #11624 ) ;
#60761=CARTESIAN_POINT ( 'NONE',  ( 2.933277810221831761, -6.376774720514424288, 21.39432064584807947 ) ) ;
#60763=CARTESIAN_POINT ( 'NONE',  ( -28.98875734969026396, 5.965225279485572685, -0.08597719988137648983 ) ) ;
#60770=EDGE_CURVE ( 'NONE', #79708, #69943, #89151, .T. ) ;
#60794=ORIENTED_EDGE ( 'NONE', *, *, #51393, .T. ) ;
#60804=EDGE_LOOP ( 'NONE', ( #48936, #86069, #56182, #68039, #71953, #27516 ) ) ;
#60820=EDGE_CURVE ( 'NONE', #74863, #13066, #27255, .T. ) ;
#60823=CARTESIAN_POINT ( 'NONE',  ( 4.912344403463128728, -5.876774720514406525, 19.26008510998990886 ) ) ;
#60832=EDGE_CURVE ( 'NONE', #27382, #75557, #81543, .T. ) ;
#60834=DIRECTION ( 'NONE',  ( 0.000000000000000000, 0.000000000000000000, -1.000000000000000000 ) ) ;
#60841=LINE ( 'NONE', #91759, #89422 ) ;
#60848=CARTESIAN_POINT ( 'NONE',  ( -5.891025641025637860, -6.376774720514427841, 21.75000000000000711 ) ) ;
#60857=VECTOR ( 'NONE', #1990, 1000.000000000000000 ) ;
#60859=CARTESIAN_POINT ( 'NONE',  ( 1.305682803664691249, -0.3587747205144265483, 29.57950906855421991 ) ) ;
#60882=CARTESIAN_POINT ( 'NONE',  ( 33.41263754283357912, -3.496799131921995762, -12.47286811689047070 ) ) ;
#60888=EDGE_CURVE ( 'NONE', #57568, #9886, #93490, .T. ) ;
#60891=CARTESIAN_POINT ( 'NONE',  ( -1.030996059302438761, -5.876774720514415407, 20.06599527532949878 ) ) ;
#60896=ORIENTED_EDGE ( 'NONE', *, *, #26053, .T. ) ;
#60908=DIRECTION ( 'NONE',  ( -0.000000000000000000, 1.000000000000000000, -0.000000000000000000 ) ) ;
#60914=DIRECTION ( 'NONE',  ( 0.000000000000000000, 0.000000000000000000, -1.000000000000000000 ) ) ;
#60918=EDGE_CURVE ( 'NONE', #31713, #16621, #59424, .T. ) ;
#60919=DIRECTION ( 'NONE',  ( 0.000000000000000000, 0.000000000000000000, -1.000000000000000000 ) ) ;
#60927=ORIENTED_EDGE ( 'NONE', *, *, #8404, .T. ) ;
#60929=CARTESIAN_POINT ( 'NONE',  ( -4.537657931416015700, -5.876774720514410077, 19.25713806424188235 ) ) ;
#60930=CARTESIAN_POINT ( 'NONE',  ( 3.474198977381013798, -5.876774720514426065, 21.79108561604954986 ) ) ;
#60942=DIRECTION ( 'NONE',  ( 0.000000000000000000, 0.000000000000000000, 1.000000000000000000 ) ) ;
#60948=EDGE_CURVE ( 'NONE', #35163, #23209, #62199, .T. ) ;
#60953=ORIENTED_EDGE ( 'NONE', *, *, #92946, .T. ) ;
#60959=CARTESIAN_POINT ( 'NONE',  ( 6.881670032588234953, -3.316774720514422903, -27.26384557944684062 ) ) ;
#60966=AXIS2_PLACEMENT_3D ( 'NONE', #729, #63657, #9339 ) ;
#60972=CARTESIAN_POINT ( 'NONE',  ( 31.99559323149412648, -3.570691370340881576, -11.82294999027247862 ) ) ;
#60978=DIRECTION ( 'NONE',  ( 0.000000000000000000, 0.000000000000000000, 1.000000000000000000 ) ) ;
#60989=ORIENTED_EDGE ( 'NONE', *, *, #12416, .T. ) ;
#60993=EDGE_LOOP ( 'NONE', ( #46406, #55938, #11990, #95111 ) ) ;
#60996=CARTESIAN_POINT ( 'NONE',  ( -13.57581083383197296, -6.376774720514426953, 19.78786796564403616 ) ) ;
#60999=ADVANCED_FACE ( 'NONE', ( #93122 ), #96481, .F. ) ;
#61009=ADVANCED_FACE ( 'NONE', ( #31736 ), #7387, .T. ) ;
#61011=CARTESIAN_POINT ( 'NONE',  ( 6.672787727097600374, -5.349622116134226779, -25.44584804566076031 ) ) ;
#61018=EDGE_CURVE ( 'NONE', #71823, #54115, #39843, .T. ) ;
#61020=VECTOR ( 'NONE', #62305, 1000.000000000000000 ) ;
#61022=VECTOR ( 'NONE', #87377, 1000.000000000000000 ) ;
#61037=DIRECTION ( 'NONE',  ( -0.000000000000000000, 1.000000000000000000, -0.000000000000000000 ) ) ;
#61044=EDGE_LOOP ( 'NONE', ( #26646, #740, #56940, #24947 ) ) ;
#61070=ORIENTED_EDGE ( 'NONE', *, *, #44163, .F. ) ;
#61074=LINE ( 'NONE', #52959, #31681 ) ;
#61079=CARTESIAN_POINT ( 'NONE',  ( 7.477175500793984853, -5.876774720514417183, 20.66439772633092176 ) ) ;
#61081=CARTESIAN_POINT ( 'NONE',  ( -0.9257915630711897048, -6.376774720514408301, 19.25892998154168012 ) ) ;
#61095=CARTESIAN_POINT ( 'NONE',  ( 22.33191539159863481, -4.132774720514426292, -16.26852658953813346 ) ) ;
#61104=DIRECTION ( 'NONE',  ( -0.000000000000000000, -1.000000000000000000, -0.000000000000000000 ) ) ;
#61108=CARTESIAN_POINT ( 'NONE',  ( 32.53135143123563466, 5.965225279485572685, 6.926385399448451885 ) ) ;
#61117=LINE ( 'NONE', #43890, #56958 ) ;
#61122=DIRECTION ( 'NONE',  ( -0.000000000000000000, -1.000000000000000000, -0.000000000000000000 ) ) ;
#61129=DIRECTION ( 'NONE',  ( -2.439088438507244272E-15, -0.000000000000000000, -1.000000000000000000 ) ) ;
#61130=B_SPLINE_CURVE_WITH_KNOTS ( 'NONE', 3,
 ( #4184, #43250, #42269, #66107, #65604, #27017 ),
 .UNSPECIFIED., .F., .F.,
 ( 4, 2, 4 ),
 ( 1.437692738331097786, 1.447547036373233009, 1.457401334415368233 ),
 .UNSPECIFIED. ) ;
#61154=EDGE_CURVE ( 'NONE', #59202, #14898, #67199, .T. ) ;
#61157=CARTESIAN_POINT ( 'NONE',  ( 9.278253834636469577, -5.876774720514426953, 18.51871304725684553 ) ) ;
#61159=CIRCLE ( 'NONE', #20570, 2.999999999999999112 ) ;
#61162=CARTESIAN_POINT ( 'NONE',  ( 0.3670296583442628213, -5.876774720514417183, 20.26087634804755311 ) ) ;
#61178=EDGE_LOOP ( 'NONE', ( #84234, #76070, #63226, #15366 ) ) ;
#61187=EDGE_CURVE ( 'NONE', #29990, #19469, #35170, .T. ) ;
#61189=CARTESIAN_POINT ( 'NONE',  ( -3.108974358974359475, -5.876774720514416295, 20.36458333333334281 ) ) ;
#61191=DIRECTION ( 'NONE',  ( -1.895872651340772790E-16, 0.000000000000000000, -1.000000000000000000 ) ) ;
#61201=CARTESIAN_POINT ( 'NONE',  ( 4.518205171808153509, -6.376774720514406525, 19.05004583296150500 ) ) ;
#61216=CARTESIAN_POINT ( 'NONE',  ( 31.79364159983995464, 6.475225279485573360, -11.59305536555894278 ) ) ;
#61218=AXIS2_PLACEMENT_3D ( 'NONE', #94124, #2801, #64719 ) ;
#61227=PLANE ( 'NONE',  #9847 ) ;
#61240=CARTESIAN_POINT ( 'NONE',  ( -2.283364382221138467, -5.876774720514410077, 19.46427715384223944 ) ) ;
#61242=FACE_OUTER_BOUND ( 'NONE', #9141, .T. ) ;
#61247=DIRECTION ( 'NONE',  ( -0.000000000000000000, 1.000000000000000000, -0.000000000000000000 ) ) ;
#61250=AXIS2_PLACEMENT_3D ( 'NONE', #70570, #8173, #77165 ) ;
#61251=CARTESIAN_POINT ( 'NONE',  ( 4.966983519792414370, -5.876774720514415407, 19.83633487160803099 ) ) ;
#61252=CARTESIAN_POINT ( 'NONE',  ( 30.73873608389078527, 2.297196155479665158, 24.67598410064776715 ) ) ;
#61265=CARTESIAN_POINT ( 'NONE',  ( 3.474198977381013798, -5.876774720514426065, 21.79108561604954986 ) ) ;
#61269=LINE ( 'NONE', #60271, #41635 ) ;
#61284=CARTESIAN_POINT ( 'NONE',  ( -5.837039262820512775, -6.376774720514413630, 19.76512419871795245 ) ) ;
#61293=DIRECTION ( 'NONE',  ( 0.000000000000000000, -1.000000000000000000, 0.000000000000000000 ) ) ;
#61297=ORIENTED_EDGE ( 'NONE', *, *, #24930, .F. ) ;
#61306=LINE ( 'NONE', #67417, #85475 ) ;
#61323=ORIENTED_EDGE ( 'NONE', *, *, #46005, .F. ) ;
#61324=CARTESIAN_POINT ( 'NONE',  ( 3.797776442307698286, -5.876774720514399419, 18.16025641025640525 ) ) ;
#61328=CARTESIAN_POINT ( 'NONE',  ( -5.891025641025637860, -6.376774720514427841, 21.75000000000000711 ) ) ;
#61331=DIRECTION ( 'NONE',  ( 6.267148949376394486E-16, -1.000000000000000000, -5.583826031377232793E-16 ) ) ;
#61332=DIRECTION ( 'NONE',  ( -0.000000000000000000, 1.000000000000000000, -0.000000000000000000 ) ) ;
#61338=EDGE_CURVE ( 'NONE', #71272, #32855, #54701, .T. ) ;
#61341=EDGE_LOOP ( 'NONE', ( #18346, #89536, #11485, #39957 ) ) ;
#61347=CARTESIAN_POINT ( 'NONE',  ( 31.60706529141452137, -4.540774720514427543, 26.12024523944105070 ) ) ;
#61367=CARTESIAN_POINT ( 'NONE',  ( 32.73857899460458754, 5.965225279485572685, -13.20677013500358399 ) ) ;
#61372=CARTESIAN_POINT ( 'NONE',  ( 15.22086173316507285, -2.682774720514426559, -27.22822144916453624 ) ) ;
#61390=PLANE ( 'NONE',  #39576 ) ;
#61414=DIRECTION ( 'NONE',  ( -0.000000000000000000, 1.000000000000000000, -0.000000000000000000 ) ) ;
#61422=ORIENTED_EDGE ( 'NONE', *, *, #61754, .F. ) ;
#61443=CARTESIAN_POINT ( 'NONE',  ( -25.92875734969025814, -6.376774720514426953, 30.51402280011862089 ) ) ;
#61447=ORIENTED_EDGE ( 'NONE', *, *, #14033, .F. ) ;
#61448=AXIS2_PLACEMENT_3D ( 'NONE', #31809, #38915, #8468 ) ;
#61456=AXIS2_PLACEMENT_3D ( 'NONE', #45563, #53177, #99326 ) ;
#61458=CARTESIAN_POINT ( 'NONE',  ( 10.01577673925062584, -3.316774720514425567, -27.02510548822787584 ) ) ;
#61461=ORIENTED_EDGE ( 'NONE', *, *, #75003, .T. ) ;
#61485=VERTEX_POINT ( 'NONE', #28490 ) ;
#61494=EDGE_CURVE ( 'NONE', #13745, #5619, #21365, .T. ) ;
#61499=CARTESIAN_POINT ( 'NONE',  ( 32.45853543194704116, -0.3587747205144265483, 9.169203677920338080 ) ) ;
#61500=DIRECTION ( 'NONE',  ( -0.000000000000000000, 0.000000000000000000, -1.000000000000000000 ) ) ;
#61502=CIRCLE ( 'NONE', #59912, 251.4258649670780699 ) ;
#61503=LINE ( 'NONE', #54891, #31118 ) ;
#61507=ADVANCED_FACE ( 'NONE', ( #90890 ), #67572, .F. ) ;
#61520=CARTESIAN_POINT ( 'NONE',  ( -1.140932434931746582E-13, -5.876774720514426953, 21.78128695274321203 ) ) ;
#61521=CARTESIAN_POINT ( 'NONE',  ( -1.649669150391666506, -5.876774720514411854, 19.67464842890028365 ) ) ;
#61527=( BOUNDED_SURFACE ( )  B_SPLINE_SURFACE ( 3, 2, ( 
 ( #64863, #98131, #66730 ),
 ( #21501, #5295, #87670 ),
 ( #33880, #44871, #51981 ),
 ( #64359, #95777, #95280 ),
 ( #82909, #90528, #82416 ),
 ( #18151, #36254, #5795 ),
 ( #97641, #29128, #28638 ),
 ( #49124, #88173, #75297 ),
 ( #28144, #20509, #52478 ),
 ( #60105, #67717, #51480 ),
 ( #2945, #13894, #91029 ),
 ( #36749, #80051, #57240 ) ),
 .UNSPECIFIED., .F., .F., .T. ) 
 B_SPLINE_SURFACE_WITH_KNOTS ( ( 4, 2, 2, 2, 2, 4 ),
 ( 3, 3 ),
 ( 5.963111948670274387E-19, 0.0004805055694112242209, 0.0007207583541168360603, 0.0009610111388224478997, 0.001441516708233671470, 0.001922022277644895149 ),
 ( 0.000000000000000000, 1.000000000000000000 ),
 .UNSPECIFIED. ) 
 GEOMETRIC_REPRESENTATION_ITEM ( )  RATIONAL_B_SPLINE_SURFACE ( (
 ( 1.000000000000000000, 0.6532382444175209857, 1.000000000000000000),
 ( 1.000000000000000000, 0.6532227097440629349, 1.000000000000000000),
 ( 1.000000000000000000, 0.6547852517831300734, 1.000000000000000000),
 ( 1.000000000000000000, 0.6591574828660964336, 1.000000000000000000),
 ( 1.000000000000000000, 0.6609310395923762016, 1.000000000000000000),
 ( 1.000000000000000000, 0.6650742797340818413, 1.000000000000000000),
 ( 1.000000000000000000, 0.6674600455423553846, 1.000000000000000000),
 ( 1.000000000000000000, 0.6751670852230186037, 1.000000000000000000),
 ( 1.000000000000000000, 0.6812390391297645786, 1.000000000000000000),
 ( 1.000000000000000000, 0.6938890553660238547, 1.000000000000000000),
 ( 1.000000000000000000, 0.7006220437376451393, 1.000000000000000000),
 ( 1.000000000000000000, 0.7071067811865475727, 1.000000000000000000) ) ) 
 REPRESENTATION_ITEM ( '' )  SURFACE ( )  );
#61530=DIRECTION ( 'NONE',  ( 2.168404344971008868E-16, 0.000000000000000000, 1.000000000000000000 ) ) ;
#61531=FACE_OUTER_BOUND ( 'NONE', #156, .T. ) ;
#61532=ORIENTED_EDGE ( 'NONE', *, *, #96745, .T. ) ;
#61542=ORIENTED_EDGE ( 'NONE', *, *, #44720, .T. ) ;
#61546=B_SPLINE_SURFACE_WITH_KNOTS ( 'NONE', 3, 1, ( 
 ( #14977, #70775 ),
 ( #100190, #24586 ),
 ( #53570, #30710 ),
 ( #38815, #46939 ),
 ( #55560, #15475 ),
 ( #39817, #23075 ),
 ( #8371, #86494 ),
 ( #1272, #47943 ),
 ( #55058, #54550 ),
 ( #84495, #45950 ),
 ( #76861, #39316 ),
 ( #757, #69780 ),
 ( #85488, #54066 ),
 ( #84990, #46436 ),
 ( #77368, #31201 ),
 ( #62174, #31710 ),
 ( #62677, #18977 ),
 ( #10369, #65191 ),
 ( #88502, #33206 ) ),
 .UNSPECIFIED., .F., .F., .F.,
 ( 4, 1, 1, 1, 1, 1, 1, 1, 1, 1, 1, 1, 1, 1, 1, 1, 4 ),
 ( 2, 2 ),
 ( 0.000000000000000000, 0.06976287284686377710, 0.1345149942976650026, 0.1951193525406911267, 0.2509143402908639020, 0.3026968495153159466, 0.3502960464810119801, 0.3933858467586653918, 0.4329734110072621656, 0.5070892430766293923, 0.5787491638444322017, 0.6502280224451006951, 0.7224618180302712078, 0.7938856428547002020, 0.8631290414909040809, 0.9313229315869653302, 1.000000000000000000 ),
 ( 0.000000000000000000, 1.000000000000000000 ),
 .UNSPECIFIED. ) ;
#61553=CARTESIAN_POINT ( 'NONE',  ( 0.3670296583442628213, -6.376774720514417183, 20.26087634804755311 ) ) ;
#61558=CARTESIAN_POINT ( 'NONE',  ( 3.552794897967157528, -5.876774720514401196, 18.18650940196788568 ) ) ;
#61561=DIRECTION ( 'NONE',  ( 0.000000000000000000, 0.000000000000000000, -1.000000000000000000 ) ) ;
#61562=DIRECTION ( 'NONE',  ( 1.000000000000000000, 0.000000000000000000, 0.000000000000000000 ) ) ;
#61576=CARTESIAN_POINT ( 'NONE',  ( 31.01539214510854237, -4.736880496761925130, -2.146553774717921304 ) ) ;
#61585=CARTESIAN_POINT ( 'NONE',  ( -1.064504969004270052, -6.376774720514408301, 19.35667676486395905 ) ) ;
#61586=ORIENTED_EDGE ( 'NONE', *, *, #44079, .T. ) ;
#61589=CARTESIAN_POINT ( 'NONE',  ( 15.63605935613269438, 6.475225279485573360, -27.55169773172585934 ) ) ;
#61598=AXIS2_PLACEMENT_3D ( 'NONE', #91698, #35928, #53165 ) ;
#61599=FACE_OUTER_BOUND ( 'NONE', #87192, .T. ) ;
#61628=CARTESIAN_POINT ( 'NONE',  ( 4.647438682898014761, -6.376774720514417183, 20.26932200457894950 ) ) ;
#61643=AXIS2_PLACEMENT_3D ( 'NONE', #14478, #55057, #69274 ) ;
#61647=ORIENTED_EDGE ( 'NONE', *, *, #22981, .T. ) ;
#61648=LINE ( 'NONE', #83965, #33308 ) ;
#61653=ORIENTED_EDGE ( 'NONE', *, *, #60918, .T. ) ;
#61655=CARTESIAN_POINT ( 'NONE',  ( -0.1037292527911751056, -5.876774720514413630, 19.53657742262743824 ) ) ;
#61672=CARTESIAN_POINT ( 'NONE',  ( 4.967948717948723392, -6.376774720514415407, 20.00140224358974095 ) ) ;
#61684=CARTESIAN_POINT ( 'NONE',  ( 9.150000000000007461, -6.376774720514426953, 11.88602120139451834 ) ) ;
#61687=LINE ( 'NONE', #37834, #35130 ) ;
#61717=FACE_OUTER_BOUND ( 'NONE', #78444, .T. ) ;
#61727=EDGE_LOOP ( 'NONE', ( #82917, #65744, #31806, #83585 ) ) ;
#61733=CARTESIAN_POINT ( 'NONE',  ( 14.76093561896379214, -3.316774720514426456, -26.55548769130089681 ) ) ;
#61736=CARTESIAN_POINT ( 'NONE',  ( -5.205649524681222218, -5.876774720514407413, 19.16400979764067714 ) ) ;
#61737=AXIS2_PLACEMENT_3D ( 'NONE', #86755, #1024, #40597 ) ;
#61739=CARTESIAN_POINT ( 'NONE',  ( -2.599001758237162285, -5.876774720514411854, 19.60308799987317485 ) ) ;
#61741=CARTESIAN_POINT ( 'NONE',  ( -15.54901181048698255, -6.376774720514426953, -55.62515100798455592 ) ) ;
#61746=DIRECTION ( 'NONE',  ( 0.1254312216594016816, 0.000000000000000000, 0.9921023176230514551 ) ) ;
#61750=CARTESIAN_POINT ( 'NONE',  ( 4.588387839717440464, -5.876774720514402084, 18.52756237589653665 ) ) ;
#61751=CARTESIAN_POINT ( 'NONE',  ( -24.57525087998974200, -0.3587747205143967943, -15.45548830044932664 ) ) ;
#61752=ORIENTED_EDGE ( 'NONE', *, *, #11539, .T. ) ;
#61754=EDGE_CURVE ( 'NONE', #45760, #40197, #96801, .T. ) ;
#61778=CARTESIAN_POINT ( 'NONE',  ( -5.293508136514246232, -6.376774720514408301, 19.18727597066021318 ) ) ;
#61787=CARTESIAN_POINT ( 'NONE',  ( -5.457842845122470976, -5.876774720514410077, 19.25892998154168367 ) ) ;
#61788=CARTESIAN_POINT ( 'NONE',  ( -15.82668884360736961, 5.965225279485572685, 42.07822029717483758 ) ) ;
#61795=ORIENTED_EDGE ( 'NONE', *, *, #61964, .T. ) ;
#61804=VECTOR ( 'NONE', #67475, 1000.000000000000000 ) ;
#61811=( GEOMETRIC_REPRESENTATION_CONTEXT ( 3 ) GLOBAL_UNCERTAINTY_ASSIGNED_CONTEXT ( ( #98675 ) ) GLOBAL_UNIT_ASSIGNED_CONTEXT ( ( #84581, #46039, #76960 ) ) REPRESENTATION_CONTEXT ( 'NONE', 'WORKASPACE' ) );
#61818=DIRECTION ( 'NONE',  ( 1.000000000000000000, 0.000000000000000000, 0.000000000000000000 ) ) ;
#61821=CARTESIAN_POINT ( 'NONE',  ( 4.967948717948723392, -6.376774720514415407, 20.00140224358974095 ) ) ;
#61831=EDGE_CURVE ( 'NONE', #79185, #17321, #74128, .T. ) ;
#61855=DIRECTION ( 'NONE',  ( -0.000000000000000000, 1.000000000000000000, -0.000000000000000000 ) ) ;
#61862=DIRECTION ( 'NONE',  ( -0.06486421869277853025, 0.000000000000000000, 0.9978940991575085961 ) ) ;
#61870=CARTESIAN_POINT ( 'NONE',  ( -6.377963355984652694, -6.376774720514411854, 19.53740760792478426 ) ) ;
#61874=CARTESIAN_POINT ( 'NONE',  ( 9.150000000000000355, -5.876774720514426953, -15.70000000000000284 ) ) ;
#61880=VECTOR ( 'NONE', #5691, 1000.000000000000000 ) ;
#61881=ORIENTED_EDGE ( 'NONE', *, *, #52231, .T. ) ;
#61886=LINE ( 'NONE', #85201, #2734 ) ;
#61894=CARTESIAN_POINT ( 'NONE',  ( 15.58962545129234556, -1.684774720514426560, -26.91365498785467736 ) ) ;
#61913=EDGE_LOOP ( 'NONE', ( #70743, #85135, #20015, #45416, #14885, #62539, #43303, #95541 ) ) ;
#61919=VERTEX_POINT ( 'NONE', #82165 ) ;
#61921=AXIS2_PLACEMENT_3D ( 'NONE', #90327, #43171, #51776 ) ;
#61923=EDGE_LOOP ( 'NONE', ( #79378, #27213, #2628, #100319 ) ) ;
#61936=CARTESIAN_POINT ( 'NONE',  ( 25.17305609041493142, -5.157291146176350871, -8.664675380811843297 ) ) ;
#61942=LINE ( 'NONE', #7645, #89038 ) ;
#61943=VECTOR ( 'NONE', #5925, 1000.000000000000000 ) ;
#61944=CARTESIAN_POINT ( 'NONE',  ( 13.91401389203221406, -0.3587747205144265483, 158.0376437107427137 ) ) ;
#61949=ORIENTED_EDGE ( 'NONE', *, *, #57042, .T. ) ;
#61964=EDGE_CURVE ( 'NONE', #39283, #99333, #31374, .T. ) ;
#61965=CARTESIAN_POINT ( 'NONE',  ( 31.68084058116295409, -4.801908866063379300, 29.09855526763849198 ) ) ;
#61981=CARTESIAN_POINT ( 'NONE',  ( -4.568292318365942073, 5.965225279485572685, 30.06720597538392425 ) ) ;
#61984=FACE_OUTER_BOUND ( 'NONE', #33608, .T. ) ;
#61987=ORIENTED_EDGE ( 'NONE', *, *, #22477, .T. ) ;
#61992=ORIENTED_EDGE ( 'NONE', *, *, #33925, .F. ) ;
#61996=CARTESIAN_POINT ( 'NONE',  ( 31.74473449900405697, -4.976825198871215328, -4.259190951192157293 ) ) ;
#61997=CARTESIAN_POINT ( 'NONE',  ( 5.635247460261607166, -6.376774720514424288, 21.53093896358932469 ) ) ;
#61999=CARTESIAN_POINT ( 'NONE',  ( 3.787259615384621636, -6.376774720514404748, 18.51923076923076650 ) ) ;
#62015=EDGE_CURVE ( 'NONE', #7626, #40793, #68441, .T. ) ;
#62016=CARTESIAN_POINT ( 'NONE',  ( 0.03625801282051022839, -5.876774720514410077, 19.27714342948718240 ) ) ;
#62017=ORIENTED_EDGE ( 'NONE', *, *, #45259, .T. ) ;
#62026=CARTESIAN_POINT ( 'NONE',  ( -28.98875734969026396, 5.965225279485572685, 10.11402280011862587 ) ) ;
#62038=DIRECTION ( 'NONE',  ( 0.000000000000000000, -1.000000000000000000, 0.000000000000000000 ) ) ;
#62044=CARTESIAN_POINT ( 'NONE',  ( 13.91401389203221406, 5.965225279485572685, 158.0376437107427137 ) ) ;
#62045=CARTESIAN_POINT ( 'NONE',  ( 10.24059822343757808, -5.876774720514426953, 22.08128695274315945 ) ) ;
#62065=ORIENTED_EDGE ( 'NONE', *, *, #80875, .T. ) ;
#62073=CARTESIAN_POINT ( 'NONE',  ( -6.818021687177533430, -6.376774720514408301, 19.14905311829361167 ) ) ;
#62081=EDGE_CURVE ( 'NONE', #40266, #37899, #93521, .T. ) ;
#62087=ORIENTED_EDGE ( 'NONE', *, *, #82760, .T. ) ;
#62105=CARTESIAN_POINT ( 'NONE',  ( 3.632744579681756569, -6.376774720514402972, 18.17103827887095946 ) ) ;
#62111=CARTESIAN_POINT ( 'NONE',  ( 282.9764569301858046, -0.3587747205144265483, 20.79159422840526616 ) ) ;
#62112=VERTEX_POINT ( 'NONE', #22242 ) ;
#62116=DIRECTION ( 'NONE',  ( -0.8264557562326033668, 6.845827386180409975E-16, -0.5630016722799281448 ) ) ;
#62127=AXIS2_PLACEMENT_3D ( 'NONE', #87913, #93503, #48356 ) ;
#62130=CARTESIAN_POINT ( 'NONE',  ( 0.3906119451836247425, -5.876774720514418071, 20.56083401959467594 ) ) ;
#62148=ORIENTED_EDGE ( 'NONE', *, *, #22363, .F. ) ;
#62151=VECTOR ( 'NONE', #28017, 1000.000000000000000 ) ;
#62159=EDGE_CURVE ( 'NONE', #96649, #34238, #58592, .T. ) ;
#62162=DIRECTION ( 'NONE',  ( -0.000000000000000000, 1.000000000000000000, -0.000000000000000000 ) ) ;
#62165=CARTESIAN_POINT ( 'NONE',  ( 3.825381322105384285, -6.376774720514401196, 18.16071977647550995 ) ) ;
#62167=VERTEX_POINT ( 'NONE', #79042 ) ;
#62168=FACE_OUTER_BOUND ( 'NONE', #6402, .T. ) ;
#62171=ORIENTED_EDGE ( 'NONE', *, *, #85339, .F. ) ;
#62174=CARTESIAN_POINT ( 'NONE',  ( -4.743266218460161276, -6.376774720514413630, 19.49357334786887108 ) ) ;
#62180=DIRECTION ( 'NONE',  ( -1.000000000000000000, 0.000000000000000000, 1.895872651340772790E-16 ) ) ;
#62186=FACE_OUTER_BOUND ( 'NONE', #100212, .T. ) ;
#62190=CARTESIAN_POINT ( 'NONE',  ( 3.825970207471427020, -6.376774720514402972, 18.52126221587801780 ) ) ;
#62191=EDGE_CURVE ( 'NONE', #73552, #81441, #97152, .T. ) ;
#62199=LINE ( 'NONE', #92625, #72408 ) ;
#62202=CARTESIAN_POINT ( 'NONE',  ( -27.96875734969026084, -6.376774720514426953, -0.08597719988137648983 ) ) ;
#62205=DIRECTION ( 'NONE',  ( 0.000000000000000000, 1.000000000000000000, 0.000000000000000000 ) ) ;
#62207=ORIENTED_EDGE ( 'NONE', *, *, #59500, .T. ) ;
#62210=ADVANCED_FACE ( 'NONE', ( #89539 ), #55235, .T. ) ;
#62212=EDGE_LOOP ( 'NONE', ( #7028, #2055, #3510, #39180 ) ) ;
#62213=VECTOR ( 'NONE', #97226, 1000.000000000000114 ) ;
#62214=VERTEX_POINT ( 'NONE', #930 ) ;
#62220=FACE_OUTER_BOUND ( 'NONE', #27346, .T. ) ;
#62236=DIRECTION ( 'NONE',  ( 0.000000000000000000, -1.000000000000000000, 0.000000000000000000 ) ) ;
#62241=CARTESIAN_POINT ( 'NONE',  ( -2.794644232660540961, -5.876774720514416295, 20.26757654895259009 ) ) ;
#62244=DIRECTION ( 'NONE',  ( 0.000000000000000000, -1.000000000000000000, 0.000000000000000000 ) ) ;
#62245=CARTESIAN_POINT ( 'NONE',  ( 4.190829928318763109, -5.876774720514402084, 18.23548058298382557 ) ) ;
#62257=CARTESIAN_POINT ( 'NONE',  ( 13.91401389203221406, -3.316774720514426456, 158.0376437107427137 ) ) ;
#62267=EDGE_CURVE ( 'NONE', #57214, #15127, #37250, .T. ) ;
#62268=FACE_OUTER_BOUND ( 'NONE', #86009, .T. ) ;
#62277=AXIS2_PLACEMENT_3D ( 'NONE', #79241, #71647, #16343 ) ;
#62286=CARTESIAN_POINT ( 'NONE',  ( -5.293508136514246232, -6.376774720514410077, 19.18727597066021318 ) ) ;
#62288=DIRECTION ( 'NONE',  ( 0.000000000000000000, 0.000000000000000000, 1.000000000000000000 ) ) ;
#62290=DIRECTION ( 'NONE',  ( -0.1254312216594016538, 0.000000000000000000, -0.9921023176230513441 ) ) ;
#62305=DIRECTION ( 'NONE',  ( 0.000000000000000000, 1.000000000000000000, 0.000000000000000000 ) ) ;
#62310=CIRCLE ( 'NONE', #12085, 251.4258649670780699 ) ;
#62313=ORIENTED_EDGE ( 'NONE', *, *, #63667, .F. ) ;
#62314=CARTESIAN_POINT ( 'NONE',  ( -27.96875734969026084, 6.143225279485574397, 23.50402280011861933 ) ) ;
#62318=PLANE ( 'NONE',  #55069 ) ;
#62331=CARTESIAN_POINT ( 'NONE',  ( 14.76093561896379214, 5.965225279485572685, -26.55548769130089681 ) ) ;
#62336=EDGE_LOOP ( 'NONE', ( #9758, #97956 ) ) ;
#62354=CARTESIAN_POINT ( 'NONE',  ( -53.01255352321339842, 1.477225279485574028, 35.59556822165056644 ) ) ;
#62369=CARTESIAN_POINT ( 'NONE',  ( 6.420673076923079314, -6.376774720514427841, 21.83974358974358765 ) ) ;
#62374=AXIS2_PLACEMENT_3D ( 'NONE', #51634, #88702, #97796 ) ;
#62378=CARTESIAN_POINT ( 'NONE',  ( 12.16765770914787304, 6.475225279485573360, -27.57618308014988173 ) ) ;
#62385=CARTESIAN_POINT ( 'NONE',  ( -0.9827876235267493099, -6.376774720514415407, 19.81240905262004404 ) ) ;
#62396=EDGE_CURVE ( 'NONE', #63282, #42731, #12896, .T. ) ;
#62399=ADVANCED_FACE ( 'NONE', ( #67217 ), #45372, .F. ) ;
#62401=VECTOR ( 'NONE', #83333, 1000.000000000000000 ) ;
#62403=CARTESIAN_POINT ( 'NONE',  ( -4.141025641025642301, -6.376774720514408301, 19.19230769230769695 ) ) ;
#62418=DIRECTION ( 'NONE',  ( -0.000000000000000000, 1.000000000000000000, -0.000000000000000000 ) ) ;
#62426=CARTESIAN_POINT ( 'NONE',  ( -4.977357939505175466, -5.876774720514410077, 19.14913681718893557 ) ) ;
#62441=CARTESIAN_POINT ( 'NONE',  ( 4.966987340572156739, -5.876774720514418071, 20.16530235339958210 ) ) ;
#62454=CARTESIAN_POINT ( 'NONE',  ( 2.904244945035652670, -6.376774720514415407, 20.04207437776001299 ) ) ;
#62459=DIRECTION ( 'NONE',  ( 0.000000000000000000, 0.000000000000000000, -1.000000000000000000 ) ) ;
#62461=CARTESIAN_POINT ( 'NONE',  ( 31.62551770808318707, -4.240436435409185911, 26.92952082091879973 ) ) ;
#62468=FACE_OUTER_BOUND ( 'NONE', #70214, .T. ) ;
#62469=CARTESIAN_POINT ( 'NONE',  ( -5.544977400725785266, -5.876774720514411854, 19.92818918856636401 ) ) ;
#62474=ORIENTED_EDGE ( 'NONE', *, *, #34992, .T. ) ;
#62476=CARTESIAN_POINT ( 'NONE',  ( 2.993365552154886089, -6.376774720514413630, 19.24059921568563425 ) ) ;
#62478=CARTESIAN_POINT ( 'NONE',  ( -9.150000000000000355, -5.876774720514426953, -15.69999999999999929 ) ) ;
#62482=CIRCLE ( 'NONE', #2515, 8.452410033082758289 ) ;
#62486=VECTOR ( 'NONE', #21333, 1000.000000000000000 ) ;
#62487=LINE ( 'NONE', #39636, #73976 ) ;
#62492=ORIENTED_EDGE ( 'NONE', *, *, #12453, .T. ) ;
#62495=DIRECTION ( 'NONE',  ( 0.000000000000000000, 0.000000000000000000, -1.000000000000000000 ) ) ;
#62497=CARTESIAN_POINT ( 'NONE',  ( 6.132272708306365949, -6.376774720514424288, 21.80683391321003839 ) ) ;
#62506=CARTESIAN_POINT ( 'NONE',  ( 22.02124265030973760, 6.143225279485574397, 13.95402280011862395 ) ) ;
#62509=EDGE_CURVE ( 'NONE', #35033, #96004, #24006, .T. ) ;
#62516=CARTESIAN_POINT ( 'NONE',  ( 5.464387484610083057, -6.376774720514420736, 21.31215092858952431 ) ) ;
#62517=ORIENTED_EDGE ( 'NONE', *, *, #63921, .F. ) ;
#62523=CARTESIAN_POINT ( 'NONE',  ( -65.05438548721848235, 6.143225279485573509, 29.49402280011861777 ) ) ;
#62535=CARTESIAN_POINT ( 'NONE',  ( -6.185411026474866958, -6.376774720514411854, 19.34586827028016742 ) ) ;
#62536=LINE ( 'NONE', #86368, #63188 ) ;
#62539=ORIENTED_EDGE ( 'NONE', *, *, #15491, .F. ) ;
#62551=CARTESIAN_POINT ( 'NONE',  ( 2.790451961050095520, -5.876774720514409189, 18.85195250256714417 ) ) ;
#62558=FACE_OUTER_BOUND ( 'NONE', #27871, .T. ) ;
#62572=CARTESIAN_POINT ( 'NONE',  ( 7.267403311989051318, -6.376774720514426065, 21.43157132964656952 ) ) ;
#62575=CARTESIAN_POINT ( 'NONE',  ( 6.555906488453394410, -6.376774720514426065, 21.46941147007026274 ) ) ;
#62576=ORIENTED_EDGE ( 'NONE', *, *, #19409, .T. ) ;
#62584=DIRECTION ( 'NONE',  ( -1.000000000000000000, 0.000000000000000000, -2.338552693767719605E-15 ) ) ;
#62595=CARTESIAN_POINT ( 'NONE',  ( -20.27875734969026311, -5.356774720514425603, 24.00402280011862288 ) ) ;
#62596=ADVANCED_FACE ( 'NONE', ( #3200 ), #48868, .F. ) ;
#62599=LINE ( 'NONE', #93525, #26373 ) ;
#62601=DIRECTION ( 'NONE',  ( 0.000000000000000000, 0.000000000000000000, -1.000000000000000000 ) ) ;
#62615=CIRCLE ( 'NONE', #57771, 129.7684398600581517 ) ;
#62619=CARTESIAN_POINT ( 'NONE',  ( -20.27875734969026311, -4.776774720514394446, 25.40402280011861080 ) ) ;
#62643=CARTESIAN_POINT ( 'NONE',  ( -4.993225604111835914, 5.965225279485592225, -29.11654937215278593 ) ) ;
#62657=EDGE_CURVE ( 'NONE', #26067, #86027, #65607, .T. ) ;
#62665=CARTESIAN_POINT ( 'NONE',  ( -4.141025641025642301, -6.376774720514408301, 19.19230769230769695 ) ) ;
#62667=VERTEX_POINT ( 'NONE', #27021 ) ;
#62669=CARTESIAN_POINT ( 'NONE',  ( 3.036358173076929123, -6.376774720514420736, 20.87990785256409865 ) ) ;
#62671=CARTESIAN_POINT ( 'NONE',  ( 2.790451961050095520, -6.376774720514408301, 18.85195250256714417 ) ) ;
#62674=ORIENTED_EDGE ( 'NONE', *, *, #92973, .F. ) ;
#62677=CARTESIAN_POINT ( 'NONE',  ( -4.854568188115255367, -6.376774720514410077, 19.46611907402017394 ) ) ;
#62686=CARTESIAN_POINT ( 'NONE',  ( -1.409217194013772101, -5.876774720514418071, 20.11414146978959749 ) ) ;
#62689=DIRECTION ( 'NONE',  ( -0.000000000000000000, 1.000000000000000000, -0.000000000000000000 ) ) ;
#62693=CARTESIAN_POINT ( 'NONE',  ( -0.4909855769230799249, -6.376774720514410077, 19.14743589743590491 ) ) ;
#62694=VERTEX_POINT ( 'NONE', #9790 ) ;
#62696=ORIENTED_EDGE ( 'NONE', *, *, #36745, .F. ) ;
#62702=CARTESIAN_POINT ( 'NONE',  ( -28.84663072490566194, 5.965225279485572685, 28.73989617533406715 ) ) ;
#62703=CARTESIAN_POINT ( 'NONE',  ( 9.464509667910858681, -5.356774720513593380, -27.03659963401723942 ) ) ;
#62705=LINE ( 'NONE', #84519, #25879 ) ;
#62707=DIRECTION ( 'NONE',  ( -0.000000000000000000, 1.000000000000000000, -0.000000000000000000 ) ) ;
#62719=DIRECTION ( 'NONE',  ( -0.000000000000000000, 1.000000000000000000, -0.000000000000000000 ) ) ;
#62724=CARTESIAN_POINT ( 'NONE',  ( 14.70320764097976074, -3.414808732104013256, -28.39448918867740446 ) ) ;
#62729=CARTESIAN_POINT ( 'NONE',  ( -4.141025641025642301, -5.876774720514411854, 19.63681891025641235 ) ) ;
#62735=EDGE_CURVE ( 'NONE', #3834, #97929, #17908, .T. ) ;
#62760=DIRECTION ( 'NONE',  ( 0.000000000000000000, 1.000000000000000000, 0.000000000000000000 ) ) ;
#62762=AXIS2_PLACEMENT_3D ( 'NONE', #15654, #46623, #431 ) ;
#62767=DIRECTION ( 'NONE',  ( 0.4725087886537609472, -0.000000000000000000, 0.8813259582271223413 ) ) ;
#62770=CARTESIAN_POINT ( 'NONE',  ( 25.61870917940689196, 5.965225279485572685, 29.49402280011862487 ) ) ;
#62783=CARTESIAN_POINT ( 'NONE',  ( -2.794644232660540961, -6.376774720514415407, 20.26757654895259009 ) ) ;
#62801=CARTESIAN_POINT ( 'NONE',  ( 30.53060340732036337, -4.132774720517318201, 3.744237563515920634E-15 ) ) ;
#62802=LINE ( 'NONE', #93716, #97077 ) ;
#62803=ORIENTED_EDGE ( 'NONE', *, *, #67515, .F. ) ;
#62814=CYLINDRICAL_SURFACE ( 'NONE', #42874, 2.040000000000000036 ) ;
#62831=EDGE_LOOP ( 'NONE', ( #89534, #55301, #47962, #62313 ) ) ;
#62837=CARTESIAN_POINT ( 'NONE',  ( -29.49875734969026198, 5.965225279485572685, 10.11402280011862587 ) ) ;
#62839=AXIS2_PLACEMENT_3D ( 'NONE', #69075, #34763, #60978 ) ;
#62844=ORIENTED_EDGE ( 'NONE', *, *, #30239, .F. ) ;
#62848=DIRECTION ( 'NONE',  ( -0.000000000000000000, -1.000000000000000000, -0.000000000000000000 ) ) ;
#62851=CARTESIAN_POINT ( 'NONE',  ( 27.53860345374771867, 1.477225279485574028, -9.482392034746242260 ) ) ;
#62859=EDGE_CURVE ( 'NONE', #25204, #94122, #32008, .T. ) ;
#62862=EDGE_LOOP ( 'NONE', ( #80147, #40194, #87340, #23285 ) ) ;
#62874=CYLINDRICAL_SURFACE ( 'NONE', #16814, 2.249999999999998668 ) ;
#62876=EDGE_CURVE ( 'NONE', #5494, #47230, #87164, .T. ) ;
#62878=FACE_OUTER_BOUND ( 'NONE', #85878, .T. ) ;
#62888=AXIS2_PLACEMENT_3D ( 'NONE', #54595, #62719, #7908 ) ;
#62901=CARTESIAN_POINT ( 'NONE',  ( -1.030996059302438761, -6.376774720514415407, 20.06599527532949878 ) ) ;
#62910=ORIENTED_EDGE ( 'NONE', *, *, #96853, .F. ) ;
#62920=VECTOR ( 'NONE', #84996, 1000.000000000000000 ) ;
#62922=ORIENTED_EDGE ( 'NONE', *, *, #88205, .F. ) ;
#62926=ORIENTED_EDGE ( 'NONE', *, *, #78757, .T. ) ;
#62929=LINE ( 'NONE', #80133, #48062 ) ;
#62930=VECTOR ( 'NONE', #56405, 1000.000000000000000 ) ;
#62937=FACE_OUTER_BOUND ( 'NONE', #43844, .T. ) ;
#62968=EDGE_LOOP ( 'NONE', ( #16442, #57561, #49329, #75261 ) ) ;
#62969=CARTESIAN_POINT ( 'NONE',  ( -15.82668884360736961, -1.684774720514424118, 42.07822029717483758 ) ) ;
#62974=VECTOR ( 'NONE', #53149, 1000.000000000000000 ) ;
#62976=CARTESIAN_POINT ( 'NONE',  ( 31.63505726983280297, -3.634951944882593988, 27.30823744647568674 ) ) ;
#62985=CARTESIAN_POINT ( 'NONE',  ( -5.576923076923076650, -5.876774720514418071, 20.44941907051282470 ) ) ;
#62998=DIRECTION ( 'NONE',  ( -0.000000000000000000, 1.000000000000000000, -0.000000000000000000 ) ) ;
#63002=CIRCLE ( 'NONE', #50034, 2.039999999999998703 ) ;
#63017=CARTESIAN_POINT ( 'NONE',  ( -5.023036858974361252, -5.876774720514410077, 19.14743589743590846 ) ) ;
#63026=CARTESIAN_POINT ( 'NONE',  ( -3.085512303079157359, -5.876774720514415407, 19.95084900476495093 ) ) ;
#63034=VECTOR ( 'NONE', #42971, 1000.000000000000000 ) ;
#63049=PLANE ( 'NONE',  #3224 ) ;
#63051=ORIENTED_EDGE ( 'NONE', *, *, #11070, .F. ) ;
#63059=VERTEX_POINT ( 'NONE', #48754 ) ;
#63072=PLANE ( 'NONE',  #11436 ) ;
#63083=VERTEX_POINT ( 'NONE', #34017 ) ;
#63085=CARTESIAN_POINT ( 'NONE',  ( -19.80875734969026425, -0.3587747205144265483, 31.02402280011862246 ) ) ;
#63088=VERTEX_POINT ( 'NONE', #40633 ) ;
#63098=DIRECTION ( 'NONE',  ( 0.000000000000000000, 0.000000000000000000, 1.000000000000000000 ) ) ;
#63100=DIRECTION ( 'NONE',  ( -0.000000000000000000, 1.000000000000000000, -0.000000000000000000 ) ) ;
#63108=CARTESIAN_POINT ( 'NONE',  ( 4.959846025536391423, -6.376774720514417183, 20.32314756232572250 ) ) ;
#63112=DIRECTION ( 'NONE',  ( 0.000000000000000000, 0.000000000000000000, -1.000000000000000000 ) ) ;
#63115=CIRCLE ( 'NONE', #12891, 130.2784398600581710 ) ;
#63116=ORIENTED_EDGE ( 'NONE', *, *, #30239, .T. ) ;
#63118=VECTOR ( 'NONE', #82609, 1000.000000000000000 ) ;
#63123=CARTESIAN_POINT ( 'NONE',  ( 3.165726958143470160, -5.876774720514421624, 21.14296526391294506 ) ) ;
#63124=CARTESIAN_POINT ( 'NONE',  ( 4.281508569253434260, -6.376774720514422512, 21.28700241941785265 ) ) ;
#63125=CARTESIAN_POINT ( 'NONE',  ( 6.727764423076923350, -6.376774720514413630, 19.76442307692307665 ) ) ;
#63126=DIRECTION ( 'NONE',  ( 1.000000000000000000, 0.000000000000000000, 0.000000000000000000 ) ) ;
#63150=CARTESIAN_POINT ( 'NONE',  ( -29.49875734969026198, -0.3587747205144262708, 7.870022800118625206 ) ) ;
#63158=CARTESIAN_POINT ( 'NONE',  ( -4.141025641025642301, -5.876774720514412742, 19.63681891025641235 ) ) ;
#63161=VECTOR ( 'NONE', #87176, 1000.000000000000000 ) ;
#63162=EDGE_CURVE ( 'NONE', #35655, #13725, #4533, .T. ) ;
#63163=EDGE_CURVE ( 'NONE', #32836, #25405, #60368, .T. ) ;
#63167=DIRECTION ( 'NONE',  ( -0.000000000000000000, 1.000000000000000000, -0.000000000000000000 ) ) ;
#63171=VERTEX_POINT ( 'NONE', #89798 ) ;
#63172=CARTESIAN_POINT ( 'NONE',  ( 23.91005183030481263, -2.682774720514426559, -14.40591128290692069 ) ) ;
#63188=VECTOR ( 'NONE', #93464, 1000.000000000000114 ) ;
#63190=AXIS2_PLACEMENT_3D ( 'NONE', #49942, #2258, #42332 ) ;
#63193=CARTESIAN_POINT ( 'NONE',  ( 9.278253834636473130, -6.376774720514426953, 18.21871304725684482 ) ) ;
#63201=DIRECTION ( 'NONE',  ( 0.000000000000000000, 0.000000000000000000, 1.000000000000000000 ) ) ;
#63202=CARTESIAN_POINT ( 'NONE',  ( 10.73283225838973642, -5.356774720506346732, -27.03068772369604744 ) ) ;
#63213=CARTESIAN_POINT ( 'NONE',  ( -5.891025641025639636, -6.376774720514420736, 20.75510817307693046 ) ) ;
#63216=PLANE ( 'NONE',  #36796 ) ;
#63219=EDGE_CURVE ( 'NONE', #32487, #96155, #44127, .T. ) ;
#63226=ORIENTED_EDGE ( 'NONE', *, *, #43488, .F. ) ;
#63232=DIRECTION ( 'NONE',  ( 0.000000000000000000, 0.000000000000000000, -1.000000000000000000 ) ) ;
#63234=CARTESIAN_POINT ( 'NONE',  ( -5.115065434581078208, -5.876774720514409189, 19.15054976246387497 ) ) ;
#63247=CARTESIAN_POINT ( 'NONE',  ( 13.32458981842495049, -5.152774720514427642, -26.34181586963115507 ) ) ;
#63250=CARTESIAN_POINT ( 'NONE',  ( 4.334227700317904386, -5.876774720514402972, 18.30971318885719157 ) ) ;
#63253=DIRECTION ( 'NONE',  ( 0.000000000000000000, -1.000000000000000000, 0.000000000000000000 ) ) ;
#63265=CARTESIAN_POINT ( 'NONE',  ( 7.089543269230769162, -6.376774720514413630, 19.75741185897435415 ) ) ;
#63267=CARTESIAN_POINT ( 'NONE',  ( 4.518955212990007908, -5.876774720514421624, 20.94857968174986951 ) ) ;
#63276=CARTESIAN_POINT ( 'NONE',  ( -28.98875734969026041, -0.3587747205144265483, 25.61802280011862720 ) ) ;
#63279=CARTESIAN_POINT ( 'NONE',  ( 15.22396167909262488, -3.565890571771469286, -27.22573842070922367 ) ) ;
#63282=VERTEX_POINT ( 'NONE', #29389 ) ;
#63286=CARTESIAN_POINT ( 'NONE',  ( -7.641025641025640525, -5.876774720514418071, 20.36458333333334281 ) ) ;
#63311=DIRECTION ( 'NONE',  ( -1.000000000000000000, -0.000000000000000000, 0.000000000000000000 ) ) ;
#63312=EDGE_CURVE ( 'NONE', #87273, #43589, #70461, .T. ) ;
#63314=EDGE_CURVE ( 'NONE', #15357, #3028, #92781, .T. ) ;
#63316=CARTESIAN_POINT ( 'NONE',  ( 4.653515142448186204, -5.876774720514414518, 19.86181745814487343 ) ) ;
#63324=VECTOR ( 'NONE', #84009, 1000.000000000000000 ) ;
#63325=ORIENTED_EDGE ( 'NONE', *, *, #49228, .T. ) ;
#63330=VERTEX_POINT ( 'NONE', #946 ) ;
#63338=CARTESIAN_POINT ( 'NONE',  ( 0.000000000000000000, -5.876774720514426953, 0.000000000000000000 ) ) ;
#63342=VERTEX_POINT ( 'NONE', #31896 ) ;
#63345=AXIS2_PLACEMENT_3D ( 'NONE', #20966, #89493, #13352 ) ;
#63346=DIRECTION ( 'NONE',  ( -0.000000000000000000, 1.000000000000000000, -0.000000000000000000 ) ) ;
#63356=LINE ( 'NONE', #47119, #8123 ) ;
#63359=ADVANCED_FACE ( 'NONE', ( #6557 ), #38006, .T. ) ;
#63361=ORIENTED_EDGE ( 'NONE', *, *, #6468, .T. ) ;
#63363=CARTESIAN_POINT ( 'NONE',  ( 32.85081302853804885, -3.622774720514426949, -13.10817780685210643 ) ) ;
#63371=CARTESIAN_POINT ( 'NONE',  ( -29.49875734969025842, 5.965225279485572685, 17.86602280011862476 ) ) ;
#63374=DIRECTION ( 'NONE',  ( 0.000000000000000000, -1.000000000000000000, 0.000000000000000000 ) ) ;
#63386=DIRECTION ( 'NONE',  ( 0.000000000000000000, -1.000000000000000000, 0.000000000000000000 ) ) ;
#63391=ORIENTED_EDGE ( 'NONE', *, *, #45427, .T. ) ;
#63396=ORIENTED_EDGE ( 'NONE', *, *, #32578, .F. ) ;
#63399=CARTESIAN_POINT ( 'NONE',  ( 7.311104923646705167, -6.376774720514415407, 20.13320233724603980 ) ) ;
#63405=CARTESIAN_POINT ( 'NONE',  ( 13.91401389203221406, -3.316774720514426456, 158.0376437107427137 ) ) ;
#63415=PLANE ( 'NONE',  #18700 ) ;
#63416=EDGE_CURVE ( 'NONE', #67214, #5889, #16662, .T. ) ;
#63423=ORIENTED_EDGE ( 'NONE', *, *, #27493, .T. ) ;
#63424=ADVANCED_FACE ( 'NONE', ( #94285 ), #2960, .F. ) ;
#63426=CARTESIAN_POINT ( 'NONE',  ( -1.540913562699879114, -5.876774720514409189, 19.44316438561912008 ) ) ;
#63430=EDGE_CURVE ( 'NONE', #80664, #30045, #70965, .T. ) ;
#63441=CARTESIAN_POINT ( 'NONE',  ( 0.3627416911114360598, -6.376774720514411854, 19.59793130852656873 ) ) ;
#63447=DIRECTION ( 'NONE',  ( 0.000000000000000000, 0.000000000000000000, 1.000000000000000000 ) ) ;
#63451=CARTESIAN_POINT ( 'NONE',  ( 25.06178640545682867, -4.997093759973374461, -9.841412737801366717 ) ) ;
#63458=ORIENTED_EDGE ( 'NONE', *, *, #59500, .F. ) ;
#63466=ORIENTED_EDGE ( 'NONE', *, *, #51188, .F. ) ;
#63467=CARTESIAN_POINT ( 'NONE',  ( 32.56681547219513817, -5.361656835957732348, -1.802091617189489403 ) ) ;
#63472=CARTESIAN_POINT ( 'NONE',  ( 2.955024617976266033, -5.876774720514415407, 20.58370193283586858 ) ) ;
#63478=CARTESIAN_POINT ( 'NONE',  ( -20.77875734969026311, -5.356774720514425603, 27.31649921512899937 ) ) ;
#63482=CARTESIAN_POINT ( 'NONE',  ( 3.252401863874215593, -0.3587747205143964613, -29.35688408629929214 ) ) ;
#63493=ORIENTED_EDGE ( 'NONE', *, *, #10631, .F. ) ;
#63495=CARTESIAN_POINT ( 'NONE',  ( -1.358974358974355257, -5.876774720514426953, 21.75000000000000711 ) ) ;
#63509=CARTESIAN_POINT ( 'NONE',  ( 6.404294203292168142, -5.876774720514416295, 20.09052689972686423 ) ) ;
#63511=CARTESIAN_POINT ( 'NONE',  ( 22.02124265030973760, -5.356774720514425603, 16.20402280011862217 ) ) ;
#63512=PLANE ( 'NONE',  #8621 ) ;
#63528=DIRECTION ( 'NONE',  ( 0.000000000000000000, 0.000000000000000000, 1.000000000000000000 ) ) ;
#63529=ADVANCED_FACE ( 'NONE', ( #47446 ), #86499, .T. ) ;
#63536=DIRECTION ( 'NONE',  ( -0.000000000000000000, 1.000000000000000000, -0.000000000000000000 ) ) ;
#63541=EDGE_CURVE ( 'NONE', #27095, #31243, #31716, .T. ) ;
#63563=CARTESIAN_POINT ( 'NONE',  ( 5.786755829966409692, -6.376774720514413630, 19.89762986309224857 ) ) ;
#63566=VERTEX_POINT ( 'NONE', #15480 ) ;
#63587=CARTESIAN_POINT ( 'NONE',  ( 6.955725288069978696, -6.376774720514426065, 21.70430095680336890 ) ) ;
#63592=CARTESIAN_POINT ( 'NONE',  ( -20.27875734969026311, 6.143225279485574397, 24.00402280011862288 ) ) ;
#63594=ORIENTED_EDGE ( 'NONE', *, *, #47375, .F. ) ;
#63595=ORIENTED_EDGE ( 'NONE', *, *, #95872, .T. ) ;
#63596=ORIENTED_EDGE ( 'NONE', *, *, #2700, .T. ) ;
#63614=CARTESIAN_POINT ( 'NONE',  ( 4.819673832743241348, -6.376774720514422512, 21.07066438048017076 ) ) ;
#63625=ADVANCED_FACE ( 'NONE', ( #262 ), #55566, .F. ) ;
#63628=CARTESIAN_POINT ( 'NONE',  ( 3.036358173076929123, -5.876774720514419847, 20.87990785256409865 ) ) ;
#63629=CARTESIAN_POINT ( 'NONE',  ( 4.628547153713393314, -6.376774720514418959, 20.50654586986123817 ) ) ;
#63631=CARTESIAN_POINT ( 'NONE',  ( 27.53860345374771867, -2.682774720514426559, -9.482392034746242260 ) ) ;
#63632=CARTESIAN_POINT ( 'NONE',  ( 5.920986267150416538, -6.376774720514422512, 21.32549308339960348 ) ) ;
#63649=ORIENTED_EDGE ( 'NONE', *, *, #13469, .T. ) ;
#63653=EDGE_LOOP ( 'NONE', ( #84986, #95287, #79094, #50544 ) ) ;
#63657=DIRECTION ( 'NONE',  ( -0.000000000000000000, -1.000000000000000000, -0.000000000000000000 ) ) ;
#63659=ADVANCED_FACE ( 'NONE', ( #94105 ), #77373, .F. ) ;
#63660=VERTEX_POINT ( 'NONE', #30716 ) ;
#63667=EDGE_CURVE ( 'NONE', #38147, #68993, #23081, .T. ) ;
#63670=FACE_OUTER_BOUND ( 'NONE', #8509, .T. ) ;
#63675=ORIENTED_EDGE ( 'NONE', *, *, #533, .F. ) ;
#63678=DIRECTION ( 'NONE',  ( 0.000000000000000000, 0.000000000000000000, 1.000000000000000000 ) ) ;
#63680=CARTESIAN_POINT ( 'NONE',  ( 33.96422015159436114, 5.965225279485572685, -7.233236000911337449 ) ) ;
#63710=ORIENTED_EDGE ( 'NONE', *, *, #91528, .F. ) ;
#63714=VECTOR ( 'NONE', #99838, 1000.000000000000000 ) ;
#63718=DIRECTION ( 'NONE',  ( 0.000000000000000000, 0.000000000000000000, -1.000000000000000000 ) ) ;
#63722=DIRECTION ( 'NONE',  ( -1.226388327005079762E-16, 0.000000000000000000, 1.000000000000000000 ) ) ;
#63729=CARTESIAN_POINT ( 'NONE',  ( 32.33217928425156629, 6.475225279485573360, -12.20610769812808982 ) ) ;
#63734=ORIENTED_EDGE ( 'NONE', *, *, #34691, .T. ) ;
#63742=LINE ( 'NONE', #40876, #58750 ) ;
#63746=VECTOR ( 'NONE', #5460, 1000.000000000000000 ) ;
#63752=CARTESIAN_POINT ( 'NONE',  ( -26.91814428177455909, -0.3587747205144265483, 29.98490496616818746 ) ) ;
#63757=CARTESIAN_POINT ( 'NONE',  ( -27.25988310792305214, 5.965225279485572685, 30.32664379231667695 ) ) ;
#63760=CARTESIAN_POINT ( 'NONE',  ( 27.53860345374808105, -4.772774720514425972, -6.982392034746241372 ) ) ;
#63768=LINE ( 'NONE', #17564, #72318 ) ;
#63775=CARTESIAN_POINT ( 'NONE',  ( 2.649863049427662709, -6.376774720514420736, 20.71861240329949538 ) ) ;
#63777=CARTESIAN_POINT ( 'NONE',  ( 32.45853543194704116, -0.3587747205144265483, 9.169203677920338080 ) ) ;
#63779=VECTOR ( 'NONE', #21415, 1000.000000000000000 ) ;
#63783=DIRECTION ( 'NONE',  ( -1.000000000000000000, -0.000000000000000000, 0.000000000000000000 ) ) ;
#63784=DIRECTION ( 'NONE',  ( -0.1254312216594016538, -0.000000000000000000, -0.9921023176230513441 ) ) ;
#63790=VERTEX_POINT ( 'NONE', #55145 ) ;
#63798=ORIENTED_EDGE ( 'NONE', *, *, #51458, .T. ) ;
#63807=DIRECTION ( 'NONE',  ( -0.000000000000000000, -1.000000000000000000, -0.000000000000000000 ) ) ;
#63818=VECTOR ( 'NONE', #58585, 1000.000000000000000 ) ;
#63823=CARTESIAN_POINT ( 'NONE',  ( 4.547289707988324103, -6.376774720514410077, 19.12266226838056582 ) ) ;
#63828=LINE ( 'NONE', #48595, #36120 ) ;
#63829=CIRCLE ( 'NONE', #20040, 0.3000000000000016542 ) ;
#63843=ORIENTED_EDGE ( 'NONE', *, *, #56096, .F. ) ;
#63851=CIRCLE ( 'NONE', #18409, 4.080000000000000071 ) ;
#63859=CARTESIAN_POINT ( 'NONE',  ( -6.752792875861700850, -6.376774720514411854, 19.46247113826586528 ) ) ;
#63880=DIRECTION ( 'NONE',  ( 0.000000000000000000, 0.000000000000000000, -1.000000000000000000 ) ) ;
#63882=CARTESIAN_POINT ( 'NONE',  ( 5.557675543255346184, -6.376774720514415407, 20.10561748372801461 ) ) ;
#63883=EDGE_CURVE ( 'NONE', #92103, #5494, #92075, .T. ) ;
#63885=CARTESIAN_POINT ( 'NONE',  ( 0.000000000000000000, -5.876774720514426953, 0.000000000000000000 ) ) ;
#63899=VECTOR ( 'NONE', #15962, 1000.000000000000000 ) ;
#63903=DIRECTION ( 'NONE',  ( 0.000000000000000000, 0.000000000000000000, 1.000000000000000000 ) ) ;
#63904=VERTEX_POINT ( 'NONE', #12808 ) ;
#63913=DIRECTION ( 'NONE',  ( 0.000000000000000000, -1.000000000000000000, 0.000000000000000000 ) ) ;
#63921=EDGE_CURVE ( 'NONE', #55695, #18015, #51896, .T. ) ;
#63926=CARTESIAN_POINT ( 'NONE',  ( 32.33217928425143839, -1.682774720514426114, -12.20610769812824437 ) ) ;
#63933=ORIENTED_EDGE ( 'NONE', *, *, #25723, .T. ) ;
#63950=VERTEX_POINT ( 'NONE', #2863 ) ;
#63951=CARTESIAN_POINT ( 'NONE',  ( -6.128026245051341192, -6.376774720514410077, 19.39236848396478763 ) ) ;
#63966=CARTESIAN_POINT ( 'NONE',  ( 3.879810481058463711, -5.876774720514427841, 21.83835767234735670 ) ) ;
#63967=ORIENTED_EDGE ( 'NONE', *, *, #72697, .T. ) ;
#63972=ORIENTED_EDGE ( 'NONE', *, *, #17995, .T. ) ;
#63983=ORIENTED_EDGE ( 'NONE', *, *, #25349, .T. ) ;
#63988=CARTESIAN_POINT ( 'NONE',  ( 29.65417061107837071, -5.752153662292248448, 28.02209566695815823 ) ) ;
#63998=ADVANCED_FACE ( 'NONE', ( #26181 ), #33795, .F. ) ;
#64000=EDGE_LOOP ( 'NONE', ( #58347, #2325, #76104, #22936, #35536, #21836, #65598, #39335, #28447, #13807, #8908, #85019, #16386, #35672, #9236, #53057, #308, #86271, #24555, #77732 ) ) ;
#64005=DIRECTION ( 'NONE',  ( -1.000000000000000000, -0.000000000000000000, 0.000000000000000000 ) ) ;
#64006=EDGE_LOOP ( 'NONE', ( #93088, #12885 ) ) ;
#64011=B_SPLINE_CURVE_WITH_KNOTS ( 'NONE', 3,
 ( #40803, #88988, #96102, #95095, #3265, #11852, #87480, #65175 ),
 .UNSPECIFIED., .F., .F.,
 ( 4, 2, 2, 4 ),
 ( 0.0001293435094372204610, 0.002876179024813956854, 0.004249596782502322069, 0.005623014540190688151 ),
 .UNSPECIFIED. ) ;
#64021=CARTESIAN_POINT ( 'NONE',  ( 5.671814302646631667, -5.876774720514418959, 20.58085404595000512 ) ) ;
#64029=DIRECTION ( 'NONE',  ( 0.000000000000000000, -1.000000000000000000, 0.000000000000000000 ) ) ;
#64052=EDGE_LOOP ( 'NONE', ( #77176, #29410, #28582, #80298 ) ) ;
#64055=CIRCLE ( 'NONE', #96409, 28.96799999999999642 ) ;
#64059=EDGE_LOOP ( 'NONE', ( #29799, #59681, #54593, #9008 ) ) ;
#64066=ORIENTED_EDGE ( 'NONE', *, *, #75635, .T. ) ;
#64068=CARTESIAN_POINT ( 'NONE',  ( 7.139069293134643779, -6.376774720514422512, 20.58118917620081945 ) ) ;
#64069=CARTESIAN_POINT ( 'NONE',  ( 5.326923076923078426, -6.376774720514420736, 20.76772836538461320 ) ) ;
#64077=DIRECTION ( 'NONE',  ( -0.9496245541219264785, -0.000000000000000000, -0.3133898629642195011 ) ) ;
#64082=ORIENTED_EDGE ( 'NONE', *, *, #88205, .T. ) ;
#64083=VECTOR ( 'NONE', #8106, 1000.000000000000000 ) ;
#64104=DIRECTION ( 'NONE',  ( -0.000000000000000000, -1.000000000000000000, -0.000000000000000000 ) ) ;
#64109=CARTESIAN_POINT ( 'NONE',  ( 14.76093561896378148, -3.316774720514426456, -26.55548769130088971 ) ) ;
#64116=CARTESIAN_POINT ( 'NONE',  ( -5.514838905578028694, -5.876774720514408301, 19.81240905262003338 ) ) ;
#64122=CARTESIAN_POINT ( 'NONE',  ( 4.819673832743241348, -5.876774720514421624, 21.07066438048017076 ) ) ;
#64123=CYLINDRICAL_SURFACE ( 'NONE', #18818, 0.8160000000000007248 ) ;
#64134=CARTESIAN_POINT ( 'NONE',  ( 3.671066620544169101, -5.876774720514423400, 21.47597918715562670 ) ) ;
#64136=DIRECTION ( 'NONE',  ( 0.000000000000000000, -1.000000000000000000, 0.000000000000000000 ) ) ;
#64142=LINE ( 'NONE', #25550, #12159 ) ;
#64147=DIRECTION ( 'NONE',  ( -0.7512896232465786639, -0.000000000000000000, -0.6599726524652470561 ) ) ;
#64157=CARTESIAN_POINT ( 'NONE',  ( -10.79305683637731406, 5.965225279485594001, -27.49869550653260930 ) ) ;
#64168=CARTESIAN_POINT ( 'NONE',  ( 29.80070917940689412, 5.965225279485572685, 27.39560796525321607 ) ) ;
#64183=CARTESIAN_POINT ( 'NONE',  ( 2.747717285871495108, -6.376774720514404748, 18.94713297040818034 ) ) ;
#64200=B_SPLINE_CURVE_WITH_KNOTS ( 'NONE', 3,
 ( #26924, #65514, #43158, #97430, #89816, #36521, #52260, #35042, #50267, #81208, #51261, #5075, #73107, #82200, #66013, #3596 ),
 .UNSPECIFIED., .F., .F.,
 ( 4, 2, 2, 2, 2, 2, 2, 4 ),
 ( -2.132270449955935040E-05, 0.0007770955584725032679, 0.001176304689958539498, 0.001575513821444575729, 0.001974722952930611959, 0.002373932084416648623, 0.002773141215902684420, 0.003172350347388721084 ),
 .UNSPECIFIED. ) ;
#64204=VERTEX_POINT ( 'NONE', #2615 ) ;
#64208=VERTEX_POINT ( 'NONE', #33055 ) ;
#64210=PLANE ( 'NONE',  #61218 ) ;
#64215=DIRECTION ( 'NONE',  ( 0.000000000000000000, 0.000000000000000000, -1.000000000000000000 ) ) ;
#64217=ORIENTED_EDGE ( 'NONE', *, *, #35751, .F. ) ;
#64222=EDGE_CURVE ( 'NONE', #28254, #35481, #87329, .T. ) ;
#64225=ORIENTED_EDGE ( 'NONE', *, *, #53937, .T. ) ;
#64226=CARTESIAN_POINT ( 'NONE',  ( 31.62034159138967837, -4.397688677367943555, -2.670054032269225885 ) ) ;
#64227=AXIS2_PLACEMENT_3D ( 'NONE', #77844, #16452, #70757 ) ;
#64235=VECTOR ( 'NONE', #11257, 1000.000000000000227 ) ;
#64243=AXIS2_PLACEMENT_3D ( 'NONE', #67269, #98188, #59657 ) ;
#64258=DIRECTION ( 'NONE',  ( 1.000000000000000000, 0.000000000000000000, 0.000000000000000000 ) ) ;
#64262=PLANE ( 'NONE',  #53288 ) ;
#64277=CARTESIAN_POINT ( 'NONE',  ( 4.329581153495547063, -6.376774720514422512, 21.24220543808225869 ) ) ;
#64288=VECTOR ( 'NONE', #3105, 1000.000000000000000 ) ;
#64322=DIRECTION ( 'NONE',  ( 0.06283980576413537855, 0.000000000000000000, 0.9980236263794188822 ) ) ;
#64326=CARTESIAN_POINT ( 'NONE',  ( 4.547289707988324103, -5.876774720514410966, 19.12266226838056582 ) ) ;
#64330=PLANE ( 'NONE',  #10253 ) ;
#64339=ORIENTED_EDGE ( 'NONE', *, *, #4539, .T. ) ;
#64341=CARTESIAN_POINT ( 'NONE',  ( -5.970505764849975527, -5.876774720514411854, 19.55848054040323802 ) ) ;
#64345=ORIENTED_EDGE ( 'NONE', *, *, #68246, .F. ) ;
#64348=AXIS2_PLACEMENT_3D ( 'NONE', #6750, #98097, #61561 ) ;
#64359=CARTESIAN_POINT ( 'NONE',  ( 29.70909950603835625, -4.224653874731083114, 27.99670097642948008 ) ) ;
#64360=CARTESIAN_POINT ( 'NONE',  ( -6.815415664272417295, -5.876774720514410077, 19.46427715384223234 ) ) ;
#64365=VERTEX_POINT ( 'NONE', #43175 ) ;
#64367=CARTESIAN_POINT ( 'NONE',  ( -19.80875734969026425, -0.3587747205144265483, 30.51402280011862089 ) ) ;
#64371=LINE ( 'NONE', #9050, #68015 ) ;
#64383=AXIS2_PLACEMENT_3D ( 'NONE', #26127, #64725, #19507 ) ;
#64385=DIRECTION ( 'NONE',  ( 0.000000000000000000, 1.000000000000000000, 0.000000000000000000 ) ) ;
#64387=CARTESIAN_POINT ( 'NONE',  ( 5.400898774349120579, -6.376774720514417183, 20.36357656736558042 ) ) ;
#64410=CARTESIAN_POINT ( 'NONE',  ( -1.044639546681034536, -5.876774720514417183, 20.34213149456667580 ) ) ;
#64414=VECTOR ( 'NONE', #37090, 1000.000000000000000 ) ;
#64418=CARTESIAN_POINT ( 'NONE',  ( 4.465438306463536122, -6.376774720514426065, 21.59631214011467293 ) ) ;
#64422=AXIS2_PLACEMENT_3D ( 'NONE', #9674, #78657, #72089 ) ;
#64445=ORIENTED_EDGE ( 'NONE', *, *, #67524, .T. ) ;
#64451=EDGE_LOOP ( 'NONE', ( #34103, #90769, #36851, #57463 ) ) ;
#64452=CARTESIAN_POINT ( 'NONE',  ( -6.499903988472228278, -5.876774720514408301, 19.18381548539529646 ) ) ;
#64453=DIRECTION ( 'NONE',  ( -0.000000000000000000, 1.000000000000000000, -0.000000000000000000 ) ) ;
#64456=VECTOR ( 'NONE', #98881, 1000.000000000000000 ) ;
#64470=DIRECTION ( 'NONE',  ( 0.000000000000000000, 0.000000000000000000, 1.000000000000000000 ) ) ;
#64499=CARTESIAN_POINT ( 'NONE',  ( -29.49875734969025842, 5.965225279485572685, 23.37402280011862743 ) ) ;
#64511=ORIENTED_EDGE ( 'NONE', *, *, #27441, .F. ) ;
#64515=LINE ( 'NONE', #1082, #22059 ) ;
#64524=CARTESIAN_POINT ( 'NONE',  ( -7.536766146225033047, -5.876774720514412742, 19.63296556618507438 ) ) ;
#64529=CARTESIAN_POINT ( 'NONE',  ( 27.53860345374808105, -1.682774720514426114, -1.272392034746785860 ) ) ;
#64541=DIRECTION ( 'NONE',  ( -0.000000000000000000, -1.000000000000000000, -0.000000000000000000 ) ) ;
#64573=VERTEX_POINT ( 'NONE', #84206 ) ;
#64584=ORIENTED_EDGE ( 'NONE', *, *, #74077, .T. ) ;
#64586=CARTESIAN_POINT ( 'NONE',  ( 11.94353453780502683, -5.048182838635504766, -26.89061828217040784 ) ) ;
#64592=CARTESIAN_POINT ( 'NONE',  ( 16.26279755680689476, 5.965225279485572685, -27.67997040356619110 ) ) ;
#64594=ORIENTED_EDGE ( 'NONE', *, *, #97424, .T. ) ;
#64595=DIRECTION ( 'NONE',  ( 0.000000000000000000, 0.000000000000000000, 1.000000000000000000 ) ) ;
#64606=EDGE_CURVE ( 'NONE', #53312, #60724, #30427, .T. ) ;
#64610=AXIS2_PLACEMENT_3D ( 'NONE', #93059, #55525, #71745 ) ;
#64618=DIRECTION ( 'NONE',  ( -1.334402673828313093E-16, 0.000000000000000000, -1.000000000000000000 ) ) ;
#64622=VERTEX_POINT ( 'NONE', #68496 ) ;
#64624=CARTESIAN_POINT ( 'NONE',  ( -4.968349358974361252, -6.376774720514411854, 19.46153846153847056 ) ) ;
#64627=EDGE_CURVE ( 'NONE', #39794, #54462, #95423, .T. ) ;
#64628=CARTESIAN_POINT ( 'NONE',  ( 4.959846025536391423, -5.876774720514417183, 20.32314756232572250 ) ) ;
#64631=EDGE_CURVE ( 'NONE', #31048, #451, #91325, .T. ) ;
#64647=DIRECTION ( 'NONE',  ( -0.7071067811865474617, -0.000000000000000000, -0.7071067811865474617 ) ) ;
#64651=VERTEX_POINT ( 'NONE', #48166 ) ;
#64658=CARTESIAN_POINT ( 'NONE',  ( -6.818021687177533430, -6.376774720514408301, 19.14905311829361167 ) ) ;
#64671=FACE_OUTER_BOUND ( 'NONE', #77488, .T. ) ;
#64672=ORIENTED_EDGE ( 'NONE', *, *, #68576, .F. ) ;
#64673=DIRECTION ( 'NONE',  ( 0.000000000000000000, 0.000000000000000000, -1.000000000000000000 ) ) ;
#64677=LINE ( 'NONE', #86974, #77708 ) ;
#64686=ORIENTED_EDGE ( 'NONE', *, *, #11656, .F. ) ;
#64693=DIRECTION ( 'NONE',  ( 4.448048651795327725E-16, 1.000000000000000000, 7.118365844322534241E-16 ) ) ;
#64696=EDGE_CURVE ( 'NONE', #12570, #76880, #86217, .T. ) ;
#64704=CARTESIAN_POINT ( 'NONE',  ( 32.70426658926474062, -3.547616055647111022, -3.273583889775387057 ) ) ;
#64711=CARTESIAN_POINT ( 'NONE',  ( -0.2200237740140755516, -6.376774720514408301, 19.17724329193115551 ) ) ;
#64713=ADVANCED_BREP_SHAPE_REPRESENTATION ( '', ( #44893, #37391 ), #61811 ) ;
#64719=DIRECTION ( 'NONE',  ( -1.000000000000000000, -0.000000000000000000, 0.000000000000000000 ) ) ;
#64725=DIRECTION ( 'NONE',  ( 0.000000000000000000, -1.000000000000000000, 0.000000000000000000 ) ) ;
#64733=AXIS2_PLACEMENT_3D ( 'NONE', #33725, #58079, #10887 ) ;
#64734=CARTESIAN_POINT ( 'NONE',  ( -5.895658455092926076, -6.376774720514418959, 20.50445910983877340 ) ) ;
#64739=VECTOR ( 'NONE', #93840, 1000.000000000000000 ) ;
#64755=FACE_OUTER_BOUND ( 'NONE', #72253, .T. ) ;
#64760=CARTESIAN_POINT ( 'NONE',  ( 27.86270917940689174, 5.965225279485572685, 29.49402280011862487 ) ) ;
#64773=DIRECTION ( 'NONE',  ( 0.000000000000000000, 0.000000000000000000, -1.000000000000000000 ) ) ;
#64781=CARTESIAN_POINT ( 'NONE',  ( 11.56983764158150052, 5.965225279485572685, 28.29037853177889517 ) ) ;
#64784=CIRCLE ( 'NONE', #19397, 1.700000000000000178 ) ;
#64785=CARTESIAN_POINT ( 'NONE',  ( 13.91401389203221406, 5.965225279485572685, 158.0376437107427137 ) ) ;
#64794=CIRCLE ( 'NONE', #11308, 3.500000000000000000 ) ;
#64798=DIRECTION ( 'NONE',  ( 0.000000000000000000, 1.000000000000000000, 1.478457507934778393E-16 ) ) ;
#64800=CARTESIAN_POINT ( 'NONE',  ( 0.3910256410256418569, -5.876774720514419847, 20.67377804487180271 ) ) ;
#64813=CARTESIAN_POINT ( 'NONE',  ( -0.08860454909227881426, -5.876774720514410077, 19.21747685089457036 ) ) ;
#64818=( BOUNDED_SURFACE ( )  B_SPLINE_SURFACE ( 3, 2, ( 
 ( #22356, #5655, #98491 ),
 ( #15761, #6153, #67574 ),
 ( #28993, #37106, #45723 ),
 ( #98992, #22855, #29483 ) ),
 .UNSPECIFIED., .F., .F., .T. ) 
 B_SPLINE_SURFACE_WITH_KNOTS ( ( 4, 4 ),
 ( 3, 3 ),
 ( 0.004439845973569162343, 0.004703938444645663561 ),
 ( 0.000000000000000000, 1.000000000000000000 ),
 .UNSPECIFIED. ) 
 GEOMETRIC_REPRESENTATION_ITEM ( )  RATIONAL_B_SPLINE_SURFACE ( (
 ( 1.000000000000000000, 0.9005394799515968884, 1.000000000000000000),
 ( 1.000000000000000000, 0.9005352985759397244, 1.000000000000000000),
 ( 1.000000000000000000, 0.8990570573199264670, 1.000000000000000000),
 ( 1.000000000000000000, 0.8962098481621324497, 1.000000000000000000) ) ) 
 REPRESENTATION_ITEM ( '' )  SURFACE ( )  );
#64840=VERTEX_POINT ( 'NONE', #65411 ) ;
#64847=CARTESIAN_POINT ( 'NONE',  ( -6.020540257910568904, -5.876774720514411854, 19.49847411603315095 ) ) ;
#64854=EDGE_CURVE ( 'NONE', #39047, #64365, #28925, .T. ) ;
#64863=CARTESIAN_POINT ( 'NONE',  ( 29.70220533433690946, -3.316774720514426456, 28.20564067601640801 ) ) ;
#64865=CARTESIAN_POINT ( 'NONE',  ( -7.326923076923076650, -5.876774720514417183, 20.36318108974359831 ) ) ;
#64868=CARTESIAN_POINT ( 'NONE',  ( 32.45853543194704116, 5.965225279485572685, 9.169203677920338080 ) ) ;
#64870=CYLINDRICAL_SURFACE ( 'NONE', #74044, 2.040000000000000036 ) ;
#64871=DIRECTION ( 'NONE',  ( -1.250865172912931245E-15, 6.879758451021121945E-15, -1.000000000000000000 ) ) ;
#64877=AXIS2_PLACEMENT_3D ( 'NONE', #59036, #20947, #82847 ) ;
#64884=EDGE_CURVE ( 'NONE', #18359, #20944, #95329, .T. ) ;
#64911=CARTESIAN_POINT ( 'NONE',  ( 30.43908124610670285, -2.682774720514426559, -13.86910542224428866 ) ) ;
#64917=CARTESIAN_POINT ( 'NONE',  ( 4.689770114687411784, -6.376774720514424288, 21.33175327469028915 ) ) ;
#64932=EDGE_LOOP ( 'NONE', ( #96371, #66574, #3270, #81161 ) ) ;
#64936=DIRECTION ( 'NONE',  ( 0.000000000000000000, -1.000000000000000000, 0.000000000000000000 ) ) ;
#64937=CARTESIAN_POINT ( 'NONE',  ( -4.929522925832174884, -0.3587747205143967943, -28.63504101147569614 ) ) ;
#64938=AXIS2_PLACEMENT_3D ( 'NONE', #92032, #95537, #26024 ) ;
#64942=ORIENTED_EDGE ( 'NONE', *, *, #66991, .F. ) ;
#64944=VECTOR ( 'NONE', #20342, 1000.000000000000000 ) ;
#64952=CARTESIAN_POINT ( 'NONE',  ( -6.185411026474866958, -5.876774720514411854, 19.34586827028016742 ) ) ;
#64956=ORIENTED_EDGE ( 'NONE', *, *, #993, .T. ) ;
#64957=FACE_OUTER_BOUND ( 'NONE', #53581, .T. ) ;
#64961=B_SPLINE_CURVE_WITH_KNOTS ( 'NONE', 3,
 ( #47064, #71399, #77978, #39442 ),
 .UNSPECIFIED., .F., .F.,
 ( 4, 4 ),
 ( 0.000000000000000000, 0.001749918372063935697 ),
 .UNSPECIFIED. ) ;
#64963=DIRECTION ( 'NONE',  ( -1.000000000000000000, -0.000000000000000000, 0.000000000000000000 ) ) ;
#64979=CARTESIAN_POINT ( 'NONE',  ( 2.677468215678941110, -6.376774720514418959, 20.83735685176740304 ) ) ;
#64980=FACE_OUTER_BOUND ( 'NONE', #48005, .T. ) ;
#64991=CARTESIAN_POINT ( 'NONE',  ( 5.097264368846809113, 1.579225279485572342, -27.56135813788808875 ) ) ;
#64995=CIRCLE ( 'NONE', #29247, 1.325999999999943446 ) ;
#64997=DIRECTION ( 'NONE',  ( 0.000000000000000000, 0.000000000000000000, 1.000000000000000000 ) ) ;
#65015=DIRECTION ( 'NONE',  ( 0.000000000000000000, 0.000000000000000000, -1.000000000000000000 ) ) ;
#65022=CARTESIAN_POINT ( 'NONE',  ( -7.338700834008208496, -5.876774720514410966, 19.35116211686183263 ) ) ;
#65041=CARTESIAN_POINT ( 'NONE',  ( -10.11875734969026297, -6.376774720514426953, 30.51402280011862089 ) ) ;
#65064=CARTESIAN_POINT ( 'NONE',  ( 7.111284305517425075, -6.376774720514422512, 21.05363841023157434 ) ) ;
#65070=CARTESIAN_POINT ( 'NONE',  ( 6.509931258083027750, -5.876774720514417183, 20.09204137875607188 ) ) ;
#65081=LINE ( 'NONE', #73661, #67543 ) ;
#65082=VERTEX_POINT ( 'NONE', #29303 ) ;
#65099=CARTESIAN_POINT ( 'NONE',  ( 6.627987042499408510, -6.376774720514424288, 21.45334999081212146 ) ) ;
#65103=VERTEX_POINT ( 'NONE', #98811 ) ;
#65105=VERTEX_POINT ( 'NONE', #22178 ) ;
#65111=CARTESIAN_POINT ( 'NONE',  ( -1.044871794871790938, -6.376774720514427841, 21.75000000000000355 ) ) ;
#65119=CARTESIAN_POINT ( 'NONE',  ( -5.576843645946834016, -6.376774720514418959, 20.41272575174755133 ) ) ;
#65127=VERTEX_POINT ( 'NONE', #84089 ) ;
#65136=CARTESIAN_POINT ( 'NONE',  ( -1.568769572606061535, -6.376774720514415407, 19.76359802465961835 ) ) ;
#65140=EDGE_CURVE ( 'NONE', #63171, #60621, #98586, .T. ) ;
#65162=DIRECTION ( 'NONE',  ( 1.000000000000000000, 0.000000000000000000, 0.000000000000000000 ) ) ;
#65163=DIRECTION ( 'NONE',  ( 0.000000000000000000, 0.000000000000000000, 1.000000000000000000 ) ) ;
#65167=CARTESIAN_POINT ( 'NONE',  ( 22.02124265030973760, 6.143225279485574397, 16.20402280011862217 ) ) ;
#65168=LINE ( 'NONE', #43800, #10699 ) ;
#65172=DIRECTION ( 'NONE',  ( 1.000000000000000000, 0.000000000000000000, 0.000000000000000000 ) ) ;
#65175=CARTESIAN_POINT ( 'NONE',  ( 10.86264265030973952, 5.965225279485574461, -28.05717073599341305 ) ) ;
#65179=CARTESIAN_POINT ( 'NONE',  ( -5.023036858974361252, -6.376774720514410077, 19.14743589743590846 ) ) ;
#65182=CARTESIAN_POINT ( 'NONE',  ( 14.76093561896378148, -3.316774720514426456, -26.55548769130088971 ) ) ;
#65189=DIRECTION ( 'NONE',  ( 0.7512896232465891000, 1.109416176496794925E-16, 0.6599726524652351767 ) ) ;
#65191=CARTESIAN_POINT ( 'NONE',  ( -4.930333147521421822, -5.876774720514410077, 19.46306892155547530 ) ) ;
#65194=ORIENTED_EDGE ( 'NONE', *, *, #9905, .T. ) ;
#65196=CARTESIAN_POINT ( 'NONE',  ( -29.49875734969025842, -0.3587747205144265483, 17.86602280011862476 ) ) ;
#65200=CARTESIAN_POINT ( 'NONE',  ( 29.77147767949874790, -5.356774720514425603, 26.15915692125051706 ) ) ;
#65208=CIRCLE ( 'NONE', #76456, 3.979149600822063704 ) ;
#65227=DIRECTION ( 'NONE',  ( 0.000000000000000000, 1.000000000000000000, 0.000000000000000000 ) ) ;
#65231=ORIENTED_EDGE ( 'NONE', *, *, #100148, .T. ) ;
#65232=AXIS2_PLACEMENT_3D ( 'NONE', #4481, #57770, #13563 ) ;
#65233=EDGE_LOOP ( 'NONE', ( #33878, #47143, #80403, #90230 ) ) ;
#65235=CARTESIAN_POINT ( 'NONE',  ( 31.31121903262429029, -5.174141622015902442, 0.9154248472334550746 ) ) ;
#65240=ORIENTED_EDGE ( 'NONE', *, *, #52760, .F. ) ;
#65246=CARTESIAN_POINT ( 'NONE',  ( 2.650685085285006348, -6.376774720514410077, 19.28073557658628445 ) ) ;
#65255=CARTESIAN_POINT ( 'NONE',  ( -20.27875734969026311, 6.143225279485574397, 26.25402280011862288 ) ) ;
#65260=AXIS2_PLACEMENT_3D ( 'NONE', #100248, #86552, #17037 ) ;
#65263=LINE ( 'NONE', #49019, #95267 ) ;
#65271=DIRECTION ( 'NONE',  ( 0.000000000000000000, -1.000000000000000000, 0.000000000000000000 ) ) ;
#65274=LINE ( 'NONE', #10446, #2633 ) ;
#65276=ADVANCED_FACE ( 'NONE', ( #96214 ), #19074, .T. ) ;
#65286=ORIENTED_EDGE ( 'NONE', *, *, #34116, .T. ) ;
#65292=ORIENTED_EDGE ( 'NONE', *, *, #71297, .F. ) ;
#65295=CARTESIAN_POINT ( 'NONE',  ( -27.13414387080440093, 5.965225279485594001, -10.21530720150730254 ) ) ;
#65307=DIRECTION ( 'NONE',  ( 0.000000000000000000, 1.000000000000000000, 0.000000000000000000 ) ) ;
#65312=CARTESIAN_POINT ( 'NONE',  ( -0.2200237740140755516, -6.376774720514408301, 19.17724329193115551 ) ) ;
#65318=AXIS2_PLACEMENT_3D ( 'NONE', #76506, #46086, #85634 ) ;
#65364=LINE ( 'NONE', #64868, #25715 ) ;
#65367=CARTESIAN_POINT ( 'NONE',  ( -4.141025641025642301, -6.376774720514408301, 19.19230769230769695 ) ) ;
#65369=LINE ( 'NONE', #73456, #3202 ) ;
#65370=VECTOR ( 'NONE', #34050, 1000.000000000000000 ) ;
#65393=EDGE_CURVE ( 'NONE', #34332, #8750, #16954, .T. ) ;
#65399=ORIENTED_EDGE ( 'NONE', *, *, #45299, .F. ) ;
#65406=DIRECTION ( 'NONE',  ( -0.000000000000000000, 0.000000000000000000, -1.000000000000000000 ) ) ;
#65411=CARTESIAN_POINT ( 'NONE',  ( -11.64875734969026233, 5.965225279485572685, 30.51402280011862089 ) ) ;
#65421=CARTESIAN_POINT ( 'NONE',  ( -9.278253834636473130, -5.876774720514426953, 18.21871304725684482 ) ) ;
#65426=DIRECTION ( 'NONE',  ( 0.000000000000000000, -1.000000000000000000, 0.000000000000000000 ) ) ;
#65440=DIRECTION ( 'NONE',  ( -0.9496245541219264785, 6.845827386180410961E-16, -0.3133898629642195011 ) ) ;
#65443=CARTESIAN_POINT ( 'NONE',  ( 7.166666666666668739, -5.876774720514419847, 20.78665865384614975 ) ) ;
#65444=ORIENTED_EDGE ( 'NONE', *, *, #60394, .T. ) ;
#65450=CARTESIAN_POINT ( 'NONE',  ( -8.978253834636468866, -5.876774720514426953, 18.51871304725684553 ) ) ;
#65462=DIRECTION ( 'NONE',  ( 2.504262461560503484E-15, -6.886721769291384876E-15, 1.000000000000000000 ) ) ;
#65463=CARTESIAN_POINT ( 'NONE',  ( 5.930937628982182908, -5.876774720514417183, 20.24478033514397524 ) ) ;
#65468=ORIENTED_EDGE ( 'NONE', *, *, #13711, .F. ) ;
#65477=DIRECTION ( 'NONE',  ( 2.417950247244706201E-16, -8.673617379884035472E-16, -1.000000000000000000 ) ) ;
#65494=CARTESIAN_POINT ( 'NONE',  ( 30.53060340732035982, 1.477225279485574028, 19.84760796525321425 ) ) ;
#65498=ORIENTED_EDGE ( 'NONE', *, *, #94038, .T. ) ;
#65499=CARTESIAN_POINT ( 'NONE',  ( 4.612744205187371271, -5.876774720514418959, 20.61169588237105188 ) ) ;
#65514=CARTESIAN_POINT ( 'NONE',  ( -10.37843575862113887, -5.356774720514428267, 27.71903885537846435 ) ) ;
#65517=ORIENTED_EDGE ( 'NONE', *, *, #53006, .T. ) ;
#65518=EDGE_CURVE ( 'NONE', #28958, #18679, #70750, .T. ) ;
#65520=CARTESIAN_POINT ( 'NONE',  ( 5.730633878096764278, -5.876774720514418959, 20.45679216967608838 ) ) ;
#65522=VERTEX_POINT ( 'NONE', #70246 ) ;
#65542=ORIENTED_EDGE ( 'NONE', *, *, #75476, .F. ) ;
#65554=DIRECTION ( 'NONE',  ( 0.09721092304694051167, 0.000000000000000000, -0.9952638024365005887 ) ) ;
#65557=ADVANCED_FACE ( 'NONE', ( #86964 ), #41815, .T. ) ;
#65565=EDGE_LOOP ( 'NONE', ( #77657, #7379, #21447, #89390 ) ) ;
#65566=ORIENTED_EDGE ( 'NONE', *, *, #72810, .F. ) ;
#65584=ORIENTED_EDGE ( 'NONE', *, *, #55124, .T. ) ;
#65589=ORIENTED_EDGE ( 'NONE', *, *, #3527, .F. ) ;
#65595=CARTESIAN_POINT ( 'NONE',  ( -19.77875734969026311, 6.143225279485574397, 27.35402280011862430 ) ) ;
#65597=CARTESIAN_POINT ( 'NONE',  ( 6.826756808399247589, -5.876774720514423400, 21.36722843294932161 ) ) ;
#65598=ORIENTED_EDGE ( 'NONE', *, *, #74789, .T. ) ;
#65603=ORIENTED_EDGE ( 'NONE', *, *, #54722, .F. ) ;
#65604=CARTESIAN_POINT ( 'NONE',  ( 30.53060340732036693, -5.278445918605220832, 6.049079371708084629 ) ) ;
#65607=LINE ( 'NONE', #57987, #41771 ) ;
#65616=CARTESIAN_POINT ( 'NONE',  ( -4.968349358974361252, -5.876774720514410077, 19.46153846153847056 ) ) ;
#65624=DIRECTION ( 'NONE',  ( 0.000000000000000000, 0.000000000000000000, -1.000000000000000000 ) ) ;
#65629=CARTESIAN_POINT ( 'NONE',  ( 30.61643171304413613, -3.478988201194511909, 27.37433008668280365 ) ) ;
#65635=CARTESIAN_POINT ( 'NONE',  ( 8.978253834636468866, -5.876774720514426953, 18.51871304725684553 ) ) ;
#65638=DIRECTION ( 'NONE',  ( 0.000000000000000000, 0.000000000000000000, 1.000000000000000000 ) ) ;
#65645=VERTEX_POINT ( 'NONE', #71756 ) ;
#65649=DIRECTION ( 'NONE',  ( -0.000000000000000000, 1.000000000000000000, -0.000000000000000000 ) ) ;
#65650=AXIS2_PLACEMENT_3D ( 'NONE', #88084, #10953, #64773 ) ;
#65651=CARTESIAN_POINT ( 'NONE',  ( 10.68713020350923060, -6.376774720514430506, -28.05292731626249392 ) ) ;
#65653=CARTESIAN_POINT ( 'NONE',  ( -6.901944873432418248, -5.876774720514410077, 19.15221817653406688 ) ) ;
#65657=CARTESIAN_POINT ( 'NONE',  ( 30.53060340732036337, -4.740660005057330650, -2.970021620632059101 ) ) ;
#65663=FACE_OUTER_BOUND ( 'NONE', #17876, .T. ) ;
#65675=ADVANCED_FACE ( 'NONE', ( #96577 ), #67732, .T. ) ;
#65680=LINE ( 'NONE', #88995, #31614 ) ;
#65684=LINE ( 'NONE', #42834, #68090 ) ;
#65685=DIRECTION ( 'NONE',  ( 1.000000000000000000, -1.988296846060374587E-13, 0.000000000000000000 ) ) ;
#65692=FACE_OUTER_BOUND ( 'NONE', #42514, .T. ) ;
#65705=VERTEX_POINT ( 'NONE', #82349 ) ;
#65720=DIRECTION ( 'NONE',  ( 0.7071067811865476838, 0.000000000000000000, -0.7071067811865474617 ) ) ;
#65731=DIRECTION ( 'NONE',  ( 0.000000000000000000, -1.000000000000000000, 0.000000000000000000 ) ) ;
#65732=VERTEX_POINT ( 'NONE', #27580 ) ;
#65744=ORIENTED_EDGE ( 'NONE', *, *, #90586, .T. ) ;
#65748=DIRECTION ( 'NONE',  ( 0.000000000000000000, 1.000000000000000000, 0.000000000000000000 ) ) ;
#65752=AXIS2_PLACEMENT_3D ( 'NONE', #48571, #40938, #79495 ) ;
#65759=CARTESIAN_POINT ( 'NONE',  ( -12.65407072091355722, -0.3587747205143968499, -26.15404995688569301 ) ) ;
#65763=CARTESIAN_POINT ( 'NONE',  ( 282.9764569301858046, 6.475225279485573360, 20.79159422840526616 ) ) ;
#65775=CARTESIAN_POINT ( 'NONE',  ( 3.160575456146155204, -6.376774720514408301, 18.86877352677795372 ) ) ;
#65784=CARTESIAN_POINT ( 'NONE',  ( -1.304987980769231948, -5.876774720514413630, 19.76512419871795245 ) ) ;
#65787=EDGE_CURVE ( 'NONE', #10045, #18831, #95343, .T. ) ;
#65802=CARTESIAN_POINT ( 'NONE',  ( 0.03625801282051022839, -5.876774720514410077, 19.27714342948718240 ) ) ;
#65803=VERTEX_POINT ( 'NONE', #63926 ) ;
#65804=CARTESIAN_POINT ( 'NONE',  ( 31.93426202889373400, -0.3587747205144265483, 6.907000118922838716 ) ) ;
#65806=ORIENTED_EDGE ( 'NONE', *, *, #64884, .T. ) ;
#65807=EDGE_LOOP ( 'NONE', ( #65240, #29352, #72448, #16676 ) ) ;
#65808=ORIENTED_EDGE ( 'NONE', *, *, #97937, .F. ) ;
#65823=ORIENTED_EDGE ( 'NONE', *, *, #25024, .T. ) ;
#65828=PLANE ( 'NONE',  #52002 ) ;
#65852=ADVANCED_FACE ( 'NONE', ( #2006 ), #51753, .F. ) ;
#65855=VERTEX_POINT ( 'NONE', #79614 ) ;
#65857=CARTESIAN_POINT ( 'NONE',  ( -7.318926569091948942, -5.876774720514417183, 20.09505574050193033 ) ) ;
#65861=EDGE_CURVE ( 'NONE', #56523, #13066, #41064, .T. ) ;
#65862=ORIENTED_EDGE ( 'NONE', *, *, #41198, .T. ) ;
#65864=DIRECTION ( 'NONE',  ( -1.000000000000000000, 0.000000000000000000, -0.000000000000000000 ) ) ;
#65875=EDGE_CURVE ( 'NONE', #67215, #21350, #72519, .T. ) ;
#65890=VECTOR ( 'NONE', #66873, 1000.000000000000000 ) ;
#65903=VECTOR ( 'NONE', #50309, 1000.000000000000000 ) ;
#65908=DIRECTION ( 'NONE',  ( 0.000000000000000000, -1.000000000000000000, 0.000000000000000000 ) ) ;
#65912=CARTESIAN_POINT ( 'NONE',  ( 4.038745349937860496, -6.376774720514429617, 21.81354843764681206 ) ) ;
#65913=FACE_OUTER_BOUND ( 'NONE', #49215, .T. ) ;
#65921=CARTESIAN_POINT ( 'NONE',  ( -0.02075734969026423599, -0.3587747205144213303, -0.08597719988137648983 ) ) ;
#65932=VECTOR ( 'NONE', #66436, 1000.000000000000000 ) ;
#65934=DIRECTION ( 'NONE',  ( 0.000000000000000000, -1.000000000000000000, 0.000000000000000000 ) ) ;
#65939=CARTESIAN_POINT ( 'NONE',  ( 6.429811694900724461, -5.876774720514425177, 21.48000018967326596 ) ) ;
#65945=CARTESIAN_POINT ( 'NONE',  ( 2.909586618535765723, -5.876774720514411854, 19.75512108203924200 ) ) ;
#65950=CARTESIAN_POINT ( 'NONE',  ( 10.22568704553358643, 6.475225279485576024, -27.02513721610328901 ) ) ;
#65951=EDGE_CURVE ( 'NONE', #12570, #95752, #57795, .T. ) ;
#65954=EDGE_CURVE ( 'NONE', #33122, #54335, #19208, .T. ) ;
#65961=CARTESIAN_POINT ( 'NONE',  ( 6.199338013146583393, -5.876774720514415407, 20.11757922567734980 ) ) ;
#65964=ORIENTED_EDGE ( 'NONE', *, *, #58819, .T. ) ;
#65974=VERTEX_POINT ( 'NONE', #81116 ) ;
#65976=CARTESIAN_POINT ( 'NONE',  ( 0.000000000000000000, -4.056774720514426669, 0.000000000000000000 ) ) ;
#65977=CARTESIAN_POINT ( 'NONE',  ( 2.611202098145462891, -6.376774720514420736, 20.45574432200782766 ) ) ;
#65979=AXIS2_PLACEMENT_3D ( 'NONE', #12739, #58938, #90874 ) ;
#65999=CARTESIAN_POINT ( 'NONE',  ( 4.647438682898014761, -5.876774720514418071, 20.26932200457894950 ) ) ;
#66002=CARTESIAN_POINT ( 'NONE',  ( -28.98875734969026041, -0.3587747205144262708, 15.62202280011862321 ) ) ;
#66010=AXIS2_PLACEMENT_3D ( 'NONE', #78767, #32106, #55462 ) ;
#66012=CARTESIAN_POINT ( 'NONE',  ( 0.000000000000000000, -5.876774720514426953, 0.000000000000000000 ) ) ;
#66013=CARTESIAN_POINT ( 'NONE',  ( -10.21384395349167562, -3.451719627175087179, 29.49402280011861777 ) ) ;
#66015=ADVANCED_FACE ( 'NONE', ( #20202 ), #58783, .T. ) ;
#66022=B_SPLINE_CURVE_WITH_KNOTS ( 'NONE', 3,
 ( #80155, #41606, #63279, #86588, #54161, #38414, #31300, #1370, #85585, #69367, #77956, #23678, #78465, #6969 ),
 .UNSPECIFIED., .F., .F.,
 ( 4, 2, 2, 1, 1, 2, 2, 4 ),
 ( 0.000000000000000000, 0.2500000000000028311, 0.3750000000000009992, 0.4374999999999976130, 0.4687499999999932276, 0.4843749999999957256, 0.4999999999999982236, 1.000000000000000000 ),
 .UNSPECIFIED. ) ;
#66023=CARTESIAN_POINT ( 'NONE',  ( 6.110660513271839456, -6.376774720514422512, 21.43053473047838509 ) ) ;
#66025=CARTESIAN_POINT ( 'NONE',  ( 32.53135143123563466, 5.965225279485572685, 6.926385399448451885 ) ) ;
#66028=CARTESIAN_POINT ( 'NONE',  ( 13.57581083383196940, -5.876774720514426953, 20.21213203435597094 ) ) ;
#66035=CARTESIAN_POINT ( 'NONE',  ( -24.57525087998973845, 5.965225279485572685, -15.45548830044932309 ) ) ;
#66037=DIRECTION ( 'NONE',  ( -0.000000000000000000, 1.000000000000000000, -0.000000000000000000 ) ) ;
#66040=CARTESIAN_POINT ( 'NONE',  ( -20.27875734969026311, 6.143225279485574397, 24.00402280011862288 ) ) ;
#66042=ORIENTED_EDGE ( 'NONE', *, *, #68576, .T. ) ;
#66047=CARTESIAN_POINT ( 'NONE',  ( 22.02124265030973760, 7.743225279485574042, 17.60402280011862075 ) ) ;
#66063=B_SPLINE_CURVE_WITH_KNOTS ( 'NONE', 3,
 ( #48748, #79670, #10169, #13148, #74072, #14148, #75543, #76046, #91285, #52232, #82173, #20261, #43123, #5543, #12156, #20759, #4565, #59851, #35513 ),
 .UNSPECIFIED., .F., .F.,
 ( 4, 1, 1, 1, 1, 1, 1, 1, 1, 1, 1, 1, 1, 1, 1, 1, 4 ),
 ( 0.000000000000000000, 0.07560433049574548370, 0.1479650154827359954, 0.2187969985237009085, 0.2894704453213758910, 0.3597242180874983819, 0.4297077387530445769, 0.5004965198485837874, 0.5744290198679491422, 0.6139472962286710578, 0.6571552698261118319, 0.7039727697209380297, 0.7549389848168008843, 0.8097066112894878431, 0.8688329536985502921, 0.9323854739325977414, 1.000000000000000000 ),
 .UNSPECIFIED. ) ;
#66067=CARTESIAN_POINT ( 'NONE',  ( 15.01911467442479875, -4.015204461132630520, -28.37592028203562933 ) ) ;
#66087=CYLINDRICAL_SURFACE ( 'NONE', #79827, 2.040000000000000036 ) ;
#66100=ADVANCED_FACE ( 'NONE', ( #22691, #68885 ), #5986, .T. ) ;
#66104=ORIENTED_EDGE ( 'NONE', *, *, #87344, .T. ) ;
#66107=CARTESIAN_POINT ( 'NONE',  ( 30.53060340732035982, -5.168677327241859132, 8.808792533107787648 ) ) ;
#66108=DIRECTION ( 'NONE',  ( -0.000000000000000000, -1.000000000000000000, -0.000000000000000000 ) ) ;
#66128=ORIENTED_EDGE ( 'NONE', *, *, #6946, .F. ) ;
#66130=CARTESIAN_POINT ( 'NONE',  ( 2.903846153846159517, -5.876774720514415407, 19.99999999999999289 ) ) ;
#66137=CARTESIAN_POINT ( 'NONE',  ( -27.96875734969026084, 6.143225279485574397, 23.50402280011861933 ) ) ;
#66140=LINE ( 'NONE', #49908, #44548 ) ;
#66145=ORIENTED_EDGE ( 'NONE', *, *, #7752, .F. ) ;
#66151=CARTESIAN_POINT ( 'NONE',  ( 10.68713020350585197, -3.316774720514176877, -28.05292731652309257 ) ) ;
#66153=DIRECTION ( 'NONE',  ( 0.000000000000000000, -1.000000000000000000, 0.000000000000000000 ) ) ;
#66163=CARTESIAN_POINT ( 'NONE',  ( 6.420673076923079314, -6.376774720514427841, 21.83974358974358765 ) ) ;
#66165=TOROIDAL_SURFACE ( 'NONE', #11033, 25.90800000000000125, 2.040000000000000036 ) ;
#66169=CARTESIAN_POINT ( 'NONE',  ( -1.836964591723098117, -5.876774720514409189, 19.23384392940399223 ) ) ;
#66175=AXIS2_PLACEMENT_3D ( 'NONE', #40601, #2045, #64963 ) ;
#66179=ORIENTED_EDGE ( 'NONE', *, *, #86875, .F. ) ;
#66192=DIRECTION ( 'NONE',  ( 0.000000000000000000, 1.478457507934778393E-16, -1.000000000000000000 ) ) ;
#66193=CARTESIAN_POINT ( 'NONE',  ( 0.3910256410256418014, -6.376774720514418959, 20.67377804487179915 ) ) ;
#66195=CYLINDRICAL_SURFACE ( 'NONE', #5926, 0.3000000000000016542 ) ;
#66199=CARTESIAN_POINT ( 'NONE',  ( 3.063121397228215859, -5.876774720514420736, 20.95210102656095685 ) ) ;
#66200=EDGE_CURVE ( 'NONE', #69513, #77700, #45229, .T. ) ;
#66204=CARTESIAN_POINT ( 'NONE',  ( 30.53060340732035982, -1.682774720514426114, -1.272392034746785860 ) ) ;
#66223=VERTEX_POINT ( 'NONE', #69389 ) ;
#66231=CARTESIAN_POINT ( 'NONE',  ( -10.24059822343757808, -5.876774720514426953, 22.08128695274315945 ) ) ;
#66234=DIRECTION ( 'NONE',  ( 0.000000000000000000, 0.000000000000000000, -1.000000000000000000 ) ) ;
#66242=EDGE_CURVE ( 'NONE', #40322, #26067, #30661, .T. ) ;
#66252=EDGE_CURVE ( 'NONE', #87707, #43715, #6326, .T. ) ;
#66261=CARTESIAN_POINT ( 'NONE',  ( -4.213970605900704491, -5.876774720514416295, 20.02963804100705758 ) ) ;
#66267=DIRECTION ( 'NONE',  ( -0.06486421869277853025, 0.000000000000000000, 0.9978940991575084851 ) ) ;
#66269=DIRECTION ( 'NONE',  ( 0.000000000000000000, 0.000000000000000000, -1.000000000000000000 ) ) ;
#66278=CARTESIAN_POINT ( 'NONE',  ( 26.37445894957760473, 1.477225279485574028, -11.69480419648520986 ) ) ;
#66281=ORIENTED_EDGE ( 'NONE', *, *, #14774, .F. ) ;
#66296=DIRECTION ( 'NONE',  ( 0.000000000000000000, -1.000000000000000000, 0.000000000000000000 ) ) ;
#66298=DIRECTION ( 'NONE',  ( -2.682707457723910108E-15, 0.000000000000000000, -1.000000000000000000 ) ) ;
#66311=DIRECTION ( 'NONE',  ( 0.000000000000000000, 0.000000000000000000, 1.000000000000000000 ) ) ;
#66319=ORIENTED_EDGE ( 'NONE', *, *, #12471, .T. ) ;
#66325=ORIENTED_EDGE ( 'NONE', *, *, #52356, .F. ) ;
#66326=ADVANCED_FACE ( 'NONE', ( #23198 ), #8985, .T. ) ;
#66327=CARTESIAN_POINT ( 'NONE',  ( -29.49875734969026198, 5.965225279485572685, 0.1180228001186258285 ) ) ;
#66329=VERTEX_POINT ( 'NONE', #78990 ) ;
#66337=ORIENTED_EDGE ( 'NONE', *, *, #86197, .F. ) ;
#66338=EDGE_CURVE ( 'NONE', #49051, #66356, #62802, .T. ) ;
#66347=AXIS2_PLACEMENT_3D ( 'NONE', #6199, #97551, #43777 ) ;
#66350=ORIENTED_EDGE ( 'NONE', *, *, #11572, .T. ) ;
#66355=DIRECTION ( 'NONE',  ( 0.000000000000000000, 0.000000000000000000, 1.000000000000000000 ) ) ;
#66356=VERTEX_POINT ( 'NONE', #40449 ) ;
#66357=CARTESIAN_POINT ( 'NONE',  ( -5.238752036864926964, -6.376774720514410077, 19.51517878119694061 ) ) ;
#66358=CARTESIAN_POINT ( 'NONE',  ( 0.000000000000000000, 1.477225279485574028, 19.84760796525321425 ) ) ;
#66363=CARTESIAN_POINT ( 'NONE',  ( -0.5830141525297981575, -6.376774720514411854, 19.15054976246387497 ) ) ;
#66373=AXIS2_PLACEMENT_3D ( 'NONE', #52730, #12658, #30382 ) ;
#66381=LINE ( 'NONE', #97310, #65890 ) ;
#66385=VECTOR ( 'NONE', #70516, 1000.000000000000000 ) ;
#66386=ORIENTED_EDGE ( 'NONE', *, *, #81764, .T. ) ;
#66388=VECTOR ( 'NONE', #20313, 1000.000000000000000 ) ;
#66400=EDGE_CURVE ( 'NONE', #25949, #58927, #25170, .T. ) ;
#66401=DIRECTION ( 'NONE',  ( -0.000000000000000000, -1.000000000000000000, -0.000000000000000000 ) ) ;
#66404=CARTESIAN_POINT ( 'NONE',  ( 5.654871928786437074, -6.376774720514420736, 20.64717925217163952 ) ) ;
#66405=EDGE_CURVE ( 'NONE', #20944, #63660, #32326, .T. ) ;
#66406=EDGE_CURVE ( 'NONE', #8499, #15369, #64961, .T. ) ;
#66411=PLANE ( 'NONE',  #971 ) ;
#66414=LINE ( 'NONE', #19695, #18794 ) ;
#66419=CARTESIAN_POINT ( 'NONE',  ( 10.54059822343757880, -5.876774720514426953, 23.12308057603841149 ) ) ;
#66425=ORIENTED_EDGE ( 'NONE', *, *, #46680, .T. ) ;
#66428=EDGE_CURVE ( 'NONE', #84887, #38539, #33282, .T. ) ;
#66430=CARTESIAN_POINT ( 'NONE',  ( 15.14080536460164517, -5.152774720514427642, -26.62908960815038384 ) ) ;
#66436=DIRECTION ( 'NONE',  ( -0.000000000000000000, 0.000000000000000000, -1.000000000000000000 ) ) ;
#66440=CARTESIAN_POINT ( 'NONE',  ( 6.403846153846157740, -5.876774720514425177, 21.48076923076922995 ) ) ;
#66454=CARTESIAN_POINT ( 'NONE',  ( 8.205893897551582938, 6.475225279485575136, -27.11136772256261196 ) ) ;
#66466=CYLINDRICAL_SURFACE ( 'NONE', #29665, 0.3000000000000016542 ) ;
#66476=ADVANCED_FACE ( 'NONE', ( #34833 ), #45881, .T. ) ;
#66481=CARTESIAN_POINT ( 'NONE',  ( 2.880689065218799083, -6.376774720514426065, 21.31732089891691828 ) ) ;
#66496=DIRECTION ( 'NONE',  ( 4.838869102739856157E-16, 0.000000000000000000, -1.000000000000000000 ) ) ;
#66502=CARTESIAN_POINT ( 'NONE',  ( -25.92875734969026524, -5.356774720514425603, -0.08597719988137648983 ) ) ;
#66516=VERTEX_POINT ( 'NONE', #3398 ) ;
#66519=VECTOR ( 'NONE', #35713, 1000.000000000000000 ) ;
#66520=CARTESIAN_POINT ( 'NONE',  ( 5.696197030082937651, -5.876774720514421624, 21.05387829558662816 ) ) ;
#66522=ORIENTED_EDGE ( 'NONE', *, *, #72539, .F. ) ;
#66525=LINE ( 'NONE', #46157, #48359 ) ;
#66527=DIRECTION ( 'NONE',  ( -0.000000000000000000, -1.000000000000000000, -0.000000000000000000 ) ) ;
#66534=EDGE_CURVE ( 'NONE', #9124, #40720, #36472, .T. ) ;
#66535=EDGE_CURVE ( 'NONE', #88108, #98244, #4111, .T. ) ;
#66536=VECTOR ( 'NONE', #17152, 1000.000000000000000 ) ;
#66537=LINE ( 'NONE', #41174, #6460 ) ;
#66540=VECTOR ( 'NONE', #50421, 1000.000000000000000 ) ;
#66541=EDGE_CURVE ( 'NONE', #69177, #67333, #10546, .T. ) ;
#66571=CARTESIAN_POINT ( 'NONE',  ( 14.43441819133218296, -3.316774720514428232, -28.36222020317221038 ) ) ;
#66574=ORIENTED_EDGE ( 'NONE', *, *, #25073, .T. ) ;
#66578=ADVANCED_FACE ( 'NONE', ( #36827 ), #90113, .F. ) ;
#66585=ORIENTED_EDGE ( 'NONE', *, *, #36513, .T. ) ;
#66601=CARTESIAN_POINT ( 'NONE',  ( 29.62646972375975096, -5.339663449004302009, 28.46301402826327731 ) ) ;
#66620=CARTESIAN_POINT ( 'NONE',  ( 4.261846905714947731, -5.876774720514426953, 21.73176331363731251 ) ) ;
#66633=CARTESIAN_POINT ( 'NONE',  ( -1.428094109758638819, -6.376774720514415407, 20.04104409779160179 ) ) ;
#66647=PLANE ( 'NONE',  #27892 ) ;
#66648=EDGE_CURVE ( 'NONE', #96543, #14119, #67271, .T. ) ;
#66651=CARTESIAN_POINT ( 'NONE',  ( 11.40529837385589218, -6.376774720514345240, -28.07356074678033409 ) ) ;
#66654=EDGE_CURVE ( 'NONE', #31048, #47313, #85144, .T. ) ;
#66660=CARTESIAN_POINT ( 'NONE',  ( 6.274899854645557440, -6.376774720514429617, 21.83451738260096775 ) ) ;
#66661=ORIENTED_EDGE ( 'NONE', *, *, #42349, .F. ) ;
#66667=DIRECTION ( 'NONE',  ( 0.000000000000000000, 0.000000000000000000, -1.000000000000000000 ) ) ;
#66679=DIRECTION ( 'NONE',  ( 0.000000000000000000, -1.000000000000000000, 0.000000000000000000 ) ) ;
#66696=CARTESIAN_POINT ( 'NONE',  ( 29.76209104404536987, -5.356774720514427379, 26.42884784083909366 ) ) ;
#66697=DIRECTION ( 'NONE',  ( 0.000000000000000000, -1.000000000000000000, 0.000000000000000000 ) ) ;
#66700=DIRECTION ( 'NONE',  ( 0.000000000000000000, 1.000000000000000000, -0.000000000000000000 ) ) ;
#66715=FACE_OUTER_BOUND ( 'NONE', #98924, .T. ) ;
#66722=CARTESIAN_POINT ( 'NONE',  ( 9.940598223437577374, -5.876774720514426953, 22.08128695274315945 ) ) ;
#66723=VERTEX_POINT ( 'NONE', #62669 ) ;
#66725=ORIENTED_EDGE ( 'NONE', *, *, #48073, .T. ) ;
#66730=CARTESIAN_POINT ( 'NONE',  ( 30.61643171304412903, -3.316774720514426456, 27.37433008668283207 ) ) ;
#66738=CARTESIAN_POINT ( 'NONE',  ( 2.932009311892267434, -5.876774720514410077, 19.53174284846577891 ) ) ;
#66739=CARTESIAN_POINT ( 'NONE',  ( 2.677564053859940341, -5.876774720514407413, 19.16116138973293559 ) ) ;
#66751=CARTESIAN_POINT ( 'NONE',  ( 0.000000000000000000, -6.376774720514426953, 15.00000000000000178 ) ) ;
#66754=PLANE ( 'NONE',  #32087 ) ;
#66755=DIRECTION ( 'NONE',  ( 0.6599726524652365089, 0.000000000000000000, -0.7512896232465879898 ) ) ;
#66757=CARTESIAN_POINT ( 'NONE',  ( 0.000000000000000000, -5.876774720514426953, 0.000000000000000000 ) ) ;
#66771=CARTESIAN_POINT ( 'NONE',  ( 3.051095722660301934, -6.376774720514410077, 19.07493897947323092 ) ) ;
#66773=CARTESIAN_POINT ( 'NONE',  ( 7.460332110455646593, -6.376774720514418959, 20.55293369838740247 ) ) ;
#66786=CARTESIAN_POINT ( 'NONE',  ( 0.3910256410256418569, -5.876774720514419847, 20.67377804487180271 ) ) ;
#66793=VERTEX_POINT ( 'NONE', #94092 ) ;
#66794=CARTESIAN_POINT ( 'NONE',  ( -27.96875734969026084, 6.143225279485574397, 24.50402280011861933 ) ) ;
#66797=CARTESIAN_POINT ( 'NONE',  ( 29.73860345376319003, -5.356471260711259674, 19.84760796525321425 ) ) ;
#66798=ORIENTED_EDGE ( 'NONE', *, *, #95878, .F. ) ;
#66803=EDGE_LOOP ( 'NONE', ( #98858, #41713, #96924, #60226 ) ) ;
#66804=ORIENTED_EDGE ( 'NONE', *, *, #46440, .F. ) ;
#66806=DIRECTION ( 'NONE',  ( 0.7071067811865476838, 0.000000000000000000, -0.7071067811865474617 ) ) ;
#66812=EDGE_CURVE ( 'NONE', #47230, #92103, #70520, .T. ) ;
#66815=CARTESIAN_POINT ( 'NONE',  ( -5.265981236333618470E-16, -2.056774720514426669, -4.299999999999999822 ) ) ;
#66823=ADVANCED_FACE ( 'NONE', ( #86486, #7861 ), #16970, .F. ) ;
#66832=DIRECTION ( 'NONE',  ( 0.000000000000000000, 0.000000000000000000, 1.000000000000000000 ) ) ;
#66839=ORIENTED_EDGE ( 'NONE', *, *, #26105, .F. ) ;
#66841=CARTESIAN_POINT ( 'NONE',  ( -10.12789510953808758, -4.109924279452578766, 30.41617935552199370 ) ) ;
#66852=FACE_OUTER_BOUND ( 'NONE', #11248, .T. ) ;
#66858=CARTESIAN_POINT ( 'NONE',  ( -0.8460708837923186509, -6.376774720514411854, 19.21968329462762526 ) ) ;
#66869=ORIENTED_EDGE ( 'NONE', *, *, #20827, .F. ) ;
#66871=CARTESIAN_POINT ( 'NONE',  ( 10.59058046163345423, -3.703784075859317682, -26.99573265033922453 ) ) ;
#66873=DIRECTION ( 'NONE',  ( -0.000000000000000000, 1.000000000000000000, -0.000000000000000000 ) ) ;
#66880=ADVANCED_FACE ( 'NONE', ( #93090 ), #23573, .T. ) ;
#66885=DIRECTION ( 'NONE',  ( 1.000000000000000000, 0.000000000000000000, 0.000000000000000000 ) ) ;
#66886=AXIS2_PLACEMENT_3D ( 'NONE', #10431, #40392, #80449 ) ;
#66890=DIRECTION ( 'NONE',  ( 0.000000000000000000, 1.000000000000000000, 0.000000000000000000 ) ) ;
#66891=AXIS2_PLACEMENT_3D ( 'NONE', #80421, #1306, #47478 ) ;
#66895=CARTESIAN_POINT ( 'NONE',  ( 0.000000000000000000, -5.876774720514426953, 0.000000000000000000 ) ) ;
#66899=CARTESIAN_POINT ( 'NONE',  ( 3.362030615038681169, -6.376774720514424288, 21.34376340489846413 ) ) ;
#66903=DIRECTION ( 'NONE',  ( 0.000000000000000000, 0.000000000000000000, 1.000000000000000000 ) ) ;
#66909=DIRECTION ( 'NONE',  ( 0.000000000000000000, -1.000000000000000000, 0.000000000000000000 ) ) ;
#66910=CARTESIAN_POINT ( 'NONE',  ( 0.000000000000000000, 1.477225279485574028, 19.84760796525321425 ) ) ;
#66939=FACE_OUTER_BOUND ( 'NONE', #58194, .T. ) ;
#66940=EDGE_LOOP ( 'NONE', ( #100389, #61461, #35981, #67721 ) ) ;
#66946=CARTESIAN_POINT ( 'NONE',  ( 6.431189903846153300, -5.876774720514415407, 20.08974358974358765 ) ) ;
#66949=LINE ( 'NONE', #36476, #49178 ) ;
#66958=VECTOR ( 'NONE', #99640, 1000.000000000000000 ) ;
#66965=DIRECTION ( 'NONE',  ( -0.000000000000000000, -1.000000000000000000, -0.000000000000000000 ) ) ;
#66967=CARTESIAN_POINT ( 'NONE',  ( -0.9988807608215116707, -5.876774720514410966, 19.30497968945844889 ) ) ;
#66977=EDGE_CURVE ( 'NONE', #55307, #78770, #65680, .T. ) ;
#66982=CARTESIAN_POINT ( 'NONE',  ( 30.77564450787169292, -1.682774720514426114, -9.689394075852828081 ) ) ;
#66991=EDGE_CURVE ( 'NONE', #95233, #90367, #51432, .T. ) ;
#67008=CARTESIAN_POINT ( 'NONE',  ( 5.864225667603142789, -5.876774720514423400, 21.27837265517432996 ) ) ;
#67013=FACE_OUTER_BOUND ( 'NONE', #57065, .T. ) ;
#67015=DIRECTION ( 'NONE',  ( 0.000000000000000000, 1.000000000000000000, 0.000000000000000000 ) ) ;
#67017=EDGE_CURVE ( 'NONE', #25101, #53541, #90979, .T. ) ;
#67022=ADVANCED_FACE ( 'NONE', ( #5743 ), #51931, .F. ) ;
#67039=DIRECTION ( 'NONE',  ( -1.000000000000000000, 0.000000000000000000, 1.895872651340772790E-16 ) ) ;
#67043=EDGE_LOOP ( 'NONE', ( #66350, #70473 ) ) ;
#67044=VERTEX_POINT ( 'NONE', #21448 ) ;
#67049=LINE ( 'NONE', #74145, #56041 ) ;
#67051=ORIENTED_EDGE ( 'NONE', *, *, #6852, .T. ) ;
#67053=ORIENTED_EDGE ( 'NONE', *, *, #73786, .T. ) ;
#67054=CARTESIAN_POINT ( 'NONE',  ( 1.305682803664691249, 5.965225279485572685, 29.57950906855421991 ) ) ;
#67056=CARTESIAN_POINT ( 'NONE',  ( 14.62889129739783556, -4.326482771707137687, -28.09837290214700545 ) ) ;
#67059=ORIENTED_EDGE ( 'NONE', *, *, #66252, .F. ) ;
#67070=VECTOR ( 'NONE', #78989, 1000.000000000000000 ) ;
#67073=DIRECTION ( 'NONE',  ( 0.000000000000000000, -1.000000000000000000, 0.000000000000000000 ) ) ;
#67077=VERTEX_POINT ( 'NONE', #67663 ) ;
#67083=FACE_OUTER_BOUND ( 'NONE', #44518, .T. ) ;
#67087=CARTESIAN_POINT ( 'NONE',  ( 29.58888977143521970, -4.303425171653743497, 29.06172452911802750 ) ) ;
#67100=DIRECTION ( 'NONE',  ( 8.334928612639484546E-17, -1.000000000000000000, 7.321843366904296032E-17 ) ) ;
#67104=VERTEX_POINT ( 'NONE', #36204 ) ;
#67107=CARTESIAN_POINT ( 'NONE',  ( 31.59111626279633711, -6.376774720514426953, 16.27760796525321751 ) ) ;
#67126=CARTESIAN_POINT ( 'NONE',  ( -6.815415664272417295, -6.376774720514410077, 19.46427715384223234 ) ) ;
#67135=DIRECTION ( 'NONE',  ( -0.7071067811865507924, -0.000000000000000000, -0.7071067811865442421 ) ) ;
#67136=CARTESIAN_POINT ( 'NONE',  ( 4.647438682898014761, -5.876774720514417183, 20.26932200457894950 ) ) ;
#67146=CARTESIAN_POINT ( 'NONE',  ( -1.428094109758638819, -6.376774720514415407, 20.04104409779160179 ) ) ;
#67148=CARTESIAN_POINT ( 'NONE',  ( -2.243088942307695177, -5.876774720514409189, 19.14743589743590491 ) ) ;
#67149=CARTESIAN_POINT ( 'NONE',  ( 5.864177746775673050, -5.876774720514425177, 21.69926562011473337 ) ) ;
#67163=DIRECTION ( 'NONE',  ( 0.000000000000000000, 0.000000000000000000, 1.000000000000000000 ) ) ;
#67166=VERTEX_POINT ( 'NONE', #71150 ) ;
#67189=VECTOR ( 'NONE', #88223, 1000.000000000000000 ) ;
#67198=EDGE_CURVE ( 'NONE', #12570, #65127, #83546, .T. ) ;
#67199=LINE ( 'NONE', #52962, #20518 ) ;
#67202=CARTESIAN_POINT ( 'NONE',  ( 7.275731542451676859, -6.376774720514415407, 20.06332870126568224 ) ) ;
#67208=CARTESIAN_POINT ( 'NONE',  ( -27.25988310792305214, 5.965225279485572685, 30.32664379231667695 ) ) ;
#67210=VERTEX_POINT ( 'NONE', #22937 ) ;
#67211=AXIS2_PLACEMENT_3D ( 'NONE', #34845, #12497, #97733 ) ;
#67212=ADVANCED_FACE ( 'NONE', ( #55428 ), #25249, .T. ) ;
#67214=VERTEX_POINT ( 'NONE', #15339 ) ;
#67215=VERTEX_POINT ( 'NONE', #7229 ) ;
#67217=FACE_OUTER_BOUND ( 'NONE', #28341, .T. ) ;
#67228=FACE_OUTER_BOUND ( 'NONE', #53338, .T. ) ;
#67234=AXIS2_PLACEMENT_3D ( 'NONE', #48147, #47646, #80082 ) ;
#67252=LINE ( 'NONE', #36297, #91271 ) ;
#67253=EDGE_CURVE ( 'NONE', #50923, #71272, #18714, .T. ) ;
#67254=CARTESIAN_POINT ( 'NONE',  ( -1.041963229364719634, -6.376774720514417183, 20.24089781925592746 ) ) ;
#67255=CARTESIAN_POINT ( 'NONE',  ( -28.98875734969026396, 5.965225279485572685, 0.1180228001186258285 ) ) ;
#67265=CARTESIAN_POINT ( 'NONE',  ( -0.3544984435505275644, -5.876774720514409189, 19.15251819062245531 ) ) ;
#67269=CARTESIAN_POINT ( 'NONE',  ( -0.02075734969026423599, 5.965225279485572685, -0.08597719988137648983 ) ) ;
#67271=CIRCLE ( 'NONE', #23482, 3.060000000000000053 ) ;
#67277=DIRECTION ( 'NONE',  ( 0.000000000000000000, 0.000000000000000000, -1.000000000000000000 ) ) ;
#67290=VERTEX_POINT ( 'NONE', #47311 ) ;
#67293=LINE ( 'NONE', #82990, #58318 ) ;
#67296=ORIENTED_EDGE ( 'NONE', *, *, #99355, .F. ) ;
#67297=CARTESIAN_POINT ( 'NONE',  ( -2.959136224476847765, -6.376774720514413630, 19.53857357749110335 ) ) ;
#67299=LINE ( 'NONE', #73414, #51350 ) ;
#67306=VERTEX_POINT ( 'NONE', #41203 ) ;
#67307=LINE ( 'NONE', #58691, #83160 ) ;
#67316=CARTESIAN_POINT ( 'NONE',  ( -22.05275734969026047, 5.965225279485572685, 31.02402280011862246 ) ) ;
#67321=EDGE_CURVE ( 'NONE', #20076, #92445, #75425, .T. ) ;
#67327=ORIENTED_EDGE ( 'NONE', *, *, #16312, .T. ) ;
#67328=EDGE_CURVE ( 'NONE', #69030, #75743, #42712, .T. ) ;
#67331=VECTOR ( 'NONE', #32691, 1000.000000000000000 ) ;
#67332=CARTESIAN_POINT ( 'NONE',  ( 13.91401389203221406, -6.376774720514426953, 158.0376437107427137 ) ) ;
#67333=VERTEX_POINT ( 'NONE', #71649 ) ;
#67339=VECTOR ( 'NONE', #34737, 1000.000000000000000 ) ;
#67342=DIRECTION ( 'NONE',  ( 0.000000000000000000, -0.000000000000000000, 1.000000000000000000 ) ) ;
#67350=CARTESIAN_POINT ( 'NONE',  ( -2.599001758237162285, -6.376774720514413630, 19.60308799987317485 ) ) ;
#67351=DIRECTION ( 'NONE',  ( -1.709749016398430297E-16, -0.7071067811865436870, 0.7071067811865513475 ) ) ;
#67364=DIRECTION ( 'NONE',  ( 0.000000000000000000, 0.000000000000000000, 1.000000000000000000 ) ) ;
#67368=CARTESIAN_POINT ( 'NONE',  ( -4.495793269230770939, -6.376774720514410077, 19.27714342948718595 ) ) ;
#67369=EDGE_CURVE ( 'NONE', #55695, #25101, #47852, .T. ) ;
#67378=ORIENTED_EDGE ( 'NONE', *, *, #74616, .T. ) ;
#67389=CARTESIAN_POINT ( 'NONE',  ( 3.206569032998081603, -6.376774720514424288, 21.19686455982786200 ) ) ;
#67397=CARTESIAN_POINT ( 'NONE',  ( 6.830155907162054341, -5.876774720514427841, 21.76451523534627341 ) ) ;
#67401=DIRECTION ( 'NONE',  ( -8.503546450866701308E-16, 0.000000000000000000, 1.000000000000000000 ) ) ;
#67402=DIRECTION ( 'NONE',  ( 1.000000000000000000, -4.015979463811607402E-15, 0.000000000000000000 ) ) ;
#67403=ORIENTED_EDGE ( 'NONE', *, *, #38222, .F. ) ;
#67417=CARTESIAN_POINT ( 'NONE',  ( -29.49875734969026198, -0.3587747205144262708, 0.1180228001186258285 ) ) ;
#67418=AXIS2_PLACEMENT_3D ( 'NONE', #66895, #73996, #51658 ) ;
#67428=ORIENTED_EDGE ( 'NONE', *, *, #65951, .T. ) ;
#67437=CARTESIAN_POINT ( 'NONE',  ( 5.730633878096764278, -6.376774720514418959, 20.45679216967608838 ) ) ;
#67439=CARTESIAN_POINT ( 'NONE',  ( 13.91401389203221406, 5.965225279485572685, 158.0376437107427137 ) ) ;
#67448=EDGE_LOOP ( 'NONE', ( #58998, #86652 ) ) ;
#67457=EDGE_CURVE ( 'NONE', #55194, #69943, #67049, .T. ) ;
#67460=DIRECTION ( 'NONE',  ( -0.000000000000000000, -1.000000000000000000, -0.000000000000000000 ) ) ;
#67461=VECTOR ( 'NONE', #79959, 1000.000000000000000 ) ;
#67462=CARTESIAN_POINT ( 'NONE',  ( -5.576923076923076650, -6.376774720514418959, 20.44941907051282470 ) ) ;
#67467=CARTESIAN_POINT ( 'NONE',  ( 30.93860345374796594, 6.475225279485571583, 13.17908622612278435 ) ) ;
#67471=ORIENTED_EDGE ( 'NONE', *, *, #97259, .F. ) ;
#67475=DIRECTION ( 'NONE',  ( -0.000000000000000000, 1.000000000000000000, -0.000000000000000000 ) ) ;
#67476=AXIS2_PLACEMENT_3D ( 'NONE', #41334, #72289, #96607 ) ;
#67480=CARTESIAN_POINT ( 'NONE',  ( -5.891303133519534718, -6.376774720514420736, 20.71116975788854475 ) ) ;
#67486=VECTOR ( 'NONE', #63903, 1000.000000000000000 ) ;
#67491=EDGE_CURVE ( 'NONE', #7626, #8365, #19837, .T. ) ;
#67492=ORIENTED_EDGE ( 'NONE', *, *, #1100, .F. ) ;
#67496=CARTESIAN_POINT ( 'NONE',  ( 33.62498039757826263, -3.398310449788993104, -11.43903334445280784 ) ) ;
#67508=AXIS2_PLACEMENT_3D ( 'NONE', #75385, #99705, #68289 ) ;
#67513=CARTESIAN_POINT ( 'NONE',  ( 5.920986267150416538, -5.876774720514422512, 21.32549308339960348 ) ) ;
#67515=EDGE_CURVE ( 'NONE', #64622, #50083, #88822, .T. ) ;
#67518=CARTESIAN_POINT ( 'NONE',  ( 5.399550031317769339, 5.965225279485594001, -28.54570968858208246 ) ) ;
#67521=ORIENTED_EDGE ( 'NONE', *, *, #60163, .T. ) ;
#67524=EDGE_CURVE ( 'NONE', #36701, #24606, #74632, .T. ) ;
#67525=ORIENTED_EDGE ( 'NONE', *, *, #64606, .T. ) ;
#67528=VECTOR ( 'NONE', #46999, 1000.000000000000000 ) ;
#67532=ORIENTED_EDGE ( 'NONE', *, *, #74195, .F. ) ;
#67534=ORIENTED_EDGE ( 'NONE', *, *, #14202, .F. ) ;
#67539=VERTEX_POINT ( 'NONE', #45695 ) ;
#67540=CARTESIAN_POINT ( 'NONE',  ( 6.763596848542221984, -6.376774720514426065, 21.40271460634751577 ) ) ;
#67541=CARTESIAN_POINT ( 'NONE',  ( 2.745953332610513442, -5.876774720514418959, 21.05053573504278575 ) ) ;
#67543=VECTOR ( 'NONE', #4155, 1000.000000000000000 ) ;
#67552=EDGE_LOOP ( 'NONE', ( #83486, #11232, #21560, #21383 ) ) ;
#67558=CARTESIAN_POINT ( 'NONE',  ( 6.403846153846157740, -6.376774720514426065, 21.48076923076922995 ) ) ;
#67559=ORIENTED_EDGE ( 'NONE', *, *, #19602, .F. ) ;
#67564=CARTESIAN_POINT ( 'NONE',  ( -10.54059822343757880, -6.376774720514426953, 23.12308057603841149 ) ) ;
#67569=ORIENTED_EDGE ( 'NONE', *, *, #12545, .T. ) ;
#67572=PLANE ( 'NONE',  #48143 ) ;
#67574=CARTESIAN_POINT ( 'NONE',  ( 14.61581677259038692, -3.466180823938291855, -27.35847992067005308 ) ) ;
#67578=ORIENTED_EDGE ( 'NONE', *, *, #59922, .F. ) ;
#67582=ADVANCED_FACE ( 'NONE', ( #62937 ), #80605, .T. ) ;
#67595=ORIENTED_EDGE ( 'NONE', *, *, #42113, .F. ) ;
#67609=CARTESIAN_POINT ( 'NONE',  ( 33.61456970919605425, -3.316774720514426900, -11.35828564741663449 ) ) ;
#67618=LINE ( 'NONE', #89942, #67783 ) ;
#67619=AXIS2_PLACEMENT_3D ( 'NONE', #19751, #58349, #21250 ) ;
#67627=DIRECTION ( 'NONE',  ( 2.615445361545220718E-15, -6.974520964120588319E-15, 1.000000000000000000 ) ) ;
#67629=LINE ( 'NONE', #12816, #70233 ) ;
#67633=CARTESIAN_POINT ( 'NONE',  ( -1.456683411003494966, -5.876774720514415407, 19.95737465391042775 ) ) ;
#67639=ORIENTED_EDGE ( 'NONE', *, *, #47363, .F. ) ;
#67643=ADVANCED_FACE ( 'NONE', ( #25351 ), #75811, .T. ) ;
#67644=VECTOR ( 'NONE', #87781, 1000.000000000000000 ) ;
#67647=EDGE_CURVE ( 'NONE', #5613, #26949, #54850, .T. ) ;
#67654=VECTOR ( 'NONE', #57869, 1000.000000000000000 ) ;
#67655=CARTESIAN_POINT ( 'NONE',  ( 30.55456828421202076, 1.252966014080275192, 24.28055799599968623 ) ) ;
#67660=DIRECTION ( 'NONE',  ( 0.000000000000000000, 0.000000000000000000, 1.000000000000000000 ) ) ;
#67661=DIRECTION ( 'NONE',  ( 0.000000000000000000, -1.000000000000000000, 0.000000000000000000 ) ) ;
#67662=ORIENTED_EDGE ( 'NONE', *, *, #37901, .F. ) ;
#67663=CARTESIAN_POINT ( 'NONE',  ( 25.61870917940689196, -0.3587747205144265483, 29.49402280011862487 ) ) ;
#67671=EDGE_CURVE ( 'NONE', #54031, #75907, #10839, .T. ) ;
#67679=DIRECTION ( 'NONE',  ( 0.000000000000000000, 0.000000000000000000, 1.000000000000000000 ) ) ;
#67682=VERTEX_POINT ( 'NONE', #37045 ) ;
#67690=AXIS2_PLACEMENT_3D ( 'NONE', #51923, #91459, #99067 ) ;
#67696=CARTESIAN_POINT ( 'NONE',  ( 31.88667425545053291, -2.682774720514426559, -9.651215965565024035 ) ) ;
#67717=CARTESIAN_POINT ( 'NONE',  ( 30.59918777245023236, -5.333550415411136392, 26.68477081578061316 ) ) ;
#67718=CARTESIAN_POINT ( 'NONE',  ( 29.64064043116815128, 6.475225279485573360, 28.71191112024341408 ) ) ;
#67721=ORIENTED_EDGE ( 'NONE', *, *, #16659, .F. ) ;
#67723=LINE ( 'NONE', #35269, #92486 ) ;
#67726=CARTESIAN_POINT ( 'NONE',  ( 3.787259615384621636, -6.376774720514404748, 18.51923076923076650 ) ) ;
#67732=B_SPLINE_SURFACE_WITH_KNOTS ( 'NONE', 3, 1, ( 
 ( #48922, #87471 ),
 ( #2748, #11838 ),
 ( #3749, #95084 ),
 ( #25569, #72762 ),
 ( #95581, #56540 ),
 ( #10346, #72259 ),
 ( #80357, #49933 ),
 ( #73742, #26070 ),
 ( #11349, #42323 ),
 ( #17961, #57542 ),
 ( #18953, #34690 ),
 ( #58041, #50416 ),
 ( #32679, #94580 ),
 ( #25061, #59526 ),
 ( #66163, #60032 ) ),
 .UNSPECIFIED., .F., .F., .F.,
 ( 4, 1, 1, 1, 1, 1, 1, 1, 1, 1, 1, 1, 4 ),
 ( 2, 2 ),
 ( 0.000000000000000000, 0.08436071833182734458, 0.1674897660598589910, 0.2505333068873835112, 0.3353998789434969874, 0.4196274113919481463, 0.5021719904600034923, 0.5840851136372724461, 0.6672595181981534340, 0.7504339227590341999, 0.8329476815839259585, 0.9156652780073727405, 1.000000000000000000 ),
 ( 0.000000000000000000, 1.000000000000000000 ),
 .UNSPECIFIED. ) ;
#67739=CARTESIAN_POINT ( 'NONE',  ( -32.30247028140506416, 5.965225279485572685, 27.60502002861223048 ) ) ;
#67746=FACE_OUTER_BOUND ( 'NONE', #57939, .T. ) ;
#67747=CARTESIAN_POINT ( 'NONE',  ( -4.165021623707020559, -5.876774720514418071, 20.26087634804756377 ) ) ;
#67753=VECTOR ( 'NONE', #34784, 1000.000000000000000 ) ;
#67754=DIRECTION ( 'NONE',  ( -0.000000000000000000, -1.000000000000000000, -0.000000000000000000 ) ) ;
#67759=CIRCLE ( 'NONE', #82300, 2.500000000000465405 ) ;
#67779=CARTESIAN_POINT ( 'NONE',  ( -0.4362980769230789257, -5.876774720514411854, 19.46153846153846345 ) ) ;
#67783=VECTOR ( 'NONE', #68113, 1000.000000000000000 ) ;
#67793=CARTESIAN_POINT ( 'NONE',  ( 4.642799911345256270, -6.376774720514408301, 18.59646607068888713 ) ) ;
#67798=VERTEX_POINT ( 'NONE', #68006 ) ;
#67804=VERTEX_POINT ( 'NONE', #10334 ) ;
#67805=CARTESIAN_POINT ( 'NONE',  ( -0.4686347352592966087, -5.876774720514411854, 19.46274624311237034 ) ) ;
#67814=ORIENTED_EDGE ( 'NONE', *, *, #31333, .F. ) ;
#67815=CARTESIAN_POINT ( 'NONE',  ( 4.451706829556401956, -6.376774720514406525, 18.91922570401084513 ) ) ;
#67816=EDGE_LOOP ( 'NONE', ( #65468, #77351, #39223 ) ) ;
#67818=CARTESIAN_POINT ( 'NONE',  ( 30.52397162719526946, -4.695236745772901621, 19.84760796525321425 ) ) ;
#67842=ORIENTED_EDGE ( 'NONE', *, *, #97339, .T. ) ;
#67843=EDGE_LOOP ( 'NONE', ( #84770, #53205, #25737 ) ) ;
#67844=CARTESIAN_POINT ( 'NONE',  ( -5.154768636056045850, -6.376774720514413630, 19.48351902941045921 ) ) ;
#67851=CARTESIAN_POINT ( 'NONE',  ( -2.794644232660540961, -6.376774720514415407, 20.26757654895259009 ) ) ;
#67857=CYLINDRICAL_SURFACE ( 'NONE', #5339, 0.8160000000000007248 ) ;
#67861=DIRECTION ( 'NONE',  ( 0.000000000000000000, 1.000000000000000000, 0.000000000000000000 ) ) ;
#67866=CARTESIAN_POINT ( 'NONE',  ( -4.495793269230770939, -6.376774720514410077, 19.27714342948718595 ) ) ;
#67871=CARTESIAN_POINT ( 'NONE',  ( 14.61581670307174008, -6.376774720514426953, -27.35847990810646024 ) ) ;
#67872=CARTESIAN_POINT ( 'NONE',  ( 3.632573734185411851, -6.376774720514429617, 21.82795992345630509 ) ) ;
#67877=DIRECTION ( 'NONE',  ( -0.000000000000000000, -0.000000000000000000, 1.000000000000000000 ) ) ;
#67886=EDGE_CURVE ( 'NONE', #6280, #27797, #99751, .T. ) ;
#67889=CIRCLE ( 'NONE', #75968, 1.325999999999990298 ) ;
#67895=CARTESIAN_POINT ( 'NONE',  ( -5.457842845122470976, -6.376774720514410077, 19.25892998154168367 ) ) ;
#67903=LINE ( 'NONE', #61788, #49520 ) ;
#67907=PLANE ( 'NONE',  #95550 ) ;
#67909=AXIS2_PLACEMENT_3D ( 'NONE', #87226, #17723, #48691 ) ;
#67911=ORIENTED_EDGE ( 'NONE', *, *, #75212, .F. ) ;
#67934=CARTESIAN_POINT ( 'NONE',  ( 4.190829928318763109, -5.876774720514399419, 18.23548058298382557 ) ) ;
#67960=CARTESIAN_POINT ( 'NONE',  ( 10.46399479596396453, -2.682774720514426559, -27.03001098546561920 ) ) ;
#67968=AXIS2_PLACEMENT_3D ( 'NONE', #79733, #63536, #16331 ) ;
#67970=AXIS2_PLACEMENT_3D ( 'NONE', #65921, #51675, #67402 ) ;
#67995=CARTESIAN_POINT ( 'NONE',  ( 32.98371819488264833, -4.742969794006914874, -11.67826368001470172 ) ) ;
#67997=B_SPLINE_SURFACE_WITH_KNOTS ( 'NONE', 3, 1, ( 
 ( #11971, #66786 ),
 ( #3879, #97703 ),
 ( #28198, #12956 ),
 ( #43925, #50050 ),
 ( #34817, #84473 ),
 ( #60660, #61162 ),
 ( #84967, #83470 ),
 ( #6358, #6849 ),
 ( #29690, #52534 ),
 ( #53542, #14953 ),
 ( #37804, #69754 ),
 ( #45432, #15453 ),
 ( #92574, #30684 ),
 ( #75854, #92081 ),
 ( #54529, #61655 ),
 ( #53043, #83973 ),
 ( #23052, #22551 ),
 ( #13957, #5855 ),
 ( #75355, #67779 ) ),
 .UNSPECIFIED., .F., .F., .F.,
 ( 4, 1, 1, 1, 1, 1, 1, 1, 1, 1, 1, 1, 1, 1, 1, 1, 4 ),
 ( 2, 2 ),
 ( 0.000000000000000000, 0.06976287284686377710, 0.1345149942976648916, 0.1951193525406907936, 0.2509143402908634579, 0.3026968495153156136, 0.3502960464810115360, 0.3933858467586648366, 0.4329734110072616105, 0.5070892430766307246, 0.5787491638444315356, 0.6502280224451015833, 0.7224618180302719850, 0.7938856428547010902, 0.8631290414909040809, 0.9313229315869651082, 1.000000000000000000 ),
 ( 0.000000000000000000, 1.000000000000000000 ),
 .UNSPECIFIED. ) ;
#67999=CARTESIAN_POINT ( 'NONE',  ( -29.49875734969026198, 5.965225279485572685, 2.362022800118626531 ) ) ;
#68006=CARTESIAN_POINT ( 'NONE',  ( -4.141025641025642301, -5.876774720514412742, 19.63681891025641235 ) ) ;
#68009=EDGE_CURVE ( 'NONE', #56523, #47938, #52779, .T. ) ;
#68013=CARTESIAN_POINT ( 'NONE',  ( 6.251785340501501587, -5.876774720514423400, 21.46941214867599612 ) ) ;
#68015=VECTOR ( 'NONE', #95292, 1000.000000000000000 ) ;
#68019=VECTOR ( 'NONE', #3406, 1000.000000000000114 ) ;
#68024=CARTESIAN_POINT ( 'NONE',  ( 13.91401389203221406, 5.965225279485572685, 158.0376437107427137 ) ) ;
#68034=ORIENTED_EDGE ( 'NONE', *, *, #11150, .T. ) ;
#68037=AXIS2_PLACEMENT_3D ( 'NONE', #65111, #40745, #88426 ) ;
#68039=ORIENTED_EDGE ( 'NONE', *, *, #74397, .T. ) ;
#68043=ORIENTED_EDGE ( 'NONE', *, *, #81458, .T. ) ;
#68044=CARTESIAN_POINT ( 'NONE',  ( 30.57061049414810228, 4.696956328126698388, 25.28683757526521703 ) ) ;
#68046=FACE_OUTER_BOUND ( 'NONE', #41965, .T. ) ;
#68058=EDGE_LOOP ( 'NONE', ( #92615, #29792, #83198, #67559 ) ) ;
#68059=EDGE_LOOP ( 'NONE', ( #76835, #39595, #62922, #92594, #19720, #4100 ) ) ;
#68061=EDGE_CURVE ( 'NONE', #65082, #95862, #31432, .T. ) ;
#68065=DIRECTION ( 'NONE',  ( 0.000000000000000000, 0.000000000000000000, -1.000000000000000000 ) ) ;
#68080=VECTOR ( 'NONE', #24086, 1000.000000000000000 ) ;
#68081=FACE_OUTER_BOUND ( 'NONE', #27039, .T. ) ;
#68089=DIRECTION ( 'NONE',  ( -2.417950247244706201E-16, 0.000000000000000000, 1.000000000000000000 ) ) ;
#68090=VECTOR ( 'NONE', #65189, 1000.000000000000227 ) ;
#68098=CARTESIAN_POINT ( 'NONE',  ( 29.57907552799942508, -3.316774720514426456, 29.21818156447043791 ) ) ;
#68109=DIRECTION ( 'NONE',  ( -0.000000000000000000, 1.000000000000000000, -0.000000000000000000 ) ) ;
#68113=DIRECTION ( 'NONE',  ( -0.7689940216596065081, 4.164321980682960499E-15, 0.6392559695863502256 ) ) ;
#68117=ADVANCED_FACE ( 'NONE', ( #55286 ), #71507, .T. ) ;
#68120=ORIENTED_EDGE ( 'NONE', *, *, #19012, .F. ) ;
#68126=EDGE_CURVE ( 'NONE', #36399, #35863, #9596, .T. ) ;
#68128=CARTESIAN_POINT ( 'NONE',  ( -1.428094109758638819, -5.876774720514415407, 20.04104409779160179 ) ) ;
#68129=CARTESIAN_POINT ( 'NONE',  ( -6.775140224358976226, -6.376774720514408301, 19.14743589743590846 ) ) ;
#68130=CARTESIAN_POINT ( 'NONE',  ( 0.3627416911114360598, -5.876774720514411854, 19.59793130852656873 ) ) ;
#68137=ORIENTED_EDGE ( 'NONE', *, *, #55055, .F. ) ;
#68139=CARTESIAN_POINT ( 'NONE',  ( -1.390986686320385468, -6.376774720514413630, 19.62288733224860948 ) ) ;
#68142=PLANE ( 'NONE',  #67690 ) ;
#68148=EDGE_LOOP ( 'NONE', ( #54905, #68173, #58218, #12787 ) ) ;
#68149=CARTESIAN_POINT ( 'NONE',  ( 27.53860345374808105, 1.477225279485574028, -1.272392034746785860 ) ) ;
#68151=DIRECTION ( 'NONE',  ( -1.000000000000000000, -0.000000000000000000, 0.000000000000000000 ) ) ;
#68152=CARTESIAN_POINT ( 'NONE',  ( 31.27206728860909024, -4.132774720514318822, -3.930752063305056332 ) ) ;
#68153=VERTEX_POINT ( 'NONE', #24810 ) ;
#68156=DIRECTION ( 'NONE',  ( 0.000000000000000000, 0.000000000000000000, -1.000000000000000000 ) ) ;
#68164=DIRECTION ( 'NONE',  ( 0.000000000000000000, -1.000000000000000000, 0.000000000000000000 ) ) ;
#68165=CARTESIAN_POINT ( 'NONE',  ( -17.66201745896767505, -6.376774720514425177, -23.06272557202527906 ) ) ;
#68169=CARTESIAN_POINT ( 'NONE',  ( 6.546094359317672584, -6.376774720514411854, 19.73546617144828375 ) ) ;
#68173=ORIENTED_EDGE ( 'NONE', *, *, #11745, .F. ) ;
#68187=CARTESIAN_POINT ( 'NONE',  ( -0.4909855769230799249, -6.376774720514410077, 19.14743589743590491 ) ) ;
#68195=VERTEX_POINT ( 'NONE', #57295 ) ;
#68196=DIRECTION ( 'NONE',  ( 0.000000000000000000, 0.000000000000000000, -1.000000000000000000 ) ) ;
#68203=EDGE_CURVE ( 'NONE', #31070, #3112, #46319, .T. ) ;
#68210=ORIENTED_EDGE ( 'NONE', *, *, #72583, .F. ) ;
#68211=LINE ( 'NONE', #51990, #13472 ) ;
#68212=CARTESIAN_POINT ( 'NONE',  ( 2.790451961050095520, -6.376774720514408301, 18.85195250256714417 ) ) ;
#68232=DIRECTION ( 'NONE',  ( -0.000000000000000000, 0.000000000000000000, -1.000000000000000000 ) ) ;
#68235=CARTESIAN_POINT ( 'NONE',  ( 13.10664265030973930, 5.965225279485574461, -28.64597719988137570 ) ) ;
#68237=EDGE_CURVE ( 'NONE', #1158, #92467, #95990, .T. ) ;
#68241=VECTOR ( 'NONE', #62116, 1000.000000000000114 ) ;
#68242=CARTESIAN_POINT ( 'NONE',  ( -1.044871794871793602, -6.376774720514418959, 20.44941907051282115 ) ) ;
#68246=EDGE_CURVE ( 'NONE', #24236, #54115, #21187, .T. ) ;
#68256=ADVANCED_FACE ( 'NONE', ( #12077 ), #41557, .F. ) ;
#68259=ADVANCED_FACE ( 'NONE', ( #20688 ), #28810, .T. ) ;
#68277=ORIENTED_EDGE ( 'NONE', *, *, #84330, .F. ) ;
#68287=CARTESIAN_POINT ( 'NONE',  ( -2.285970405126252825, -5.876774720514407413, 19.14905311829361167 ) ) ;
#68289=DIRECTION ( 'NONE',  ( 0.000000000000000000, 0.000000000000000000, 1.000000000000000000 ) ) ;
#68301=ORIENTED_EDGE ( 'NONE', *, *, #55778, .T. ) ;
#68309=LINE ( 'NONE', #99240, #30294 ) ;
#68315=ORIENTED_EDGE ( 'NONE', *, *, #14124, .T. ) ;
#68319=CARTESIAN_POINT ( 'NONE',  ( -10.13340495651384288, -4.304508339349029988, 30.35717091805029355 ) ) ;
#68324=EDGE_CURVE ( 'NONE', #54335, #70415, #44737, .T. ) ;
#68336=CARTESIAN_POINT ( 'NONE',  ( 0.000000000000000000, -5.356774720514425603, 6.000000000000000888 ) ) ;
#68338=PLANE ( 'NONE',  #74983 ) ;
#68341=CARTESIAN_POINT ( 'NONE',  ( -2.750773227259631692, -5.876774720514411854, 19.84584863393302001 ) ) ;
#68348=PLANE ( 'NONE',  #3688 ) ;
#68355=EDGE_CURVE ( 'NONE', #55838, #7066, #8471, .T. ) ;
#68356=CARTESIAN_POINT ( 'NONE',  ( -0.02075734969026423599, -3.316774720514426456, -29.05397719988137339 ) ) ;
#68358=CARTESIAN_POINT ( 'NONE',  ( -4.886549725601808447, -6.376774720514410077, 19.15251819062245175 ) ) ;
#68372=CARTESIAN_POINT ( 'NONE',  ( 31.13513474936814163, -4.540774720514427543, 3.331262582247520143 ) ) ;
#68379=CIRCLE ( 'NONE', #8474, 4.299999999999999822 ) ;
#68383=CARTESIAN_POINT ( 'NONE',  ( -5.837039262820512775, -6.376774720514413630, 19.76512419871795245 ) ) ;
#68392=CARTESIAN_POINT ( 'NONE',  ( -29.49875734969026198, 5.965225279485572685, 7.870022800118625206 ) ) ;
#68422=ORIENTED_EDGE ( 'NONE', *, *, #7526, .T. ) ;
#68423=CARTESIAN_POINT ( 'NONE',  ( 4.531089049250198286, -6.376774720514404748, 18.46391971337801508 ) ) ;
#68430=CARTESIAN_POINT ( 'NONE',  ( 5.696197030082937651, -6.376774720514422512, 21.05387829558662816 ) ) ;
#68435=VECTOR ( 'NONE', #68745, 1000.000000000000000 ) ;
#68438=LINE ( 'NONE', #98372, #58641 ) ;
#68441=LINE ( 'NONE', #53727, #78968 ) ;
#68444=CARTESIAN_POINT ( 'NONE',  ( -0.02075734969026423599, -5.356774720514425603, -0.08597719988137648983 ) ) ;
#68446=CARTESIAN_POINT ( 'NONE',  ( -0.7614568544629641833, -5.876774720514408301, 19.18727597066020962 ) ) ;
#68472=CIRCLE ( 'NONE', #81439, 1.399999999999988143 ) ;
#68496=CARTESIAN_POINT ( 'NONE',  ( 5.184553252003285984, 5.965225279485572685, -28.06387035751381731 ) ) ;
#68506=EDGE_CURVE ( 'NONE', #20975, #48508, #87093, .T. ) ;
#68512=ORIENTED_EDGE ( 'NONE', *, *, #5711, .F. ) ;
#68515=ORIENTED_EDGE ( 'NONE', *, *, #6222, .T. ) ;
#68518=B_SPLINE_CURVE_WITH_KNOTS ( 'NONE', 3,
 ( #98159, #30657, #15920, #61628, #46888, #63629, #69728, #8318, #24034, #47890, #206, #1715, #15422, #23019, #32651, #92548, #63124, #78316, #71227, #54008, #31151, #56011, #85945 ),
 .UNSPECIFIED., .F., .F.,
 ( 4, 1, 1, 1, 1, 1, 1, 1, 1, 1, 1, 1, 1, 1, 1, 1, 1, 1, 1, 1, 4 ),
 ( 0.000000000000000000, 0.07295106587586808189, 0.1415836941865457888, 0.2059264601708682696, 0.2653013571846069008, 0.3205972327139294809, 0.3718165030988108688, 0.4187897697094533633, 0.4616987286157644976, 0.5021335821035667335, 0.5408043152926478303, 0.5781805253279665990, 0.6142968652075149194, 0.6496782432647882910, 0.6842994600896379342, 0.7183589527723613921, 0.7520808646475963810, 0.8176524386023853452, 0.8797220764054369813, 0.9399655597309874988, 1.000000000000000000 ),
 .UNSPECIFIED. ) ;
#68519=VECTOR ( 'NONE', #60752, 1000.000000000000000 ) ;
#68530=CARTESIAN_POINT ( 'NONE',  ( -4.495793269230770939, -6.376774720514410077, 19.27714342948718595 ) ) ;
#68531=CARTESIAN_POINT ( 'NONE',  ( 3.714529970114099022, -5.876774720514425177, 21.83853177191107520 ) ) ;
#68551=VERTEX_POINT ( 'NONE', #33301 ) ;
#68561=CARTESIAN_POINT ( 'NONE',  ( -4.926336369345164279, 5.965225279485592225, -28.61095484066304451 ) ) ;
#68568=ADVANCED_FACE ( 'NONE', ( #80478 ), #49548, .F. ) ;
#68576=EDGE_CURVE ( 'NONE', #34762, #93291, #26616, .T. ) ;
#68577=CARTESIAN_POINT ( 'NONE',  ( -29.49875734969025842, -0.3587747205144265483, 25.61802280011862720 ) ) ;
#68586=DIRECTION ( 'NONE',  ( -0.000000000000000000, -1.000000000000000000, -0.000000000000000000 ) ) ;
#68590=DIRECTION ( 'NONE',  ( 0.000000000000000000, -1.000000000000000000, 0.000000000000000000 ) ) ;
#68600=ORIENTED_EDGE ( 'NONE', *, *, #24774, .F. ) ;
#68602=CARTESIAN_POINT ( 'NONE',  ( -1.394533802543915124, -6.376774720514413630, 20.19722303762275573 ) ) ;
#68604=PLANE ( 'NONE',  #68766 ) ;
#68605=CARTESIAN_POINT ( 'NONE',  ( -7.326923076923076650, -6.376774720514417183, 20.36318108974359831 ) ) ;
#68620=CARTESIAN_POINT ( 'NONE',  ( -1.358974358974357921, -6.376774720514420736, 20.75510817307693046 ) ) ;
#68624=CARTESIAN_POINT ( 'NONE',  ( 0.1309051665272248643, -5.876774720514413630, 19.34190049657482291 ) ) ;
#68627=( BOUNDED_SURFACE ( )  B_SPLINE_SURFACE ( 3, 2, ( 
 ( #54359, #45736, #91898 ),
 ( #38619, #84287, #69579 ),
 ( #6666, #83790, #14269 ),
 ( #6169, #60482, #37620 ) ),
 .UNSPECIFIED., .F., .F., .T. ) 
 B_SPLINE_SURFACE_WITH_KNOTS ( ( 4, 4 ),
 ( 3, 3 ),
 ( 0.004439845973569162343, 0.004703938444645663561 ),
 ( 0.000000000000000000, 1.000000000000000000 ),
 .UNSPECIFIED. ) 
 GEOMETRIC_REPRESENTATION_ITEM ( )  RATIONAL_B_SPLINE_SURFACE ( (
 ( 1.000000000000000000, 0.9005394799515968884, 1.000000000000000000),
 ( 1.000000000000000000, 0.9005352985759393913, 1.000000000000000000),
 ( 1.000000000000000000, 0.8990570573199260229, 1.000000000000000000),
 ( 1.000000000000000000, 0.8962098481621323387, 1.000000000000000000) ) ) 
 REPRESENTATION_ITEM ( '' )  SURFACE ( )  );
#68633=CARTESIAN_POINT ( 'NONE',  ( 282.9764569301858046, -0.6647747205144264315, 20.79159422840526616 ) ) ;
#68636=CARTESIAN_POINT ( 'NONE',  ( -10.54059822343757880, -6.376774720514426953, 22.82308057603841078 ) ) ;
#68647=VERTEX_POINT ( 'NONE', #4858 ) ;
#68653=ORIENTED_EDGE ( 'NONE', *, *, #44528, .T. ) ;
#68668=CARTESIAN_POINT ( 'NONE',  ( 6.666194146093591399, -6.376774720514413630, 19.75460921626947908 ) ) ;
#68670=ORIENTED_EDGE ( 'NONE', *, *, #54318, .T. ) ;
#68681=CARTESIAN_POINT ( 'NONE',  ( -7.024122139145243082, -6.376774720514408301, 19.17707164986947532 ) ) ;
#68694=VERTEX_POINT ( 'NONE', #65784 ) ;
#68696=EDGE_CURVE ( 'NONE', #40720, #6280, #58157, .T. ) ;
#68699=CARTESIAN_POINT ( 'NONE',  ( 10.54059822343757880, -5.876774720514426953, 22.82308057603841078 ) ) ;
#68709=DIRECTION ( 'NONE',  ( 0.000000000000000000, 0.000000000000000000, 1.000000000000000000 ) ) ;
#68710=ADVANCED_FACE ( 'NONE', ( #73869 ), #90094, .F. ) ;
#68711=ORIENTED_EDGE ( 'NONE', *, *, #28062, .T. ) ;
#68714=DIRECTION ( 'NONE',  ( -0.000000000000000000, 1.000000000000000000, -0.000000000000000000 ) ) ;
#68726=DIRECTION ( 'NONE',  ( -0.000000000000000000, -1.000000000000000000, -0.000000000000000000 ) ) ;
#68734=EDGE_CURVE ( 'NONE', #95233, #20446, #98248, .T. ) ;
#68739=EDGE_CURVE ( 'NONE', #62167, #65645, #986, .T. ) ;
#68741=CARTESIAN_POINT ( 'NONE',  ( -2.104002878010082789, -6.376774720514410077, 19.15289935703627222 ) ) ;
#68745=DIRECTION ( 'NONE',  ( -0.000000000000000000, 1.000000000000000000, -0.000000000000000000 ) ) ;
#68748=ORIENTED_EDGE ( 'NONE', *, *, #79350, .F. ) ;
#68755=ORIENTED_EDGE ( 'NONE', *, *, #11150, .F. ) ;
#68756=CARTESIAN_POINT ( 'NONE',  ( -10.58858228176428540, -0.3587747205144061202, -27.03148018517017803 ) ) ;
#68761=CARTESIAN_POINT ( 'NONE',  ( -3.826923076923074429, -6.376774720514427841, 21.75000000000000355 ) ) ;
#68766=AXIS2_PLACEMENT_3D ( 'NONE', #7189, #61500, #21902 ) ;
#68773=DIRECTION ( 'NONE',  ( 0.000000000000000000, 0.000000000000000000, 1.000000000000000000 ) ) ;
#68784=CARTESIAN_POINT ( 'NONE',  ( -3.103301570662693187, -5.876774720514418071, 20.14409848895067512 ) ) ;
#68790=CARTESIAN_POINT ( 'NONE',  ( -4.141439336867657417, -6.376774720514418959, 20.56083401959468304 ) ) ;
#68796=ORIENTED_EDGE ( 'NONE', *, *, #48598, .T. ) ;
#68797=CARTESIAN_POINT ( 'NONE',  ( 4.413617546364139166, -6.376774720514406525, 18.86076033669171181 ) ) ;
#68800=ORIENTED_EDGE ( 'NONE', *, *, #59642, .F. ) ;
#68807=DIRECTION ( 'NONE',  ( -0.000000000000000000, 1.000000000000000000, -0.000000000000000000 ) ) ;
#68810=ORIENTED_EDGE ( 'NONE', *, *, #27450, .T. ) ;
#68818=ADVANCED_FACE ( 'NONE', ( #100165 ), #29187, .F. ) ;
#68823=ORIENTED_EDGE ( 'NONE', *, *, #87484, .F. ) ;
#68829=CARTESIAN_POINT ( 'NONE',  ( 15.32643653063177958, -2.682774720514426559, -27.14485409495429380 ) ) ;
#68836=CARTESIAN_POINT ( 'NONE',  ( 29.73860345376319003, -4.772774720514425972, -8.849814207987163783 ) ) ;
#68840=PLANE ( 'NONE',  #94602 ) ;
#68845=LINE ( 'NONE', #29778, #24745 ) ;
#68860=CARTESIAN_POINT ( 'NONE',  ( 3.714529970114099022, -5.876774720514426065, 21.83853177191107520 ) ) ;
#68863=CARTESIAN_POINT ( 'NONE',  ( 27.53860345374771867, -4.772774720514425972, -9.482392034746242260 ) ) ;
#68868=CARTESIAN_POINT ( 'NONE',  ( 30.09341516180546350, 1.477225279485574028, -11.39311774897855933 ) ) ;
#68873=CARTESIAN_POINT ( 'NONE',  ( 4.127614219445591814, -5.876774720514408301, 18.60403502951120558 ) ) ;
#68880=CARTESIAN_POINT ( 'NONE',  ( -5.755030174389611730, -5.876774720514410077, 19.56655654527324728 ) ) ;
#68885=FACE_OUTER_BOUND ( 'NONE', #60051, .T. ) ;
#68886=ORIENTED_EDGE ( 'NONE', *, *, #12306, .T. ) ;
#68888=ORIENTED_EDGE ( 'NONE', *, *, #2603, .F. ) ;
#68917=CARTESIAN_POINT ( 'NONE',  ( 4.531089049250198286, -5.876774720514402972, 18.46391971337801508 ) ) ;
#68927=DIRECTION ( 'NONE',  ( -0.06283980576413537855, 0.000000000000000000, -0.9980236263794188822 ) ) ;
#68933=ADVANCED_FACE ( 'NONE', ( #47918 ), #55538, .T. ) ;
#68941=FACE_OUTER_BOUND ( 'NONE', #56173, .T. ) ;
#68943=CARTESIAN_POINT ( 'NONE',  ( -0.4909855769230799249, -5.876774720514410077, 19.14743589743590491 ) ) ;
#68950=CARTESIAN_POINT ( 'NONE',  ( 10.46399479596398052, -3.316774720514422903, -27.03001098546561209 ) ) ;
#68956=DIRECTION ( 'NONE',  ( -0.000000000000000000, -1.000000000000000000, -0.000000000000000000 ) ) ;
#68958=LINE ( 'NONE', #22262, #14640 ) ;
#68967=CARTESIAN_POINT ( 'NONE',  ( -5.891025641025639636, -5.876774720514419847, 20.75510817307693046 ) ) ;
#68976=ORIENTED_EDGE ( 'NONE', *, *, #73723, .T. ) ;
#68980=VECTOR ( 'NONE', #62162, 1000.000000000000000 ) ;
#68986=VECTOR ( 'NONE', #51848, 1000.000000000000000 ) ;
#68988=VECTOR ( 'NONE', #93904, 1000.000000000000000 ) ;
#68991=AXIS2_PLACEMENT_3D ( 'NONE', #98989, #90394, #29479 ) ;
#68993=VERTEX_POINT ( 'NONE', #63150 ) ;
#69015=DIRECTION ( 'NONE',  ( 0.000000000000000000, 0.000000000000000000, -1.000000000000000000 ) ) ;
#69016=EDGE_CURVE ( 'NONE', #9746, #3529, #79351, .T. ) ;
#69030=VERTEX_POINT ( 'NONE', #3258 ) ;
#69036=DIRECTION ( 'NONE',  ( 0.000000000000000000, -1.000000000000000000, 0.000000000000000000 ) ) ;
#69054=AXIS2_PLACEMENT_3D ( 'NONE', #41156, #57396, #72109 ) ;
#69055=CARTESIAN_POINT ( 'NONE',  ( 2.903846153846159517, -5.876774720514415407, 19.99999999999999289 ) ) ;
#69057=CARTESIAN_POINT ( 'NONE',  ( 29.73860345376319358, -5.356774720514427379, 1.647607965253214957 ) ) ;
#69060=AXIS2_PLACEMENT_3D ( 'NONE', #38628, #68586, #7173 ) ;
#69061=DIRECTION ( 'NONE',  ( 0.000000000000000000, -1.000000000000000000, 0.000000000000000000 ) ) ;
#69069=EDGE_CURVE ( 'NONE', #67077, #75528, #65168, .T. ) ;
#69075=CARTESIAN_POINT ( 'NONE',  ( 0.000000000000000000, -5.876774720514426953, 0.000000000000000000 ) ) ;
#69085=ORIENTED_EDGE ( 'NONE', *, *, #1726, .T. ) ;
#69096=CARTESIAN_POINT ( 'NONE',  ( 0.3910256410256441884, -5.876774720514426953, 21.75000000000000000 ) ) ;
#69106=DIRECTION ( 'NONE',  ( 0.1827036106964188000, -3.614007241618350743E-15, -0.9831680378442393398 ) ) ;
#69108=CARTESIAN_POINT ( 'NONE',  ( -1.409217194013772101, -6.376774720514417183, 20.11414146978959749 ) ) ;
#69116=B_SPLINE_CURVE_WITH_KNOTS ( 'NONE', 3,
 ( #9880, #72794, #74282, #43835, #59569, #4279, #20482, #88514, #11880, #18990, #57579, #90009, #66199, #90501, #74768 ),
 .UNSPECIFIED., .F., .F.,
 ( 4, 1, 1, 1, 1, 1, 1, 1, 1, 1, 1, 1, 4 ),
 ( 0.000000000000000000, 0.1128134007444584058, 0.2253938839207300371, 0.3395948145627014636, 0.4596754102248630236, 0.5217351900879338977, 0.5839258387389175686, 0.6481741447653697197, 0.7138810381130681337, 0.7810044549073911213, 0.8514509275565554924, 0.9240506926641786078, 1.000000000000000000 ),
 .UNSPECIFIED. ) ;
#69122=ADVANCED_FACE ( 'NONE', ( #65663 ), #60455, .F. ) ;
#69126=ADVANCED_FACE ( 'NONE', ( #34692 ), #96579, .F. ) ;
#69130=EDGE_CURVE ( 'NONE', #18512, #63950, #90626, .T. ) ;
#69137=CARTESIAN_POINT ( 'NONE',  ( -6.020540257910568904, -6.376774720514411854, 19.49847411603315095 ) ) ;
#69139=ORIENTED_EDGE ( 'NONE', *, *, #6710, .F. ) ;
#69161=ORIENTED_EDGE ( 'NONE', *, *, #69471, .T. ) ;
#69168=ORIENTED_EDGE ( 'NONE', *, *, #42902, .T. ) ;
#69174=CARTESIAN_POINT ( 'NONE',  ( 7.479587785762670471, -5.876774720514417183, 20.73799387832858088 ) ) ;
#69177=VERTEX_POINT ( 'NONE', #35192 ) ;
#69184=ORIENTED_EDGE ( 'NONE', *, *, #11907, .T. ) ;
#69185=DIRECTION ( 'NONE',  ( 1.611864046919725738E-15, -7.253388211138766116E-15, 1.000000000000000000 ) ) ;
#69189=CARTESIAN_POINT ( 'NONE',  ( 21.89392097122634340, -4.278466574096848163, -16.39911395417462003 ) ) ;
#69191=CARTESIAN_POINT ( 'NONE',  ( 5.464387484610083057, -5.876774720514420736, 21.31215092858952431 ) ) ;
#69209=DIRECTION ( 'NONE',  ( 0.000000000000000000, 1.000000000000000000, 0.000000000000000000 ) ) ;
#69222=DIRECTION ( 'NONE',  ( 0.000000000000000000, 0.000000000000000000, -1.000000000000000000 ) ) ;
#69228=DIRECTION ( 'NONE',  ( 0.000000000000000000, 0.000000000000000000, -1.000000000000000000 ) ) ;
#69247=ORIENTED_EDGE ( 'NONE', *, *, #67671, .F. ) ;
#69249=VERTEX_POINT ( 'NONE', #99056 ) ;
#69271=VECTOR ( 'NONE', #4310, 1000.000000000000000 ) ;
#69274=DIRECTION ( 'NONE',  ( 0.000000000000000000, 0.000000000000000000, 1.000000000000000000 ) ) ;
#69279=CARTESIAN_POINT ( 'NONE',  ( -2.369893591381136755, -5.876774720514409189, 19.15221817653405623 ) ) ;
#69286=B_SPLINE_CURVE_WITH_KNOTS ( 'NONE', 3,
 ( #38235, #73943, #99131, #4440, #43001, #69191, #52982, #77287, #30624, #29630, #60605, #35390, #83411, #22000, #53982 ),
 .UNSPECIFIED., .F., .F.,
 ( 4, 1, 1, 1, 1, 1, 1, 1, 1, 1, 1, 1, 4 ),
 ( 0.000000000000000000, 0.08594794314412859682, 0.1691252118806910454, 0.2503991071860492412, 0.3322897361388358339, 0.4133642879158805905, 0.4941722833711898466, 0.5760217353866382561, 0.6607569692540066209, 0.7457831259137440716, 0.8300435929752246755, 0.9140275458206831294, 1.000000000000000000 ),
 .UNSPECIFIED. ) ;
#69291=CARTESIAN_POINT ( 'NONE',  ( 4.639502537026700679, -6.376774720514415407, 19.60647575951318800 ) ) ;
#69295=VERTEX_POINT ( 'NONE', #52911 ) ;
#69305=ORIENTED_EDGE ( 'NONE', *, *, #6389, .T. ) ;
#69330=CARTESIAN_POINT ( 'NONE',  ( -2.532641601674031850, -5.876774720514408301, 19.55266968305501507 ) ) ;
#69335=EDGE_CURVE ( 'NONE', #57212, #14292, #100374, .T. ) ;
#69344=CARTESIAN_POINT ( 'NONE',  ( 4.642799911345256270, -5.876774720514408301, 18.59646607068888713 ) ) ;
#69349=CARTESIAN_POINT ( 'NONE',  ( 14.76093561896379214, 6.475225279485574248, -26.55548769130089681 ) ) ;
#69354=CARTESIAN_POINT ( 'NONE',  ( 5.399550031316281640, -0.3587747205144061202, -28.54570968857217395 ) ) ;
#69363=ORIENTED_EDGE ( 'NONE', *, *, #48646, .F. ) ;
#69367=CARTESIAN_POINT ( 'NONE',  ( 14.98902733942698617, -3.496957042870280752, -27.33343847194423404 ) ) ;
#69368=ADVANCED_FACE ( 'NONE', ( #7213 ), #38162, .T. ) ;
#69369=EDGE_CURVE ( 'NONE', #8388, #56523, #92448, .T. ) ;
#69389=CARTESIAN_POINT ( 'NONE',  ( 0.000000000000000000, -4.056774720514426669, 6.000000000000000888 ) ) ;
#69419=ORIENTED_EDGE ( 'NONE', *, *, #6710, .T. ) ;
#69420=CARTESIAN_POINT ( 'NONE',  ( 4.959895098850171102, -5.876774720514410077, 19.67755022954121813 ) ) ;
#69425=LINE ( 'NONE', #62837, #13929 ) ;
#69447=CARTESIAN_POINT ( 'NONE',  ( -2.794871794871791604, -6.376774720514427841, 21.75000000000001066 ) ) ;
#69457=DIRECTION ( 'NONE',  ( -0.000000000000000000, 1.000000000000000000, -0.000000000000000000 ) ) ;
#69469=CARTESIAN_POINT ( 'NONE',  ( -5.912814555383966386, -5.876774720514418071, 20.28973052848695602 ) ) ;
#69470=CARTESIAN_POINT ( 'NONE',  ( 3.252401863874215593, -0.3587747205143964613, -29.35688408629929214 ) ) ;
#69471=EDGE_CURVE ( 'NONE', #47313, #86012, #17847, .T. ) ;
#69477=ADVANCED_FACE ( 'NONE', ( #8731 ), #85851, .F. ) ;
#69482=EDGE_CURVE ( 'NONE', #96543, #97326, #56673, .T. ) ;
#69495=CARTESIAN_POINT ( 'NONE',  ( -0.9078848932494473223, -5.876774720514411854, 19.67454710845354171 ) ) ;
#69513=VERTEX_POINT ( 'NONE', #66047 ) ;
#69522=FACE_OUTER_BOUND ( 'NONE', #35942, .T. ) ;
#69534=EDGE_CURVE ( 'NONE', #56694, #1020, #20823, .T. ) ;
#69535=CARTESIAN_POINT ( 'NONE',  ( 3.398286024651508530, -5.876774720514429617, 21.76255057507181334 ) ) ;
#69546=CARTESIAN_POINT ( 'NONE',  ( 25.98063551284147721, -4.258790553513050803, -11.44815252197057021 ) ) ;
#69556=VERTEX_POINT ( 'NONE', #5611 ) ;
#69557=ORIENTED_EDGE ( 'NONE', *, *, #20905, .T. ) ;
#69569=DIRECTION ( 'NONE',  ( -0.7071067811865507924, 0.000000000000000000, 0.7071067811865442421 ) ) ;
#69573=CARTESIAN_POINT ( 'NONE',  ( 31.66639312903740944, -5.493490882720638346, 28.57493973316426406 ) ) ;
#69578=DIRECTION ( 'NONE',  ( 0.6599726524652353987, 0.000000000000000000, -0.7512896232465889890 ) ) ;
#69579=CARTESIAN_POINT ( 'NONE',  ( 14.43441820105630136, -3.540887625665272598, -28.36222020492957796 ) ) ;
#69582=VECTOR ( 'NONE', #34052, 1000.000000000000000 ) ;
#69585=ORIENTED_EDGE ( 'NONE', *, *, #95849, .T. ) ;
#69592=EDGE_CURVE ( 'NONE', #44878, #37372, #90849, .T. ) ;
#69596=EDGE_CURVE ( 'NONE', #63904, #65522, #37397, .T. ) ;
#69606=DIRECTION ( 'NONE',  ( -0.03244919754393515293, 0.000000000000000000, 0.9994733861282923959 ) ) ;
#69608=CARTESIAN_POINT ( 'NONE',  ( -2.196420576317535289, -5.876774720514410077, 19.14926908420044782 ) ) ;
#69609=VECTOR ( 'NONE', #5875, 1000.000000000000000 ) ;
#69613=EDGE_CURVE ( 'NONE', #20446, #55815, #63115, .T. ) ;
#69624=AXIS2_PLACEMENT_3D ( 'NONE', #73618, #80734, #96951 ) ;
#69627=VECTOR ( 'NONE', #36360, 1000.000000000000000 ) ;
#69628=CARTESIAN_POINT ( 'NONE',  ( 4.784292611718075072, -6.376774720514426953, -25.54547254883186014 ) ) ;
#69629=CARTESIAN_POINT ( 'NONE',  ( 5.635247460261607166, -6.376774720514424288, 21.53093896358932469 ) ) ;
#69636=ORIENTED_EDGE ( 'NONE', *, *, #52871, .F. ) ;
#69647=ORIENTED_EDGE ( 'NONE', *, *, #63162, .T. ) ;
#69650=CARTESIAN_POINT ( 'NONE',  ( -20.27875734969026311, -4.776774720514394446, 22.60402280011863496 ) ) ;
#69666=CARTESIAN_POINT ( 'NONE',  ( 32.95642386911166710, -3.601225610321291182, -13.01540364303327380 ) ) ;
#69677=CARTESIAN_POINT ( 'NONE',  ( -3.108974358974359475, -6.376774720514417183, 20.36458333333334281 ) ) ;
#69679=CARTESIAN_POINT ( 'NONE',  ( -7.640476926272304681, -6.376774720514415407, 20.25188360057253689 ) ) ;
#69683=FACE_OUTER_BOUND ( 'NONE', #57847, .T. ) ;
#69691=VECTOR ( 'NONE', #9016, 1000.000000000000000 ) ;
#69693=CIRCLE ( 'NONE', #12894, 28.45799999999999486 ) ;
#69698=CARTESIAN_POINT ( 'NONE',  ( -20.77875734969026311, -3.316774720514426456, 27.45402280011862572 ) ) ;
#69704=ORIENTED_EDGE ( 'NONE', *, *, #5458, .T. ) ;
#69711=CARTESIAN_POINT ( 'NONE',  ( 3.325015365150250535, -6.376774720514402972, 18.26971317031913955 ) ) ;
#69712=FACE_OUTER_BOUND ( 'NONE', #4722, .T. ) ;
#69722=EDGE_CURVE ( 'NONE', #54541, #18086, #31953, .T. ) ;
#69728=CARTESIAN_POINT ( 'NONE',  ( 4.612744205187371271, -6.376774720514418959, 20.61169588237105188 ) ) ;
#69730=FACE_OUTER_BOUND ( 'NONE', #85612, .T. ) ;
#69735=CARTESIAN_POINT ( 'NONE',  ( 29.80070917940689412, -6.376774720514426953, 27.39560796525321607 ) ) ;
#69737=CARTESIAN_POINT ( 'NONE',  ( 0.2428503871269292180, -5.876774720514414518, 19.85590024959437017 ) ) ;
#69741=FACE_OUTER_BOUND ( 'NONE', #27014, .T. ) ;
#69754=CARTESIAN_POINT ( 'NONE',  ( 0.2428503871269292180, -5.876774720514413630, 19.85590024959437017 ) ) ;
#69771=DIRECTION ( 'NONE',  ( -0.6599726524652346216, 0.000000000000000000, 0.7512896232465895441 ) ) ;
#69780=CARTESIAN_POINT ( 'NONE',  ( -4.358143420448500116, -5.876774720514413630, 19.75705121608222115 ) ) ;
#69782=ORIENTED_EDGE ( 'NONE', *, *, #49844, .T. ) ;
#69788=CARTESIAN_POINT ( 'NONE',  ( -1.359786310227693251, -5.876774720514417183, 20.62654306927474579 ) ) ;
#69793=ORIENTED_EDGE ( 'NONE', *, *, #31459, .F. ) ;
#69798=ORIENTED_EDGE ( 'NONE', *, *, #93305, .F. ) ;
#69799=DIRECTION ( 'NONE',  ( 0.000000000000000000, 0.000000000000000000, -1.000000000000000000 ) ) ;
#69801=CARTESIAN_POINT ( 'NONE',  ( 5.109298100551870725, -5.356774720514426491, -27.55941679637891895 ) ) ;
#69802=CARTESIAN_POINT ( 'NONE',  ( 30.09341516180546350, -1.682774720514426114, -13.89311774897855933 ) ) ;
#69803=DIRECTION ( 'NONE',  ( 0.000000000000000000, 0.000000000000000000, 1.000000000000000000 ) ) ;
#69806=ORIENTED_EDGE ( 'NONE', *, *, #2249, .T. ) ;
#69815=AXIS2_PLACEMENT_3D ( 'NONE', #17499, #78881, #56584 ) ;
#69818=ORIENTED_EDGE ( 'NONE', *, *, #51852, .T. ) ;
#69819=EDGE_CURVE ( 'NONE', #20487, #36206, #7610, .T. ) ;
#69821=CARTESIAN_POINT ( 'NONE',  ( 14.43441819135929194, -3.316774720514426456, -28.36222020317710957 ) ) ;
#69823=ORIENTED_EDGE ( 'NONE', *, *, #57831, .T. ) ;
#69832=VECTOR ( 'NONE', #22005, 1000.000000000000000 ) ;
#69841=DIRECTION ( 'NONE',  ( 0.7512896232465891000, 0.000000000000000000, 0.6599726524652351767 ) ) ;
#69845=DIRECTION ( 'NONE',  ( 0.000000000000000000, 0.000000000000000000, -1.000000000000000000 ) ) ;
#69850=CARTESIAN_POINT ( 'NONE',  ( 3.825381322105384285, -5.876774720514401196, 18.16071977647550995 ) ) ;
#69862=CARTESIAN_POINT ( 'NONE',  ( 3.181132013147180970, -5.876774720514426065, 21.64201922499777808 ) ) ;
#69866=VERTEX_POINT ( 'NONE', #96722 ) ;
#69885=CARTESIAN_POINT ( 'NONE',  ( -5.530932042872791499, -5.876774720514408301, 19.30497968945844534 ) ) ;
#69887=CARTESIAN_POINT ( 'NONE',  ( 2.903846153846159517, -6.376774720514415407, 19.99999999999999289 ) ) ;
#69900=DIRECTION ( 'NONE',  ( -0.06283980576413537855, 0.000000000000000000, -0.9980236263794188822 ) ) ;
#69915=ORIENTED_EDGE ( 'NONE', *, *, #99072, .T. ) ;
#69917=LINE ( 'NONE', #38466, #69691 ) ;
#69918=ORIENTED_EDGE ( 'NONE', *, *, #71297, .T. ) ;
#69919=ORIENTED_EDGE ( 'NONE', *, *, #2950, .F. ) ;
#69920=CARTESIAN_POINT ( 'NONE',  ( 4.966983519792414370, -5.876774720514413630, 19.83633487160803099 ) ) ;
#69926=CARTESIAN_POINT ( 'NONE',  ( -10.24059822343757986, -5.876774720514426953, 22.82308057603840368 ) ) ;
#69928=VERTEX_POINT ( 'NONE', #11486 ) ;
#69931=FACE_OUTER_BOUND ( 'NONE', #15766, .T. ) ;
#69943=VERTEX_POINT ( 'NONE', #20592 ) ;
#69965=VERTEX_POINT ( 'NONE', #65804 ) ;
#69976=ORIENTED_EDGE ( 'NONE', *, *, #8486, .F. ) ;
#69988=EDGE_CURVE ( 'NONE', #20487, #17929, #17764, .T. ) ;
#69996=CARTESIAN_POINT ( 'NONE',  ( 5.271800844963591359, -5.356774720514425603, -28.56638892015329034 ) ) ;
#70013=CARTESIAN_POINT ( 'NONE',  ( 2.976770017179964700, -6.376774720514420736, 20.68690469677381927 ) ) ;
#70017=AXIS2_PLACEMENT_3D ( 'NONE', #1345, #15048, #53638 ) ;
#70043=CIRCLE ( 'NONE', #37595, 28.96799999999999287 ) ;
#70044=DIRECTION ( 'NONE',  ( 0.000000000000000000, 1.000000000000000000, 0.000000000000000000 ) ) ;
#70056=CARTESIAN_POINT ( 'NONE',  ( 3.004381791450704942, -6.376774720514420736, 20.78526834885430219 ) ) ;
#70061=ADVANCED_FACE ( 'NONE', ( #62168 ), #38310, .F. ) ;
#70064=CARTESIAN_POINT ( 'NONE',  ( 31.63910543787568130, -6.180494461685818841, 27.51903215948834358 ) ) ;
#70071=DIRECTION ( 'NONE',  ( -2.327730190238738523E-16, 1.000000000000000000, 8.064610422320909082E-16 ) ) ;
#70076=ADVANCED_FACE ( 'NONE', ( #92101 ), #60677, .F. ) ;
#70117=DIRECTION ( 'NONE',  ( 0.000000000000000000, 1.000000000000000000, 0.000000000000000000 ) ) ;
#70119=CARTESIAN_POINT ( 'NONE',  ( -2.711489738547795625, -5.876774720514410966, 19.27798293355755632 ) ) ;
#70124=VECTOR ( 'NONE', #97123, 1000.000000000000000 ) ;
#70133=AXIS2_PLACEMENT_3D ( 'NONE', #41387, #48507, #34279 ) ;
#70135=LINE ( 'NONE', #83858, #98716 ) ;
#70139=CARTESIAN_POINT ( 'NONE',  ( -6.369015873774380943, -6.376774720514413630, 19.23384392940399934 ) ) ;
#70142=ORIENTED_EDGE ( 'NONE', *, *, #53511, .F. ) ;
#70144=DIRECTION ( 'NONE',  ( 1.334402673828313339E-16, 0.000000000000000000, -1.000000000000000000 ) ) ;
#70150=CIRCLE ( 'NONE', #8597, 0.2999999999999981570 ) ;
#70152=CYLINDRICAL_SURFACE ( 'NONE', #9352, 3.349999999999998757 ) ;
#70153=CARTESIAN_POINT ( 'NONE',  ( 2.884397429187188333, -5.876774720514406525, 18.67943752795919110 ) ) ;
#70156=EDGE_CURVE ( 'NONE', #94109, #63282, #72242, .T. ) ;
#70158=DIRECTION ( 'NONE',  ( 0.000000000000000000, 1.000000000000000000, 0.000000000000000000 ) ) ;
#70162=EDGE_CURVE ( 'NONE', #65127, #93325, #32392, .T. ) ;
#70177=ORIENTED_EDGE ( 'NONE', *, *, #76107, .F. ) ;
#70178=CARTESIAN_POINT ( 'NONE',  ( 11.13529270535513760, -4.132774720514426292, -26.87372982997969117 ) ) ;
#70182=VERTEX_POINT ( 'NONE', #63680 ) ;
#70193=CARTESIAN_POINT ( 'NONE',  ( 20.98059139286874242, -4.383336229084510371, -17.13711341628515328 ) ) ;
#70207=CARTESIAN_POINT ( 'NONE',  ( 8.978253834636468866, -5.876774720514426953, 0.000000000000000000 ) ) ;
#70214=EDGE_LOOP ( 'NONE', ( #36063, #40473, #87541, #82516 ) ) ;
#70225=CARTESIAN_POINT ( 'NONE',  ( 5.641653616409716854, -6.376774720514420736, 20.81030773351227481 ) ) ;
#70232=CARTESIAN_POINT ( 'NONE',  ( 0.1739078616027790736, -5.876774720514415407, 19.75705121608222115 ) ) ;
#70233=VECTOR ( 'NONE', #76699, 1000.000000000000000 ) ;
#70234=LINE ( 'NONE', #7827, #100291 ) ;
#70243=DIRECTION ( 'NONE',  ( 0.000000000000000000, -1.000000000000000000, 0.000000000000000000 ) ) ;
#70246=CARTESIAN_POINT ( 'NONE',  ( 27.53860345374808105, -4.772774720514425972, -8.321925749325261634 ) ) ;
#70249=ORIENTED_EDGE ( 'NONE', *, *, #2249, .F. ) ;
#70262=CARTESIAN_POINT ( 'NONE',  ( 32.16024265030974050, 5.965225279485572685, 14.03360796525321774 ) ) ;
#70267=ORIENTED_EDGE ( 'NONE', *, *, #57378, .T. ) ;
#70269=ADVANCED_FACE ( 'NONE', ( #59547 ), #90485, .F. ) ;
#70276=PLANE ( 'NONE',  #47001 ) ;
#70283=CARTESIAN_POINT ( 'NONE',  ( 0.000000000000000000, -4.056774720514426669, 6.000000000000000888 ) ) ;
#70301=ORIENTED_EDGE ( 'NONE', *, *, #30185, .F. ) ;
#70302=CARTESIAN_POINT ( 'NONE',  ( -2.794871794871795156, -6.376774720514417183, 20.36318108974359475 ) ) ;
#70304=CARTESIAN_POINT ( 'NONE',  ( 10.73283225829863952, -3.316774720511335595, -27.03068772560423838 ) ) ;
#70307=CARTESIAN_POINT ( 'NONE',  ( -20.77875734969026311, 6.143225279485574397, 27.31649921512899937 ) ) ;
#70312=VERTEX_POINT ( 'NONE', #75253 ) ;
#70322=ORIENTED_EDGE ( 'NONE', *, *, #12321, .F. ) ;
#70328=CARTESIAN_POINT ( 'NONE',  ( -4.169309590939843879, -5.876774720514411854, 19.59793130852656518 ) ) ;
#70334=CARTESIAN_POINT ( 'NONE',  ( -5.654682302363691626, -5.876774720514410077, 19.41635569784906323 ) ) ;
#70350=VERTEX_POINT ( 'NONE', #69650 ) ;
#70359=DIRECTION ( 'NONE',  ( 0.000000000000000000, 1.478457507934778393E-16, -1.000000000000000000 ) ) ;
#70362=AXIS2_PLACEMENT_3D ( 'NONE', #99425, #6085, #7584 ) ;
#70367=PLANE ( 'NONE',  #94764 ) ;
#70371=VECTOR ( 'NONE', #34462, 1000.000000000000000 ) ;
#70372=CARTESIAN_POINT ( 'NONE',  ( -2.772696838893043747, -6.376774720514413630, 19.95463486386180207 ) ) ;
#70374=EDGE_LOOP ( 'NONE', ( #33118, #65231 ) ) ;
#70377=CARTESIAN_POINT ( 'NONE',  ( 4.613443512364428400, -5.876774720514412742, 19.38647409819875733 ) ) ;
#70385=CARTESIAN_POINT ( 'NONE',  ( -5.824076695599092801, -6.376774720514413630, 19.72913074730691108 ) ) ;
#70394=VERTEX_POINT ( 'NONE', #68152 ) ;
#70408=CARTESIAN_POINT ( 'NONE',  ( 4.017909867803298063, -5.876774720514403860, 18.55402206357357286 ) ) ;
#70415=VERTEX_POINT ( 'NONE', #60554 ) ;
#70418=EDGE_LOOP ( 'NONE', ( #45466, #9514 ) ) ;
#70419=CARTESIAN_POINT ( 'NONE',  ( -7.999999999999996447, -5.876774720514426953, 22.50000000000000355 ) ) ;
#70420=EDGE_LOOP ( 'NONE', ( #80261, #51033, #89997, #25320, #16518, #90150, #17438, #83864, #55937, #88171, #49782, #19116, #48155, #31242, #97916, #9688, #74127, #57708, #52573, #87667, #7741, #93332, #748, #98217, #46705, #51311, #85490, #81506, #66839, #50478, #91760, #68800, #99745, #89985, #73592, #6773, #34375, #66661, #86817, #10761, #58525, #18873, #74749, #29400, #35502, #70177, #59589, #93721, #1948, #21394, #52972, #55226, #50203, #56035, #41261, #77010, #14308, #63649, #81315, #29744, #86350, #37079, #636, #70322, #62844, #48146, #34113, #22360, #60081, #32631, #14368, #4665, #56185, #6518, #11603, #86638, #16848, #56587, #81541, #96720, #17976, #5676, #90730, #12747, #18429, #95882, #34632, #50486, #44012, #8666, #10748, #14720, #36228, #50734, #89443, #6848, #92223, #25189, #25107, #13002, #64942 ) ) ;
#70440=CARTESIAN_POINT ( 'NONE',  ( -10.24059822343757808, -6.376774720514426953, 17.17691942396160698 ) ) ;
#70441=ORIENTED_EDGE ( 'NONE', *, *, #41778, .T. ) ;
#70451=AXIS2_PLACEMENT_3D ( 'NONE', #49457, #19479, #43335 ) ;
#70458=CARTESIAN_POINT ( 'NONE',  ( 10.83356970694445209, -2.682774720514426114, -27.03405577723113140 ) ) ;
#70461=LINE ( 'NONE', #60859, #59583 ) ;
#70470=CARTESIAN_POINT ( 'NONE',  ( 5.367993895751241418, -6.376774720514418959, 20.45854982692612722 ) ) ;
#70472=CARTESIAN_POINT ( 'NONE',  ( 32.98733314340959311, -0.3587747205144265483, 2.074222136288530027 ) ) ;
#70473=ORIENTED_EDGE ( 'NONE', *, *, #66200, .T. ) ;
#70485=AXIS2_PLACEMENT_3D ( 'NONE', #834, #63253, #55640 ) ;
#70489=CARTESIAN_POINT ( 'NONE',  ( 9.843544857143434967, 6.475225279485573360, -27.49819965379373343 ) ) ;
#70495=CARTESIAN_POINT ( 'NONE',  ( -1.012926118674504883, -5.876774720514415407, 19.92818918856637822 ) ) ;
#70505=DIRECTION ( 'NONE',  ( 0.000000000000000000, 1.000000000000000000, 0.000000000000000000 ) ) ;
#70512=EDGE_LOOP ( 'NONE', ( #81678, #11721, #81193, #40941, #83527, #36596, #84700, #46299, #72178, #64672, #52360, #86115, #80424, #74375, #70580, #69139, #7185, #82491, #35910, #96273 ) ) ;
#70515=CARTESIAN_POINT ( 'NONE',  ( -7.304748120944324796, -5.876774720514418071, 19.95463486386180563 ) ) ;
#70516=DIRECTION ( 'NONE',  ( -1.286817348990133655E-16, 0.000000000000000000, 1.000000000000000000 ) ) ;
#70520=CIRCLE ( 'NONE', #12200, 91.74549126261076992 ) ;
#70560=VERTEX_POINT ( 'NONE', #8747 ) ;
#70565=CARTESIAN_POINT ( 'NONE',  ( 31.61404304915243202, -4.508643932895013862, 26.44173824648443727 ) ) ;
#70570=CARTESIAN_POINT ( 'NONE',  ( -41.32836283488544638, -4.132774720514426292, 39.26872235229541985 ) ) ;
#70572=AXIS2_PLACEMENT_3D ( 'NONE', #56136, #26168, #96676 ) ;
#70573=EDGE_CURVE ( 'NONE', #75496, #83737, #62536, .T. ) ;
#70577=ADVANCED_FACE ( 'NONE', ( #16852 ), #63049, .T. ) ;
#70580=ORIENTED_EDGE ( 'NONE', *, *, #45028, .F. ) ;
#70582=CARTESIAN_POINT ( 'NONE',  ( -20.27875734969026311, 7.743225279485574042, 25.40402280011862146 ) ) ;
#70584=FACE_OUTER_BOUND ( 'NONE', #33732, .T. ) ;
#70585=VECTOR ( 'NONE', #8794, 1000.000000000000000 ) ;
#70590=CARTESIAN_POINT ( 'NONE',  ( -16.22218391600152643, -6.376774720514426953, -54.85883559227303863 ) ) ;
#70596=EDGE_CURVE ( 'NONE', #93033, #2149, #79750, .T. ) ;
#70617=DIRECTION ( 'NONE',  ( 0.9831680378442392287, 0.000000000000000000, 0.1827036106964188000 ) ) ;
#70649=CARTESIAN_POINT ( 'NONE',  ( 6.910430652544937935, -5.876774720514418071, 20.24472806504191169 ) ) ;
#70652=EDGE_CURVE ( 'NONE', #92001, #51471, #72655, .T. ) ;
#70655=ORIENTED_EDGE ( 'NONE', *, *, #5015, .T. ) ;
#70657=CARTESIAN_POINT ( 'NONE',  ( 3.797776442307698286, -5.876774720514402084, 18.16025641025640525 ) ) ;
#70668=ORIENTED_EDGE ( 'NONE', *, *, #60323, .F. ) ;
#70674=CARTESIAN_POINT ( 'NONE',  ( -7.635352852713973348, -6.376774720514415407, 20.14409848895066091 ) ) ;
#70678=LINE ( 'NONE', #93500, #30153 ) ;
#70683=AXIS2_PLACEMENT_3D ( 'NONE', #6183, #52869, #6682 ) ;
#70687=DIRECTION ( 'NONE',  ( -0.9913618264504693300, -5.365801633547209345E-16, 0.1311553622875920033 ) ) ;
#70692=CARTESIAN_POINT ( 'NONE',  ( 27.53860345374808105, -5.356774720496559894, 1.647607965253213402 ) ) ;
#70693=PLANE ( 'NONE',  #91281 ) ;
#70707=DIRECTION ( 'NONE',  ( -0.000000000000000000, 1.000000000000000000, -0.000000000000000000 ) ) ;
#70743=ORIENTED_EDGE ( 'NONE', *, *, #85492, .F. ) ;
#70750=LINE ( 'NONE', #46911, #20873 ) ;
#70753=FACE_OUTER_BOUND ( 'NONE', #71321, .T. ) ;
#70757=DIRECTION ( 'NONE',  ( 0.000000000000000000, 0.000000000000000000, 1.000000000000000000 ) ) ;
#70759=ORIENTED_EDGE ( 'NONE', *, *, #83388, .T. ) ;
#70760=AXIS2_PLACEMENT_3D ( 'NONE', #35758, #43865, #74795 ) ;
#70761=DIRECTION ( 'NONE',  ( 0.000000000000000000, -1.000000000000000000, 0.000000000000000000 ) ) ;
#70770=CARTESIAN_POINT ( 'NONE',  ( 2.650685085285006348, -6.376774720514410077, 19.28073557658628445 ) ) ;
#70772=VERTEX_POINT ( 'NONE', #89866 ) ;
#70775=CARTESIAN_POINT ( 'NONE',  ( -4.141025641025641413, -5.876774720514419847, 20.67377804487180271 ) ) ;
#70781=DIRECTION ( 'NONE',  ( 0.000000000000000000, 0.000000000000000000, -1.000000000000000000 ) ) ;
#70783=VECTOR ( 'NONE', #91050, 1000.000000000000000 ) ;
#70784=EDGE_CURVE ( 'NONE', #42731, #41980, #24950, .T. ) ;
#70787=ORIENTED_EDGE ( 'NONE', *, *, #36492, .T. ) ;
#70793=ORIENTED_EDGE ( 'NONE', *, *, #95620, .F. ) ;
#70796=AXIS2_PLACEMENT_3D ( 'NONE', #96227, #81500, #42452 ) ;
#70799=EDGE_CURVE ( 'NONE', #8977, #29704, #20838, .T. ) ;
#70805=CARTESIAN_POINT ( 'NONE',  ( 8.309867465290103894, -5.356774720514426491, -25.05695269341429920 ) ) ;
#70814=ORIENTED_EDGE ( 'NONE', *, *, #47375, .T. ) ;
#70816=VECTOR ( 'NONE', #84280, 1000.000000000000000 ) ;
#70818=ORIENTED_EDGE ( 'NONE', *, *, #92369, .F. ) ;
#70820=DIRECTION ( 'NONE',  ( -0.000000000000000000, 1.000000000000000000, -0.000000000000000000 ) ) ;
#70827=EDGE_LOOP ( 'NONE', ( #77403, #56214, #71694, #79769 ) ) ;
#70828=ORIENTED_EDGE ( 'NONE', *, *, #41819, .T. ) ;
#70832=VECTOR ( 'NONE', #91628, 1000.000000000000000 ) ;
#70839=VECTOR ( 'NONE', #3339, 1000.000000000000000 ) ;
#70854=CARTESIAN_POINT ( 'NONE',  ( 4.912344403463128728, -5.876774720514409189, 19.26008510998990886 ) ) ;
#70855=DIRECTION ( 'NONE',  ( 1.000000000000000000, 0.000000000000000000, 0.000000000000000000 ) ) ;
#70857=CARTESIAN_POINT ( 'NONE',  ( 32.73857899460460175, -1.684774720514424118, -13.20677013500359820 ) ) ;
#70869=CARTESIAN_POINT ( 'NONE',  ( 2.591664760199015927, -6.376774720514417183, 20.15921530338947321 ) ) ;
#70871=CARTESIAN_POINT ( 'NONE',  ( 4.518955212990007908, -6.376774720514422512, 20.94857968174986951 ) ) ;
#70885=EDGE_CURVE ( 'NONE', #53709, #15278, #28544, .T. ) ;
#70895=CARTESIAN_POINT ( 'NONE',  ( -5.378122165843598701, -5.876774720514410077, 19.21968329462762526 ) ) ;
#70908=CARTESIAN_POINT ( 'NONE',  ( 10.75273025779354263, -6.376774720514426953, 16.96478738960562893 ) ) ;
#70911=VECTOR ( 'NONE', #91268, 1000.000000000000000 ) ;
#70916=CARTESIAN_POINT ( 'NONE',  ( 4.647383884978952828, -5.876774720514412742, 19.72975307774251164 ) ) ;
#70937=DIRECTION ( 'NONE',  ( -0.000000000000000000, 1.000000000000000000, -0.000000000000000000 ) ) ;
#70944=CARTESIAN_POINT ( 'NONE',  ( 31.82032313667048484, 5.965225279485572685, 9.148483289431936782 ) ) ;
#70952=VECTOR ( 'NONE', #88188, 1000.000000000000000 ) ;
#70954=CARTESIAN_POINT ( 'NONE',  ( 3.180076745125955284, -6.376774720514426953, -28.87659520466658236 ) ) ;
#70958=FACE_BOUND ( 'NONE', #67448, .T. ) ;
#70965=LINE ( 'NONE', #63371, #9361 ) ;
#70975=EDGE_CURVE ( 'NONE', #55815, #64204, #50698, .T. ) ;
#70979=LINE ( 'NONE', #31406, #10505 ) ;
#70980=CARTESIAN_POINT ( 'NONE',  ( -6.720452724358975338, -6.376774720514411854, 19.46153846153846700 ) ) ;
#70984=VECTOR ( 'NONE', #51101, 1000.000000000000000 ) ;
#70994=CARTESIAN_POINT ( 'NONE',  ( 13.74975846015576586, 6.475225279485573360, -27.72022515045486557 ) ) ;
#70995=VERTEX_POINT ( 'NONE', #65450 ) ;
#71006=VECTOR ( 'NONE', #64258, 1000.000000000000000 ) ;
#71011=DIRECTION ( 'NONE',  ( 0.000000000000000000, 0.000000000000000000, 1.000000000000000000 ) ) ;
#71024=CARTESIAN_POINT ( 'NONE',  ( -7.188523146553190912, -5.876774720514413630, 19.66116880005639800 ) ) ;
#71025=ORIENTED_EDGE ( 'NONE', *, *, #38769, .F. ) ;
#71028=DIRECTION ( 'NONE',  ( 2.338552693767719605E-15, 0.000000000000000000, 1.000000000000000000 ) ) ;
#71037=CARTESIAN_POINT ( 'NONE',  ( -6.265203266387573855, -5.876774720514408301, 19.29154511076646017 ) ) ;
#71043=CARTESIAN_POINT ( 'NONE',  ( 8.026968004785691946, -3.316774720514427344, -28.15626605682496830 ) ) ;
#71047=CARTESIAN_POINT ( 'NONE',  ( 25.72842579859213430, -5.175431684531299759, -7.741149173772083003 ) ) ;
#71048=FACE_OUTER_BOUND ( 'NONE', #78858, .T. ) ;
#71058=CARTESIAN_POINT ( 'NONE',  ( 30.53060340732036337, -5.297812262124697469, 1.539714685317310483 ) ) ;
#71070=CARTESIAN_POINT ( 'NONE',  ( 2.955024617976266033, -6.376774720514415407, 20.58370193283586858 ) ) ;
#71084=CARTESIAN_POINT ( 'NONE',  ( -0.4362980769230789257, -5.876774720514411854, 19.46153846153846345 ) ) ;
#71085=CARTESIAN_POINT ( 'NONE',  ( -24.90875734969025501, 5.965225279485572685, 30.51402280011862089 ) ) ;
#71095=VECTOR ( 'NONE', #86711, 1000.000000000000227 ) ;
#71100=EDGE_CURVE ( 'NONE', #13448, #56620, #75013, .T. ) ;
#71107=CARTESIAN_POINT ( 'NONE',  ( 5.993553214355093139, -5.876774720514417183, 20.20316077874593930 ) ) ;
#71111=DIRECTION ( 'NONE',  ( -0.000000000000000000, 0.000000000000000000, -1.000000000000000000 ) ) ;
#71113=CARTESIAN_POINT ( 'NONE',  ( 32.06540688909004189, -1.682774720514426114, -12.44045471929205249 ) ) ;
#71130=VECTOR ( 'NONE', #27453, 1000.000000000000000 ) ;
#71139=EDGE_CURVE ( 'NONE', #12619, #36399, #28856, .T. ) ;
#71144=EDGE_CURVE ( 'NONE', #51587, #83112, #41879, .T. ) ;
#71148=PLANE ( 'NONE',  #62277 ) ;
#71150=CARTESIAN_POINT ( 'NONE',  ( 0.000000000000000000, -2.056774720514426669, 3.500000000000000000 ) ) ;
#71157=CARTESIAN_POINT ( 'NONE',  ( 7.087697398486194622, -6.376774720514418959, 20.45710073441444621 ) ) ;
#71158=CARTESIAN_POINT ( 'NONE',  ( 5.344006250707635353, -6.376774720514418959, 20.55781796641452885 ) ) ;
#71176=AXIS2_PLACEMENT_3D ( 'NONE', #47012, #85561, #16044 ) ;
#71192=VERTEX_POINT ( 'NONE', #87141 ) ;
#71193=ORIENTED_EDGE ( 'NONE', *, *, #41778, .F. ) ;
#71205=CARTESIAN_POINT ( 'NONE',  ( -5.574014511416001127, -6.376774720514415407, 20.24089781925592391 ) ) ;
#71206=AXIS2_PLACEMENT_3D ( 'NONE', #48125, #39999, #9547 ) ;
#71207=EDGE_CURVE ( 'NONE', #49492, #49812, #69917, .T. ) ;
#71208=CARTESIAN_POINT ( 'NONE',  ( 31.04236049493789906, 6.475225279485573360, 19.84760796525321780 ) ) ;
#71210=CARTESIAN_POINT ( 'NONE',  ( 4.967948717948723392, -5.876774720514415407, 20.00140224358974095 ) ) ;
#71226=CARTESIAN_POINT ( 'NONE',  ( 3.165726958143470160, -6.376774720514422512, 21.14296526391294506 ) ) ;
#71227=CARTESIAN_POINT ( 'NONE',  ( 4.127208352283176396, -6.376774720514424288, 21.39624840817692686 ) ) ;
#71234=ADVANCED_FACE ( 'NONE', ( #78511 ), #62318, .T. ) ;
#71241=FACE_OUTER_BOUND ( 'NONE', #7864, .T. ) ;
#71256=DIRECTION ( 'NONE',  ( 0.000000000000000000, -1.000000000000000000, 0.000000000000000000 ) ) ;
#71258=CARTESIAN_POINT ( 'NONE',  ( 282.9764569301858046, -6.376774720514426953, 20.79159422840526616 ) ) ;
#71272=VERTEX_POINT ( 'NONE', #24238 ) ;
#71273=AXIS2_PLACEMENT_3D ( 'NONE', #8869, #1270, #48444 ) ;
#71280=ORIENTED_EDGE ( 'NONE', *, *, #74633, .F. ) ;
#71282=AXIS2_PLACEMENT_3D ( 'NONE', #86266, #78631, #87264 ) ;
#71284=DIRECTION ( 'NONE',  ( 0.8264557562326034779, 0.000000000000000000, 0.5630016722799281448 ) ) ;
#71291=CARTESIAN_POINT ( 'NONE',  ( 0.03625801282051022839, -6.376774720514410077, 19.27714342948718240 ) ) ;
#71292=AXIS2_PLACEMENT_3D ( 'NONE', #79216, #9718, #32048 ) ;
#71296=ORIENTED_EDGE ( 'NONE', *, *, #3147, .T. ) ;
#71297=EDGE_CURVE ( 'NONE', #100201, #92001, #11313, .T. ) ;
#71314=PLANE ( 'NONE',  #52123 ) ;
#71321=EDGE_LOOP ( 'NONE', ( #69305, #86982, #50679, #45853 ) ) ;
#71350=LINE ( 'NONE', #63757, #46668 ) ;
#71355=CARTESIAN_POINT ( 'NONE',  ( 4.692776824272364422, -5.876774720514406525, 18.67160386110882442 ) ) ;
#71365=AXIS2_PLACEMENT_3D ( 'NONE', #71935, #12013, #73427 ) ;
#71366=CARTESIAN_POINT ( 'NONE',  ( 27.53860345374771867, -4.132774720517318201, -9.482392034746242260 ) ) ;
#71368=VECTOR ( 'NONE', #20448, 1000.000000000000000 ) ;
#71369=CARTESIAN_POINT ( 'NONE',  ( 11.62916340711181284, -0.3587747205144265483, 28.75961759920349792 ) ) ;
#71372=CARTESIAN_POINT ( 'NONE',  ( 4.573489327750471567, -6.376774720514420736, 20.79634280254998657 ) ) ;
#71391=ORIENTED_EDGE ( 'NONE', *, *, #94359, .F. ) ;
#71399=CARTESIAN_POINT ( 'NONE',  ( 30.53060340732036337, -5.340035977923286659, 2.705756132044235152 ) ) ;
#71410=CARTESIAN_POINT ( 'NONE',  ( 19.75748517575715368, -0.3587747205144265483, 28.87153971905864580 ) ) ;
#71413=CARTESIAN_POINT ( 'NONE',  ( 4.639502537026700679, -6.376774720514415407, 19.60647575951318800 ) ) ;
#71419=B_SPLINE_CURVE_WITH_KNOTS ( 'NONE', 3,
 ( #57290, #2485, #4846, #66773, #72499, #95326, #41046, #97691, #63399, #86705, #80098, #33419, #94316, #28186, #10583 ),
 .UNSPECIFIED., .F., .F.,
 ( 4, 1, 1, 1, 1, 1, 1, 1, 1, 1, 1, 1, 4 ),
 ( 0.000000000000000000, 0.09781818961471311358, 0.1997260534018265310, 0.3052763574779380207, 0.4158114905382894744, 0.4744722311435595752, 0.5372738797760960860, 0.6036574205596552112, 0.6742988630901243230, 0.7498344853162268731, 0.8285984767571009657, 0.9123777781577814272, 1.000000000000000000 ),
 .UNSPECIFIED. ) ;
#71424=VERTEX_POINT ( 'NONE', #4415 ) ;
#71430=ADVANCED_FACE ( 'NONE', ( #49100 ), #58204, .F. ) ;
#71442=ORIENTED_EDGE ( 'NONE', *, *, #741, .F. ) ;
#71447=EDGE_CURVE ( 'NONE', #92224, #79658, #72928, .T. ) ;
#71450=VERTEX_POINT ( 'NONE', #3429 ) ;
#71455=CARTESIAN_POINT ( 'NONE',  ( -7.304748120944324796, -6.376774720514417183, 19.95463486386180563 ) ) ;
#71460=VERTEX_POINT ( 'NONE', #2926 ) ;
#71461=CARTESIAN_POINT ( 'NONE',  ( 5.271800844830267785, 5.965225279485592225, -28.56638892017480913 ) ) ;
#71480=CARTESIAN_POINT ( 'NONE',  ( 5.786755829966409692, -6.376774720514413630, 19.89762986309224857 ) ) ;
#71498=ORIENTED_EDGE ( 'NONE', *, *, #13338, .F. ) ;
#71507=CYLINDRICAL_SURFACE ( 'NONE', #90078, 4.299999999999999822 ) ;
#71527=CARTESIAN_POINT ( 'NONE',  ( -6.815415664272417295, -5.876774720514410966, 19.46427715384223234 ) ) ;
#71539=CARTESIAN_POINT ( 'NONE',  ( -5.837039262820512775, -5.876774720514413630, 19.76512419871795245 ) ) ;
#71561=ORIENTED_EDGE ( 'NONE', *, *, #95836, .F. ) ;
#71564=ORIENTED_EDGE ( 'NONE', *, *, #1565, .F. ) ;
#71568=EDGE_LOOP ( 'NONE', ( #74943, #289, #8756, #69976 ) ) ;
#71569=CARTESIAN_POINT ( 'NONE',  ( 31.68302997424993350, -5.121054483180515149, -3.958552486145202831 ) ) ;
#71580=CARTESIAN_POINT ( 'NONE',  ( 29.58033090225963591, -3.719533051881441121, 29.19816577366266941 ) ) ;
#71588=DIRECTION ( 'NONE',  ( 1.000000000000000000, 0.000000000000000000, 0.000000000000000000 ) ) ;
#71602=CARTESIAN_POINT ( 'NONE',  ( 4.784292611718075072, -3.316774720514426456, -25.54547254883186014 ) ) ;
#71621=CARTESIAN_POINT ( 'NONE',  ( 31.53822845103994865, -4.132774720514425404, -2.786383594989611634 ) ) ;
#71623=CARTESIAN_POINT ( 'NONE',  ( 9.354492577077031967, -4.915585290655217321, -26.27927344818281696 ) ) ;
#71626=B_SPLINE_CURVE_WITH_KNOTS ( 'NONE', 3,
 ( #86754, #48720, #48210, #72051, #71043, #26861, #50702, #73540, #73051, #96873, #88266, #81149 ),
 .UNSPECIFIED., .F., .F.,
 ( 4, 2, 2, 2, 2, 4 ),
 ( 8.673617379884035472E-19, 0.002088620103345146476, 0.003132930155017719064, 0.004177240206690291217, 0.006265860310035430321, 0.008354480413380570292 ),
 .UNSPECIFIED. ) ;
#71627=AXIS2_PLACEMENT_3D ( 'NONE', #59896, #66527, #51272 ) ;
#71634=DIRECTION ( 'NONE',  ( -1.000000000000000000, 0.000000000000000000, 2.246662546894773332E-15 ) ) ;
#71635=CARTESIAN_POINT ( 'NONE',  ( 30.53060340732036693, -4.132774720514426292, -5.153186819891554471 ) ) ;
#71637=ORIENTED_EDGE ( 'NONE', *, *, #91235, .T. ) ;
#71647=DIRECTION ( 'NONE',  ( 0.5630016722799281448, 5.365801633547219206E-16, -0.8264557562326033668 ) ) ;
#71648=ORIENTED_EDGE ( 'NONE', *, *, #2351, .F. ) ;
#71649=CARTESIAN_POINT ( 'NONE',  ( 13.57581083383196940, -5.876774720514426953, 20.21213203435597094 ) ) ;
#71654=ORIENTED_EDGE ( 'NONE', *, *, #653, .T. ) ;
#71657=CARTESIAN_POINT ( 'NONE',  ( 7.164391295225654765, -6.376774720514420736, 20.71606273170883838 ) ) ;
#71664=LINE ( 'NONE', #10256, #64235 ) ;
#71666=ADVANCED_FACE ( 'NONE', ( #95896 ), #58353, .F. ) ;
#71678=FACE_OUTER_BOUND ( 'NONE', #35846, .T. ) ;
#71680=ORIENTED_EDGE ( 'NONE', *, *, #4303, .T. ) ;
#71689=ORIENTED_EDGE ( 'NONE', *, *, #90788, .T. ) ;
#71694=ORIENTED_EDGE ( 'NONE', *, *, #94920, .F. ) ;
#71700=CIRCLE ( 'NONE', #14963, 80.18232118519038920 ) ;
#71709=CARTESIAN_POINT ( 'NONE',  ( -5.439936175300728927, -5.876774720514408301, 19.67454710845353816 ) ) ;
#71712=VERTEX_POINT ( 'NONE', #27884 ) ;
#71713=CARTESIAN_POINT ( 'NONE',  ( 4.967948717948723392, -6.376774720514415407, 20.00140224358974095 ) ) ;
#71715=FACE_OUTER_BOUND ( 'NONE', #76758, .T. ) ;
#71716=EDGE_CURVE ( 'NONE', #93143, #11983, #10667, .T. ) ;
#71718=DIRECTION ( 'NONE',  ( -0.000000000000000000, 1.000000000000000000, -0.000000000000000000 ) ) ;
#71727=CARTESIAN_POINT ( 'NONE',  ( 3.045412351277957175, -6.376774720514422512, 20.90433128744512814 ) ) ;
#71745=DIRECTION ( 'NONE',  ( 2.338552693767719605E-15, 0.000000000000000000, 1.000000000000000000 ) ) ;
#71754=VERTEX_POINT ( 'NONE', #61347 ) ;
#71756=CARTESIAN_POINT ( 'NONE',  ( -4.929522925832178437, 5.965225279485572685, -28.63504101147568903 ) ) ;
#71760=CARTESIAN_POINT ( 'NONE',  ( -25.92875734969025814, -3.316774720514426456, 26.43402280011862615 ) ) ;
#71769=CARTESIAN_POINT ( 'NONE',  ( -10.58858228176428717, 5.965225279485594001, -27.03148018517017093 ) ) ;
#71775=CARTESIAN_POINT ( 'NONE',  ( 3.398951772795901771, -6.376774720514402972, 18.23562605320997676 ) ) ;
#71782=LINE ( 'NONE', #95109, #76261 ) ;
#71791=CARTESIAN_POINT ( 'NONE',  ( -1.428094109758638819, -5.876774720514416295, 20.04104409779160179 ) ) ;
#71803=AXIS2_PLACEMENT_3D ( 'NONE', #81089, #41536, #58749 ) ;
#71806=ORIENTED_EDGE ( 'NONE', *, *, #37780, .T. ) ;
#71808=DIRECTION ( 'NONE',  ( 0.000000000000000000, -1.000000000000000000, 0.000000000000000000 ) ) ;
#71816=ORIENTED_EDGE ( 'NONE', *, *, #93018, .T. ) ;
#71823=VERTEX_POINT ( 'NONE', #60848 ) ;
#71825=CARTESIAN_POINT ( 'NONE',  ( 30.61866831821571111, -5.272393720821680674, 0.8164977272573440414 ) ) ;
#71833=DIRECTION ( 'NONE',  ( -0.000000000000000000, 1.000000000000000000, -0.000000000000000000 ) ) ;
#71834=VECTOR ( 'NONE', #54442, 1000.000000000000000 ) ;
#71843=EDGE_LOOP ( 'NONE', ( #97231, #70267, #40455, #37625 ) ) ;
#71869=DIRECTION ( 'NONE',  ( 0.000000000000000000, 0.000000000000000000, -1.000000000000000000 ) ) ;
#71871=CARTESIAN_POINT ( 'NONE',  ( 6.727764423076923350, -6.376774720514413630, 19.76442307692307665 ) ) ;
#71874=EDGE_CURVE ( 'NONE', #21858, #68694, #29620, .T. ) ;
#71878=DIRECTION ( 'NONE',  ( -1.000000000000000000, -2.464095846557964090E-17, 0.000000000000000000 ) ) ;
#71881=DIRECTION ( 'NONE',  ( 0.000000000000000000, 0.000000000000000000, -1.000000000000000000 ) ) ;
#71886=EDGE_CURVE ( 'NONE', #39047, #63950, #100363, .T. ) ;
#71891=CARTESIAN_POINT ( 'NONE',  ( 31.04236049493789906, 5.965225279485572685, 19.84760796525321780 ) ) ;
#71904=ORIENTED_EDGE ( 'NONE', *, *, #81071, .F. ) ;
#71921=FACE_OUTER_BOUND ( 'NONE', #80137, .T. ) ;
#71923=VERTEX_POINT ( 'NONE', #9541 ) ;
#71926=VECTOR ( 'NONE', #9046, 1000.000000000000000 ) ;
#71934=CARTESIAN_POINT ( 'NONE',  ( 14.76093561896379214, 6.475225279485573360, -27.88148769130088667 ) ) ;
#71935=CARTESIAN_POINT ( 'NONE',  ( -0.02075734969026423599, -6.376774720514426953, -0.08597719988137648983 ) ) ;
#71937=ORIENTED_EDGE ( 'NONE', *, *, #3766, .T. ) ;
#71944=LINE ( 'NONE', #81042, #38180 ) ;
#71953=ORIENTED_EDGE ( 'NONE', *, *, #92161, .F. ) ;
#71963=CARTESIAN_POINT ( 'NONE',  ( -5.576690828732316696, -6.376774720514417183, 20.34213149456667935 ) ) ;
#71967=CARTESIAN_POINT ( 'NONE',  ( 12.66784028006542151, -2.682774720514427003, -27.12025593822526304 ) ) ;
#71968=EDGE_CURVE ( 'NONE', #2798, #21553, #63356, .T. ) ;
#71978=CARTESIAN_POINT ( 'NONE',  ( 31.79364159983995464, -6.376774720514426953, -11.59305536555894278 ) ) ;
#71993=DIRECTION ( 'NONE',  ( -0.000000000000000000, -1.000000000000000000, -0.000000000000000000 ) ) ;
#71998=CARTESIAN_POINT ( 'NONE',  ( 14.52511747680497933, 6.475225279485573360, -27.86035006098926559 ) ) ;
#71999=EDGE_CURVE ( 'NONE', #65732, #15617, #25262, .T. ) ;
#72005=CARTESIAN_POINT ( 'NONE',  ( -1.041963229364719634, -5.876774720514417183, 20.24089781925592746 ) ) ;
#72009=CARTESIAN_POINT ( 'NONE',  ( -4.141025641025638748, -6.376774720514427841, 21.75000000000000355 ) ) ;
#72017=EDGE_CURVE ( 'NONE', #69295, #52438, #55239, .T. ) ;
#72022=DIRECTION ( 'NONE',  ( 1.000000000000000000, 0.000000000000000000, 0.000000000000000000 ) ) ;
#72035=EDGE_CURVE ( 'NONE', #18359, #60162, #32380, .T. ) ;
#72043=VECTOR ( 'NONE', #38140, 1000.000000000000000 ) ;
#72046=CARTESIAN_POINT ( 'NONE',  ( -6.728471858368818559, -5.876774720514408301, 19.14926908420045137 ) ) ;
#72051=CARTESIAN_POINT ( 'NONE',  ( 7.681304422638354445, -3.316774720514426900, -28.19747436301255661 ) ) ;
#72064=CARTESIAN_POINT ( 'NONE',  ( 4.948291700218025113, -5.876774720514418071, 20.47145334051262111 ) ) ;
#72068=ORIENTED_EDGE ( 'NONE', *, *, #18061, .T. ) ;
#72070=ORIENTED_EDGE ( 'NONE', *, *, #50523, .T. ) ;
#72075=CARTESIAN_POINT ( 'NONE',  ( 0.06697178475903577122, -6.376774720514410077, 19.29815762497054976 ) ) ;
#72082=ORIENTED_EDGE ( 'NONE', *, *, #97679, .T. ) ;
#72089=DIRECTION ( 'NONE',  ( 0.000000000000000000, 0.000000000000000000, -1.000000000000000000 ) ) ;
#72093=CARTESIAN_POINT ( 'NONE',  ( -17.97250661212648026, -0.3587747205144057872, -23.43622901028613725 ) ) ;
#72097=ORIENTED_EDGE ( 'NONE', *, *, #90288, .T. ) ;
#72109=DIRECTION ( 'NONE',  ( 0.000000000000000000, 0.000000000000000000, -1.000000000000000000 ) ) ;
#72114=CARTESIAN_POINT ( 'NONE',  ( -6.818021687177533430, -5.876774720514409189, 19.14905311829361167 ) ) ;
#72122=CARTESIAN_POINT ( 'NONE',  ( -28.47875734969025885, 5.965225279485572685, -0.08597719988137300651 ) ) ;
#72137=DIRECTION ( 'NONE',  ( 0.000000000000000000, 1.000000000000000000, 0.000000000000000000 ) ) ;
#72139=ORIENTED_EDGE ( 'NONE', *, *, #79386, .T. ) ;
#72150=VECTOR ( 'NONE', #55393, 1000.000000000000114 ) ;
#72154=CARTESIAN_POINT ( 'NONE',  ( 29.68479148105952703, -1.682774720514426114, -9.431263391055123790 ) ) ;
#72161=VERTEX_POINT ( 'NONE', #58716 ) ;
#72164=CARTESIAN_POINT ( 'NONE',  ( 6.156881756163101294, -6.376774720514413630, 19.74809127057764968 ) ) ;
#72169=CARTESIAN_POINT ( 'NONE',  ( 2.747717285871495108, -5.876774720514405637, 18.94713297040818034 ) ) ;
#72177=ORIENTED_EDGE ( 'NONE', *, *, #43189, .F. ) ;
#72178=ORIENTED_EDGE ( 'NONE', *, *, #44079, .F. ) ;
#72180=AXIS2_PLACEMENT_3D ( 'NONE', #50024, #88577, #72355 ) ;
#72185=ORIENTED_EDGE ( 'NONE', *, *, #74077, .F. ) ;
#72192=CARTESIAN_POINT ( 'NONE',  ( 6.944081373883786767, -6.376774720514424288, 21.27829155525578031 ) ) ;
#72193=ORIENTED_EDGE ( 'NONE', *, *, #94113, .F. ) ;
#72196=VECTOR ( 'NONE', #24607, 999.9999999999998863 ) ;
#72200=CARTESIAN_POINT ( 'NONE',  ( 5.885012508251304730, 6.475225279485574248, -27.43431635654696521 ) ) ;
#72201=LINE ( 'NONE', #41758, #54613 ) ;
#72204=CARTESIAN_POINT ( 'NONE',  ( 8.978253834636468866, -5.876774720514426953, 21.48128695274316158 ) ) ;
#72222=AXIS2_PLACEMENT_3D ( 'NONE', #59897, #67015, #90828 ) ;
#72226=CARTESIAN_POINT ( 'NONE',  ( 3.128267882468583228, -5.876774720514423400, 21.08409277973916218 ) ) ;
#72232=CARTESIAN_POINT ( 'NONE',  ( 5.766314450391940127, -6.376774720514424288, 21.17177008079512035 ) ) ;
#72242=B_SPLINE_CURVE_WITH_KNOTS ( 'NONE', 3,
 ( #48441, #1266, #24082, #9864, #93588, #40814, #71775, #16972, #87492, #8864, #26091, #47936, #2270, #2770, #32698, #39812, #62671, #64183, #18476, #86488, #70770, #95104, #94600, #56057, #57063, #17981, #25589 ),
 .UNSPECIFIED., .F., .F.,
 ( 4, 1, 1, 1, 1, 1, 1, 1, 1, 1, 1, 1, 1, 1, 1, 1, 1, 1, 1, 1, 1, 1, 1, 1, 4 ),
 ( 0.000000000000000000, 0.03378811616271038681, 0.06719393237388025797, 0.09986241085682510954, 0.1325666121262582542, 0.1651511732547865374, 0.1979131873557924692, 0.2313190035669614730, 0.2650832782673732679, 0.2992553087581151794, 0.3343985665049788447, 0.3699428235093072392, 0.4062835607000603866, 0.4440638196985079444, 0.4829977068727749345, 0.5233544466133041029, 0.5655365896041484319, 0.6096129240658189063, 0.6563908113764170826, 0.7058854949364568032, 0.7583245002617304831, 0.8138317829411497728, 0.8727945590393887398, 0.9347222295400740011, 1.000000000000000000 ),
 .UNSPECIFIED. ) ;
#72246=CARTESIAN_POINT ( 'NONE',  ( 11.22265027773143231, -6.376774720513926908, -28.06709888789093554 ) ) ;
#72249=ADVANCED_FACE ( 'NONE', ( #14018 ), #89667, .T. ) ;
#72253=EDGE_LOOP ( 'NONE', ( #40021, #21944, #83514, #89166 ) ) ;
#72259=CARTESIAN_POINT ( 'NONE',  ( 7.343377932919765705, -5.876774720514422512, 21.31293098237466310 ) ) ;
#72286=ORIENTED_EDGE ( 'NONE', *, *, #45427, .F. ) ;
#72288=CARTESIAN_POINT ( 'NONE',  ( 7.165897526731081157, -5.876774720514420736, 20.76279523443833597 ) ) ;
#72289=DIRECTION ( 'NONE',  ( -1.000000000000000000, -0.000000000000000000, 0.000000000000000000 ) ) ;
#72293=CARTESIAN_POINT ( 'NONE',  ( 29.57907552799941087, 5.965225279485572685, 29.21818156447043791 ) ) ;
#72297=FACE_OUTER_BOUND ( 'NONE', #25525, .T. ) ;
#72305=FACE_OUTER_BOUND ( 'NONE', #88244, .T. ) ;
#72318=VECTOR ( 'NONE', #18062, 1000.000000000000000 ) ;
#72320=ORIENTED_EDGE ( 'NONE', *, *, #80950, .F. ) ;
#72346=CARTESIAN_POINT ( 'NONE',  ( 15.97264540888995299, -3.405665504423739609, -27.93485543958162864 ) ) ;
#72352=FACE_OUTER_BOUND ( 'NONE', #28733, .T. ) ;
#72355=DIRECTION ( 'NONE',  ( 0.000000000000000000, 0.000000000000000000, -1.000000000000000000 ) ) ;
#72357=B_SPLINE_CURVE_WITH_KNOTS ( 'NONE', 3,
 ( #91119, #76869, #7876, #7372, #29223, #45463, #44461, #23085, #44962, #29722, #14487, #30211, #13985, #76380, #38326, #54075, #68790, #15482, #77375 ),
 .UNSPECIFIED., .F., .F.,
 ( 4, 1, 1, 1, 1, 1, 1, 1, 1, 1, 1, 1, 1, 1, 1, 1, 4 ),
 ( 0.000000000000000000, 0.06867706841303471144, 0.1368709585090958913, 0.2061143571452998258, 0.2775381819697287922, 0.3497719775548993604, 0.4212508361555678538, 0.4929107569233706077, 0.5670265889927378344, 0.6066141532413346082, 0.6497039535189880199, 0.6973031504846840534, 0.7490856597091360980, 0.8048806474593088733, 0.8654850057023349974, 0.9302371271531362229, 1.000000000000000000 ),
 .UNSPECIFIED. ) ;
#72365=VECTOR ( 'NONE', #90923, 1000.000000000000000 ) ;
#72366=CARTESIAN_POINT ( 'NONE',  ( 14.83405752585718496, -4.881907540129191148, -27.54622755360254516 ) ) ;
#72373=DIRECTION ( 'NONE',  ( -0.9994733861282923959, 0.000000000000000000, -0.03244919754393515293 ) ) ;
#72375=CARTESIAN_POINT ( 'NONE',  ( 5.184553252003285984, 6.475225279485573360, -28.06387035751381731 ) ) ;
#72382=EDGE_CURVE ( 'NONE', #86899, #9886, #90008, .T. ) ;
#72384=CARTESIAN_POINT ( 'NONE',  ( -2.786875287040666560, -6.376774720514417183, 20.09505574050193388 ) ) ;
#72402=CARTESIAN_POINT ( 'NONE',  ( -0.4453066574538939171, -5.876774720514410077, 19.14913681718892491 ) ) ;
#72408=VECTOR ( 'NONE', #47466, 1000.000000000000000 ) ;
#72417=DIRECTION ( 'NONE',  ( -0.000000000000000000, 1.000000000000000000, -0.000000000000000000 ) ) ;
#72418=AXIS2_PLACEMENT_3D ( 'NONE', #37422, #92189, #66885 ) ;
#72421=CARTESIAN_POINT ( 'NONE',  ( 4.647383884978952828, -6.376774720514411854, 19.72975307774251164 ) ) ;
#72433=ORIENTED_EDGE ( 'NONE', *, *, #39252, .F. ) ;
#72446=ADVANCED_FACE ( 'NONE', ( #62220 ), #61227, .F. ) ;
#72448=ORIENTED_EDGE ( 'NONE', *, *, #53371, .F. ) ;
#72452=CARTESIAN_POINT ( 'NONE',  ( -7.324001883147635894, -5.876774720514413630, 20.17732409774492197 ) ) ;
#72458=DIRECTION ( 'NONE',  ( -0.000000000000000000, 1.000000000000000000, -0.000000000000000000 ) ) ;
#72467=CARTESIAN_POINT ( 'NONE',  ( -1.122631020312409245, -6.376774720514413630, 19.41635569784906679 ) ) ;
#72471=VECTOR ( 'NONE', #86721, 1000.000000000000114 ) ;
#72473=VECTOR ( 'NONE', #73798, 1000.000000000000000 ) ;
#72482=ORIENTED_EDGE ( 'NONE', *, *, #68324, .F. ) ;
#72495=CYLINDRICAL_SURFACE ( 'NONE', #99897, 0.3000000000000016542 ) ;
#72498=CARTESIAN_POINT ( 'NONE',  ( -9.150000000000000355, -6.376774720514426953, -15.69999999999999929 ) ) ;
#72499=CARTESIAN_POINT ( 'NONE',  ( 7.433267315672343223, -6.376774720514418959, 20.43888261666079842 ) ) ;
#72505=AXIS2_PLACEMENT_3D ( 'NONE', #50331, #26494, #42729 ) ;
#72511=DIRECTION ( 'NONE',  ( -0.000000000000000000, 0.000000000000000000, -1.000000000000000000 ) ) ;
#72515=LINE ( 'NONE', #19202, #41691 ) ;
#72519=LINE ( 'NONE', #73020, #35534 ) ;
#72529=CIRCLE ( 'NONE', #28770, 28.45799999999999486 ) ;
#72539=EDGE_CURVE ( 'NONE', #58613, #22171, #85534, .T. ) ;
#72541=CARTESIAN_POINT ( 'NONE',  ( 2.993365552154886089, -5.876774720514413630, 19.24059921568563425 ) ) ;
#72546=CARTESIAN_POINT ( 'NONE',  ( 14.61581676225068449, -3.316774720514424679, -27.35847991880143226 ) ) ;
#72554=DIRECTION ( 'NONE',  ( 0.7512896232465891000, 0.000000000000000000, 0.6599726524652352877 ) ) ;
#72560=EDGE_LOOP ( 'NONE', ( #25082, #74116, #43461, #97250, #37761, #11287, #49895, #74331, #87889, #10410, #74541, #71680, #11504, #5248, #90116, #37454, #99693, #84650, #76367, #36588, #91613, #53458, #13094, #27832 ) ) ;
#72583=EDGE_CURVE ( 'NONE', #16640, #77030, #3333, .T. ) ;
#72593=ORIENTED_EDGE ( 'NONE', *, *, #51852, .F. ) ;
#72600=ORIENTED_EDGE ( 'NONE', *, *, #4458, .F. ) ;
#72617=DIRECTION ( 'NONE',  ( 0.000000000000000000, 0.000000000000000000, 1.000000000000000000 ) ) ;
#72630=DIRECTION ( 'NONE',  ( -0.000000000000000000, -1.000000000000000000, -0.000000000000000000 ) ) ;
#72636=CARTESIAN_POINT ( 'NONE',  ( 6.044871794871792048, -5.876774720514402084, 18.16025641025640880 ) ) ;
#72647=DIRECTION ( 'NONE',  ( -1.000000000000000000, 0.000000000000000000, -0.000000000000000000 ) ) ;
#72654=CARTESIAN_POINT ( 'NONE',  ( 7.164812103570541879, -6.376774720514422512, 20.85668272347560404 ) ) ;
#72655=LINE ( 'NONE', #3645, #19417 ) ;
#72660=CARTESIAN_POINT ( 'NONE',  ( 6.586338672804227024, -5.876774720514415407, 20.10086663068103618 ) ) ;
#72661=CARTESIAN_POINT ( 'NONE',  ( 5.326923076923078426, -5.876774720514419847, 20.76772836538461320 ) ) ;
#72665=DIRECTION ( 'NONE',  ( 0.000000000000000000, 0.000000000000000000, 1.000000000000000000 ) ) ;
#72668=VECTOR ( 'NONE', #70359, 1000.000000000000000 ) ;
#72673=CARTESIAN_POINT ( 'NONE',  ( 12.46431485231495806, -4.283161447665844612, -27.85634418129429690 ) ) ;
#72679=EDGE_CURVE ( 'NONE', #27602, #49448, #28645, .T. ) ;
#72686=AXIS2_PLACEMENT_3D ( 'NONE', #44665, #99431, #98935 ) ;
#72687=CARTESIAN_POINT ( 'NONE',  ( 7.072045900997899537, -6.376774720514427841, 21.62824307385093192 ) ) ;
#72690=CARTESIAN_POINT ( 'NONE',  ( 7.166040305186291093, -6.376774720514420736, 20.81030863372915718 ) ) ;
#72692=CARTESIAN_POINT ( 'NONE',  ( 29.58519688192010832, -4.109013365083094449, 29.12059310601990703 ) ) ;
#72693=FACE_OUTER_BOUND ( 'NONE', #13009, .T. ) ;
#72694=EDGE_CURVE ( 'NONE', #49218, #56694, #67723, .T. ) ;
#72697=EDGE_CURVE ( 'NONE', #79616, #58859, #32531, .T. ) ;
#72707=CARTESIAN_POINT ( 'NONE',  ( -4.568292318365942073, -0.3587747205144265483, 30.06720597538392425 ) ) ;
#72713=CARTESIAN_POINT ( 'NONE',  ( -5.563047341353722253, -5.876774720514411854, 20.06599527532950589 ) ) ;
#72720=CARTESIAN_POINT ( 'NONE',  ( 14.61581670307174008, -2.682774720514426559, -27.35847990810646024 ) ) ;
#72728=ORIENTED_EDGE ( 'NONE', *, *, #3422, .T. ) ;
#72729=CARTESIAN_POINT ( 'NONE',  ( 3.063121397228215859, -6.376774720514420736, 20.95210102656095685 ) ) ;
#72730=CARTESIAN_POINT ( 'NONE',  ( -1.743696941008423984, -6.376774720514413630, 19.59984006504825160 ) ) ;
#72735=AXIS2_PLACEMENT_3D ( 'NONE', #51228, #51730, #44117 ) ;
#72738=CARTESIAN_POINT ( 'NONE',  ( -1.714505518806294145E-16, -7.835183881457442823, 1.399999999999999911 ) ) ;
#72746=CARTESIAN_POINT ( 'NONE',  ( 32.16024265030974050, 5.965225279485572685, 14.03360796525321774 ) ) ;
#72748=CARTESIAN_POINT ( 'NONE',  ( 9.818046095193736278, -3.316774720514088504, -28.04791984001701621 ) ) ;
#72750=CARTESIAN_POINT ( 'NONE',  ( -7.567681410454951241, -6.376774720514411854, 19.71630089903357330 ) ) ;
#72753=DIRECTION ( 'NONE',  ( -8.334928612639484546E-17, 1.000000000000000000, -7.321843366904296032E-17 ) ) ;
#72762=CARTESIAN_POINT ( 'NONE',  ( 7.448826589983275959, -5.876774720514420736, 21.05250386848070221 ) ) ;
#72763=CARTESIAN_POINT ( 'NONE',  ( 7.462166178408539352, 5.965225279485572685, -27.67315496249664974 ) ) ;
#72764=DIRECTION ( 'NONE',  ( -0.9822594791677485837, 0.000000000000000000, 0.1875268396392987258 ) ) ;
#72771=CARTESIAN_POINT ( 'NONE',  ( -4.495793269230770939, -5.876774720514410077, 19.27714342948718595 ) ) ;
#72781=ORIENTED_EDGE ( 'NONE', *, *, #13328, .T. ) ;
#72789=DIRECTION ( 'NONE',  ( 0.000000000000000000, 0.000000000000000000, 1.000000000000000000 ) ) ;
#72794=CARTESIAN_POINT ( 'NONE',  ( 3.748501943728875574, -5.876774720514426065, 21.47917144995767558 ) ) ;
#72804=CARTESIAN_POINT ( 'NONE',  ( 6.184520403203634942, -6.376774720514426953, -25.32021290018218451 ) ) ;
#72810=EDGE_CURVE ( 'NONE', #27095, #15127, #93520, .T. ) ;
#72820=ORIENTED_EDGE ( 'NONE', *, *, #79158, .T. ) ;
#72823=VECTOR ( 'NONE', #81896, 1000.000000000000000 ) ;
#72825=CARTESIAN_POINT ( 'NONE',  ( -6.602379858799704238, -6.376774720514410077, 19.46575348430202723 ) ) ;
#72829=AXIS2_PLACEMENT_3D ( 'NONE', #34572, #36056, #19327 ) ;
#72832=CARTESIAN_POINT ( 'NONE',  ( 29.73860345376319358, -5.356653620851810516, 18.57591152018007463 ) ) ;
#72840=CARTESIAN_POINT ( 'NONE',  ( -29.49875734969026198, -0.3587747205144265483, 2.362022800118626531 ) ) ;
#72843=FACE_OUTER_BOUND ( 'NONE', #64932, .T. ) ;
#72844=ORIENTED_EDGE ( 'NONE', *, *, #15633, .F. ) ;
#72846=CARTESIAN_POINT ( 'NONE',  ( -24.90875734969025501, -6.376774720514426953, 30.51402280011862089 ) ) ;
#72848=PLANE ( 'NONE',  #66886 ) ;
#72856=PLANE ( 'NONE',  #70572 ) ;
#72866=CARTESIAN_POINT ( 'NONE',  ( 29.73860345376319358, 1.477225279485574028, 7.190646357373898680E-15 ) ) ;
#72869=CARTESIAN_POINT ( 'NONE',  ( 3.121233215686890272, -6.376774720514404748, 18.93204046835445808 ) ) ;
#72876=ADVANCED_FACE ( 'NONE', ( #77789 ), #14900, .F. ) ;
#72878=FACE_OUTER_BOUND ( 'NONE', #32580, .T. ) ;
#72886=CARTESIAN_POINT ( 'NONE',  ( 30.61643171304413613, -6.376774720514426953, 27.37433008668288181 ) ) ;
#72887=AXIS2_PLACEMENT_3D ( 'NONE', #31194, #54545, #60181 ) ;
#72909=CARTESIAN_POINT ( 'NONE',  ( 2.955024617976266033, -6.376774720514415407, 20.58370193283586858 ) ) ;
#72928=LINE ( 'NONE', #48603, #94016 ) ;
#72932=EDGE_CURVE ( 'NONE', #83384, #19254, #26076, .T. ) ;
#72938=EDGE_CURVE ( 'NONE', #98879, #65855, #82787, .T. ) ;
#72943=ADVANCED_FACE ( 'NONE', ( #55485 ), #86423, .T. ) ;
#72947=CIRCLE ( 'NONE', #24324, 130.2784398600581710 ) ;
#72953=CARTESIAN_POINT ( 'NONE',  ( -7.264088518202086675, -5.876774720514411854, 19.78976258633487717 ) ) ;
#72957=ADVANCED_FACE ( 'NONE', ( #3210 ), #7805, .T. ) ;
#72960=FACE_OUTER_BOUND ( 'NONE', #56103, .T. ) ;
#72963=FACE_OUTER_BOUND ( 'NONE', #84480, .T. ) ;
#72975=CIRCLE ( 'NONE', #98877, 2.040000000000000036 ) ;
#72982=ORIENTED_EDGE ( 'NONE', *, *, #48997, .F. ) ;
#72984=EDGE_CURVE ( 'NONE', #71754, #7198, #85252, .T. ) ;
#72987=CARTESIAN_POINT ( 'NONE',  ( -1.358974358974355257, -6.376774720514427841, 21.75000000000000711 ) ) ;
#72989=CARTESIAN_POINT ( 'NONE',  ( -19.37210865224160017, 5.965225279485592225, -21.60955166348795586 ) ) ;
#72999=EDGE_CURVE ( 'NONE', #78995, #28435, #35644, .T. ) ;
#73002=DIRECTION ( 'NONE',  ( 0.2488812114211666759, 0.000000000000000000, 0.9685340172660599212 ) ) ;
#73013=PLANE ( 'NONE',  #10694 ) ;
#73020=CARTESIAN_POINT ( 'NONE',  ( 9.150000000000003908, -5.876774720514426953, 11.88602120139451834 ) ) ;
#73024=EDGE_LOOP ( 'NONE', ( #38700, #66337, #87624, #47382 ) ) ;
#73038=DIRECTION ( 'NONE',  ( 0.7071067811865507924, 0.000000000000000000, -0.7071067811865442421 ) ) ;
#73040=VERTEX_POINT ( 'NONE', #81811 ) ;
#73051=CARTESIAN_POINT ( 'NONE',  ( 10.81255391457704640, -3.316774720514425123, -28.05044903510771803 ) ) ;
#73058=LINE ( 'NONE', #34485, #91889 ) ;
#73059=DIRECTION ( 'NONE',  ( 0.6599726524652352877, 0.000000000000000000, -0.7512896232465891000 ) ) ;
#73060=LINE ( 'NONE', #83646, #54099 ) ;
#73064=ORIENTED_EDGE ( 'NONE', *, *, #18337, .T. ) ;
#73070=CARTESIAN_POINT ( 'NONE',  ( 0.1309051665272248643, -5.876774720514413630, 19.34190049657482291 ) ) ;
#73073=CARTESIAN_POINT ( 'NONE',  ( 2.649863049427662709, -6.376774720514420736, 20.71861240329949538 ) ) ;
#73082=CARTESIAN_POINT ( 'NONE',  ( 9.478389368232452483, -2.682774720514426559, -23.17485683983816003 ) ) ;
#73092=FACE_OUTER_BOUND ( 'NONE', #56308, .T. ) ;
#73102=CARTESIAN_POINT ( 'NONE',  ( 9.315600972258346602, 5.965225279485572685, 28.35070303307545458 ) ) ;
#73103=CARTESIAN_POINT ( 'NONE',  ( -6.741682653110981249, -0.3587747205144265483, 30.62569541381301619 ) ) ;
#73107=CARTESIAN_POINT ( 'NONE',  ( -10.21991166328316325, -3.845527176268170422, 29.42879868625613327 ) ) ;
#73112=ORIENTED_EDGE ( 'NONE', *, *, #75476, .T. ) ;
#73114=CARTESIAN_POINT ( 'NONE',  ( -7.138063944469604571, -5.876774720514409189, 19.21974929698718881 ) ) ;
#73122=LINE ( 'NONE', #80221, #23513 ) ;
#73132=CYLINDRICAL_SURFACE ( 'NONE', #31596, 3.349999999999998757 ) ;
#73144=ADVANCED_FACE ( 'NONE', ( #70584 ), #37628, .F. ) ;
#73157=ORIENTED_EDGE ( 'NONE', *, *, #37780, .F. ) ;
#73161=CARTESIAN_POINT ( 'NONE',  ( 5.344006250707635353, -5.876774720514418071, 20.55781796641452885 ) ) ;
#73163=EDGE_CURVE ( 'NONE', #34608, #67104, #78177, .T. ) ;
#73170=FACE_OUTER_BOUND ( 'NONE', #22455, .T. ) ;
#73177=ORIENTED_EDGE ( 'NONE', *, *, #81684, .T. ) ;
#73188=CARTESIAN_POINT ( 'NONE',  ( -20.27875734969026311, 6.143225279485574397, 21.75402280011862644 ) ) ;
#73207=CARTESIAN_POINT ( 'NONE',  ( -24.90875734969025501, -6.376774720514426953, 26.43402280011862615 ) ) ;
#73213=CARTESIAN_POINT ( 'NONE',  ( -5.576690828732316696, -6.376774720514417183, 20.34213149456667935 ) ) ;
#73215=ORIENTED_EDGE ( 'NONE', *, *, #19012, .T. ) ;
#73219=FACE_OUTER_BOUND ( 'NONE', #95383, .T. ) ;
#73224=CARTESIAN_POINT ( 'NONE',  ( 2.911360383046243783, -5.876774720514418071, 20.24673073119071276 ) ) ;
#73229=CARTESIAN_POINT ( 'NONE',  ( 32.40199294184732537, 5.965225279485572685, -12.82361242714782712 ) ) ;
#73234=LINE ( 'NONE', #72738, #52656 ) ;
#73243=CARTESIAN_POINT ( 'NONE',  ( 11.51813299235546673, -6.376774720514426953, -25.01561358505534471 ) ) ;
#73245=CARTESIAN_POINT ( 'NONE',  ( -7.586742644780859912, -5.876774720514413630, 19.78730719034165020 ) ) ;
#73250=PLANE ( 'NONE',  #85173 ) ;
#73251=DIRECTION ( 'NONE',  ( 0.000000000000000000, -1.000000000000000000, 0.000000000000000000 ) ) ;
#73255=CARTESIAN_POINT ( 'NONE',  ( 9.843544857143434967, 6.475225279485573360, -27.49819965379373343 ) ) ;
#73266=DIRECTION ( 'NONE',  ( -1.000000000000000000, 0.000000000000000000, -0.000000000000000000 ) ) ;
#73270=VECTOR ( 'NONE', #65731, 1000.000000000000000 ) ;
#73275=EDGE_LOOP ( 'NONE', ( #40696, #66798, #75132, #73514 ) ) ;
#73277=LINE ( 'NONE', #82864, #55133 ) ;
#73284=FACE_OUTER_BOUND ( 'NONE', #99944, .T. ) ;
#73287=CARTESIAN_POINT ( 'NONE',  ( 32.54003107466018463, -4.047905215973556459, -1.500050581001865169 ) ) ;
#73291=CARTESIAN_POINT ( 'NONE',  ( 33.61456970919605425, -3.316774720514426900, -11.35828564741663449 ) ) ;
#73293=VECTOR ( 'NONE', #22646, 1000.000000000000000 ) ;
#73295=CIRCLE ( 'NONE', #61921, 2.249999999999998668 ) ;
#73310=LINE ( 'NONE', #18509, #20591 ) ;
#73312=ORIENTED_EDGE ( 'NONE', *, *, #51159, .F. ) ;
#73314=CARTESIAN_POINT ( 'NONE',  ( 6.963174204274080736, -6.376774720514415407, 20.29202897614545975 ) ) ;
#73318=EDGE_CURVE ( 'NONE', #497, #92630, #11526, .T. ) ;
#73331=VECTOR ( 'NONE', #40835, 1000.000000000000000 ) ;
#73332=ORIENTED_EDGE ( 'NONE', *, *, #71447, .T. ) ;
#73340=DIRECTION ( 'NONE',  ( 0.000000000000000000, 1.000000000000000000, 1.478457507934778393E-16 ) ) ;
#73350=CARTESIAN_POINT ( 'NONE',  ( -29.49875734969026198, -0.3587747205144265483, 10.11402280011862587 ) ) ;
#73358=DIRECTION ( 'NONE',  ( 0.000000000000000000, 0.000000000000000000, -1.000000000000000000 ) ) ;
#73362=CARTESIAN_POINT ( 'NONE',  ( 15.99960863614630391, -3.577630190450220571, -27.91116951066582175 ) ) ;
#73397=ORIENTED_EDGE ( 'NONE', *, *, #74802, .T. ) ;
#73405=VECTOR ( 'NONE', #4410, 1000.000000000000000 ) ;
#73414=CARTESIAN_POINT ( 'NONE',  ( -10.24059822343752479, -5.876774720514426953, -2.394817856121274864E-14 ) ) ;
#73417=DIRECTION ( 'NONE',  ( 0.000000000000000000, 0.000000000000000000, 1.000000000000000000 ) ) ;
#73426=CARTESIAN_POINT ( 'NONE',  ( -25.92875734969025814, -3.316774720514426456, 0.7300228001186309656 ) ) ;
#73427=DIRECTION ( 'NONE',  ( 0.000000000000000000, 0.000000000000000000, -1.000000000000000000 ) ) ;
#73429=ORIENTED_EDGE ( 'NONE', *, *, #62735, .T. ) ;
#73436=AXIS2_PLACEMENT_3D ( 'NONE', #61944, #70044, #93368 ) ;
#73448=CARTESIAN_POINT ( 'NONE',  ( -6.905879715866854340, -5.876774720514411854, 19.48240003225459560 ) ) ;
#73454=DIRECTION ( 'NONE',  ( -1.000000000000000000, 0.000000000000000000, 0.000000000000000000 ) ) ;
#73456=CARTESIAN_POINT ( 'NONE',  ( 9.543201319291914093E-14, -5.876774720514426953, 18.21871304725679508 ) ) ;
#73460=CARTESIAN_POINT ( 'NONE',  ( -0.9257915630711897048, -6.376774720514410077, 19.25892998154168012 ) ) ;
#73473=LINE ( 'NONE', #97306, #13680 ) ;
#73482=FACE_OUTER_BOUND ( 'NONE', #7793, .T. ) ;
#73484=LINE ( 'NONE', #20184, #574 ) ;
#73496=CARTESIAN_POINT ( 'NONE',  ( 4.854822496258163866, -6.376774720514422512, 20.96950945262037891 ) ) ;
#73514=ORIENTED_EDGE ( 'NONE', *, *, #55984, .F. ) ;
#73525=CARTESIAN_POINT ( 'NONE',  ( 32.06540688909007741, 6.475225279485573360, -12.44045471929204716 ) ) ;
#73529=CARTESIAN_POINT ( 'NONE',  ( 6.480733632922428988, -5.876774720514425177, 21.47849199606610782 ) ) ;
#73534=ORIENTED_EDGE ( 'NONE', *, *, #8697, .F. ) ;
#73535=CARTESIAN_POINT ( 'NONE',  ( 3.362850247043494001, -5.876774720514404748, 18.65880685207958223 ) ) ;
#73538=ORIENTED_EDGE ( 'NONE', *, *, #96787, .F. ) ;
#73540=CARTESIAN_POINT ( 'NONE',  ( 10.11589461582716076, -3.316774720514427344, -28.03692668899584106 ) ) ;
#73548=CARTESIAN_POINT ( 'NONE',  ( 5.641025641025643189, -6.376774720514420736, 20.78665865384615330 ) ) ;
#73552=VERTEX_POINT ( 'NONE', #82685 ) ;
#73564=CARTESIAN_POINT ( 'NONE',  ( 3.769931535195356620, -6.376774720514429617, 21.83933825178638699 ) ) ;
#73571=EDGE_CURVE ( 'NONE', #86922, #91581, #28396, .T. ) ;
#73572=AXIS2_PLACEMENT_3D ( 'NONE', #92449, #60536, #91450 ) ;
#73592=ORIENTED_EDGE ( 'NONE', *, *, #31333, .T. ) ;
#73618=CARTESIAN_POINT ( 'NONE',  ( 27.53860345374808105, 1.477225279485574028, 0.000000000000000000 ) ) ;
#73625=VECTOR ( 'NONE', #79711, 1000.000000000000000 ) ;
#73626=CARTESIAN_POINT ( 'NONE',  ( 0.000000000000000000, -2.682774720514426559, 0.000000000000000000 ) ) ;
#73628=ORIENTED_EDGE ( 'NONE', *, *, #56485, .T. ) ;
#73631=EDGE_CURVE ( 'NONE', #96474, #63904, #14763, .T. ) ;
#73635=EDGE_LOOP ( 'NONE', ( #70818, #55207, #92573, #90519 ) ) ;
#73636=CARTESIAN_POINT ( 'NONE',  ( 33.74607884027702909, -0.3587747205144265483, -4.999864028243830916 ) ) ;
#73653=CARTESIAN_POINT ( 'NONE',  ( 14.52861783435694676, -3.922795597833769410, -28.30212872328112539 ) ) ;
#73660=CARTESIAN_POINT ( 'NONE',  ( 5.641025641025643189, -5.876774720514419847, 20.78665865384615330 ) ) ;
#73661=CARTESIAN_POINT ( 'NONE',  ( 10.75273025779354796, -5.876774720514426953, 23.03521261039436752 ) ) ;
#73662=EDGE_CURVE ( 'NONE', #76914, #24236, #35030, .T. ) ;
#73663=ORIENTED_EDGE ( 'NONE', *, *, #86679, .F. ) ;
#73679=CARTESIAN_POINT ( 'NONE',  ( 5.627902640648289712, -5.876774720514414518, 20.02890049923285787 ) ) ;
#73685=VERTEX_POINT ( 'NONE', #66002 ) ;
#73688=CARTESIAN_POINT ( 'NONE',  ( 13.82660648177921914, 6.475225279485573360, -27.21585177491302332 ) ) ;
#73711=DIRECTION ( 'NONE',  ( 0.000000000000000000, 0.000000000000000000, -1.000000000000000000 ) ) ;
#73723=EDGE_CURVE ( 'NONE', #39562, #32487, #99613, .T. ) ;
#73730=TOROIDAL_SURFACE ( 'NONE', #70485, 1.020000000000000018, 2.040000000000000036 ) ;
#73731=CARTESIAN_POINT ( 'NONE',  ( 9.777643287007670381, -6.376774720514424288, -24.98776412748719977 ) ) ;
#73733=CARTESIAN_POINT ( 'NONE',  ( 22.81105451610979173, 6.475225279485573360, -18.46691820600746681 ) ) ;
#73742=CARTESIAN_POINT ( 'NONE',  ( 7.176111537430461595, -6.376774720514424288, 21.53668079471899333 ) ) ;
#73746=PLANE ( 'NONE',  #89792 ) ;
#73749=CARTESIAN_POINT ( 'NONE',  ( -2.196420576317535289, -5.876774720514409189, 19.14926908420044782 ) ) ;
#73752=CARTESIAN_POINT ( 'NONE',  ( 30.56047832681635867, 2.297196155479663826, 24.67598410064777070 ) ) ;
#73755=VECTOR ( 'NONE', #75107, 1000.000000000000000 ) ;
#73763=ORIENTED_EDGE ( 'NONE', *, *, #46492, .T. ) ;
#73765=DIRECTION ( 'NONE',  ( 0.000000000000000000, 0.000000000000000000, -1.000000000000000000 ) ) ;
#73772=CARTESIAN_POINT ( 'NONE',  ( 7.139069293134643779, -5.876774720514421624, 20.58118917620081945 ) ) ;
#73773=FACE_OUTER_BOUND ( 'NONE', #47569, .T. ) ;
#73776=CARTESIAN_POINT ( 'NONE',  ( 29.75286985256398253, -5.302859984505953861, 26.69689370802097272 ) ) ;
#73778=ORIENTED_EDGE ( 'NONE', *, *, #57979, .F. ) ;
#73780=DIRECTION ( 'NONE',  ( -0.9952638024365005887, 0.000000000000000000, -0.09721092304694052555 ) ) ;
#73783=CARTESIAN_POINT ( 'NONE',  ( 15.32643653063178668, -2.682774720514426559, -27.14485409495428314 ) ) ;
#73785=ORIENTED_EDGE ( 'NONE', *, *, #96407, .F. ) ;
#73786=EDGE_CURVE ( 'NONE', #98742, #37689, #822, .T. ) ;
#73798=DIRECTION ( 'NONE',  ( -0.000000000000000000, 1.000000000000000000, -0.000000000000000000 ) ) ;
#73808=VECTOR ( 'NONE', #52904, 1000.000000000000000 ) ;
#73810=CARTESIAN_POINT ( 'NONE',  ( 15.99960863614631101, -3.577630190450212577, -27.91116951066581819 ) ) ;
#73822=EDGE_CURVE ( 'NONE', #65645, #20807, #30772, .T. ) ;
#73830=ORIENTED_EDGE ( 'NONE', *, *, #92480, .T. ) ;
#73833=CARTESIAN_POINT ( 'NONE',  ( -7.326923076923074873, -6.376774720514427841, 21.75000000000001066 ) ) ;
#73845=CIRCLE ( 'NONE', #5746, 91.74549126261076992 ) ;
#73858=CARTESIAN_POINT ( 'NONE',  ( -0.7827064370038755436, -6.376774720514410077, 19.55912026249540148 ) ) ;
#73859=CARTESIAN_POINT ( 'NONE',  ( 2.904396343079095111, -6.376774720514415407, 19.95793242748194984 ) ) ;
#73869=FACE_OUTER_BOUND ( 'NONE', #76750, .T. ) ;
#73882=EDGE_LOOP ( 'NONE', ( #17728, #19996, #184, #87758 ) ) ;
#73890=CARTESIAN_POINT ( 'NONE',  ( 13.36367879947601445, -5.876774720514426953, 20.00000000000000355 ) ) ;
#73897=DIRECTION ( 'NONE',  ( 0.000000000000000000, 0.000000000000000000, -1.000000000000000000 ) ) ;
#73901=CARTESIAN_POINT ( 'NONE',  ( -0.9540731552372990754, -5.876774720514412742, 19.74568812963596542 ) ) ;
#73903=AXIS2_PLACEMENT_3D ( 'NONE', #29167, #74836, #43414 ) ;
#73936=CARTESIAN_POINT ( 'NONE',  ( -10.21560369921944833, -5.622950887248190810, 29.47514638292475553 ) ) ;
#73937=B_SPLINE_CURVE_WITH_KNOTS ( 'NONE', 3,
 ( #94942, #88338, #25429, #42677, #24921 ),
 .UNSPECIFIED., .F., .F.,
 ( 4, 1, 4 ),
 ( 0.1431656576382807078, 0.2545924338564266032, 0.2890741368561012825 ),
 .UNSPECIFIED. ) ;
#73943=CARTESIAN_POINT ( 'NONE',  ( 5.328346181807287252, -5.876774720514418959, 20.81670806933143680 ) ) ;
#73947=CARTESIAN_POINT ( 'NONE',  ( 29.73828978136053891, -4.772774720514425972, -4.021765098496577373 ) ) ;
#73951=PLANE ( 'NONE',  #89724 ) ;
#73969=ORIENTED_EDGE ( 'NONE', *, *, #52786, .T. ) ;
#73976=VECTOR ( 'NONE', #97666, 1000.000000000000000 ) ;
#73984=CARTESIAN_POINT ( 'NONE',  ( -9.150000000000000355, -5.876774720514426953, -15.69999999999999929 ) ) ;
#73990=AXIS2_PLACEMENT_3D ( 'NONE', #28445, #96971, #81746 ) ;
#73991=CARTESIAN_POINT ( 'NONE',  ( 31.52236416363829363, -4.132774720514426292, -3.023391441407382807 ) ) ;
#73995=VERTEX_POINT ( 'NONE', #4335 ) ;
#73996=DIRECTION ( 'NONE',  ( 0.000000000000000000, -1.000000000000000000, 0.000000000000000000 ) ) ;
#73998=EDGE_CURVE ( 'NONE', #27719, #74013, #57135, .T. ) ;
#74013=VERTEX_POINT ( 'NONE', #74823 ) ;
#74014=ORIENTED_EDGE ( 'NONE', *, *, #4027, .T. ) ;
#74016=ORIENTED_EDGE ( 'NONE', *, *, #70596, .T. ) ;
#74021=AXIS2_PLACEMENT_3D ( 'NONE', #37213, #68164, #67679 ) ;
#74029=VERTEX_POINT ( 'NONE', #66751 ) ;
#74030=CIRCLE ( 'NONE', #12451, 0.3000000000000016542 ) ;
#74039=CARTESIAN_POINT ( 'NONE',  ( 11.80640562518893866, 6.475225279485576024, -27.06722565682295567 ) ) ;
#74044=AXIS2_PLACEMENT_3D ( 'NONE', #94779, #26274, #3454 ) ;
#74047=CARTESIAN_POINT ( 'NONE',  ( 5.697397333356354565, -6.376774720514418959, 20.51730809691671809 ) ) ;
#74059=VECTOR ( 'NONE', #54094, 1000.000000000000000 ) ;
#74064=CARTESIAN_POINT ( 'NONE',  ( 2.598243466966731585, -6.376774720514413630, 20.31174627870924709 ) ) ;
#74072=CARTESIAN_POINT ( 'NONE',  ( -2.606012662418322634, -6.376774720514410077, 19.21974929698718881 ) ) ;
#74077=EDGE_CURVE ( 'NONE', #92630, #62167, #61117, .T. ) ;
#74080=DIRECTION ( 'NONE',  ( -0.7512896232465891000, -0.000000000000000000, -0.6599726524652351767 ) ) ;
#74086=PLANE ( 'NONE',  #49095 ) ;
#74093=ORIENTED_EDGE ( 'NONE', *, *, #37159, .T. ) ;
#74109=CARTESIAN_POINT ( 'NONE',  ( -20.27875734969026311, -6.376774720514428729, 24.00402280011862288 ) ) ;
#74116=ORIENTED_EDGE ( 'NONE', *, *, #46680, .F. ) ;
#74120=DIRECTION ( 'NONE',  ( -0.000000000000000000, 1.000000000000000000, -0.000000000000000000 ) ) ;
#74121=LINE ( 'NONE', #65041, #22101 ) ;
#74122=EDGE_CURVE ( 'NONE', #36349, #36077, #36775, .T. ) ;
#74124=FACE_OUTER_BOUND ( 'NONE', #50182, .T. ) ;
#74127=ORIENTED_EDGE ( 'NONE', *, *, #92946, .F. ) ;
#74128=CIRCLE ( 'NONE', #67619, 28.96799999999999287 ) ;
#74144=ORIENTED_EDGE ( 'NONE', *, *, #96911, .F. ) ;
#74145=CARTESIAN_POINT ( 'NONE',  ( 10.86264265030973952, 5.965225279485574461, -28.64597719988137570 ) ) ;
#74157=AXIS2_PLACEMENT_3D ( 'NONE', #17000, #95134, #9390 ) ;
#74178=LINE ( 'NONE', #4674, #33595 ) ;
#74190=EDGE_CURVE ( 'NONE', #45914, #77609, #81211, .T. ) ;
#74195=EDGE_CURVE ( 'NONE', #44951, #80766, #78312, .T. ) ;
#74196=PLANE ( 'NONE',  #99743 ) ;
#74197=CARTESIAN_POINT ( 'NONE',  ( 15.92621150404962016, 6.475225279485573360, -27.29681269571043245 ) ) ;
#74201=ORIENTED_EDGE ( 'NONE', *, *, #38775, .T. ) ;
#74204=AXIS2_PLACEMENT_3D ( 'NONE', #84501, #14984, #45462 ) ;
#74209=LINE ( 'NONE', #12789, #40124 ) ;
#74216=MECHANICAL_CONTEXT ( 'NONE', #89372, 'mechanical' ) ;
#74219=CARTESIAN_POINT ( 'NONE',  ( 6.365284455128204399, -6.376774720514413630, 19.73076923076922640 ) ) ;
#74221=CARTESIAN_POINT ( 'NONE',  ( 32.76434349455507089, -3.489637856041424957, -3.883594654058048157 ) ) ;
#74222=FACE_OUTER_BOUND ( 'NONE', #77979, .T. ) ;
#74223=DIRECTION ( 'NONE',  ( 0.000000000000000000, -1.000000000000000000, 0.000000000000000000 ) ) ;
#74231=CARTESIAN_POINT ( 'NONE',  ( 9.146648804565860047, -6.376774720514257311, -28.07004961687618660 ) ) ;
#74233=DIRECTION ( 'NONE',  ( 0.000000000000000000, 0.000000000000000000, 1.000000000000000000 ) ) ;
#74235=CARTESIAN_POINT ( 'NONE',  ( 13.91401389203221406, -0.3587747205144265483, 158.0376437107427137 ) ) ;
#74237=ORIENTED_EDGE ( 'NONE', *, *, #67369, .T. ) ;
#74239=CARTESIAN_POINT ( 'NONE',  ( 30.53060340732036693, -5.220834790565956673, 0.4094854120269050823 ) ) ;
#74240=CARTESIAN_POINT ( 'NONE',  ( 6.420673076923079314, -5.876774720514426953, 21.83974358974358765 ) ) ;
#74254=DIRECTION ( 'NONE',  ( 0.000000000000000000, 0.000000000000000000, 1.000000000000000000 ) ) ;
#74256=AXIS2_PLACEMENT_3D ( 'NONE', #68868, #39915, #46043 ) ;
#74260=CARTESIAN_POINT ( 'NONE',  ( 3.036358173076929123, -6.376774720514420736, 20.87990785256409865 ) ) ;
#74275=CARTESIAN_POINT ( 'NONE',  ( -28.32169924589829080, -0.3587747205143964613, -8.244178532169451401 ) ) ;
#74278=CARTESIAN_POINT ( 'NONE',  ( 32.33217928425143839, -1.682774720514426114, -12.20610769812824437 ) ) ;
#74282=CARTESIAN_POINT ( 'NONE',  ( 3.671066620544169101, -5.876774720514424288, 21.47597918715562670 ) ) ;
#74287=ORIENTED_EDGE ( 'NONE', *, *, #26586, .F. ) ;
#74297=CARTESIAN_POINT ( 'NONE',  ( 7.089543269230769162, -5.876774720514413630, 19.75741185897435415 ) ) ;
#74304=CARTESIAN_POINT ( 'NONE',  ( 7.139069293134643779, -6.376774720514422512, 20.58118917620081945 ) ) ;
#74309=ORIENTED_EDGE ( 'NONE', *, *, #93972, .F. ) ;
#74314=EDGE_CURVE ( 'NONE', #49492, #50837, #202, .T. ) ;
#74324=CARTESIAN_POINT ( 'NONE',  ( 3.672440828437461224, -5.876774720514402972, 18.52532110411518573 ) ) ;
#74325=CARTESIAN_POINT ( 'NONE',  ( 2.628295812946869425, -6.376774720514411854, 19.40849182188139110 ) ) ;
#74331=ORIENTED_EDGE ( 'NONE', *, *, #42798, .T. ) ;
#74339=LINE ( 'NONE', #43894, #2935 ) ;
#74345=CARTESIAN_POINT ( 'NONE',  ( -4.930333147521421822, -5.876774720514410966, 19.46306892155547530 ) ) ;
#74349=CARTESIAN_POINT ( 'NONE',  ( 32.40199294184732537, 6.475225279485573360, -12.82361242714782712 ) ) ;
#74351=PLANE ( 'NONE',  #94527 ) ;
#74352=CARTESIAN_POINT ( 'NONE',  ( 30.93860345374796594, 6.475225279485573360, 19.84760796525321780 ) ) ;
#74357=AXIS2_PLACEMENT_3D ( 'NONE', #329, #62244, #1343 ) ;
#74375=ORIENTED_EDGE ( 'NONE', *, *, #83611, .F. ) ;
#74381=VERTEX_POINT ( 'NONE', #34659 ) ;
#74386=VECTOR ( 'NONE', #1381, 1000.000000000000000 ) ;
#74395=ORIENTED_EDGE ( 'NONE', *, *, #97337, .F. ) ;
#74397=EDGE_CURVE ( 'NONE', #47456, #73995, #10001, .T. ) ;
#74420=CARTESIAN_POINT ( 'NONE',  ( -4.977357939505175466, -5.876774720514410077, 19.14913681718893557 ) ) ;
#74431=CARTESIAN_POINT ( 'NONE',  ( 30.93860345374796594, 6.475225279485573360, 28.07639619989136293 ) ) ;
#74437=DIRECTION ( 'NONE',  ( 0.000000000000000000, 1.000000000000000000, 0.000000000000000000 ) ) ;
#74447=EDGE_CURVE ( 'NONE', #67104, #27095, #2217, .T. ) ;
#74450=CARTESIAN_POINT ( 'NONE',  ( -1.304987980769231948, -6.376774720514415407, 19.76512419871795245 ) ) ;
#74472=AXIS2_PLACEMENT_3D ( 'NONE', #36437, #19702, #4992 ) ;
#74503=ORIENTED_EDGE ( 'NONE', *, *, #65861, .F. ) ;
#74530=ORIENTED_EDGE ( 'NONE', *, *, #48646, .T. ) ;
#74532=EDGE_CURVE ( 'NONE', #32327, #71712, #24500, .T. ) ;
#74540=DIRECTION ( 'NONE',  ( 0.000000000000000000, -1.000000000000000000, 0.000000000000000000 ) ) ;
#74541=ORIENTED_EDGE ( 'NONE', *, *, #79272, .T. ) ;
#74555=CARTESIAN_POINT ( 'NONE',  ( -27.86046284349298219, -0.3587747205143967943, -8.091963836038763347 ) ) ;
#74558=CARTESIAN_POINT ( 'NONE',  ( -0.5218785734906133955, -5.876774720514409189, 19.14848118821636547 ) ) ;
#74562=CARTESIAN_POINT ( 'NONE',  ( 10.46399479596396453, -2.682774720514426559, -27.03001098546561920 ) ) ;
#74579=CARTESIAN_POINT ( 'NONE',  ( 22.02124265030973760, 6.143225279485574397, 18.45402280011862217 ) ) ;
#74591=CIRCLE ( 'NONE', #30847, 91.74549126261076992 ) ;
#74593=CARTESIAN_POINT ( 'NONE',  ( 5.654014271574485662, -5.876774720514419847, 20.92503208403226722 ) ) ;
#74616=EDGE_CURVE ( 'NONE', #44958, #54031, #5193, .T. ) ;
#74626=ORIENTED_EDGE ( 'NONE', *, *, #32773, .T. ) ;
#74630=ORIENTED_EDGE ( 'NONE', *, *, #29836, .F. ) ;
#74632=LINE ( 'NONE', #97958, #31684 ) ;
#74633=EDGE_CURVE ( 'NONE', #90630, #17609, #90928, .T. ) ;
#74636=ORIENTED_EDGE ( 'NONE', *, *, #71447, .F. ) ;
#74639=CARTESIAN_POINT ( 'NONE',  ( 3.252401863874210264, 5.965225279485592225, -29.35688408629928858 ) ) ;
#74640=CARTESIAN_POINT ( 'NONE',  ( 15.35137209921566992, -4.335618847589873148, -28.31916638425216348 ) ) ;
#74643=ORIENTED_EDGE ( 'NONE', *, *, #99121, .F. ) ;
#74652=CARTESIAN_POINT ( 'NONE',  ( 11.96746718618548577, -4.832654890647344104, -27.30666805081000348 ) ) ;
#74653=ORIENTED_EDGE ( 'NONE', *, *, #46115, .F. ) ;
#74661=CARTESIAN_POINT ( 'NONE',  ( -5.912814555383966386, -5.876774720514418071, 20.28973052848695602 ) ) ;
#74666=DIRECTION ( 'NONE',  ( -1.334402673828313093E-16, 0.000000000000000000, -1.000000000000000000 ) ) ;
#74671=CARTESIAN_POINT ( 'NONE',  ( -28.98875734969026041, -6.376774720514426953, 0.7300228001186309656 ) ) ;
#74672=ORIENTED_EDGE ( 'NONE', *, *, #59623, .T. ) ;
#74705=CARTESIAN_POINT ( 'NONE',  ( 5.402409956206937203, -6.376774720514424288, 21.18719775722114917 ) ) ;
#74706=CARTESIAN_POINT ( 'NONE',  ( 9.940598223437573822, -6.376774720514426953, 21.78128695274315874 ) ) ;
#74713=CARTESIAN_POINT ( 'NONE',  ( 13.02836919244612623, -3.777199458296179646, -28.16488413836729521 ) ) ;
#74719=VECTOR ( 'NONE', #53375, 1000.000000000000000 ) ;
#74721=CARTESIAN_POINT ( 'NONE',  ( -1.568769572606061535, -5.876774720514415407, 19.76359802465961835 ) ) ;
#74724=CARTESIAN_POINT ( 'NONE',  ( 6.132272708306365949, -6.376774720514424288, 21.80683391321003839 ) ) ;
#74749=ORIENTED_EDGE ( 'NONE', *, *, #91528, .T. ) ;
#74755=CARTESIAN_POINT ( 'NONE',  ( 282.9764569301858046, 6.475225279485573360, 20.79159422840526616 ) ) ;
#74757=EDGE_CURVE ( 'NONE', #24982, #14570, #11030, .T. ) ;
#74764=CARTESIAN_POINT ( 'NONE',  ( 6.420673076923079314, -5.876774720514427841, 21.83974358974358765 ) ) ;
#74765=CARTESIAN_POINT ( 'NONE',  ( 33.96422015159436114, -0.3587747205144265483, -7.233236000911337449 ) ) ;
#74768=CARTESIAN_POINT ( 'NONE',  ( 3.036358173076929123, -5.876774720514420736, 20.87990785256409865 ) ) ;
#74786=ORIENTED_EDGE ( 'NONE', *, *, #27283, .T. ) ;
#74789=EDGE_CURVE ( 'NONE', #9388, #62667, #46072, .T. ) ;
#74795=DIRECTION ( 'NONE',  ( 0.000000000000000000, 0.000000000000000000, 1.000000000000000000 ) ) ;
#74802=EDGE_CURVE ( 'NONE', #37700, #23800, #1902, .T. ) ;
#74809=CARTESIAN_POINT ( 'NONE',  ( 3.160575456146155204, -6.376774720514408301, 18.86877352677795372 ) ) ;
#74811=FACE_OUTER_BOUND ( 'NONE', #28114, .T. ) ;
#74818=ORIENTED_EDGE ( 'NONE', *, *, #54648, .F. ) ;
#74823=CARTESIAN_POINT ( 'NONE',  ( -10.24059822343757808, -6.376774720514426953, 17.91871304725684766 ) ) ;
#74828=CARTESIAN_POINT ( 'NONE',  ( -24.97666371003640151, 5.965225279485592225, -15.72894043976419098 ) ) ;
#74836=DIRECTION ( 'NONE',  ( 0.000000000000000000, -1.000000000000000000, 0.000000000000000000 ) ) ;
#74840=CARTESIAN_POINT ( 'NONE',  ( 3.085011456917871264, -6.376774720514408301, 19.00082519311127172 ) ) ;
#74848=CARTESIAN_POINT ( 'NONE',  ( -0.4453066574538939171, -5.876774720514410077, 19.14913681718892491 ) ) ;
#74852=DIRECTION ( 'NONE',  ( -0.000000000000000000, -1.000000000000000000, -0.000000000000000000 ) ) ;
#74863=VERTEX_POINT ( 'NONE', #52265 ) ;
#74878=CARTESIAN_POINT ( 'NONE',  ( -27.25988310792305214, -0.3587747205144265483, 30.32664379231667695 ) ) ;
#74890=CARTESIAN_POINT ( 'NONE',  ( 22.81105451610979173, 1.477225279485574028, -18.46691820600746681 ) ) ;
#74912=ORIENTED_EDGE ( 'NONE', *, *, #52871, .T. ) ;
#74922=CARTESIAN_POINT ( 'NONE',  ( -5.000686017310577824, -6.376774720514411854, 19.46274624311237034 ) ) ;
#74930=CARTESIAN_POINT ( 'NONE',  ( -2.772696838893043747, -5.876774720514411854, 19.95463486386180207 ) ) ;
#74931=PLANE ( 'NONE',  #36743 ) ;
#74943=ORIENTED_EDGE ( 'NONE', *, *, #60389, .F. ) ;
#74951=LINE ( 'NONE', #90692, #21504 ) ;
#74963=EDGE_LOOP ( 'NONE', ( #30222, #55944, #10111, #79365 ) ) ;
#74965=CARTESIAN_POINT ( 'NONE',  ( -3.826923076923074429, -6.376774720514427841, 21.75000000000000355 ) ) ;
#74971=CARTESIAN_POINT ( 'NONE',  ( 6.273728352332436309, -6.376774720514415407, 20.10092598260902008 ) ) ;
#74974=CARTESIAN_POINT ( 'NONE',  ( 3.557932825399831689, -6.376774720514429617, 21.44518044978141091 ) ) ;
#74975=B_SPLINE_SURFACE_WITH_KNOTS ( 'NONE', 3, 1, ( 
 ( #39265, #84940 ),
 ( #70225, #15425 ),
 ( #705, #31652 ),
 ( #41277, #74593 ),
 ( #94552, #25039 ),
 ( #58884, #66520 ),
 ( #1718, #40275 ),
 ( #72232, #4603 ),
 ( #35550, #32654 ),
 ( #96940, #67008 ),
 ( #63632, #89825 ),
 ( #20295, #56014 ),
 ( #51267, #16930 ),
 ( #66023, #82208 ),
 ( #9821, #17938 ),
 ( #50776, #5083 ),
 ( #95061, #48899 ),
 ( #43166, #86943 ),
 ( #79825, #27434 ) ),
 .UNSPECIFIED., .F., .F., .F.,
 ( 4, 1, 1, 1, 1, 1, 1, 1, 1, 1, 1, 1, 1, 1, 1, 1, 4 ),
 ( 2, 2 ),
 ( 0.000000000000000000, 0.06185264594669137583, 0.1212838306153700696, 0.1807779320756104369, 0.2392732340142800229, 0.2986414352139401540, 0.3581858222417109161, 0.4207600867589704752, 0.4852046730216416082, 0.5503622689482856600, 0.6136499245309111616, 0.6766234955168239917, 0.7391080134690120040, 0.8021647022429441165, 0.8667165971324768403, 0.9320376285055436139, 1.000000000000000000 ),
 ( 0.000000000000000000, 1.000000000000000000 ),
 .UNSPECIFIED. ) ;
#74977=CARTESIAN_POINT ( 'NONE',  ( 10.54059822343757702, -5.876774720514426953, 17.17691942396159988 ) ) ;
#74982=CARTESIAN_POINT ( 'NONE',  ( -10.54059822343757880, -5.876774720514426953, 23.12308057603841149 ) ) ;
#74983=AXIS2_PLACEMENT_3D ( 'NONE', #34525, #19776, #76424 ) ;
#75001=CARTESIAN_POINT ( 'NONE',  ( 29.57907552799942863, -6.376774720514426953, 29.21818156447040948 ) ) ;
#75002=LINE ( 'NONE', #6506, #44943 ) ;
#75003=EDGE_CURVE ( 'NONE', #92987, #69513, #37535, .T. ) ;
#75009=VECTOR ( 'NONE', #28531, 1000.000000000000000 ) ;
#75013=LINE ( 'NONE', #13116, #30792 ) ;
#75022=CARTESIAN_POINT ( 'NONE',  ( 5.930937628982182908, -6.376774720514417183, 20.24478033514397524 ) ) ;
#75025=DIRECTION ( 'NONE',  ( -0.9496245541219264785, 6.845827386180410961E-16, -0.3133898629642195011 ) ) ;
#75027=ORIENTED_EDGE ( 'NONE', *, *, #10647, .F. ) ;
#75033=VECTOR ( 'NONE', #77446, 1000.000000000000000 ) ;
#75034=EDGE_CURVE ( 'NONE', #53330, #1588, #18196, .T. ) ;
#75041=DIRECTION ( 'NONE',  ( -0.000000000000000000, 1.000000000000000000, -0.000000000000000000 ) ) ;
#75043=CARTESIAN_POINT ( 'NONE',  ( -1.292025413547811308, -5.876774720514412742, 19.72913074730690752 ) ) ;
#75046=CARTESIAN_POINT ( 'NONE',  ( -20.77875734969026311, -5.356774720514426491, 27.45402280011862217 ) ) ;
#75050=CARTESIAN_POINT ( 'NONE',  ( 29.64064043116815128, 5.965225279485572685, 28.71191112024341408 ) ) ;
#75069=AXIS2_PLACEMENT_3D ( 'NONE', #92257, #84646, #83140 ) ;
#75091=DIRECTION ( 'NONE',  ( 0.000000000000000000, 0.000000000000000000, 1.000000000000000000 ) ) ;
#75096=EDGE_CURVE ( 'NONE', #43147, #10045, #32924, .T. ) ;
#75098=ORIENTED_EDGE ( 'NONE', *, *, #46604, .F. ) ;
#75099=VECTOR ( 'NONE', #56981, 1000.000000000000000 ) ;
#75104=LINE ( 'NONE', #5601, #46788 ) ;
#75105=CARTESIAN_POINT ( 'NONE',  ( 6.326958800731953048, -5.876774720514425177, 21.47849181751607972 ) ) ;
#75107=DIRECTION ( 'NONE',  ( -0.000000000000000000, 1.000000000000000000, -0.000000000000000000 ) ) ;
#75108=VECTOR ( 'NONE', #80076, 1000.000000000000000 ) ;
#75114=ORIENTED_EDGE ( 'NONE', *, *, #18061, .F. ) ;
#75132=ORIENTED_EDGE ( 'NONE', *, *, #69069, .F. ) ;
#75133=DIRECTION ( 'NONE',  ( -0.000000000000000000, 1.000000000000000000, -0.000000000000000000 ) ) ;
#75140=CARTESIAN_POINT ( 'NONE',  ( 15.48350366603649064, -4.450064631498825918, -28.28653584630414386 ) ) ;
#75146=DIRECTION ( 'NONE',  ( 0.000000000000000000, 0.000000000000000000, -1.000000000000000000 ) ) ;
#75160=CARTESIAN_POINT ( 'NONE',  ( -5.891303133519534718, -5.876774720514420736, 20.71116975788854475 ) ) ;
#75161=B_SPLINE_CURVE_WITH_KNOTS ( 'NONE', 3,
 ( #65443, #40191, #86363, #81136, #82134, #48311, #9228, #20222, #16847, #1637, #88760, #51193, #47806, #11615, #96362, #11123, #73529, #65939, #66440 ),
 .UNSPECIFIED., .F., .F.,
 ( 4, 1, 1, 1, 1, 1, 1, 1, 1, 1, 1, 1, 1, 1, 1, 1, 4 ),
 ( 0.000000000000000000, 0.06184170298390879311, 0.1212623730944467210, 0.1807459488653150592, 0.2392309018221055461, 0.2983075587884643221, 0.3581827976158475924, 0.4203592307800689265, 0.4847924155141841718, 0.5499384837666866366, 0.6137182775404276258, 0.6766807072496321407, 0.7391541704483172159, 0.8021997032403536121, 0.8667401776163008442, 0.9320496524002468419, 1.000000000000000000 ),
 .UNSPECIFIED. ) ;
#75165=DIRECTION ( 'NONE',  ( 0.000000000000000000, -1.000000000000000000, 0.000000000000000000 ) ) ;
#75166=DIRECTION ( 'NONE',  ( 0.000000000000000000, 0.000000000000000000, 1.000000000000000000 ) ) ;
#75168=CARTESIAN_POINT ( 'NONE',  ( -13.57581083383197296, -5.876774720514426953, 19.78786796564403616 ) ) ;
#75170=CARTESIAN_POINT ( 'NONE',  ( 29.75874681941402855, -6.376774720514429617, 26.36094095093186596 ) ) ;
#75181=ORIENTED_EDGE ( 'NONE', *, *, #17729, .T. ) ;
#75191=EDGE_CURVE ( 'NONE', #1282, #91104, #79737, .T. ) ;
#75208=CARTESIAN_POINT ( 'NONE',  ( -7.324001883147635894, -6.376774720514413630, 20.17732409774492197 ) ) ;
#75212=EDGE_CURVE ( 'NONE', #13162, #5889, #51143, .T. ) ;
#75218=CARTESIAN_POINT ( 'NONE',  ( 13.59451591917074431, -3.316774720514426456, -28.23515841827053308 ) ) ;
#75225=CARTESIAN_POINT ( 'NONE',  ( -2.148731487934370410, -6.376774720514411854, 19.46295461892501422 ) ) ;
#75228=CARTESIAN_POINT ( 'NONE',  ( 15.14080536460164517, -5.152774720514427642, -26.62908960815038384 ) ) ;
#75234=CARTESIAN_POINT ( 'NONE',  ( -20.27875734969026311, 7.743225279485574042, 26.25402280011862288 ) ) ;
#75235=ADVANCED_FACE ( 'NONE', ( #82588 ), #52143, .T. ) ;
#75242=CARTESIAN_POINT ( 'NONE',  ( -28.98875734969026041, 5.965225279485572685, 25.61802280011862720 ) ) ;
#75249=CARTESIAN_POINT ( 'NONE',  ( -10.75273025779354796, -5.876774720514426953, 23.03521261039436752 ) ) ;
#75253=CARTESIAN_POINT ( 'NONE',  ( -6.914873625533459744, -0.3587747205144265483, 29.95171384920748281 ) ) ;
#75261=ORIENTED_EDGE ( 'NONE', *, *, #48652, .T. ) ;
#75276=CARTESIAN_POINT ( 'NONE',  ( 15.92621150404962371, 5.965225279485572685, -27.29681269571043245 ) ) ;
#75297=CARTESIAN_POINT ( 'NONE',  ( 30.60441873609196151, -4.296715115238376015, 26.89749680779764773 ) ) ;
#75298=CARTESIAN_POINT ( 'NONE',  ( 0.000000000000000000, -7.835183881457442823, -1.399999999999999911 ) ) ;
#75308=CARTESIAN_POINT ( 'NONE',  ( 3.552794897967157528, -5.876774720514402084, 18.18650940196788568 ) ) ;
#75316=VECTOR ( 'NONE', #99164, 1000.000000000000000 ) ;
#75336=EDGE_CURVE ( 'NONE', #18831, #92224, #30288, .T. ) ;
#75338=PLANE ( 'NONE',  #50008 ) ;
#75339=CARTESIAN_POINT ( 'NONE',  ( -1.836964591723098117, -6.376774720514410077, 19.23384392940399223 ) ) ;
#75352=ORIENTED_EDGE ( 'NONE', *, *, #90583, .T. ) ;
#75355=CARTESIAN_POINT ( 'NONE',  ( -0.4362980769230789257, -6.376774720514411854, 19.46153846153846345 ) ) ;
#75370=CARTESIAN_POINT ( 'NONE',  ( 14.61581670307174008, -2.682774720514426559, -27.35847990810646024 ) ) ;
#75373=VERTEX_POINT ( 'NONE', #15564 ) ;
#75383=DIRECTION ( 'NONE',  ( 0.000000000000000000, 0.000000000000000000, -1.000000000000000000 ) ) ;
#75385=CARTESIAN_POINT ( 'NONE',  ( -53.01255352321339842, -2.682774720514426559, 35.59556822165056644 ) ) ;
#75397=ORIENTED_EDGE ( 'NONE', *, *, #35592, .F. ) ;
#75401=DIRECTION ( 'NONE',  ( -0.000000000000000000, 1.000000000000000000, -0.000000000000000000 ) ) ;
#75404=ORIENTED_EDGE ( 'NONE', *, *, #69016, .F. ) ;
#75410=ORIENTED_EDGE ( 'NONE', *, *, #48432, .T. ) ;
#75425=CIRCLE ( 'NONE', #86812, 1.836000000000002075 ) ;
#75430=CARTESIAN_POINT ( 'NONE',  ( -2.786875287040666560, -5.876774720514415407, 20.09505574050193388 ) ) ;
#75437=DIRECTION ( 'NONE',  ( 0.000000000000000000, 0.000000000000000000, -1.000000000000000000 ) ) ;
#75443=EDGE_CURVE ( 'NONE', #9124, #27797, #47032, .T. ) ;
#75447=DIRECTION ( 'NONE',  ( 0.000000000000000000, -1.000000000000000000, 0.000000000000000000 ) ) ;
#75452=AXIS2_PLACEMENT_3D ( 'NONE', #75714, #91441, #14317 ) ;
#75471=DIRECTION ( 'NONE',  ( -0.000000000000000000, -1.000000000000000000, -0.000000000000000000 ) ) ;
#75472=DIRECTION ( 'NONE',  ( 7.994117400814786717E-16, 0.000000000000000000, -1.000000000000000000 ) ) ;
#75476=EDGE_CURVE ( 'NONE', #49712, #49492, #75958, .T. ) ;
#75477=CARTESIAN_POINT ( 'NONE',  ( 7.475222833218381879, -5.876774720514418959, 20.91460388675487891 ) ) ;
#75488=CIRCLE ( 'NONE', #69054, 2.249999999999998668 ) ;
#75496=VERTEX_POINT ( 'NONE', #29797 ) ;
#75513=EDGE_LOOP ( 'NONE', ( #777, #18111, #10619, #62087 ) ) ;
#75514=CARTESIAN_POINT ( 'NONE',  ( 4.692776824272364422, -6.376774720514406525, 18.67160386110882442 ) ) ;
#75523=CARTESIAN_POINT ( 'NONE',  ( 5.872047395031165351, -6.376774720514415407, 20.29192741308114734 ) ) ;
#75528=VERTEX_POINT ( 'NONE', #62770 ) ;
#75541=ADVANCED_FACE ( 'NONE', ( #41417 ), #1979, .T. ) ;
#75543=CARTESIAN_POINT ( 'NONE',  ( -2.806649551956928335, -6.376774720514411854, 19.35116211686183618 ) ) ;
#75545=DIRECTION ( 'NONE',  ( -0.9980236263794188822, 0.000000000000000000, 0.06283980576413539243 ) ) ;
#75551=ADVANCED_FACE ( 'NONE', ( #1361 ), #31802, .F. ) ;
#75552=DIRECTION ( 'NONE',  ( 0.000000000000000000, 0.000000000000000000, -1.000000000000000000 ) ) ;
#75557=VERTEX_POINT ( 'NONE', #71871 ) ;
#75565=ORIENTED_EDGE ( 'NONE', *, *, #1310, .T. ) ;
#75567=CARTESIAN_POINT ( 'NONE',  ( 15.10569527345119845, -2.682774720514426114, -27.29188918592609525 ) ) ;
#75570=CARTESIAN_POINT ( 'NONE',  ( -19.77875734969026311, 6.143225279485574397, 27.31649921512899937 ) ) ;
#75574=DIRECTION ( 'NONE',  ( -0.000000000000000000, 1.000000000000000000, -0.000000000000000000 ) ) ;
#75579=DIRECTION ( 'NONE',  ( 1.000000000000000000, -3.639962309748244178E-15, 0.000000000000000000 ) ) ;
#75580=VERTEX_POINT ( 'NONE', #94185 ) ;
#75593=CARTESIAN_POINT ( 'NONE',  ( -4.141025641025641413, -6.376774720514420736, 20.67377804487180271 ) ) ;
#75603=DIRECTION ( 'NONE',  ( -0.000000000000000000, 1.000000000000000000, -0.000000000000000000 ) ) ;
#75606=CIRCLE ( 'NONE', #18911, 84.48086791635431325 ) ;
#75607=CARTESIAN_POINT ( 'NONE',  ( 22.02124265030973760, -7.835183881457444599, 16.20402280011862217 ) ) ;
#75616=ADVANCED_FACE ( 'NONE', ( #56654 ), #92873, .T. ) ;
#75621=CARTESIAN_POINT ( 'NONE',  ( 2.832419239133125544, -5.876774720514421624, 21.23415460623727213 ) ) ;
#75629=CARTESIAN_POINT ( 'NONE',  ( 14.78821595474767747, -4.792189181182639146, -27.68628040864140516 ) ) ;
#75635=EDGE_CURVE ( 'NONE', #53330, #55838, #58680, .T. ) ;
#75637=ADVANCED_FACE ( 'NONE', ( #98047 ), #66647, .F. ) ;
#75638=CARTESIAN_POINT ( 'NONE',  ( -3.108974358974355923, -6.376774720514427841, 21.75000000000001066 ) ) ;
#75643=ORIENTED_EDGE ( 'NONE', *, *, #18756, .F. ) ;
#75649=CARTESIAN_POINT ( 'NONE',  ( -6.680782769985652791, -5.876774720514411854, 19.46295461892502132 ) ) ;
#75658=ADVANCED_FACE ( 'NONE', ( #6206 ), #37161, .T. ) ;
#75659=CIRCLE ( 'NONE', #98407, 130.7884398600581335 ) ;
#75672=EDGE_CURVE ( 'NONE', #70772, #35113, #36661, .T. ) ;
#75680=EDGE_CURVE ( 'NONE', #52968, #57568, #16934, .T. ) ;
#75696=CARTESIAN_POINT ( 'NONE',  ( -1.359786310227693251, -6.376774720514417183, 20.62654306927474579 ) ) ;
#75698=DIRECTION ( 'NONE',  ( 0.000000000000000000, 0.000000000000000000, -1.000000000000000000 ) ) ;
#75706=ORIENTED_EDGE ( 'NONE', *, *, #35569, .F. ) ;
#75707=DIRECTION ( 'NONE',  ( -0.000000000000000000, -1.000000000000000000, -0.000000000000000000 ) ) ;
#75714=CARTESIAN_POINT ( 'NONE',  ( 0.000000000000000000, -7.835183881457442823, 0.000000000000000000 ) ) ;
#75720=VECTOR ( 'NONE', #44235, 1000.000000000000000 ) ;
#75729=CARTESIAN_POINT ( 'NONE',  ( 8.000000000000003553, -5.876774720514426953, 0.000000000000000000 ) ) ;
#75743=VERTEX_POINT ( 'NONE', #37615 ) ;
#75744=LINE ( 'NONE', #13851, #35645 ) ;
#75746=CARTESIAN_POINT ( 'NONE',  ( -0.2112149364088803105, -6.376774720514410077, 19.49357334786886398 ) ) ;
#75761=LINE ( 'NONE', #46324, #71834 ) ;
#75764=ORIENTED_EDGE ( 'NONE', *, *, #71100, .T. ) ;
#75783=DIRECTION ( 'NONE',  ( -1.000000000000000000, 0.000000000000000000, 0.000000000000000000 ) ) ;
#75785=CARTESIAN_POINT ( 'NONE',  ( 32.33465265239741626, -4.457608646344818126, 0.9133233228923198777 ) ) ;
#75788=VERTEX_POINT ( 'NONE', #44740 ) ;
#75790=ORIENTED_EDGE ( 'NONE', *, *, #55778, .F. ) ;
#75804=CARTESIAN_POINT ( 'NONE',  ( 3.020285327128866992, -5.876774720514406525, 19.15473963397401391 ) ) ;
#75806=VECTOR ( 'NONE', #38857, 1000.000000000000000 ) ;
#75807=CARTESIAN_POINT ( 'NONE',  ( -65.05438548721849656, -5.356774720514425603, 23.50402280011858736 ) ) ;
#75811=B_SPLINE_SURFACE_WITH_KNOTS ( 'NONE', 3, 1, ( 
 ( #87759, #48204 ),
 ( #57331, #72046 ),
 ( #1526, #41091 ),
 ( #2530, #64452 ),
 ( #49213, #32465 ),
 ( #88260, #71037 ),
 ( #80645, #64952 ),
 ( #63951, #95365 ),
 ( #48714, #18243 ),
 ( #33462, #11131 ),
 ( #56828, #9628 ),
 ( #80143, #10633 ),
 ( #41594, #79133 ),
 ( #3033, #42100 ),
 ( #55822, #71539 ) ),
 .UNSPECIFIED., .F., .F., .F.,
 ( 4, 1, 1, 1, 1, 1, 1, 1, 1, 1, 1, 1, 4 ),
 ( 2, 2 ),
 ( 0.000000000000000000, 0.1183849129606683315, 0.2344384882140509996, 0.3525851839391772602, 0.4731673593536162015, 0.5350581108286729393, 0.5975237332646003985, 0.6605170696247790740, 0.7251603465314728769, 0.7908841475025374379, 0.8587744642336310186, 0.9282339358416601405, 1.000000000000000000 ),
 ( 0.000000000000000000, 1.000000000000000000 ),
 .UNSPECIFIED. ) ;
#75822=DIRECTION ( 'NONE',  ( 0.000000000000000000, -1.000000000000000000, 0.000000000000000000 ) ) ;
#75827=CARTESIAN_POINT ( 'NONE',  ( -4.854568188115255367, -5.876774720514410077, 19.46611907402017394 ) ) ;
#75835=AXIS2_PLACEMENT_3D ( 'NONE', #26788, #89191, #49149 ) ;
#75836=DIRECTION ( 'NONE',  ( 0.000000000000000000, 1.478457507934778393E-16, -1.000000000000000000 ) ) ;
#75837=CARTESIAN_POINT ( 'NONE',  ( -0.9078848932494473223, -6.376774720514411854, 19.67454710845354171 ) ) ;
#75854=CARTESIAN_POINT ( 'NONE',  ( -0.001774553997815280816, -6.376774720514413630, 19.59623724171353487 ) ) ;
#75858=CIRCLE ( 'NONE', #83977, 1.020000000000000018 ) ;
#75879=DIRECTION ( 'NONE',  ( -0.000000000000000000, 1.000000000000000000, -0.000000000000000000 ) ) ;
#75880=DIRECTION ( 'NONE',  ( -0.000000000000000000, 1.000000000000000000, -0.000000000000000000 ) ) ;
#75882=EDGE_CURVE ( 'NONE', #68195, #51970, #68379, .T. ) ;
#75883=VERTEX_POINT ( 'NONE', #47236 ) ;
#75884=CARTESIAN_POINT ( 'NONE',  ( -2.889365861140832159, -5.876774720514409189, 19.43823095447973870 ) ) ;
#75893=EDGE_LOOP ( 'NONE', ( #97392, #18945, #14910, #52336 ) ) ;
#75894=CARTESIAN_POINT ( 'NONE',  ( 4.486687842132109694, -6.376774720514410077, 18.98221446873611029 ) ) ;
#75895=EDGE_LOOP ( 'NONE', ( #15707, #85533, #46138, #76143 ) ) ;
#75896=B_SPLINE_SURFACE_WITH_KNOTS ( 'NONE', 3, 1, ( 
 ( #30797, #100276 ),
 ( #13561, #22662 ),
 ( #5954, #68860 ),
 ( #67872, #52638 ),
 ( #98801, #23161 ),
 ( #6462, #61265 ),
 ( #83574, #60267 ),
 ( #53650, #53150 ),
 ( #14565, #30286 ),
 ( #84574, #69862 ),
 ( #37419, #45038 ),
 ( #76453, #38404 ),
 ( #54153, #99301 ),
 ( #60761, #91683 ),
 ( #85076, #99778 ),
 ( #15065, #46523 ),
 ( #46033, #76954 ),
 ( #7952, #38906 ),
 ( #342, #31290 ),
 ( #90699, #21177 ),
 ( #63775, #32794 ),
 ( #25175, #86578 ),
 ( #39904, #17569 ),
 ( #18069, #95197 ),
 ( #70869, #78956 ),
 ( #79467, #48031 ),
 ( #1359, #9958 ) ),
 .UNSPECIFIED., .F., .F., .F.,
 ( 4, 1, 1, 1, 1, 1, 1, 1, 1, 1, 1, 1, 1, 1, 1, 1, 1, 1, 1, 1, 1, 1, 1, 1, 4 ),
 ( 2, 2 ),
 ( 0.000000000000000000, 0.03382411656725048399, 0.06729808750146204499, 0.1002802584818396348, 0.1330193052712239643, 0.1657361602733768979, 0.1987916522134082209, 0.2323715308488600861, 0.2664085106932945202, 0.3010156638683363362, 0.3361963658896798268, 0.3719718800539335568, 0.4085735935688276088, 0.4463941065015575305, 0.4852253093620474411, 0.5253715673688824639, 0.5672243359416908604, 0.6110807138143398154, 0.6577496272202332239, 0.7070202039764021951, 0.7592353208322853986, 0.8144842367739216771, 0.8732268335334771869, 0.9349367103827220804, 1.000000000000000000 ),
 ( 0.000000000000000000, 1.000000000000000000 ),
 .UNSPECIFIED. ) ;
#75901=DIRECTION ( 'NONE',  ( 0.7071067811865476838, 0.000000000000000000, -0.7071067811865474617 ) ) ;
#75907=VERTEX_POINT ( 'NONE', #54856 ) ;
#75908=DIRECTION ( 'NONE',  ( -0.1311553622875919756, 6.845827386180409975E-16, -0.9913618264504692190 ) ) ;
#75913=ORIENTED_EDGE ( 'NONE', *, *, #45327, .F. ) ;
#75914=CARTESIAN_POINT ( 'NONE',  ( -10.36589631659242627, -6.376774720514426065, 27.85486277704324110 ) ) ;
#75917=ORIENTED_EDGE ( 'NONE', *, *, #1162, .T. ) ;
#75922=ORIENTED_EDGE ( 'NONE', *, *, #74447, .T. ) ;
#75923=DIRECTION ( 'NONE',  ( 0.000000000000000000, 0.000000000000000000, 1.000000000000000000 ) ) ;
#75925=DIRECTION ( 'NONE',  ( 0.000000000000000000, -1.000000000000000000, 0.000000000000000000 ) ) ;
#75955=CARTESIAN_POINT ( 'NONE',  ( -28.47875734969025885, 5.965225279485572685, -0.08597719988137125791 ) ) ;
#75958=LINE ( 'NONE', #6464, #10078 ) ;
#75963=LINE ( 'NONE', #53157, #2431 ) ;
#75968=AXIS2_PLACEMENT_3D ( 'NONE', #23030, #8329, #39274 ) ;
#75969=ADVANCED_FACE ( 'NONE', ( #1063 ), #78656, .T. ) ;
#75973=CARTESIAN_POINT ( 'NONE',  ( -5.023036858974361252, -6.376774720514410077, 19.14743589743590846 ) ) ;
#75980=DIRECTION ( 'NONE',  ( 0.6392559695863496705, 0.000000000000000000, 0.7689940216596069522 ) ) ;
#75987=VECTOR ( 'NONE', #56805, 1000.000000000000000 ) ;
#76000=EDGE_CURVE ( 'NONE', #65103, #81032, #554, .T. ) ;
#76013=VECTOR ( 'NONE', #10440, 1000.000000000000000 ) ;
#76017=CARTESIAN_POINT ( 'NONE',  ( 4.468667172983064262, -6.376774720514401196, 18.40700896291420463 ) ) ;
#76024=CARTESIAN_POINT ( 'NONE',  ( 5.641025641025643189, -5.876774720514419847, 20.78665865384615330 ) ) ;
#76026=CARTESIAN_POINT ( 'NONE',  ( 5.641025641025643189, -6.376774720514420736, 20.78665865384615330 ) ) ;
#76027=VERTEX_POINT ( 'NONE', #59225 ) ;
#76039=DIRECTION ( 'NONE',  ( 0.000000000000000000, 0.000000000000000000, 1.000000000000000000 ) ) ;
#76045=VERTEX_POINT ( 'NONE', #11172 ) ;
#76046=CARTESIAN_POINT ( 'NONE',  ( -2.889365861140832159, -6.376774720514410077, 19.43823095447973870 ) ) ;
#76052=AXIS2_PLACEMENT_3D ( 'NONE', #90465, #45298, #22427 ) ;
#76070=ORIENTED_EDGE ( 'NONE', *, *, #19882, .F. ) ;
#76071=CARTESIAN_POINT ( 'NONE',  ( -28.98875734969026396, -0.3587747205144262708, 0.1180228001186258285 ) ) ;
#76085=B_SPLINE_SURFACE_WITH_KNOTS ( 'NONE', 3, 1, ( 
 ( #32148, #63628 ),
 ( #71727, #2720 ),
 ( #72729, #2221 ),
 ( #79820, #86936 ),
 ( #41789, #72226 ),
 ( #71226, #63123 ),
 ( #94049, #40766 ),
 ( #10317, #24535 ),
 ( #94546, #17427 ),
 ( #55504, #57514 ),
 ( #41272, #79322 ),
 ( #86441, #96059 ),
 ( #78807, #64134 ),
 ( #18922, #87440 ),
 ( #9816, #17933 ) ),
 .UNSPECIFIED., .F., .F., .F.,
 ( 4, 1, 1, 1, 1, 1, 1, 1, 1, 1, 1, 1, 4 ),
 ( 2, 2 ),
 ( 0.000000000000000000, 0.07594930733582139215, 0.1485490724434445076, 0.2189955450926088787, 0.2861189618869318663, 0.3518258552346302803, 0.4160741612610824314, 0.4782648099120661023, 0.5403245897751369764, 0.6604051854372985364, 0.7746061160792699907, 0.8871865992555415525, 1.000000000000000000 ),
 ( 0.000000000000000000, 1.000000000000000000 ),
 .UNSPECIFIED. ) ;
#76100=VECTOR ( 'NONE', #78042, 1000.000000000000000 ) ;
#76104=ORIENTED_EDGE ( 'NONE', *, *, #97236, .T. ) ;
#76107=EDGE_CURVE ( 'NONE', #71192, #1547, #70043, .T. ) ;
#76112=CARTESIAN_POINT ( 'NONE',  ( 32.98733314340959311, -0.3587747205144265483, 2.074222136288530027 ) ) ;
#76113=CARTESIAN_POINT ( 'NONE',  ( 32.15269211224249091, -4.540774720514427543, 3.401810532325273417 ) ) ;
#76120=ORIENTED_EDGE ( 'NONE', *, *, #90586, .F. ) ;
#76124=VECTOR ( 'NONE', #64618, 1000.000000000000000 ) ;
#76127=CARTESIAN_POINT ( 'NONE',  ( 9.843544857143434967, 5.965225279485572685, -27.49819965379373343 ) ) ;
#76128=CARTESIAN_POINT ( 'NONE',  ( 3.552327343495968570, -5.876774720514426953, 21.81288606793570395 ) ) ;
#76129=VERTEX_POINT ( 'NONE', #57374 ) ;
#76132=CARTESIAN_POINT ( 'NONE',  ( 14.83405752585509596, -4.881907540129173384, -27.54622755360215791 ) ) ;
#76143=ORIENTED_EDGE ( 'NONE', *, *, #37676, .T. ) ;
#76145=B_SPLINE_CURVE_WITH_KNOTS ( 'NONE', 3,
 ( #84898, #167, #93502, #23478, #32110, #46343, #45849, #77274, #54460, #77767, #85394, #94010, #15884, #46848, #78272 ),
 .UNSPECIFIED., .F., .F.,
 ( 4, 1, 1, 1, 1, 1, 1, 1, 1, 1, 1, 1, 4 ),
 ( 0.000000000000000000, 0.09781818961471311358, 0.1997260534018265310, 0.3052763574779380207, 0.4158114905382894744, 0.4744722311435595752, 0.5372738797760960860, 0.6036574205596552112, 0.6742988630901243230, 0.7498344853162268731, 0.8285984767571009657, 0.9123777781577814272, 1.000000000000000000 ),
 .UNSPECIFIED. ) ;
#76150=CARTESIAN_POINT ( 'NONE',  ( -6.100820854657341918, -5.876774720514414518, 19.76359802465961124 ) ) ;
#76167=VECTOR ( 'NONE', #64693, 1000.000000000000000 ) ;
#76168=ADVANCED_FACE ( 'NONE', ( #8424, #45997, #83544 ), #7417, .F. ) ;
#76178=VECTOR ( 'NONE', #70144, 1000.000000000000000 ) ;
#76197=LINE ( 'NONE', #74219, #97687 ) ;
#76199=CARTESIAN_POINT ( 'NONE',  ( 32.58581522646812090, -4.151341569991283897, -4.025368652865530805 ) ) ;
#76200=CARTESIAN_POINT ( 'NONE',  ( -6.752792875861700850, -6.376774720514411854, 19.46247113826586528 ) ) ;
#76207=ORIENTED_EDGE ( 'NONE', *, *, #62015, .T. ) ;
#76215=CARTESIAN_POINT ( 'NONE',  ( -2.188401442307694289, -5.876774720514411854, 19.46153846153846700 ) ) ;
#76218=EDGE_LOOP ( 'NONE', ( #86542, #52974, #34732, #65292 ) ) ;
#76220=EDGE_CURVE ( 'NONE', #76129, #88212, #77417, .T. ) ;
#76261=VECTOR ( 'NONE', #87498, 1000.000000000000000 ) ;
#76277=CARTESIAN_POINT ( 'NONE',  ( -0.5830141525297981575, -6.376774720514410077, 19.15054976246387497 ) ) ;
#76279=EDGE_LOOP ( 'NONE', ( #23710, #94622, #37056, #56578, #69184, #25425, #92810 ) ) ;
#76286=ORIENTED_EDGE ( 'NONE', *, *, #94131, .F. ) ;
#76291=DIRECTION ( 'NONE',  ( 0.000000000000000000, 1.000000000000000000, 0.000000000000000000 ) ) ;
#76299=CARTESIAN_POINT ( 'NONE',  ( 3.559170184186323915, -6.376774720514402972, 18.55412939673608719 ) ) ;
#76300=CARTESIAN_POINT ( 'NONE',  ( 3.252808283508203058, -6.376774720514402972, 18.30939203766361345 ) ) ;
#76333=CARTESIAN_POINT ( 'NONE',  ( -5.576923076923074873, -6.376774720514427841, 21.75000000000000711 ) ) ;
#76336=CARTESIAN_POINT ( 'NONE',  ( -7.641025641025638748, -6.376774720514427841, 21.75000000000001066 ) ) ;
#76342=EDGE_CURVE ( 'NONE', #11758, #47988, #63742, .T. ) ;
#76345=ORIENTED_EDGE ( 'NONE', *, *, #76602, .T. ) ;
#76347=EDGE_CURVE ( 'NONE', #2790, #64651, #88059, .T. ) ;
#76348=LINE ( 'NONE', #68756, #53389 ) ;
#76359=PLANE ( 'NONE',  #94911 ) ;
#76362=CARTESIAN_POINT ( 'NONE',  ( 4.531089049250198286, -6.376774720514404748, 18.46391971337801508 ) ) ;
#76367=ORIENTED_EDGE ( 'NONE', *, *, #73163, .T. ) ;
#76374=CYLINDRICAL_SURFACE ( 'NONE', #34750, 130.2784398600581710 ) ;
#76380=CARTESIAN_POINT ( 'NONE',  ( -4.165021623707020559, -6.376774720514417183, 20.26087634804756377 ) ) ;
#76388=CARTESIAN_POINT ( 'NONE',  ( 4.214857194124448370, -6.376774720514402972, 18.65898740197609840 ) ) ;
#76389=EDGE_LOOP ( 'NONE', ( #95816, #59353, #60953, #93235, #89236, #26115, #87213, #23863, #26839, #21321, #81982 ) ) ;
#76390=CARTESIAN_POINT ( 'NONE',  ( -27.96875734969026084, -3.316774720514426456, 0.7300228001186309656 ) ) ;
#76404=ORIENTED_EDGE ( 'NONE', *, *, #63430, .F. ) ;
#76422=CARTESIAN_POINT ( 'NONE',  ( 13.36367879947601445, -6.376774720514426953, 20.00000000000000355 ) ) ;
#76424=DIRECTION ( 'NONE',  ( 0.000000000000000000, 0.000000000000000000, -1.000000000000000000 ) ) ;
#76426=CARTESIAN_POINT ( 'NONE',  ( -3.826923076923078426, -5.876774720514409189, 19.19230769230769695 ) ) ;
#76448=ADVANCED_FACE ( 'NONE', ( #67228 ), #16749, .T. ) ;
#76453=CARTESIAN_POINT ( 'NONE',  ( 3.050049012211247579, -6.376774720514426065, 21.53019692557248632 ) ) ;
#76456=AXIS2_PLACEMENT_3D ( 'NONE', #12805, #29531, #99530 ) ;
#76471=CARTESIAN_POINT ( 'NONE',  ( 3.296548071537245495, -6.376774720514426065, 21.29143507544719682 ) ) ;
#76478=CARTESIAN_POINT ( 'NONE',  ( -5.293508136514246232, -5.876774720514408301, 19.18727597066021318 ) ) ;
#76504=EDGE_CURVE ( 'NONE', #97458, #89315, #37263, .T. ) ;
#76506=CARTESIAN_POINT ( 'NONE',  ( 0.000000000000000000, -5.876774720514426953, 0.000000000000000000 ) ) ;
#76510=CARTESIAN_POINT ( 'NONE',  ( 15.29947330337540556, -3.405372460181236960, -27.16854002387011491 ) ) ;
#76519=CARTESIAN_POINT ( 'NONE',  ( 5.671135738765417322, -6.376774720514422512, 20.99074880795119924 ) ) ;
#76524=TOROIDAL_SURFACE ( 'NONE', #29520, 3.060000000000000053, 2.040000000000000036 ) ;
#76547=LINE ( 'NONE', #54248, #88477 ) ;
#76548=CARTESIAN_POINT ( 'NONE',  ( -20.27875734969026311, -4.776774720514394446, 24.00402280011862288 ) ) ;
#76553=PLANE ( 'NONE',  #48265 ) ;
#76560=ORIENTED_EDGE ( 'NONE', *, *, #15538, .F. ) ;
#76561=DIRECTION ( 'NONE',  ( -0.9822594791677485837, 0.000000000000000000, 0.1875268396392986980 ) ) ;
#76563=CARTESIAN_POINT ( 'NONE',  ( -28.98875734969026041, -3.316774720514426456, 26.43402280011862615 ) ) ;
#76577=CARTESIAN_POINT ( 'NONE',  ( 33.24104357593923709, -3.536202174476160920, -12.73333860248705740 ) ) ;
#76594=CARTESIAN_POINT ( 'NONE',  ( 26.73860345374794534, -1.682774720514426114, -7.113848178280766099 ) ) ;
#76597=DIRECTION ( 'NONE',  ( -0.6599726524652352877, 0.000000000000000000, 0.7512896232465892110 ) ) ;
#76599=ORIENTED_EDGE ( 'NONE', *, *, #29700, .T. ) ;
#76602=EDGE_CURVE ( 'NONE', #81766, #94651, #62599, .T. ) ;
#76616=CIRCLE ( 'NONE', #29631, 251.4258649670780699 ) ;
#76623=ORIENTED_EDGE ( 'NONE', *, *, #48794, .F. ) ;
#76629=ADVANCED_FACE ( 'NONE', ( #8303 ), #15910, .T. ) ;
#76638=ORIENTED_EDGE ( 'NONE', *, *, #19771, .F. ) ;
#76639=ORIENTED_EDGE ( 'NONE', *, *, #65140, .F. ) ;
#76653=CARTESIAN_POINT ( 'NONE',  ( 31.74473449900405697, -4.976825198871215328, -4.259190951192157293 ) ) ;
#76665=DIRECTION ( 'NONE',  ( -0.000000000000000000, -1.000000000000000000, -0.000000000000000000 ) ) ;
#76681=VECTOR ( 'NONE', #75836, 1000.000000000000000 ) ;
#76685=DIRECTION ( 'NONE',  ( -0.000000000000000000, 1.000000000000000000, -0.000000000000000000 ) ) ;
#76699=DIRECTION ( 'NONE',  ( -0.000000000000000000, 1.000000000000000000, -0.000000000000000000 ) ) ;
#76703=CARTESIAN_POINT ( 'NONE',  ( -3.108974358974359475, -6.376774720514417183, 20.36458333333334281 ) ) ;
#76707=CARTESIAN_POINT ( 'NONE',  ( 0.3085469314987323020, -5.876774720514413630, 19.52341893546493523 ) ) ;
#76726=CARTESIAN_POINT ( 'NONE',  ( -7.326923076923074873, -6.376774720514427841, 21.75000000000001066 ) ) ;
#76740=CARTESIAN_POINT ( 'NONE',  ( 3.769940963823357638, -5.876774720514402972, 18.16074422543206879 ) ) ;
#76745=ORIENTED_EDGE ( 'NONE', *, *, #95384, .T. ) ;
#76750=EDGE_LOOP ( 'NONE', ( #88418, #95232, #89615, #8279 ) ) ;
#76753=ORIENTED_EDGE ( 'NONE', *, *, #90090, .T. ) ;
#76754=ORIENTED_EDGE ( 'NONE', *, *, #44863, .F. ) ;
#76758=EDGE_LOOP ( 'NONE', ( #78731, #100329, #22793, #40439 ) ) ;
#76762=CARTESIAN_POINT ( 'NONE',  ( -7.617563585130437076, -6.376774720514411854, 19.95084900476494383 ) ) ;
#76763=CARTESIAN_POINT ( 'NONE',  ( 5.356969261897235768, -0.3587747205143965168, -28.55262118024313978 ) ) ;
#76764=CARTESIAN_POINT ( 'NONE',  ( 31.55236408230781819, -0.6647747205144264315, 19.84760796525321780 ) ) ;
#76768=CARTESIAN_POINT ( 'NONE',  ( 11.04644962722740864, -4.132774720514426292, -26.87113206189456704 ) ) ;
#76770=DIRECTION ( 'NONE',  ( 0.000000000000000000, -1.000000000000000000, 0.000000000000000000 ) ) ;
#76777=DIRECTION ( 'NONE',  ( -0.000000000000000000, 1.000000000000000000, -0.000000000000000000 ) ) ;
#76780=CARTESIAN_POINT ( 'NONE',  ( -27.61845239340658154, 5.965225279485594001, -10.37513603161905351 ) ) ;
#76792=CARTESIAN_POINT ( 'NONE',  ( 3.183477995988301945, -6.376774720514404748, 18.35601591497023577 ) ) ;
#76814=LINE ( 'NONE', #84444, #95884 ) ;
#76829=CARTESIAN_POINT ( 'NONE',  ( -0.005606649364735081555, -5.876774720514410077, 19.25713806424188235 ) ) ;
#76834=DIRECTION ( 'NONE',  ( 0.000000000000000000, 0.000000000000000000, 1.000000000000000000 ) ) ;
#76835=ORIENTED_EDGE ( 'NONE', *, *, #77591, .T. ) ;
#76848=DIRECTION ( 'NONE',  ( 0.000000000000000000, -1.000000000000000000, 0.000000000000000000 ) ) ;
#76852=CARTESIAN_POINT ( 'NONE',  ( 30.93860345374796594, 2.297196155479665158, 24.67598410064776715 ) ) ;
#76861=CARTESIAN_POINT ( 'NONE',  ( -4.289200894924355190, -6.376774720514413630, 19.85590024959437017 ) ) ;
#76863=AXIS2_PLACEMENT_3D ( 'NONE', #3907, #58678, #66311 ) ;
#76865=CARTESIAN_POINT ( 'NONE',  ( -3.004714864173751998, -6.376774720514411854, 19.63296556618507083 ) ) ;
#76869=CARTESIAN_POINT ( 'NONE',  ( -4.930333147521421822, -6.376774720514410077, 19.46306892155547530 ) ) ;
#76870=CARTESIAN_POINT ( 'NONE',  ( -28.32169924589829080, 5.965225279485592225, -8.244178532169447848 ) ) ;
#76872=DIRECTION ( 'NONE',  ( 0.000000000000000000, -1.000000000000000000, 0.000000000000000000 ) ) ;
#76876=CARTESIAN_POINT ( 'NONE',  ( -28.47875734969025885, 5.965225279485572685, -0.08597719988136941216 ) ) ;
#76880=VERTEX_POINT ( 'NONE', #16796 ) ;
#76881=ORIENTED_EDGE ( 'NONE', *, *, #41768, .T. ) ;
#76884=DIRECTION ( 'NONE',  ( -0.000000000000000000, 1.000000000000000000, -0.000000000000000000 ) ) ;
#76893=ORIENTED_EDGE ( 'NONE', *, *, #31061, .F. ) ;
#76914=VERTEX_POINT ( 'NONE', #26916 ) ;
#76933=CARTESIAN_POINT ( 'NONE',  ( -2.794793911895765870, -5.876774720514418071, 20.33046051580616265 ) ) ;
#76936=DIRECTION ( 'NONE',  ( 0.000000000000000000, -3.056206645085457922E-15, -1.000000000000000000 ) ) ;
#76937=CARTESIAN_POINT ( 'NONE',  ( 4.782775879418006859, -5.876774720514407413, 18.83817099474236656 ) ) ;
#76941=DIRECTION ( 'NONE',  ( 8.503546450866693616E-15, 0.000000000000000000, 1.000000000000000000 ) ) ;
#76950=EDGE_CURVE ( 'NONE', #32855, #40153, #82191, .T. ) ;
#76954=CARTESIAN_POINT ( 'NONE',  ( 2.787364042957740651, -5.876774720514424288, 21.14548745790758488 ) ) ;
#76960=( NAMED_UNIT ( * ) SI_UNIT ( $, .STERADIAN. ) SOLID_ANGLE_UNIT ( ) );
#76962=CARTESIAN_POINT ( 'NONE',  ( -13.57581083383196940, -5.876774720514426953, 20.21213203435597094 ) ) ;
#76970=CARTESIAN_POINT ( 'NONE',  ( 0.3910256410256383042, -6.376774720514408301, 19.19230769230768985 ) ) ;
#76981=LINE ( 'NONE', #100306, #41134 ) ;
#77000=CARTESIAN_POINT ( 'NONE',  ( 33.12653832968937451, -0.3587747205144265483, -7.315055336576590683 ) ) ;
#77005=VERTEX_POINT ( 'NONE', #74579 ) ;
#77010=ORIENTED_EDGE ( 'NONE', *, *, #65787, .F. ) ;
#77011=ORIENTED_EDGE ( 'NONE', *, *, #38222, .T. ) ;
#77026=CARTESIAN_POINT ( 'NONE',  ( 6.509931258083027750, -6.376774720514417183, 20.09204137875607188 ) ) ;
#77028=ORIENTED_EDGE ( 'NONE', *, *, #81807, .T. ) ;
#77030=VERTEX_POINT ( 'NONE', #42659 ) ;
#77034=ORIENTED_EDGE ( 'NONE', *, *, #70573, .F. ) ;
#77047=PLANE ( 'NONE',  #71206 ) ;
#77048=FACE_OUTER_BOUND ( 'NONE', #88167, .T. ) ;
#77054=CARTESIAN_POINT ( 'NONE',  ( 13.57581083383197296, -6.376774720514426953, 19.78786796564403616 ) ) ;
#77073=EDGE_LOOP ( 'NONE', ( #83525, #50320 ) ) ;
#77076=EDGE_CURVE ( 'NONE', #55189, #46432, #39563, .T. ) ;
#77077=AXIS2_PLACEMENT_3D ( 'NONE', #33822, #65307, #11480 ) ;
#77078=CARTESIAN_POINT ( 'NONE',  ( 33.47959399259596580, -3.475369878553063341, -12.33463419434873032 ) ) ;
#77086=VECTOR ( 'NONE', #15414, 1000.000000000000000 ) ;
#77087=CARTESIAN_POINT ( 'NONE',  ( -0.7827064370038755436, -5.876774720514410077, 19.55912026249540148 ) ) ;
#77096=VERTEX_POINT ( 'NONE', #76071 ) ;
#77099=CARTESIAN_POINT ( 'NONE',  ( 14.76093561896379214, -3.316774720514426456, -26.55548769130089681 ) ) ;
#77110=CARTESIAN_POINT ( 'NONE',  ( 2.903846153846159517, -6.376774720514415407, 19.99999999999999289 ) ) ;
#77113=ORIENTED_EDGE ( 'NONE', *, *, #23179, .T. ) ;
#77119=ORIENTED_EDGE ( 'NONE', *, *, #77466, .T. ) ;
#77122=CARTESIAN_POINT ( 'NONE',  ( -7.347880794884120722E-16, -4.056774720514426669, -6.000000000000000888 ) ) ;
#77132=CARTESIAN_POINT ( 'NONE',  ( 25.08009522652915635, -5.127174019380943193, -9.013305873660419465 ) ) ;
#77137=FACE_OUTER_BOUND ( 'NONE', #45431, .T. ) ;
#77143=EDGE_CURVE ( 'NONE', #29097, #87273, #98907, .T. ) ;
#77161=CARTESIAN_POINT ( 'NONE',  ( 31.62500054620284473, -6.365374413700245704, 26.93529845007237711 ) ) ;
#77165=DIRECTION ( 'NONE',  ( 1.420947339892994047E-14, 0.000000000000000000, -1.000000000000000000 ) ) ;
#77168=DIRECTION ( 'NONE',  ( -0.9913618264504691080, 4.164321980682960499E-15, 0.1311553622875927805 ) ) ;
#77176=ORIENTED_EDGE ( 'NONE', *, *, #1107, .F. ) ;
#77190=DIRECTION ( 'NONE',  ( 0.000000000000000000, 0.000000000000000000, 1.000000000000000000 ) ) ;
#77193=CARTESIAN_POINT ( 'NONE',  ( -1.304987980769231948, -5.876774720514413630, 19.76512419871795245 ) ) ;
#77210=CARTESIAN_POINT ( 'NONE',  ( 5.402409956206937203, -5.876774720514423400, 21.18719775722114917 ) ) ;
#77211=VECTOR ( 'NONE', #10767, 1000.000000000000000 ) ;
#77212=ORIENTED_EDGE ( 'NONE', *, *, #90788, .F. ) ;
#77229=CARTESIAN_POINT ( 'NONE',  ( -6.636054160061366503, -6.376774720514411854, 19.15289935703627933 ) ) ;
#77241=ADVANCED_FACE ( 'NONE', ( #99892 ), #100124, .T. ) ;
#77244=CIRCLE ( 'NONE', #38448, 11.85241003308275864 ) ;
#77249=DIRECTION ( 'NONE',  ( -0.000000000000000000, -1.000000000000000000, -0.000000000000000000 ) ) ;
#77260=VERTEX_POINT ( 'NONE', #23788 ) ;
#77274=CARTESIAN_POINT ( 'NONE',  ( 7.344278919687202922, -5.876774720514417183, 20.19896341048075783 ) ) ;
#77276=CARTESIAN_POINT ( 'NONE',  ( 32.54161589056530346, -4.044086941844335925, -1.517980283019001453 ) ) ;
#77277=ORIENTED_EDGE ( 'NONE', *, *, #34815, .F. ) ;
#77287=CARTESIAN_POINT ( 'NONE',  ( 5.635247460261607166, -5.876774720514424288, 21.53093896358932469 ) ) ;
#77290=EDGE_LOOP ( 'NONE', ( #48805, #75404, #72286, #86962 ) ) ;
#77291=CIRCLE ( 'NONE', #51387, 129.7684398600581517 ) ;
#77294=AXIS2_PLACEMENT_3D ( 'NONE', #93619, #16495, #8897 ) ;
#77298=CARTESIAN_POINT ( 'NONE',  ( 2.936453026386435017, -6.376774720514406525, 18.60215244312560401 ) ) ;
#77299=LINE ( 'NONE', #61108, #99849 ) ;
#77305=ORIENTED_EDGE ( 'NONE', *, *, #12334, .T. ) ;
#77325=CARTESIAN_POINT ( 'NONE',  ( -0.3982818654701407723, -5.876774720514410966, 19.46306892155547530 ) ) ;
#77334=EDGE_LOOP ( 'NONE', ( #35188, #94560, #35923, #89867 ) ) ;
#77338=ORIENTED_EDGE ( 'NONE', *, *, #8788, .T. ) ;
#77351=ORIENTED_EDGE ( 'NONE', *, *, #26642, .T. ) ;
#77358=CARTESIAN_POINT ( 'NONE',  ( 4.039061187531148178, -6.376774720514401196, 18.18637930035166761 ) ) ;
#77359=DIRECTION ( 'NONE',  ( -0.000000000000000000, 1.000000000000000000, -0.000000000000000000 ) ) ;
#77362=ORIENTED_EDGE ( 'NONE', *, *, #46869, .T. ) ;
#77368=CARTESIAN_POINT ( 'NONE',  ( -4.635780534842457001, -6.376774720514410077, 19.53657742262743113 ) ) ;
#77373=PLANE ( 'NONE',  #33786 ) ;
#77375=CARTESIAN_POINT ( 'NONE',  ( -4.141025641025641413, -6.376774720514420736, 20.67377804487180271 ) ) ;
#77377=ORIENTED_EDGE ( 'NONE', *, *, #88684, .F. ) ;
#77378=FACE_BOUND ( 'NONE', #70418, .T. ) ;
#77380=EDGE_CURVE ( 'NONE', #1020, #39331, #94803, .T. ) ;
#77389=CARTESIAN_POINT ( 'NONE',  ( 31.25756411700558601, -5.804570343751186634, -1.813502816810933949 ) ) ;
#77391=CARTESIAN_POINT ( 'NONE',  ( 10.22011794244940752, -3.316774720515020203, -27.02313658111319938 ) ) ;
#77393=LINE ( 'NONE', #23104, #89047 ) ;
#77403=ORIENTED_EDGE ( 'NONE', *, *, #65518, .T. ) ;
#77417=LINE ( 'NONE', #54606, #16657 ) ;
#77433=CARTESIAN_POINT ( 'NONE',  ( -2.786875287040666560, -5.876774720514418071, 20.09505574050193388 ) ) ;
#77436=FACE_OUTER_BOUND ( 'NONE', #28205, .T. ) ;
#77440=ORIENTED_EDGE ( 'NONE', *, *, #70156, .T. ) ;
#77446=DIRECTION ( 'NONE',  ( 1.000000000000000000, 0.000000000000000000, 0.000000000000000000 ) ) ;
#77466=EDGE_CURVE ( 'NONE', #22711, #32453, #10567, .T. ) ;
#77473=EDGE_CURVE ( 'NONE', #14898, #63088, #58256, .T. ) ;
#77483=DIRECTION ( 'NONE',  ( -0.000000000000000000, 1.000000000000000000, -0.000000000000000000 ) ) ;
#77486=ORIENTED_EDGE ( 'NONE', *, *, #31146, .T. ) ;
#77488=EDGE_LOOP ( 'NONE', ( #11640, #32459, #63710, #59833 ) ) ;
#77506=EDGE_CURVE ( 'NONE', #42081, #50071, #16722, .T. ) ;
#77511=CARTESIAN_POINT ( 'NONE',  ( 32.60294298177596062, 6.475225279485573360, -11.48871326860665043 ) ) ;
#77515=CARTESIAN_POINT ( 'NONE',  ( -1.358974358974355257, -6.376774720514427841, 21.75000000000000711 ) ) ;
#77521=FACE_BOUND ( 'NONE', #44718, .T. ) ;
#77524=EDGE_CURVE ( 'NONE', #23209, #57615, #20667, .T. ) ;
#77528=AXIS2_PLACEMENT_3D ( 'NONE', #2610, #25930, #42181 ) ;
#77529=ORIENTED_EDGE ( 'NONE', *, *, #43436, .T. ) ;
#77533=ORIENTED_EDGE ( 'NONE', *, *, #18337, .F. ) ;
#77543=CARTESIAN_POINT ( 'NONE',  ( 14.43441819135927950, -3.316774720514427344, -28.36222020317712378 ) ) ;
#77552=FACE_OUTER_BOUND ( 'NONE', #42591, .T. ) ;
#77565=CARTESIAN_POINT ( 'NONE',  ( -6.033988668995577065, -5.876774720514413630, 19.86422795159478483 ) ) ;
#77582=VECTOR ( 'NONE', #27314, 1000.000000000000000 ) ;
#77590=EDGE_CURVE ( 'NONE', #67166, #40197, #20170, .T. ) ;
#77591=EDGE_CURVE ( 'NONE', #35025, #31553, #27536, .T. ) ;
#77603=VERTEX_POINT ( 'NONE', #82079 ) ;
#77609=VERTEX_POINT ( 'NONE', #68356 ) ;
#77611=LINE ( 'NONE', #56697, #68019 ) ;
#77624=EDGE_LOOP ( 'NONE', ( #82782, #74643, #38935, #66725, #34418 ) ) ;
#77628=ORIENTED_EDGE ( 'NONE', *, *, #29816, .T. ) ;
#77635=PLANE ( 'NONE',  #20728 ) ;
#77645=ORIENTED_EDGE ( 'NONE', *, *, #66406, .F. ) ;
#77657=ORIENTED_EDGE ( 'NONE', *, *, #20612, .F. ) ;
#77661=CARTESIAN_POINT ( 'NONE',  ( 29.67519708478274865, -5.974976214603829661, 27.68766025429119537 ) ) ;
#77667=LINE ( 'NONE', #39117, #89189 ) ;
#77668=CARTESIAN_POINT ( 'NONE',  ( -5.576843645946834016, -5.876774720514418959, 20.41272575174755133 ) ) ;
#77691=CARTESIAN_POINT ( 'NONE',  ( 5.541369867593821219, -6.376774720514426065, 21.42815349816763160 ) ) ;
#77697=EDGE_CURVE ( 'NONE', #99971, #47988, #58825, .T. ) ;
#77700=VERTEX_POINT ( 'NONE', #23660 ) ;
#77708=VECTOR ( 'NONE', #25070, 1000.000000000000000 ) ;
#77712=CARTESIAN_POINT ( 'NONE',  ( -3.071531057816138333, -5.876774720514414518, 19.86545874326175110 ) ) ;
#77714=CARTESIAN_POINT ( 'NONE',  ( 5.326923076923078426, -5.876774720514419847, 20.76772836538461320 ) ) ;
#77715=VERTEX_POINT ( 'NONE', #53642 ) ;
#77732=ORIENTED_EDGE ( 'NONE', *, *, #3194, .T. ) ;
#77734=LINE ( 'NONE', #16350, #76178 ) ;
#77765=CARTESIAN_POINT ( 'NONE',  ( 6.480733632922428988, -6.376774720514426065, 21.47849199606610782 ) ) ;
#77767=CARTESIAN_POINT ( 'NONE',  ( 7.275731542451676859, -5.876774720514415407, 20.06332870126568224 ) ) ;
#77768=LINE ( 'NONE', #30613, #36263 ) ;
#77774=CARTESIAN_POINT ( 'NONE',  ( -23.59123376470063960, -5.356774720514425603, 23.50402280011862288 ) ) ;
#77782=DIRECTION ( 'NONE',  ( 0.000000000000000000, 0.000000000000000000, -1.000000000000000000 ) ) ;
#77789=FACE_OUTER_BOUND ( 'NONE', #68058, .T. ) ;
#77792=CARTESIAN_POINT ( 'NONE',  ( 4.885870204371583370, -6.376774720514420736, 20.85936027411790405 ) ) ;
#77797=DIRECTION ( 'NONE',  ( 0.000000000000000000, 0.000000000000000000, -1.000000000000000000 ) ) ;
#77798=ORIENTED_EDGE ( 'NONE', *, *, #29148, .F. ) ;
#77808=EDGE_CURVE ( 'NONE', #49731, #7781, #57516, .T. ) ;
#77822=CARTESIAN_POINT ( 'NONE',  ( 11.98973536156539943, -2.682774720514426559, -26.26140391504922178 ) ) ;
#77824=CARTESIAN_POINT ( 'NONE',  ( -7.640476926272304681, -5.876774720514415407, 20.25188360057253689 ) ) ;
#77844=CARTESIAN_POINT ( 'NONE',  ( 282.9764569301858046, -4.540774720514427543, 20.79159422840526616 ) ) ;
#77855=DIRECTION ( 'NONE',  ( -0.000000000000000000, -1.000000000000000000, -0.000000000000000000 ) ) ;
#77870=DIRECTION ( 'NONE',  ( 1.000000000000000000, 0.000000000000000000, 0.000000000000000000 ) ) ;
#77874=CARTESIAN_POINT ( 'NONE',  ( -1.380763273332680896, -5.876774720514418071, 20.28973052848695602 ) ) ;
#77880=DIRECTION ( 'NONE',  ( 0.1827036106964188555, 0.000000000000000000, -0.9831680378442393398 ) ) ;
#77894=VERTEX_POINT ( 'NONE', #60996 ) ;
#77897=CARTESIAN_POINT ( 'NONE',  ( 8.978253834636468866, -6.376774720514426953, 18.51871304725684553 ) ) ;
#77911=ORIENTED_EDGE ( 'NONE', *, *, #1189, .F. ) ;
#77924=CARTESIAN_POINT ( 'NONE',  ( -7.641025641025638748, -6.376774720514427841, 21.75000000000001066 ) ) ;
#77933=CARTESIAN_POINT ( 'NONE',  ( 13.91401389203221406, 5.965225279485572685, 27.75920385068456042 ) ) ;
#77948=DIRECTION ( 'NONE',  ( -0.000000000000000000, -1.000000000000000000, -0.000000000000000000 ) ) ;
#77949=EDGE_CURVE ( 'NONE', #68153, #98254, #6197, .T. ) ;
#77950=CARTESIAN_POINT ( 'NONE',  ( -8.978253834636468866, -5.876774720514426953, 0.000000000000000000 ) ) ;
#77956=CARTESIAN_POINT ( 'NONE',  ( 14.98380649186719538, -3.494980989714896680, -27.33501059067317485 ) ) ;
#77960=ORIENTED_EDGE ( 'NONE', *, *, #86998, .F. ) ;
#77964=CARTESIAN_POINT ( 'NONE',  ( -5.596556251055551101, -6.376774720514411854, 19.35667676486397681 ) ) ;
#77970=AXIS2_PLACEMENT_3D ( 'NONE', #96046, #2711, #57505 ) ;
#77973=CARTESIAN_POINT ( 'NONE',  ( -5.654682302363691626, -6.376774720514411854, 19.41635569784906323 ) ) ;
#77978=CARTESIAN_POINT ( 'NONE',  ( 30.53060340732036337, -5.330559497947037428, 2.122526108693120861 ) ) ;
#77979=EDGE_LOOP ( 'NONE', ( #6606, #49234, #46470, #61297 ) ) ;
#77994=DIRECTION ( 'NONE',  ( 1.000000000000000000, 0.000000000000000000, -5.238131417152343399E-15 ) ) ;
#77995=CARTESIAN_POINT ( 'NONE',  ( 4.017909867803298063, -6.376774720514402972, 18.55402206357357286 ) ) ;
#78015=DIRECTION ( 'NONE',  ( 0.000000000000000000, 0.000000000000000000, 1.000000000000000000 ) ) ;
#78019=DIRECTION ( 'NONE',  ( 0.000000000000000000, 0.000000000000000000, 1.000000000000000000 ) ) ;
#78023=ADVANCED_FACE ( 'NONE', ( #41164 ), #79206, .F. ) ;
#78025=CARTESIAN_POINT ( 'NONE',  ( 29.77147767949870527, -4.540774720514427543, 26.15915692125055614 ) ) ;
#78026=ORIENTED_EDGE ( 'NONE', *, *, #12155, .F. ) ;
#78040=ADVANCED_FACE ( 'NONE', ( #40155 ), #63512, .F. ) ;
#78042=DIRECTION ( 'NONE',  ( -0.000000000000000000, 1.000000000000000000, -0.000000000000000000 ) ) ;
#78048=VECTOR ( 'NONE', #22150, 1000.000000000000000 ) ;
#78050=DIRECTION ( 'NONE',  ( 0.000000000000000000, 0.000000000000000000, 1.000000000000000000 ) ) ;
#78054=DIRECTION ( 'NONE',  ( -0.000000000000000000, 1.000000000000000000, -0.000000000000000000 ) ) ;
#78061=FACE_OUTER_BOUND ( 'NONE', #41878, .T. ) ;
#78068=FACE_OUTER_BOUND ( 'NONE', #76218, .T. ) ;
#78069=VECTOR ( 'NONE', #10814, 1000.000000000000000 ) ;
#78097=AXIS2_PLACEMENT_3D ( 'NONE', #100355, #53724, #84655 ) ;
#78100=VERTEX_POINT ( 'NONE', #87836 ) ;
#78104=CARTESIAN_POINT ( 'NONE',  ( -7.312991930324885814, -5.876774720514414518, 20.02088365235844947 ) ) ;
#78115=AXIS2_PLACEMENT_3D ( 'NONE', #88455, #88954, #58512 ) ;
#78121=VERTEX_POINT ( 'NONE', #66025 ) ;
#78124=DIRECTION ( 'NONE',  ( -0.000000000000000000, 0.000000000000000000, -1.000000000000000000 ) ) ;
#78136=ORIENTED_EDGE ( 'NONE', *, *, #15077, .F. ) ;
#78140=B_SPLINE_CURVE_WITH_KNOTS ( 'NONE', 3,
 ( #9614, #53416, #39565, #16220, #47185, #78104, #70515, #1006, #78602, #9111, #40070, #71024, #32452, #24831, #55808, #40575, #71527, #19218, #49199 ),
 .UNSPECIFIED., .F., .F.,
 ( 4, 1, 1, 1, 1, 1, 1, 1, 1, 1, 1, 1, 1, 1, 1, 1, 4 ),
 ( 0.000000000000000000, 0.07834298519370234970, 0.1505633028794191031, 0.2161510566599780803, 0.2756797924514261533, 0.3287070503654628273, 0.3759044348322084228, 0.4173018977400322349, 0.4526927480535833936, 0.5172652917530119465, 0.5812165680623057051, 0.6453218939728029291, 0.7120244933797633680, 0.7801300447160454121, 0.8502182262116654288, 0.9226485217347378809, 1.000000000000000000 ),
 .UNSPECIFIED. ) ;
#78148=CARTESIAN_POINT ( 'NONE',  ( 3.025806405283164136, -5.876774720514419847, 20.84867811309776542 ) ) ;
#78157=EDGE_CURVE ( 'NONE', #97072, #16621, #18328, .T. ) ;
#78158=EDGE_CURVE ( 'NONE', #45042, #71192, #4101, .T. ) ;
#78159=CARTESIAN_POINT ( 'NONE',  ( 31.63608488009066733, -3.316774720514426456, 27.34773273846990804 ) ) ;
#78161=ADVANCED_FACE ( 'NONE', ( #10710 ), #34561, .F. ) ;
#78166=LINE ( 'NONE', #33515, #45444 ) ;
#78177=LINE ( 'NONE', #85810, #89246 ) ;
#78188=ORIENTED_EDGE ( 'NONE', *, *, #34671, .F. ) ;
#78189=AXIS2_PLACEMENT_3D ( 'NONE', #11323, #27048, #25544 ) ;
#78197=CARTESIAN_POINT ( 'NONE',  ( 31.90158556755667973, -4.901725665521331265, -4.230180255418043878 ) ) ;
#78205=ORIENTED_EDGE ( 'NONE', *, *, #35893, .T. ) ;
#78215=DIRECTION ( 'NONE',  ( -0.7689940216596065081, 0.000000000000000000, 0.6392559695863502256 ) ) ;
#78221=VECTOR ( 'NONE', #100333, 1000.000000000000000 ) ;
#78234=CARTESIAN_POINT ( 'NONE',  ( 22.81105451610979173, -1.684774720501991396, -18.46691820600746681 ) ) ;
#78248=CARTESIAN_POINT ( 'NONE',  ( 3.714584954927674154, -5.876774720514402972, 18.16171433633635246 ) ) ;
#78256=ORIENTED_EDGE ( 'NONE', *, *, #19976, .T. ) ;
#78258=VERTEX_POINT ( 'NONE', #3606 ) ;
#78262=DIRECTION ( 'NONE',  ( -0.000000000000000000, 1.000000000000000000, -0.000000000000000000 ) ) ;
#78268=CARTESIAN_POINT ( 'NONE',  ( 6.259688558337090036, -5.876774720514413630, 19.73360741988579292 ) ) ;
#78271=EDGE_LOOP ( 'NONE', ( #63458, #52958 ) ) ;
#78272=CARTESIAN_POINT ( 'NONE',  ( 7.089543269230769162, -5.876774720514413630, 19.75741185897435415 ) ) ;
#78283=CARTESIAN_POINT ( 'NONE',  ( -2.701720430790311767, 5.965225279485594001, -28.90526747363640681 ) ) ;
#78296=DIRECTION ( 'NONE',  ( -0.9978940991575084851, 0.000000000000000000, -0.06486421869277853025 ) ) ;
#78297=AXIS2_PLACEMENT_3D ( 'NONE', #21503, #19642, #27765 ) ;
#78299=EDGE_CURVE ( 'NONE', #13389, #41697, #15694, .T. ) ;
#78300=ORIENTED_EDGE ( 'NONE', *, *, #84533, .T. ) ;
#78301=CARTESIAN_POINT ( 'NONE',  ( 4.585161930874343206, -5.876774720514426953, 21.47592444013076118 ) ) ;
#78312=LINE ( 'NONE', #16411, #68241 ) ;
#78316=CARTESIAN_POINT ( 'NONE',  ( 4.215004826710222474, -6.376774720514427841, 21.34072927444733381 ) ) ;
#78323=AXIS2_PLACEMENT_3D ( 'NONE', #67439, #61332, #60834 ) ;
#78353=DIRECTION ( 'NONE',  ( 0.000000000000000000, 0.000000000000000000, 1.000000000000000000 ) ) ;
#78359=LINE ( 'NONE', #56559, #63899 ) ;
#78364=VECTOR ( 'NONE', #52000, 1000.000000000000000 ) ;
#78379=FACE_OUTER_BOUND ( 'NONE', #17257, .T. ) ;
#78391=LINE ( 'NONE', #48471, #99670 ) ;
#78394=CARTESIAN_POINT ( 'NONE',  ( 11.25623914429021788, -3.316774720514424235, -27.04805245727492391 ) ) ;
#78407=CARTESIAN_POINT ( 'NONE',  ( -6.487934372591614540, -6.376774720514411854, 19.49432735726520605 ) ) ;
#78411=EDGE_CURVE ( 'NONE', #20807, #35661, #73484, .T. ) ;
#78428=CARTESIAN_POINT ( 'NONE',  ( -5.755030174389611730, -5.876774720514410966, 19.56655654527324728 ) ) ;
#78443=LINE ( 'NONE', #8944, #21329 ) ;
#78444=EDGE_LOOP ( 'NONE', ( #5645, #79275, #71637, #96350 ) ) ;
#78455=CARTESIAN_POINT ( 'NONE',  ( 4.281508569253434260, -5.876774720514421624, 21.28700241941785265 ) ) ;
#78465=CARTESIAN_POINT ( 'NONE',  ( 14.76069831378246455, -3.399792337529337516, -27.38466329193519755 ) ) ;
#78467=AXIS2_PLACEMENT_3D ( 'NONE', #45953, #6876, #100194 ) ;
#78469=ORIENTED_EDGE ( 'NONE', *, *, #49228, .F. ) ;
#78481=PLANE ( 'NONE',  #21875 ) ;
#78486=DIRECTION ( 'NONE',  ( 0.000000000000000000, 0.000000000000000000, -1.000000000000000000 ) ) ;
#78490=ORIENTED_EDGE ( 'NONE', *, *, #95002, .T. ) ;
#78502=ORIENTED_EDGE ( 'NONE', *, *, #80056, .T. ) ;
#78504=DIRECTION ( 'NONE',  ( -0.000000000000000000, 1.000000000000000000, -0.000000000000000000 ) ) ;
#78511=FACE_OUTER_BOUND ( 'NONE', #73275, .T. ) ;
#78518=FACE_BOUND ( 'NONE', #60676, .T. ) ;
#78521=LINE ( 'NONE', #30863, #96166 ) ;
#78524=ADVANCED_FACE ( 'NONE', ( #34426 ), #88716, .F. ) ;
#78540=AXIS2_PLACEMENT_3D ( 'NONE', #50204, #20732, #28350 ) ;
#78542=DIRECTION ( 'NONE',  ( 0.000000000000000000, 1.000000000000000000, 0.000000000000000000 ) ) ;
#78544=FACE_BOUND ( 'NONE', #2920, .T. ) ;
#78562=CARTESIAN_POINT ( 'NONE',  ( -6.377963355984652694, -5.876774720514411854, 19.53740760792478426 ) ) ;
#78570=AXIS2_PLACEMENT_3D ( 'NONE', #36291, #20544, #90073 ) ;
#78577=LINE ( 'NONE', #72498, #67189 ) ;
#78580=CARTESIAN_POINT ( 'NONE',  ( -0.4686347352592966087, -6.376774720514411854, 19.46274624311237034 ) ) ;
#78602=CARTESIAN_POINT ( 'NONE',  ( -7.282824509310913186, -5.876774720514415407, 19.84584863393302356 ) ) ;
#78605=ORIENTED_EDGE ( 'NONE', *, *, #3766, .F. ) ;
#78608=AXIS2_PLACEMENT_3D ( 'NONE', #98206, #5869, #68773 ) ;
#78617=CARTESIAN_POINT ( 'NONE',  ( -4.886549725601808447, -6.376774720514410077, 19.15251819062245175 ) ) ;
#78627=CARTESIAN_POINT ( 'NONE',  ( 26.14999174255633463, -4.132774720517320866, -11.56127575336603286 ) ) ;
#78631=DIRECTION ( 'NONE',  ( -0.06916465693916189206, 0.000000000000000000, 0.9976052577199502336 ) ) ;
#78653=CARTESIAN_POINT ( 'NONE',  ( 282.9764569301858046, 5.965225279485572685, 20.79159422840526616 ) ) ;
#78656=PLANE ( 'NONE',  #23006 ) ;
#78657=DIRECTION ( 'NONE',  ( -0.000000000000000000, 1.000000000000000000, -0.000000000000000000 ) ) ;
#78672=AXIS2_PLACEMENT_3D ( 'NONE', #50231, #97395, #43116 ) ;
#78691=CARTESIAN_POINT ( 'NONE',  ( 5.641025641025643189, -6.376774720514420736, 20.78665865384615330 ) ) ;
#78702=CARTESIAN_POINT ( 'NONE',  ( -9.543201319291914093E-14, -5.876774720514426953, 18.21871304725679508 ) ) ;
#78705=EDGE_CURVE ( 'NONE', #65522, #15238, #20683, .T. ) ;
#78709=EDGE_CURVE ( 'NONE', #64573, #42081, #29800, .T. ) ;
#78724=VECTOR ( 'NONE', #41562, 1000.000000000000000 ) ;
#78731=ORIENTED_EDGE ( 'NONE', *, *, #5353, .F. ) ;
#78732=VECTOR ( 'NONE', #57477, 1000.000000000000000 ) ;
#78739=CARTESIAN_POINT ( 'NONE',  ( 6.058092820189922456, -6.376774720514413630, 19.77091638250125882 ) ) ;
#78742=AXIS2_PLACEMENT_3D ( 'NONE', #94419, #1078, #64005 ) ;
#78752=CARTESIAN_POINT ( 'NONE',  ( 32.84232313084854837, -4.840274619473185602, -11.71291885348858663 ) ) ;
#78757=EDGE_CURVE ( 'NONE', #18993, #66329, #93826, .T. ) ;
#78759=DIRECTION ( 'NONE',  ( 0.000000000000000000, 1.000000000000000000, 0.000000000000000000 ) ) ;
#78767=CARTESIAN_POINT ( 'NONE',  ( 0.7051282051282027341, -6.376774720514408301, 19.19230769230768985 ) ) ;
#78769=CARTESIAN_POINT ( 'NONE',  ( -1.122631020312409245, -6.376774720514411854, 19.41635569784906679 ) ) ;
#78770=VERTEX_POINT ( 'NONE', #14064 ) ;
#78778=EDGE_LOOP ( 'NONE', ( #2508, #28836, #78490, #32354, #82389, #68886 ) ) ;
#78792=CARTESIAN_POINT ( 'NONE',  ( -5.486124437288584232, -5.876774720514415407, 19.74568812963598319 ) ) ;
#78795=CARTESIAN_POINT ( 'NONE',  ( 4.885870204371583370, -5.876774720514419847, 20.85936027411790405 ) ) ;
#78805=VECTOR ( 'NONE', #70117, 1000.000000000000000 ) ;
#78807=CARTESIAN_POINT ( 'NONE',  ( 3.671066620544169101, -6.376774720514424288, 21.47597918715562670 ) ) ;
#78820=ORIENTED_EDGE ( 'NONE', *, *, #34931, .T. ) ;
#78824=DIRECTION ( 'NONE',  ( 0.5473052603538087757, -5.646564643389147554E-15, 0.8369330630277725946 ) ) ;
#78846=DIRECTION ( 'NONE',  ( 0.000000000000000000, 0.000000000000000000, -1.000000000000000000 ) ) ;
#78855=CARTESIAN_POINT ( 'NONE',  ( 22.02124265030973760, 6.143225279485574397, 16.20402280011862217 ) ) ;
#78858=EDGE_LOOP ( 'NONE', ( #38957, #39848, #89988, #35804, #89759, #81851, #35093, #95039, #67053, #51934, #68315, #70655 ) ) ;
#78860=ORIENTED_EDGE ( 'NONE', *, *, #27030, .T. ) ;
#78862=LINE ( 'NONE', #63172, #46935 ) ;
#78870=DIRECTION ( 'NONE',  ( 0.000000000000000000, 1.000000000000000000, 0.000000000000000000 ) ) ;
#78881=DIRECTION ( 'NONE',  ( -0.000000000000000000, 1.000000000000000000, -0.000000000000000000 ) ) ;
#78892=CARTESIAN_POINT ( 'NONE',  ( 6.190876379677949792, -3.316774720513832708, -27.38145114071290465 ) ) ;
#78899=EDGE_LOOP ( 'NONE', ( #51435, #44497, #32579, #86509 ) ) ;
#78910=ORIENTED_EDGE ( 'NONE', *, *, #14033, .T. ) ;
#78915=CARTESIAN_POINT ( 'NONE',  ( -8.978253834636468866, -5.876774720514426953, 18.51871304725684553 ) ) ;
#78926=CYLINDRICAL_SURFACE ( 'NONE', #55272, 0.8160000000000007248 ) ;
#78933=CARTESIAN_POINT ( 'NONE',  ( 30.45304879119406039, -1.682774720514426114, -10.07140455160086390 ) ) ;
#78940=CARTESIAN_POINT ( 'NONE',  ( -2.373828433815573735, -5.876774720514410966, 19.48240003225459915 ) ) ;
#78945=CARTESIAN_POINT ( 'NONE',  ( 4.931982383686722926, -5.876774720514412742, 19.38944687450761961 ) ) ;
#78956=CARTESIAN_POINT ( 'NONE',  ( 2.591664760199015927, -5.876774720514418071, 20.15921530338947321 ) ) ;
#78958=CARTESIAN_POINT ( 'NONE',  ( 4.016587897052070311, -6.376774720514426065, 21.44459449800855921 ) ) ;
#78966=EDGE_CURVE ( 'NONE', #50183, #55194, #81484, .T. ) ;
#78968=VECTOR ( 'NONE', #99378, 1000.000000000000000 ) ;
#78969=EDGE_CURVE ( 'NONE', #55307, #54376, #97776, .T. ) ;
#78977=CARTESIAN_POINT ( 'NONE',  ( 4.281720980632043094, -5.876774720514408301, 18.71132571341777151 ) ) ;
#78989=DIRECTION ( 'NONE',  ( -1.226388327005079762E-16, 0.000000000000000000, 1.000000000000000000 ) ) ;
#78990=CARTESIAN_POINT ( 'NONE',  ( 31.13513474936814163, -4.540774720514427543, 3.331262582247520143 ) ) ;
#78994=VERTEX_POINT ( 'NONE', #77774 ) ;
#78995=VERTEX_POINT ( 'NONE', #55983 ) ;
#78997=VERTEX_POINT ( 'NONE', #23486 ) ;
#79006=CARTESIAN_POINT ( 'NONE',  ( 4.372949846226492632, -5.876774720514405637, 18.80635842184136308 ) ) ;
#79011=EDGE_LOOP ( 'NONE', ( #34075, #34363, #92264, #74818 ) ) ;
#79029=ADVANCED_FACE ( 'NONE', ( #24003 ), #48865, .F. ) ;
#79030=CIRCLE ( 'NONE', #62839, 15.00000000000000178 ) ;
#79040=ORIENTED_EDGE ( 'NONE', *, *, #83781, .T. ) ;
#79042=CARTESIAN_POINT ( 'NONE',  ( -10.59832330691884295, 5.965225279485572685, -27.05373799718300987 ) ) ;
#79045=VECTOR ( 'NONE', #8677, 1000.000000000000000 ) ;
#79047=CARTESIAN_POINT ( 'NONE',  ( 32.50838937279093699, 1.477225279485574028, -10.74666623472941573 ) ) ;
#79052=CARTESIAN_POINT ( 'NONE',  ( -5.544977400725785266, -6.376774720514411854, 19.92818918856636401 ) ) ;
#79073=CARTESIAN_POINT ( 'NONE',  ( -6.033988668995577065, -6.376774720514413630, 19.86422795159478483 ) ) ;
#79083=CARTESIAN_POINT ( 'NONE',  ( 27.53860345374808105, -5.356774720496559894, -0.3523920347288979071 ) ) ;
#79094=ORIENTED_EDGE ( 'NONE', *, *, #23556, .F. ) ;
#79102=EDGE_CURVE ( 'NONE', #35820, #11836, #1817, .T. ) ;
#79106=EDGE_CURVE ( 'NONE', #50305, #8499, #61130, .T. ) ;
#79116=VERTEX_POINT ( 'NONE', #2689 ) ;
#79132=ORIENTED_EDGE ( 'NONE', *, *, #45299, .T. ) ;
#79133=CARTESIAN_POINT ( 'NONE',  ( -5.877732331298974877, -5.876774720514411854, 19.69174559449349005 ) ) ;
#79138=ORIENTED_EDGE ( 'NONE', *, *, #90702, .F. ) ;
#79155=ORIENTED_EDGE ( 'NONE', *, *, #80056, .F. ) ;
#79158=EDGE_CURVE ( 'NONE', #26363, #30845, #96026, .T. ) ;
#79159=ORIENTED_EDGE ( 'NONE', *, *, #9232, .F. ) ;
#79169=EDGE_CURVE ( 'NONE', #92450, #78121, #89414, .T. ) ;
#79172=VECTOR ( 'NONE', #52380, 1000.000000000000000 ) ;
#79173=CARTESIAN_POINT ( 'NONE',  ( 29.57907552664497786, -3.519868637853082571, 29.21818156430573765 ) ) ;
#79174=DIRECTION ( 'NONE',  ( 0.000000000000000000, 0.000000000000000000, 1.000000000000000000 ) ) ;
#79185=VERTEX_POINT ( 'NONE', #89911 ) ;
#79192=CARTESIAN_POINT ( 'NONE',  ( 14.79186724892429439, -4.799335165223686417, -27.67512533972776723 ) ) ;
#79202=CARTESIAN_POINT ( 'NONE',  ( -7.641025641025641413, -5.876774720514418071, 20.36458333333334636 ) ) ;
#79206=PLANE ( 'NONE',  #89597 ) ;
#79216=CARTESIAN_POINT ( 'NONE',  ( 0.000000000000000000, -4.132774720514426292, 0.000000000000000000 ) ) ;
#79217=EDGE_CURVE ( 'NONE', #1547, #57623, #81798, .T. ) ;
#79221=CARTESIAN_POINT ( 'NONE',  ( -0.02075734969026423599, -3.316774720514426456, -28.03397719988137382 ) ) ;
#79223=CARTESIAN_POINT ( 'NONE',  ( -3.108787716482549701, -5.876774720514418071, 20.32624910079993086 ) ) ;
#79226=VECTOR ( 'NONE', #53168, 1000.000000000000000 ) ;
#79241=CARTESIAN_POINT ( 'NONE',  ( -24.55517127435777169, 5.965225279485592225, -15.44180958690142802 ) ) ;
#79250=CARTESIAN_POINT ( 'NONE',  ( 7.155337544004596317, -5.876774720514417183, 20.64714842558261765 ) ) ;
#79251=CARTESIAN_POINT ( 'NONE',  ( 5.400898774349120579, -5.876774720514417183, 20.36357656736558042 ) ) ;
#79267=EDGE_CURVE ( 'NONE', #79731, #63566, #19626, .T. ) ;
#79272=EDGE_CURVE ( 'NONE', #95881, #87149, #12018, .T. ) ;
#79275=ORIENTED_EDGE ( 'NONE', *, *, #13338, .T. ) ;
#79286=ORIENTED_EDGE ( 'NONE', *, *, #58949, .T. ) ;
#79291=CARTESIAN_POINT ( 'NONE',  ( 282.9764569301858046, -4.540774720514427543, 20.79159422840526616 ) ) ;
#79295=EDGE_CURVE ( 'NONE', #20122, #15617, #27256, .T. ) ;
#79297=CYLINDRICAL_SURFACE ( 'NONE', #39499, 2.500000000000000444 ) ;
#79304=AXIS2_PLACEMENT_3D ( 'NONE', #75607, #91348, #59921 ) ;
#79308=EDGE_CURVE ( 'NONE', #94249, #67214, #28244, .T. ) ;
#79318=DIRECTION ( 'NONE',  ( -0.000000000000000000, -1.000000000000000000, -0.000000000000000000 ) ) ;
#79320=VECTOR ( 'NONE', #35122, 1000.000000000000000 ) ;
#79322=CARTESIAN_POINT ( 'NONE',  ( 3.448102555317568374, -5.876774720514423400, 21.39871091031772110 ) ) ;
#79331=EDGE_CURVE ( 'NONE', #28943, #95426, #81603, .T. ) ;
#79337=CARTESIAN_POINT ( 'NONE',  ( -7.641025641025640525, -6.376774720514417183, 20.36458333333334281 ) ) ;
#79350=EDGE_CURVE ( 'NONE', #49218, #59202, #5407, .T. ) ;
#79351=LINE ( 'NONE', #56541, #12337 ) ;
#79354=CYLINDRICAL_SURFACE ( 'NONE', #48475, 1.325999999999969647 ) ;
#79355=CARTESIAN_POINT ( 'NONE',  ( 13.91401389203221406, -6.376774720514426953, 158.0376437107427137 ) ) ;
#79365=ORIENTED_EDGE ( 'NONE', *, *, #46571, .F. ) ;
#79367=CARTESIAN_POINT ( 'NONE',  ( 27.53860345374771867, 1.477225279485574028, -9.482392034746242260 ) ) ;
#79378=ORIENTED_EDGE ( 'NONE', *, *, #45221, .F. ) ;
#79381=CARTESIAN_POINT ( 'NONE',  ( 0.000000000000000000, -5.876774720514426953, 0.000000000000000000 ) ) ;
#79385=CARTESIAN_POINT ( 'NONE',  ( -1.363607173041644582, -5.876774720514419847, 20.50445910983877340 ) ) ;
#79386=EDGE_CURVE ( 'NONE', #79408, #55323, #97154, .T. ) ;
#79389=VECTOR ( 'NONE', #17860, 1000.000000000000000 ) ;
#79395=ORIENTED_EDGE ( 'NONE', *, *, #70885, .F. ) ;
#79408=VERTEX_POINT ( 'NONE', #52581 ) ;
#79413=CARTESIAN_POINT ( 'NONE',  ( 27.53860345374808105, 1.477225279485574028, 0.000000000000000000 ) ) ;
#79427=CARTESIAN_POINT ( 'NONE',  ( -4.312370003044874167, -5.876774720514408301, 19.42522865122897358 ) ) ;
#79436=ORIENTED_EDGE ( 'NONE', *, *, #57614, .F. ) ;
#79456=EDGE_CURVE ( 'NONE', #92987, #60621, #62705, .T. ) ;
#79461=EDGE_CURVE ( 'NONE', #27315, #63342, #77393, .T. ) ;
#79465=VECTOR ( 'NONE', #81125, 1000.000000000000000 ) ;
#79467=CARTESIAN_POINT ( 'NONE',  ( 2.590395174287518643, -6.376774720514415407, 20.05492615153064762 ) ) ;
#79469=CARTESIAN_POINT ( 'NONE',  ( 4.595037417369686850, -5.876774720514419847, 20.70846556543617467 ) ) ;
#79476=CARTESIAN_POINT ( 'NONE',  ( -4.141025641025638748, -6.376774720514427841, 21.75000000000000355 ) ) ;
#79481=DIRECTION ( 'NONE',  ( -0.1875268396392987258, 0.000000000000000000, -0.9822594791677485837 ) ) ;
#79487=PLANE ( 'NONE',  #30867 ) ;
#79495=DIRECTION ( 'NONE',  ( 0.000000000000000000, 0.000000000000000000, 1.000000000000000000 ) ) ;
#79499=CARTESIAN_POINT ( 'NONE',  ( -29.49875734969025842, 5.965225279485572685, 25.61802280011862720 ) ) ;
#79514=CARTESIAN_POINT ( 'NONE',  ( 4.372949846226492632, -6.376774720514404748, 18.80635842184136308 ) ) ;
#79517=CARTESIAN_POINT ( 'NONE',  ( -9.278253834636473130, -5.876774720514426953, 21.78128695274316229 ) ) ;
#79518=DIRECTION ( 'NONE',  ( 0.000000000000000000, 0.000000000000000000, -1.000000000000000000 ) ) ;
#79539=VERTEX_POINT ( 'NONE', #69802 ) ;
#79579=DIRECTION ( 'NONE',  ( -0.000000000000000000, 0.000000000000000000, -1.000000000000000000 ) ) ;
#79586=LINE ( 'NONE', #3976, #6964 ) ;
#79590=DIRECTION ( 'NONE',  ( 0.000000000000000000, -1.000000000000000000, 0.000000000000000000 ) ) ;
#79601=DIRECTION ( 'NONE',  ( 0.000000000000000000, 0.000000000000000000, 1.000000000000000000 ) ) ;
#79610=ADVANCED_FACE ( 'NONE', ( #87530 ), #86518, .F. ) ;
#79614=CARTESIAN_POINT ( 'NONE',  ( 22.02124265030973760, 6.143225279485574397, 12.85402280011862430 ) ) ;
#79616=VERTEX_POINT ( 'NONE', #98617 ) ;
#79621=CARTESIAN_POINT ( 'NONE',  ( -1.345681049247692940, -6.376774720514410077, 19.69174559449348294 ) ) ;
#79648=CARTESIAN_POINT ( 'NONE',  ( 4.910384361841649614, -5.876774720514420736, 20.73924463800384643 ) ) ;
#79649=ORIENTED_EDGE ( 'NONE', *, *, #18749, .F. ) ;
#79658=VERTEX_POINT ( 'NONE', #20992 ) ;
#79670=CARTESIAN_POINT ( 'NONE',  ( -2.285970405126252825, -6.376774720514408301, 19.14905311829361167 ) ) ;
#79678=CARTESIAN_POINT ( 'NONE',  ( 9.940598223437577374, -6.376774720514426953, 17.91871304725684766 ) ) ;
#79680=DIRECTION ( 'NONE',  ( -0.000000000000000000, -1.000000000000000000, -0.000000000000000000 ) ) ;
#79692=CARTESIAN_POINT ( 'NONE',  ( 14.63527791052759319, -4.349658986764154633, -28.08406249416238154 ) ) ;
#79705=CARTESIAN_POINT ( 'NONE',  ( 6.059061188053544988, -5.876774720514417183, 20.16803580207560742 ) ) ;
#79708=VERTEX_POINT ( 'NONE', #27633 ) ;
#79711=DIRECTION ( 'NONE',  ( 0.000000000000000000, 0.000000000000000000, 1.000000000000000000 ) ) ;
#79719=DIRECTION ( 'NONE',  ( 0.000000000000000000, 0.000000000000000000, -1.000000000000000000 ) ) ;
#79728=ORIENTED_EDGE ( 'NONE', *, *, #95002, .F. ) ;
#79731=VERTEX_POINT ( 'NONE', #45352 ) ;
#79732=ADVANCED_FACE ( 'NONE', ( #52462 ), #60587, .F. ) ;
#79733=CARTESIAN_POINT ( 'NONE',  ( -0.02075734969026423599, -6.376774720514426953, -0.08597719988137648983 ) ) ;
#79736=DIRECTION ( 'NONE',  ( -1.000000000000000000, 0.000000000000000000, 0.000000000000000000 ) ) ;
#79737=CIRCLE ( 'NONE', #65232, 91.74549126261076992 ) ;
#79750=LINE ( 'NONE', #94477, #79389 ) ;
#79751=ORIENTED_EDGE ( 'NONE', *, *, #25531, .F. ) ;
#79752=ORIENTED_EDGE ( 'NONE', *, *, #85496, .F. ) ;
#79755=CARTESIAN_POINT ( 'NONE',  ( 6.431189903846153300, -5.876774720514415407, 20.08974358974358765 ) ) ;
#79767=CARTESIAN_POINT ( 'NONE',  ( 15.29947330337543754, 6.475225279485573360, -27.16854002387008649 ) ) ;
#79768=B_SPLINE_SURFACE_WITH_KNOTS ( 'NONE', 3, 1, ( 
 ( #28610, #27116 ),
 ( #18497, #49471 ),
 ( #96132, #58084 ),
 ( #89018, #42855 ),
 ( #19493, #43348 ),
 ( #73783, #4282 ) ),
 .UNSPECIFIED., .F., .F., .F.,
 ( 4, 2, 4 ),
 ( 2, 2 ),
 ( 0.000000000000000000, 0.5000000000000000000, 1.000000000000000000 ),
 ( 0.000000000000000000, 1.000000000000000000 ),
 .UNSPECIFIED. ) ;
#79769=ORIENTED_EDGE ( 'NONE', *, *, #93827, .F. ) ;
#79783=CARTESIAN_POINT ( 'NONE',  ( 7.164812103570541879, -6.376774720514422512, 20.85668272347560404 ) ) ;
#79785=DIRECTION ( 'NONE',  ( 0.000000000000000000, 1.000000000000000000, 0.000000000000000000 ) ) ;
#79787=ORIENTED_EDGE ( 'NONE', *, *, #24568, .T. ) ;
#79802=EDGE_LOOP ( 'NONE', ( #9769, #86470, #25211, #51541 ) ) ;
#79804=CARTESIAN_POINT ( 'NONE',  ( 31.62087157062645204, -4.386438359062696080, 26.73777224682022435 ) ) ;
#79808=CARTESIAN_POINT ( 'NONE',  ( 4.465438306463536122, -5.876774720514425177, 21.59631214011467293 ) ) ;
#79820=CARTESIAN_POINT ( 'NONE',  ( 3.094204744773375815, -6.376774720514422512, 21.02053020447315745 ) ) ;
#79821=PLANE ( 'NONE',  #34469 ) ;
#79825=CARTESIAN_POINT ( 'NONE',  ( 6.403846153846157740, -6.376774720514426065, 21.48076923076922995 ) ) ;
#79826=FACE_OUTER_BOUND ( 'NONE', #83632, .T. ) ;
#79827=AXIS2_PLACEMENT_3D ( 'NONE', #3668, #96006, #18875 ) ;
#79833=CARTESIAN_POINT ( 'NONE',  ( 3.797776442307698286, -5.876774720514427841, 21.83974358974358410 ) ) ;
#79837=CARTESIAN_POINT ( 'NONE',  ( 13.64113475014448440, -6.376774720514426953, -28.24100986136700087 ) ) ;
#79839=CARTESIAN_POINT ( 'NONE',  ( -7.138063944469604571, -6.376774720514408301, 19.21974929698718881 ) ) ;
#79847=FACE_OUTER_BOUND ( 'NONE', #2297, .T. ) ;
#79853=LINE ( 'NONE', #88483, #80084 ) ;
#79872=ORIENTED_EDGE ( 'NONE', *, *, #28380, .T. ) ;
#79878=CYLINDRICAL_SURFACE ( 'NONE', #70451, 1.399999999999998579 ) ;
#79880=CARTESIAN_POINT ( 'NONE',  ( -0.02075734969026423599, 6.475225279485573360, -28.54397719988136828 ) ) ;
#79900=CARTESIAN_POINT ( 'NONE',  ( 26.73860345374794534, 1.477225279485574028, 3.440769881205036427E-15 ) ) ;
#79903=CIRCLE ( 'NONE', #15076, 1.836000000000000743 ) ;
#79905=EDGE_CURVE ( 'NONE', #41375, #97248, #35708, .T. ) ;
#79908=DIRECTION ( 'NONE',  ( -7.163199596004101480E-14, 1.000000000000000000, 7.440411327181627631E-14 ) ) ;
#79913=DIRECTION ( 'NONE',  ( 1.797729424027682620E-15, 1.000000000000000000, 1.064096645546785541E-13 ) ) ;
#79928=EDGE_LOOP ( 'NONE', ( #28482, #89136, #93957, #84291 ) ) ;
#79929=FACE_OUTER_BOUND ( 'NONE', #79011, .T. ) ;
#79931=CARTESIAN_POINT ( 'NONE',  ( 3.509873074917118085, 5.965225279485572685, 29.15869884040363758 ) ) ;
#79950=LINE ( 'NONE', #73350, #71006 ) ;
#79959=DIRECTION ( 'NONE',  ( -0.000000000000000000, 1.000000000000000000, -0.000000000000000000 ) ) ;
#79973=VERTEX_POINT ( 'NONE', #33617 ) ;
#79977=VECTOR ( 'NONE', #1578, 1000.000000000000227 ) ;
#79995=EDGE_LOOP ( 'NONE', ( #92125, #20734, #69919, #36122 ) ) ;
#80016=LINE ( 'NONE', #49086, #61020 ) ;
#80020=VECTOR ( 'NONE', #72458, 1000.000000000000000 ) ;
#80022=ORIENTED_EDGE ( 'NONE', *, *, #28187, .F. ) ;
#80026=ORIENTED_EDGE ( 'NONE', *, *, #71886, .T. ) ;
#80046=EDGE_CURVE ( 'NONE', #94222, #35033, #90161, .T. ) ;
#80051=CARTESIAN_POINT ( 'NONE',  ( 30.58729439590573662, -5.356774720514427379, 26.14186284044631492 ) ) ;
#80052=CARTESIAN_POINT ( 'NONE',  ( -7.282824509310913186, -5.876774720514415407, 19.84584863393302356 ) ) ;
#80056=EDGE_CURVE ( 'NONE', #1389, #77260, #57474, .T. ) ;
#80058=CARTESIAN_POINT ( 'NONE',  ( -5.439936175300728927, -6.376774720514410077, 19.67454710845353816 ) ) ;
#80065=EDGE_CURVE ( 'NONE', #58859, #497, #58467, .T. ) ;
#80076=DIRECTION ( 'NONE',  ( -0.000000000000000000, 1.000000000000000000, -0.000000000000000000 ) ) ;
#80082=DIRECTION ( 'NONE',  ( 0.000000000000000000, 0.000000000000000000, -1.000000000000000000 ) ) ;
#80084=VECTOR ( 'NONE', #15582, 1000.000000000000227 ) ;
#80090=VECTOR ( 'NONE', #67661, 1000.000000000000000 ) ;
#80098=CARTESIAN_POINT ( 'NONE',  ( 7.234974673537251100, -6.376774720514415407, 19.99114326857715795 ) ) ;
#80118=ORIENTED_EDGE ( 'NONE', *, *, #29148, .T. ) ;
#80133=CARTESIAN_POINT ( 'NONE',  ( 10.24059822343752479, -5.876774720514426953, -2.394817856121274864E-14 ) ) ;
#80137=EDGE_LOOP ( 'NONE', ( #18227, #71564, #70787, #74016 ) ) ;
#80143=CARTESIAN_POINT ( 'NONE',  ( -5.923037968371668072, -6.376774720514413630, 19.62288733224861303 ) ) ;
#80145=ORIENTED_EDGE ( 'NONE', *, *, #5909, .T. ) ;
#80147=ORIENTED_EDGE ( 'NONE', *, *, #70975, .F. ) ;
#80153=CIRCLE ( 'NONE', #78467, 0.3000000000000016542 ) ;
#80155=CARTESIAN_POINT ( 'NONE',  ( 15.32643653063177958, -3.577630190450218350, -27.14485409495429380 ) ) ;
#80160=DIRECTION ( 'NONE',  ( 0.000000000000000000, -1.000000000000000000, 0.000000000000000000 ) ) ;
#80179=B_SPLINE_CURVE_WITH_KNOTS ( 'NONE', 3,
 ( #14251, #75649, #45226, #20869, #51840, #90888, #21859, #76150, #97504, #98487, #6649, #99488, #52832, #74661, #28988, #29983, #43727, #75160, #27999 ),
 .UNSPECIFIED., .F., .F.,
 ( 4, 1, 1, 1, 1, 1, 1, 1, 1, 1, 1, 1, 1, 1, 1, 1, 4 ),
 ( 0.000000000000000000, 0.06815824415599770758, 0.1347066022023564180, 0.2018649976035981897, 0.2707882662774624971, 0.3400242943604918633, 0.4080827390537212218, 0.4768131952581446398, 0.5473460643070942044, 0.5856397954238958814, 0.6288649531777639190, 0.6771532033637904791, 0.7308028113651051649, 0.7898066155325015325, 0.8543250087420142247, 0.9243651340575425035, 1.000000000000000000 ),
 .UNSPECIFIED. ) ;
#80185=AXIS2_PLACEMENT_3D ( 'NONE', #34655, #71718, #65624 ) ;
#80190=ADVANCED_FACE ( 'NONE', ( #37608 ), #64818, .F. ) ;
#80195=ORIENTED_EDGE ( 'NONE', *, *, #28939, .F. ) ;
#80197=CARTESIAN_POINT ( 'NONE',  ( 2.904396343079095111, -5.876774720514415407, 19.95793242748194984 ) ) ;
#80204=CARTESIAN_POINT ( 'NONE',  ( -24.90875734969025501, 6.475225279485573360, 26.43402280011862615 ) ) ;
#80215=ORIENTED_EDGE ( 'NONE', *, *, #50586, .T. ) ;
#80217=DIRECTION ( 'NONE',  ( -4.251773225433346808E-15, 0.000000000000000000, 1.000000000000000000 ) ) ;
#80220=CARTESIAN_POINT ( 'NONE',  ( -7.641025641025641413, -6.376774720514418959, 20.36458333333334636 ) ) ;
#80221=CARTESIAN_POINT ( 'NONE',  ( 19.72776355195876619, -6.376774720514426953, 28.39950002376592764 ) ) ;
#80225=EDGE_LOOP ( 'NONE', ( #85148, #19373, #48303, #33448 ) ) ;
#80249=AXIS2_PLACEMENT_3D ( 'NONE', #36655, #59011, #99035 ) ;
#80256=ORIENTED_EDGE ( 'NONE', *, *, #89716, .T. ) ;
#80258=CARTESIAN_POINT ( 'NONE',  ( 2.591664760199015927, -5.876774720514418071, 20.15921530338947321 ) ) ;
#80261=ORIENTED_EDGE ( 'NONE', *, *, #68734, .T. ) ;
#80263=CARTESIAN_POINT ( 'NONE',  ( 7.052174998393318184, -5.876774720514418071, 20.39928653130861136 ) ) ;
#80264=CARTESIAN_POINT ( 'NONE',  ( 5.705253819860196529, -6.376774720514415407, 19.95963554344900714 ) ) ;
#80288=CARTESIAN_POINT ( 'NONE',  ( 6.561060095583167495, -6.376774720514427841, 21.83518827598938117 ) ) ;
#80292=LINE ( 'NONE', #4676, #78732 ) ;
#80294=CARTESIAN_POINT ( 'NONE',  ( 29.57907552799943218, -3.518969226524878646, 29.21818156447044501 ) ) ;
#80298=ORIENTED_EDGE ( 'NONE', *, *, #96853, .T. ) ;
#80307=PLANE ( 'NONE',  #68037 ) ;
#80314=CARTESIAN_POINT ( 'NONE',  ( -5.554587162835583847, -5.876774720514415407, 19.99258394656885329 ) ) ;
#80316=ORIENTED_EDGE ( 'NONE', *, *, #59115, .F. ) ;
#80319=CARTESIAN_POINT ( 'NONE',  ( 13.91401389203221406, -6.376774720514426953, 158.0376437107427137 ) ) ;
#80320=CARTESIAN_POINT ( 'NONE',  ( 12.66784028006542151, -2.682774720514427003, -27.12025593822526304 ) ) ;
#80324=CARTESIAN_POINT ( 'NONE',  ( 33.13288845015618023, 5.965225279485572685, -0.1650522222209214185 ) ) ;
#80329=CARTESIAN_POINT ( 'NONE',  ( -2.070328576748420524, -6.376774720514410077, 19.46575348430201657 ) ) ;
#80344=CARTESIAN_POINT ( 'NONE',  ( 12.98941176893815275, -6.376774720518460171, -28.15829778590956067 ) ) ;
#80346=CARTESIAN_POINT ( 'NONE',  ( -7.421417143192116761, -6.376774720514411854, 19.43823095447975291 ) ) ;
#80357=CARTESIAN_POINT ( 'NONE',  ( 7.267403311989051318, -6.376774720514426065, 21.43157132964656952 ) ) ;
#80359=CARTESIAN_POINT ( 'NONE',  ( 14.52511747680497933, 6.475225279485573360, -27.86035006098926559 ) ) ;
#80385=CARTESIAN_POINT ( 'NONE',  ( 30.93860345374796594, 6.475225279485573360, 19.84760796525321780 ) ) ;
#80394=CARTESIAN_POINT ( 'NONE',  ( 29.70220533433690946, -3.451715827188561736, 28.20564067601642222 ) ) ;
#80396=ORIENTED_EDGE ( 'NONE', *, *, #70784, .F. ) ;
#80403=ORIENTED_EDGE ( 'NONE', *, *, #32422, .T. ) ;
#80407=DIRECTION ( 'NONE',  ( 0.000000000000000000, -1.000000000000000000, 0.000000000000000000 ) ) ;
#80417=DIRECTION ( 'NONE',  ( 1.000000000000000000, -1.232047923278981953E-16, 0.000000000000000000 ) ) ;
#80418=FACE_OUTER_BOUND ( 'NONE', #40723, .T. ) ;
#80421=CARTESIAN_POINT ( 'NONE',  ( -53.01255352321339842, -4.132774720514426292, 35.59556822165056644 ) ) ;
#80424=ORIENTED_EDGE ( 'NONE', *, *, #25317, .F. ) ;
#80426=EDGE_CURVE ( 'NONE', #90367, #88122, #24288, .T. ) ;
#80429=CARTESIAN_POINT ( 'NONE',  ( 29.73860345376319003, -5.356471260711259674, 19.84760796525321425 ) ) ;
#80430=EDGE_LOOP ( 'NONE', ( #47935, #35462, #34470, #97320 ) ) ;
#80431=VECTOR ( 'NONE', #50807, 1000.000000000000000 ) ;
#80436=ORIENTED_EDGE ( 'NONE', *, *, #52873, .T. ) ;
#80440=CARTESIAN_POINT ( 'NONE',  ( 29.73828978136053891, -14.82721238576461609, -4.021765098496561386 ) ) ;
#80449=DIRECTION ( 'NONE',  ( -1.000000000000000000, 0.000000000000000000, 1.104558621438292892E-14 ) ) ;
#80466=CARTESIAN_POINT ( 'NONE',  ( 16.04643365539530109, -3.607965404481770832, -27.87003593022056691 ) ) ;
#80478=FACE_OUTER_BOUND ( 'NONE', #89643, .T. ) ;
#80483=DIRECTION ( 'NONE',  ( 0.000000000000000000, 1.478457507934778393E-16, -1.000000000000000000 ) ) ;
#80486=ADVANCED_FACE ( 'NONE', ( #64980 ), #80671, .F. ) ;
#80491=EDGE_CURVE ( 'NONE', #67044, #42771, #6467, .T. ) ;
#80493=AXIS2_PLACEMENT_3D ( 'NONE', #34034, #16294, #24905 ) ;
#80504=CIRCLE ( 'NONE', #65979, 2.500000000000000444 ) ;
#80516=DIRECTION ( 'NONE',  ( -2.338552693767719605E-15, 0.000000000000000000, 1.000000000000000000 ) ) ;
#80518=ORIENTED_EDGE ( 'NONE', *, *, #53371, .T. ) ;
#80524=B_SPLINE_CURVE_WITH_KNOTS ( 'NONE', 3,
 ( #25109, #17508, #86516, #1790 ),
 .UNSPECIFIED., .F., .F.,
 ( 4, 4 ),
 ( 0.01303003236488493519, 0.01305095637151315775 ),
 .UNSPECIFIED. ) ;
#80529=ORIENTED_EDGE ( 'NONE', *, *, #18191, .T. ) ;
#80539=CIRCLE ( 'NONE', #87046, 0.8160000000000007248 ) ;
#80546=ADVANCED_FACE ( 'NONE', ( #68941 ), #36487, .T. ) ;
#80564=CARTESIAN_POINT ( 'NONE',  ( -0.7614568544629641833, -6.376774720514410077, 19.18727597066020962 ) ) ;
#80571=DIRECTION ( 'NONE',  ( -0.000000000000000000, 1.000000000000000000, -0.000000000000000000 ) ) ;
#80586=PLANE ( 'NONE',  #42622 ) ;
#80592=FACE_OUTER_BOUND ( 'NONE', #35764, .T. ) ;
#80594=CARTESIAN_POINT ( 'NONE',  ( 0.3910256410256441884, -6.376774720514427841, 21.75000000000000000 ) ) ;
#80596=PLANE ( 'NONE',  #55476 ) ;
#80600=DIRECTION ( 'NONE',  ( 0.000000000000000000, 0.000000000000000000, 1.000000000000000000 ) ) ;
#80601=VECTOR ( 'NONE', #52342, 1000.000000000000000 ) ;
#80605=B_SPLINE_SURFACE_WITH_KNOTS ( 'NONE', 3, 1, ( 
 ( #92855, #86254 ),
 ( #15733, #62426 ),
 ( #78617, #85752 ),
 ( #16237, #47199 ),
 ( #16733, #47700 ),
 ( #37578, #60929 ),
 ( #68530, #29960 ) ),
 .UNSPECIFIED., .F., .F., .F.,
 ( 4, 1, 1, 1, 4 ),
 ( 2, 2 ),
 ( 0.000000000000000000, 0.2499864026691193120, 0.4969648798681425284, 0.7462659243093365813, 1.000000000000000000 ),
 ( 0.000000000000000000, 1.000000000000000000 ),
 .UNSPECIFIED. ) ;
#80614=EDGE_CURVE ( 'NONE', #97460, #74029, #92353, .T. ) ;
#80633=EDGE_CURVE ( 'NONE', #19444, #42575, #44373, .T. ) ;
#80645=CARTESIAN_POINT ( 'NONE',  ( -6.185411026474866958, -6.376774720514411854, 19.34586827028016742 ) ) ;
#80651=CARTESIAN_POINT ( 'NONE',  ( 9.422519371942208011, 6.475225279485576024, -27.03574706870085720 ) ) ;
#80664=VERTEX_POINT ( 'NONE', #36255 ) ;
#80670=DIRECTION ( 'NONE',  ( -0.000000000000000000, -1.000000000000000000, -0.000000000000000000 ) ) ;
#80671=PLANE ( 'NONE',  #42199 ) ;
#80709=AXIS2_PLACEMENT_3D ( 'NONE', #14544, #38883, #69845 ) ;
#80715=ORIENTED_EDGE ( 'NONE', *, *, #5596, .F. ) ;
#80718=CARTESIAN_POINT ( 'NONE',  ( -7.627782137226129855, -5.876774720514414518, 20.04377961306771994 ) ) ;
#80725=VECTOR ( 'NONE', #95447, 1000.000000000000000 ) ;
#80734=DIRECTION ( 'NONE',  ( -1.000000000000000000, 0.000000000000000000, 0.000000000000000000 ) ) ;
#80744=VERTEX_POINT ( 'NONE', #67718 ) ;
#80751=EDGE_CURVE ( 'NONE', #7479, #50183, #59104, .T. ) ;
#80758=EDGE_CURVE ( 'NONE', #86899, #30864, #82700, .T. ) ;
#80766=VERTEX_POINT ( 'NONE', #31623 ) ;
#80770=CARTESIAN_POINT ( 'NONE',  ( 5.963731207934512391, -6.376774720514413630, 19.80418863844947097 ) ) ;
#80781=ORIENTED_EDGE ( 'NONE', *, *, #25925, .F. ) ;
#80799=EDGE_LOOP ( 'NONE', ( #88115, #44438, #61653, #69915 ) ) ;
#80806=CARTESIAN_POINT ( 'NONE',  ( 11.44401587981593060, 6.475225279485572472, -27.05278809890034353 ) ) ;
#80818=CARTESIAN_POINT ( 'NONE',  ( 31.62416306531753918, -4.295372699094516022, 26.87458401151571508 ) ) ;
#80822=EDGE_CURVE ( 'NONE', #39625, #22949, #45861, .T. ) ;
#80833=EDGE_CURVE ( 'NONE', #44429, #31086, #3994, .T. ) ;
#80841=AXIS2_PLACEMENT_3D ( 'NONE', #31494, #14759, #69569 ) ;
#80842=PLANE ( 'NONE',  #58659 ) ;
#80845=CARTESIAN_POINT ( 'NONE',  ( 31.59111626279633711, 5.965225279485572685, 16.27760796525321751 ) ) ;
#80851=DIRECTION ( 'NONE',  ( 0.000000000000000000, 0.000000000000000000, -1.000000000000000000 ) ) ;
#80853=CARTESIAN_POINT ( 'NONE',  ( -7.491187506528125262, -5.876774720514410077, 19.53857357749109980 ) ) ;
#80869=DIRECTION ( 'NONE',  ( 5.328431011793917330E-15, 0.000000000000000000, 1.000000000000000000 ) ) ;
#80875=EDGE_CURVE ( 'NONE', #64365, #24606, #45376, .T. ) ;
#80879=CARTESIAN_POINT ( 'NONE',  ( 31.79364159983995464, 5.965225279485572685, -11.59305536555894278 ) ) ;
#80884=CARTESIAN_POINT ( 'NONE',  ( 30.09341516180546350, 1.477225279485574028, -11.39311774897855933 ) ) ;
#80893=DIRECTION ( 'NONE',  ( 0.000000000000000000, 0.000000000000000000, 1.000000000000000000 ) ) ;
#80905=ORIENTED_EDGE ( 'NONE', *, *, #2477, .F. ) ;
#80907=DIRECTION ( 'NONE',  ( 0.000000000000000000, 0.000000000000000000, -1.000000000000000000 ) ) ;
#80909=VECTOR ( 'NONE', #67460, 1000.000000000000000 ) ;
#80922=ORIENTED_EDGE ( 'NONE', *, *, #63921, .T. ) ;
#80926=CIRCLE ( 'NONE', #48566, 11.85241003308275864 ) ;
#80932=ORIENTED_EDGE ( 'NONE', *, *, #3849, .F. ) ;
#80936=EDGE_LOOP ( 'NONE', ( #14596, #85124, #9762, #47752 ) ) ;
#80940=CARTESIAN_POINT ( 'NONE',  ( 2.589743589743596086, -6.376774720514415407, 20.00140224358974095 ) ) ;
#80941=CARTESIAN_POINT ( 'NONE',  ( 29.73860345376319358, -5.356774720496559894, 7.190646357373898680E-15 ) ) ;
#80950=EDGE_CURVE ( 'NONE', #90167, #89315, #55154, .T. ) ;
#80957=CARTESIAN_POINT ( 'NONE',  ( 1.175186991919851431, -0.3587747205144265483, 28.89597625626659649 ) ) ;
#80979=AXIS2_PLACEMENT_3D ( 'NONE', #34342, #7616, #95235 ) ;
#81008=ORIENTED_EDGE ( 'NONE', *, *, #22778, .T. ) ;
#81010=ORIENTED_EDGE ( 'NONE', *, *, #81268, .T. ) ;
#81011=ORIENTED_EDGE ( 'NONE', *, *, #78966, .T. ) ;
#81018=CARTESIAN_POINT ( 'NONE',  ( -1.012926118674504883, -5.876774720514415407, 19.92818918856637822 ) ) ;
#81032=VERTEX_POINT ( 'NONE', #70692 ) ;
#81042=CARTESIAN_POINT ( 'NONE',  ( -20.27875734969026311, -6.376774720514428729, 27.00402280011862288 ) ) ;
#81052=VECTOR ( 'NONE', #1764, 1000.000000000000000 ) ;
#81053=CARTESIAN_POINT ( 'NONE',  ( -7.131053040288445999, -6.376774720514413630, 19.60308799987318196 ) ) ;
#81059=CIRCLE ( 'NONE', #21064, 84.48086791635432746 ) ;
#81060=DIRECTION ( 'NONE',  ( 0.000000000000000000, 1.000000000000000000, 0.000000000000000000 ) ) ;
#81064=DIRECTION ( 'NONE',  ( -2.615445361545220718E-15, -0.000000000000000000, -1.000000000000000000 ) ) ;
#81070=FACE_OUTER_BOUND ( 'NONE', #89972, .T. ) ;
#81071=EDGE_CURVE ( 'NONE', #69030, #29733, #17406, .T. ) ;
#81079=CARTESIAN_POINT ( 'NONE',  ( -20.27875734969026311, 6.143225279485574397, 24.00402280011862288 ) ) ;
#81083=EDGE_CURVE ( 'NONE', #534, #18471, #21082, .T. ) ;
#81089=CARTESIAN_POINT ( 'NONE',  ( -0.02075734969026423599, -6.376774720514426953, -0.08597719988137648983 ) ) ;
#81113=EDGE_CURVE ( 'NONE', #55041, #44878, #95030, .T. ) ;
#81116=CARTESIAN_POINT ( 'NONE',  ( -27.96875734969026084, -3.316774720514426456, 26.43402280011862615 ) ) ;
#81120=ORIENTED_EDGE ( 'NONE', *, *, #94113, .T. ) ;
#81125=DIRECTION ( 'NONE',  ( 0.000000000000000000, -1.000000000000000000, 0.000000000000000000 ) ) ;
#81136=CARTESIAN_POINT ( 'NONE',  ( 7.153659783701941777, -5.876774720514421624, 20.92502190304499265 ) ) ;
#81137=VECTOR ( 'NONE', #33327, 1000.000000000000000 ) ;
#81142=ADVANCED_FACE ( 'NONE', ( #26016 ), #80307, .F. ) ;
#81149=CARTESIAN_POINT ( 'NONE',  ( 13.59451591917074431, -3.316774720514426456, -28.23515841827053308 ) ) ;
#81157=CARTESIAN_POINT ( 'NONE',  ( 6.127395130496778641, -5.876774720514417183, 20.13872869980892943 ) ) ;
#81161=ORIENTED_EDGE ( 'NONE', *, *, #7550, .F. ) ;
#81169=LINE ( 'NONE', #3062, #49753 ) ;
#81186=VECTOR ( 'NONE', #70707, 1000.000000000000000 ) ;
#81193=ORIENTED_EDGE ( 'NONE', *, *, #89586, .F. ) ;
#81194=CARTESIAN_POINT ( 'NONE',  ( 4.628547153713393314, -5.876774720514418959, 20.50654586986123817 ) ) ;
#81208=CARTESIAN_POINT ( 'NONE',  ( -10.23894677657808749, -4.339657088724310441, 29.22408179085893210 ) ) ;
#81211=CIRCLE ( 'NONE', #50422, 28.96799999999999642 ) ;
#81213=ORIENTED_EDGE ( 'NONE', *, *, #72999, .F. ) ;
#81218=VERTEX_POINT ( 'NONE', #74197 ) ;
#81229=DIRECTION ( 'NONE',  ( 0.000000000000000000, 0.000000000000000000, 1.000000000000000000 ) ) ;
#81230=LINE ( 'NONE', #11707, #71130 ) ;
#81250=ORIENTED_EDGE ( 'NONE', *, *, #34073, .T. ) ;
#81256=ORIENTED_EDGE ( 'NONE', *, *, #61494, .F. ) ;
#81260=DIRECTION ( 'NONE',  ( 0.000000000000000000, 0.000000000000000000, 1.000000000000000000 ) ) ;
#81268=EDGE_CURVE ( 'NONE', #60537, #90130, #22374, .T. ) ;
#81269=ADVANCED_FACE ( 'NONE', ( #62468 ), #68627, .T. ) ;
#81274=VECTOR ( 'NONE', #85708, 1000.000000000000000 ) ;
#81278=ORIENTED_EDGE ( 'NONE', *, *, #69819, .T. ) ;
#81289=CARTESIAN_POINT ( 'NONE',  ( 5.326923076923078426, -5.876774720514419847, 20.76772836538461320 ) ) ;
#81291=CARTESIAN_POINT ( 'NONE',  ( 7.081057417352553784, -5.876774720514423400, 21.11453472826393352 ) ) ;
#81300=CARTESIAN_POINT ( 'NONE',  ( -27.86046284349297864, -6.376774720514426953, -8.091963836038765123 ) ) ;
#81315=ORIENTED_EDGE ( 'NONE', *, *, #81113, .F. ) ;
#81320=EDGE_CURVE ( 'NONE', #77260, #99983, #77667, .T. ) ;
#81328=CARTESIAN_POINT ( 'NONE',  ( 2.955024617976266033, -5.876774720514416295, 20.58370193283586858 ) ) ;
#81330=ADVANCED_FACE ( 'NONE', ( #68081 ), #21876, .F. ) ;
#81337=CARTESIAN_POINT ( 'NONE',  ( -23.62875734969026453, 6.143225279485574397, 24.50402280011862288 ) ) ;
#81349=CARTESIAN_POINT ( 'NONE',  ( 6.783277369150963132, -3.316774720515097030, -28.31678455703255892 ) ) ;
#81351=DIRECTION ( 'NONE',  ( 0.000000000000000000, 0.000000000000000000, -1.000000000000000000 ) ) ;
#81359=B_SPLINE_CURVE_WITH_KNOTS ( 'NONE', 3,
 ( #61672, #38307, #30194, #92097, #13474, #84487, #54057, #249, #14466, #23067, #98711, #83988, #91102, #67793, #100182, #76362, #31191, #84982, #45448, #6865, #21577, #99689, #77358, #52550, #44947, #62165, #93089 ),
 .UNSPECIFIED., .F., .F.,
 ( 4, 1, 1, 1, 1, 1, 1, 1, 1, 1, 1, 1, 1, 1, 1, 1, 1, 1, 1, 1, 1, 1, 1, 1, 4 ),
 ( 0.000000000000000000, 0.06859462225874299324, 0.1332460424433017654, 0.1943125864682570259, 0.2512792231169669877, 0.3045134392563472181, 0.3542349066533249102, 0.4004805887739895653, 0.4434107549384915803, 0.4840148686163446845, 0.5232523007732032827, 0.5610423727283604389, 0.5979002393643996216, 0.6335184888561951055, 0.6683143511696515437, 0.7024956712863811292, 0.7366853535134582076, 0.7702931693607886210, 0.8034372550192486750, 0.8359129516660284143, 0.8684602457892908189, 0.9008465382431825041, 0.9334665246307077835, 0.9662575752981232835, 1.000000000000000000 ),
 .UNSPECIFIED. ) ;
#81395=CARTESIAN_POINT ( 'NONE',  ( -41.32836283488544638, -4.132774720514426292, 39.26872235229541985 ) ) ;
#81399=DIRECTION ( 'NONE',  ( 0.000000000000000000, 0.000000000000000000, 1.000000000000000000 ) ) ;
#81405=ORIENTED_EDGE ( 'NONE', *, *, #98851, .T. ) ;
#81410=EDGE_LOOP ( 'NONE', ( #64345, #92600, #23725, #19796 ) ) ;
#81419=ORIENTED_EDGE ( 'NONE', *, *, #48972, .T. ) ;
#81437=CARTESIAN_POINT ( 'NONE',  ( -13.57581083383196940, -5.876774720514426953, 20.21213203435597094 ) ) ;
#81439=AXIS2_PLACEMENT_3D ( 'NONE', #91634, #100228, #46977 ) ;
#81441=VERTEX_POINT ( 'NONE', #71084 ) ;
#81442=CARTESIAN_POINT ( 'NONE',  ( 22.02124265030973760, 6.143225279485574397, 16.20402280011862217 ) ) ;
#81455=CARTESIAN_POINT ( 'NONE',  ( -12.65407072091356433, 5.965225279485572685, -26.15404995688568590 ) ) ;
#81458=EDGE_CURVE ( 'NONE', #56886, #95847, #78166, .T. ) ;
#81477=VECTOR ( 'NONE', #14423, 1000.000000000000000 ) ;
#81484=LINE ( 'NONE', #11958, #28107 ) ;
#81487=CARTESIAN_POINT ( 'NONE',  ( -2.656471864501908975, -6.376774720514411854, 19.66116880005639800 ) ) ;
#81491=FACE_OUTER_BOUND ( 'NONE', #91355, .T. ) ;
#81500=DIRECTION ( 'NONE',  ( 1.000000000000000000, 0.000000000000000000, -1.743630241030147277E-15 ) ) ;
#81505=EDGE_CURVE ( 'NONE', #60621, #63171, #13042, .T. ) ;
#81506=ORIENTED_EDGE ( 'NONE', *, *, #95888, .F. ) ;
#81507=DIRECTION ( 'NONE',  ( 0.000000000000000000, 0.000000000000000000, 1.000000000000000000 ) ) ;
#81508=CARTESIAN_POINT ( 'NONE',  ( -0.2200237740140755516, -5.876774720514408301, 19.17724329193115551 ) ) ;
#81509=ORIENTED_EDGE ( 'NONE', *, *, #24053, .F. ) ;
#81513=VERTEX_POINT ( 'NONE', #72093 ) ;
#81530=EDGE_CURVE ( 'NONE', #100069, #89719, #43132, .T. ) ;
#81535=CARTESIAN_POINT ( 'NONE',  ( -13.89275734969026388, 5.965225279485572685, 31.02402280011862246 ) ) ;
#81541=ORIENTED_EDGE ( 'NONE', *, *, #32476, .F. ) ;
#81543=LINE ( 'NONE', #27748, #90209 ) ;
#81544=CARTESIAN_POINT ( 'NONE',  ( -5.023036858974361252, -5.876774720514410077, 19.14743589743590846 ) ) ;
#81555=DIRECTION ( 'NONE',  ( 0.000000000000000000, 0.000000000000000000, 1.000000000000000000 ) ) ;
#81563=ORIENTED_EDGE ( 'NONE', *, *, #96779, .F. ) ;
#81564=CARTESIAN_POINT ( 'NONE',  ( -5.382328594919684406, -6.376774720514413630, 19.61227901093090864 ) ) ;
#81565=CARTESIAN_POINT ( 'NONE',  ( 13.10664265030973930, 5.965225279485574461, -27.62597719988137612 ) ) ;
#81567=CARTESIAN_POINT ( 'NONE',  ( 0.000000000000000000, -5.876774720514426953, 0.000000000000000000 ) ) ;
#81568=VECTOR ( 'NONE', #56284, 1000.000000000000000 ) ;
#81587=CARTESIAN_POINT ( 'NONE',  ( 16.89397143409390623, -5.876774720514426953, 16.89397143409405899 ) ) ;
#81592=FACE_OUTER_BOUND ( 'NONE', #13091, .T. ) ;
#81593=DIRECTION ( 'NONE',  ( -1.889676989081488347E-15, 0.000000000000000000, -1.000000000000000000 ) ) ;
#81602=FACE_OUTER_BOUND ( 'NONE', #1117, .T. ) ;
#81603=B_SPLINE_CURVE_WITH_KNOTS ( 'NONE', 3,
 ( #42986, #51091, #82035, #44476, #5901, #74420, #81544 ),
 .UNSPECIFIED., .F., .F.,
 ( 4, 1, 1, 1, 4 ),
 ( 0.000000000000000000, 0.2537340756906634187, 0.5030351201318574716, 0.7500135973308806880, 1.000000000000000000 ),
 .UNSPECIFIED. ) ;
#81605=AXIS2_PLACEMENT_3D ( 'NONE', #90765, #22231, #44597 ) ;
#81624=ORIENTED_EDGE ( 'NONE', *, *, #91146, .T. ) ;
#81625=ORIENTED_EDGE ( 'NONE', *, *, #81320, .T. ) ;
#81632=ORIENTED_EDGE ( 'NONE', *, *, #58068, .F. ) ;
#81647=CARTESIAN_POINT ( 'NONE',  ( 13.91401389203221406, 5.965225279485572685, 27.75920385068456042 ) ) ;
#81650=ORIENTED_EDGE ( 'NONE', *, *, #90702, .T. ) ;
#81652=CARTESIAN_POINT ( 'NONE',  ( -10.40290173325841216, -6.376774720514426953, 27.45402280011861862 ) ) ;
#81654=EDGE_CURVE ( 'NONE', #18679, #78997, #49760, .T. ) ;
#81660=CARTESIAN_POINT ( 'NONE',  ( 29.68479148105952348, -4.772774720514425972, -9.431263391055123790 ) ) ;
#81663=VERTEX_POINT ( 'NONE', #65494 ) ;
#81665=EDGE_LOOP ( 'NONE', ( #90048, #55742, #11332, #18974 ) ) ;
#81673=CARTESIAN_POINT ( 'NONE',  ( 2.589743589743596086, -6.376774720514415407, 20.00140224358974095 ) ) ;
#81678=ORIENTED_EDGE ( 'NONE', *, *, #6286, .F. ) ;
#81684=EDGE_CURVE ( 'NONE', #64573, #36349, #28895, .T. ) ;
#81712=EDGE_LOOP ( 'NONE', ( #97849, #30428, #22060, #54695 ) ) ;
#81720=FACE_OUTER_BOUND ( 'NONE', #77624, .T. ) ;
#81731=CARTESIAN_POINT ( 'NONE',  ( -1.044871794871793602, -6.376774720514418959, 20.44941907051282115 ) ) ;
#81742=VERTEX_POINT ( 'NONE', #46129 ) ;
#81746=DIRECTION ( 'NONE',  ( 0.000000000000000000, 0.000000000000000000, -1.000000000000000000 ) ) ;
#81748=ADVANCED_FACE ( 'NONE', ( #77552 ), #8055, .T. ) ;
#81754=ORIENTED_EDGE ( 'NONE', *, *, #99415, .F. ) ;
#81764=EDGE_CURVE ( 'NONE', #86782, #24870, #68958, .T. ) ;
#81766=VERTEX_POINT ( 'NONE', #7056 ) ;
#81771=CARTESIAN_POINT ( 'NONE',  ( -27.83739072329610664, 5.965225279485592225, -8.084349702057698650 ) ) ;
#81773=DIRECTION ( 'NONE',  ( 0.9685340172660600322, 0.000000000000000000, -0.2488812114211667315 ) ) ;
#81776=ORIENTED_EDGE ( 'NONE', *, *, #29611, .T. ) ;
#81791=CARTESIAN_POINT ( 'NONE',  ( 7.136624701378261548, -6.376774720514420736, 20.99078681144753844 ) ) ;
#81795=ORIENTED_EDGE ( 'NONE', *, *, #92711, .T. ) ;
#81798=LINE ( 'NONE', #81300, #75099 ) ;
#81807=EDGE_CURVE ( 'NONE', #63342, #46359, #17914, .T. ) ;
#81811=CARTESIAN_POINT ( 'NONE',  ( 13.57581083383196940, -6.376774720514426953, 20.21213203435597094 ) ) ;
#81816=CARTESIAN_POINT ( 'NONE',  ( 3.825380556292953482, -6.376774720514427841, 21.83927723428477208 ) ) ;
#81822=ORIENTED_EDGE ( 'NONE', *, *, #12205, .T. ) ;
#81834=CARTESIAN_POINT ( 'NONE',  ( 33.61456970919605425, -3.316774720514426900, -11.35828564741663449 ) ) ;
#81842=CARTESIAN_POINT ( 'NONE',  ( 4.453188626415028217, -5.876774720514421624, 21.07953283331298167 ) ) ;
#81846=CARTESIAN_POINT ( 'NONE',  ( 10.93823315965619791, -6.376774720514427841, -24.99764212866241309 ) ) ;
#81851=ORIENTED_EDGE ( 'NONE', *, *, #57124, .T. ) ;
#81854=ORIENTED_EDGE ( 'NONE', *, *, #37639, .F. ) ;
#81857=EDGE_CURVE ( 'NONE', #70350, #15460, #8200, .T. ) ;
#81860=DIRECTION ( 'NONE',  ( 0.000000000000000000, 0.000000000000000000, 1.000000000000000000 ) ) ;
#81863=LINE ( 'NONE', #6227, #53551 ) ;
#81877=ORIENTED_EDGE ( 'NONE', *, *, #57607, .T. ) ;
#81880=DIRECTION ( 'NONE',  ( -0.000000000000000000, 1.000000000000000000, -0.000000000000000000 ) ) ;
#81886=CARTESIAN_POINT ( 'NONE',  ( 15.29947330337542688, -3.316774720514426456, -27.16854002387010070 ) ) ;
#81888=DIRECTION ( 'NONE',  ( 1.000000000000000000, 0.000000000000000000, -2.216313064514630605E-15 ) ) ;
#81890=AXIS2_PLACEMENT_3D ( 'NONE', #9357, #40318, #38807 ) ;
#81892=DIRECTION ( 'NONE',  ( -0.7512896232466861335, 0.000000000000000000, -0.6599726524651249315 ) ) ;
#81896=DIRECTION ( 'NONE',  ( -1.000000000000000000, 0.000000000000000000, -0.000000000000000000 ) ) ;
#81899=ORIENTED_EDGE ( 'NONE', *, *, #28939, .T. ) ;
#81907=CARTESIAN_POINT ( 'NONE',  ( 6.424528460793287543, -5.876774720514413630, 19.73230822599986212 ) ) ;
#81916=DIRECTION ( 'NONE',  ( 0.000000000000000000, 0.000000000000000000, -1.000000000000000000 ) ) ;
#81918=ORIENTED_EDGE ( 'NONE', *, *, #57005, .T. ) ;
#81928=ORIENTED_EDGE ( 'NONE', *, *, #81505, .F. ) ;
#81930=CARTESIAN_POINT ( 'NONE',  ( 0.7051282051282027341, -6.376774720514408301, 19.19230769230768985 ) ) ;
#81935=DIRECTION ( 'NONE',  ( -0.9496245541219268116, 6.454799914155188842E-16, -0.3133898629642187239 ) ) ;
#81950=DIRECTION ( 'NONE',  ( -0.7512896232465888779, 8.688531644690855961E-16, -0.6599726524652355097 ) ) ;
#81956=CARTESIAN_POINT ( 'NONE',  ( -4.968349358974361252, -5.876774720514412742, 19.46153846153847056 ) ) ;
#81961=CIRCLE ( 'NONE', #68991, 1.399999999999999911 ) ;
#81970=CARTESIAN_POINT ( 'NONE',  ( -1.044639546681034536, -6.376774720514417183, 20.34213149456667580 ) ) ;
#81977=CARTESIAN_POINT ( 'NONE',  ( 3.106028565906091998, -5.876774720514426953, 3.106028565906120864 ) ) ;
#81982=ORIENTED_EDGE ( 'NONE', *, *, #98851, .F. ) ;
#81983=ORIENTED_EDGE ( 'NONE', *, *, #94816, .F. ) ;
#81998=CARTESIAN_POINT ( 'NONE',  ( 27.86270917940689174, 5.965225279485572685, 29.49402280011862487 ) ) ;
#81999=ORIENTED_EDGE ( 'NONE', *, *, #35807, .T. ) ;
#82001=CARTESIAN_POINT ( 'NONE',  ( -0.4909855769230799249, -6.376774720514410077, 19.14743589743590491 ) ) ;
#82005=ORIENTED_EDGE ( 'NONE', *, *, #82760, .F. ) ;
#82013=CARTESIAN_POINT ( 'NONE',  ( -27.96875734969026084, 6.475225279485573360, -0.08597719988137648983 ) ) ;
#82015=CARTESIAN_POINT ( 'NONE',  ( -5.891025641025639636, -5.876774720514419847, 20.75510817307693046 ) ) ;
#82024=DIRECTION ( 'NONE',  ( 0.000000000000000000, 0.000000000000000000, 1.000000000000000000 ) ) ;
#82026=VECTOR ( 'NONE', #22680, 1000.000000000000000 ) ;
#82029=ORIENTED_EDGE ( 'NONE', *, *, #19522, .T. ) ;
#82035=CARTESIAN_POINT ( 'NONE',  ( -4.620655831143558601, -5.876774720514410966, 19.21747685089457036 ) ) ;
#82038=ORIENTED_EDGE ( 'NONE', *, *, #5458, .F. ) ;
#82039=AXIS2_PLACEMENT_3D ( 'NONE', #84295, #14781, #7681 ) ;
#82042=VECTOR ( 'NONE', #91694, 1000.000000000000000 ) ;
#82045=ORIENTED_EDGE ( 'NONE', *, *, #12443, .F. ) ;
#82064=FACE_OUTER_BOUND ( 'NONE', #66940, .T. ) ;
#82079=CARTESIAN_POINT ( 'NONE',  ( -7.999999999999996447, -6.376774720514426953, 22.50000000000000355 ) ) ;
#82085=VECTOR ( 'NONE', #86315, 1000.000000000000000 ) ;
#82101=DIRECTION ( 'NONE',  ( 0.000000000000000000, 0.000000000000000000, 1.000000000000000000 ) ) ;
#82103=CARTESIAN_POINT ( 'NONE',  ( 6.404294203292168142, -6.376774720514415407, 20.09052689972686423 ) ) ;
#82104=VECTOR ( 'NONE', #2687, 1000.000000000000000 ) ;
#82110=FACE_OUTER_BOUND ( 'NONE', #85034, .T. ) ;
#82115=DIRECTION ( 'NONE',  ( -0.5630016722799275897, 0.000000000000000000, 0.8264557562326038109 ) ) ;
#82119=ORIENTED_EDGE ( 'NONE', *, *, #41900, .F. ) ;
#82134=CARTESIAN_POINT ( 'NONE',  ( 7.136624701378261548, -5.876774720514420736, 20.99078681144753844 ) ) ;
#82141=CARTESIAN_POINT ( 'NONE',  ( 3.020285327128866992, -5.876774720514407413, 19.15473963397401391 ) ) ;
#82157=ORIENTED_EDGE ( 'NONE', *, *, #42383, .F. ) ;
#82165=CARTESIAN_POINT ( 'NONE',  ( -1.714505518806294145E-16, -5.876774720514426953, 1.399999999999999911 ) ) ;
#82166=CARTESIAN_POINT ( 'NONE',  ( 29.68479148105952348, -4.772774720514425972, -9.431263391055123790 ) ) ;
#82173=CARTESIAN_POINT ( 'NONE',  ( -3.035630128403670192, -6.376774720514413630, 19.71630089903357685 ) ) ;
#82174=DIRECTION ( 'NONE',  ( 0.06283980576413539243, 0.000000000000000000, 0.9980236263794188822 ) ) ;
#82175=ADVANCED_FACE ( 'NONE', ( #82064 ), #12548, .F. ) ;
#82191=LINE ( 'NONE', #42163, #13391 ) ;
#82196=AXIS2_PLACEMENT_3D ( 'NONE', #65595, #12761, #96511 ) ;
#82200=CARTESIAN_POINT ( 'NONE',  ( -10.21507754268103696, -3.584423063163226786, 29.48076484700401068 ) ) ;
#82206=DIRECTION ( 'NONE',  ( -0.000000000000000000, -1.000000000000000000, -0.000000000000000000 ) ) ;
#82208=CARTESIAN_POINT ( 'NONE',  ( 6.110660513271839456, -5.876774720514421624, 21.43053473047838509 ) ) ;
#82212=PLANE ( 'NONE',  #100172 ) ;
#82213=DIRECTION ( 'NONE',  ( 0.000000000000000000, 0.000000000000000000, -1.000000000000000000 ) ) ;
#82219=VECTOR ( 'NONE', #33025, 1000.000000000000000 ) ;
#82226=CARTESIAN_POINT ( 'NONE',  ( 26.74698519091204574, -4.772774720514425972, -10.98683230472874151 ) ) ;
#82228=VECTOR ( 'NONE', #76777, 1000.000000000000000 ) ;
#82260=VERTEX_POINT ( 'NONE', #15037 ) ;
#82267=PLANE ( 'NONE',  #88622 ) ;
#82270=CARTESIAN_POINT ( 'NONE',  ( 13.12137440454564796, -3.706387542726002682, -28.15098661896695376 ) ) ;
#82273=ORIENTED_EDGE ( 'NONE', *, *, #6382, .F. ) ;
#82287=LINE ( 'NONE', #20877, #2581 ) ;
#82290=FACE_OUTER_BOUND ( 'NONE', #94498, .T. ) ;
#82294=CARTESIAN_POINT ( 'NONE',  ( 8.255033872309153864, 6.475225279485571583, -27.10684724722607442 ) ) ;
#82300=AXIS2_PLACEMENT_3D ( 'NONE', #90375, #58937, #75146 ) ;
#82303=EDGE_LOOP ( 'NONE', ( #87982, #89775, #86820, #59288, #79132, #36819 ) ) ;
#82310=CARTESIAN_POINT ( 'NONE',  ( 3.879810481058463711, -5.876774720514426953, 21.83835767234735670 ) ) ;
#82315=AXIS2_PLACEMENT_3D ( 'NONE', #92550, #31153, #85435 ) ;
#82320=ADVANCED_FACE ( 'NONE', ( #30769 ), #74931, .F. ) ;
#82323=CARTESIAN_POINT ( 'NONE',  ( 0.3910256410256383042, -6.376774720514408301, 19.19230769230768985 ) ) ;
#82334=ORIENTED_EDGE ( 'NONE', *, *, #69592, .F. ) ;
#82336=CARTESIAN_POINT ( 'NONE',  ( 4.628547153713393314, -5.876774720514418071, 20.50654586986123817 ) ) ;
#82344=B_SPLINE_SURFACE_WITH_KNOTS ( 'NONE', 3, 1, ( 
 ( #45724, #69055 ),
 ( #62454, #39099 ),
 ( #8161, #92882 ),
 ( #85272, #16763 ),
 ( #31490, #9154 ),
 ( #32500, #1560 ),
 ( #71070, #63472 ),
 ( #94394, #23361 ),
 ( #70056, #47731 ),
 ( #1054, #78148 ),
 ( #24876, #15763 ) ),
 .UNSPECIFIED., .F., .F., .F.,
 ( 4, 1, 1, 1, 1, 1, 1, 1, 4 ),
 ( 2, 2 ),
 ( 0.000000000000000000, 0.1411571637912756305, 0.2777725246444866514, 0.4092439672982337573, 0.5356759015826428882, 0.6574965059498953934, 0.7754582459464036681, 0.8894116614046648772, 1.000000000000000000 ),
 ( 0.000000000000000000, 1.000000000000000000 ),
 .UNSPECIFIED. ) ;
#82349=CARTESIAN_POINT ( 'NONE',  ( -6.741682653110981249, 5.965225279485572685, 30.62569541381301619 ) ) ;
#82350=DIRECTION ( 'NONE',  ( 0.000000000000000000, -1.000000000000000000, 0.000000000000000000 ) ) ;
#82355=EDGE_CURVE ( 'NONE', #37700, #97841, #8434, .T. ) ;
#82356=CARTESIAN_POINT ( 'NONE',  ( -2.196420576317535289, -6.376774720514410077, 19.14926908420044782 ) ) ;
#82364=EDGE_CURVE ( 'NONE', #70394, #3440, #75606, .T. ) ;
#82371=AXIS2_PLACEMENT_3D ( 'NONE', #71366, #4720, #98043 ) ;
#82374=CARTESIAN_POINT ( 'NONE',  ( 5.802984775641024662, -6.376774720514402972, 18.35026041666666430 ) ) ;
#82381=CARTESIAN_POINT ( 'NONE',  ( -4.141025641025642301, -6.376774720514411854, 19.63681891025641235 ) ) ;
#82383=CARTESIAN_POINT ( 'NONE',  ( 29.70264281947218876, -3.584400861594816856, 28.19233905662918005 ) ) ;
#82389=ORIENTED_EDGE ( 'NONE', *, *, #96841, .F. ) ;
#82401=CARTESIAN_POINT ( 'NONE',  ( 7.234974673537251100, -5.876774720514415407, 19.99114326857715795 ) ) ;
#82409=VERTEX_POINT ( 'NONE', #78933 ) ;
#82416=CARTESIAN_POINT ( 'NONE',  ( 30.61220459279984496, -3.931892516571728446, 27.21038724104498385 ) ) ;
#82420=ORIENTED_EDGE ( 'NONE', *, *, #53255, .T. ) ;
#82423=AXIS2_PLACEMENT_3D ( 'NONE', #51608, #58718, #89669 ) ;
#82426=CARTESIAN_POINT ( 'NONE',  ( 3.085011456917871264, -6.376774720514408301, 19.00082519311127172 ) ) ;
#82449=VECTOR ( 'NONE', #8341, 1000.000000000000000 ) ;
#82460=CARTESIAN_POINT ( 'NONE',  ( 15.99960863614631101, -3.577630190450212577, -27.91116951066581819 ) ) ;
#82461=CARTESIAN_POINT ( 'NONE',  ( 3.787259615384621636, -6.376774720514404748, 18.51923076923076650 ) ) ;
#82465=CARTESIAN_POINT ( 'NONE',  ( 32.42932432802503939, 5.965225279485572685, -0.2107846672978405389 ) ) ;
#82466=CLOSED_SHELL ( 'NONE', ( #33239, #56577, #68710, #10740, #65852, #37874, #96050, #68117, #81748, #8762, #22946, #82175, #50090, #21916, #51723, #39729, #27371, #85224, #66326, #613, #46804, #9132, #71430, #4412, #92489, #32031, #93074, #22512, #76168, #70076, #41659, #97912, #62210, #44671, #17706, #37965, #223, #721, #63529, #26069, #48983, #1027, #87861, #68933, #39029, #70061, #46444, #14283, #3341, #32350, #18718, #48903, #82784, #27686, #65276, #29434, #5529, #88965, #79732, #97818, #24256, #48539, #7493, #40068, #13906, #18523, #18613, #36384, #91758, #95046, #56315, #94950, #37068, #89764, #86355, #42457, #32355, #14577, #60999, #83766, #41076, #49486, #22398, #54078, #195, #20424, #50287, #36585, #94009, #94437, #12073, #26428, #30924, #85529, #85571, #83827, #68256, #43401, #57811, #30464, #80190, #51218, #94692, #12029, #29285, #75658, #51416, #11285, #44002, #26980, #69122, #27881, #32870, #67212, #29547, #54816, #100149, #88434, #80546, #41657, #16069, #45224, #75541, #35689, #93195, #60098, #18449, #8356, #84760, #56349, #53878, #81269, #51279, #72249, #42938, #2821, #40162, #57993, #48406, #11675, #90576, #4678, #54949, #84268, #47297, #36272, #27851, #34609, #72446, #85619, #75551, #13030, #53476, #41668, #39802, #28499, #44062, #44094, #17784, #24954, #6027, #16732, #71234, #41004, #91214, #29291, #51102, #30651, #14932, #95709, #43384, #33050, #49801, #93748, #55287, #78040, #33208, #26474, #85659, #15203, #48964, #63625, #1354, #71666, #496, #26548, #49346, #49111, #27699, #59509, #75235, #15737, #62596, #81330, #84025, #67022, #21527, #13782, #61009, #11272, #10722, #53578, #70577, #16218, #98348, #99856, #59935, #41183, #22861, #56337, #33801, #56, #47004, #59881, #66015, #34756, #5914, #49796, #29176, #53944, #63424, #25137, #50719, #95425, #86877, #79029, #97974, #69126, #10401, #72876, #75969, #46118, #45708, #88721, #11515, #9043, #36740, #63998, #27318, #42976, #14260, #83700, #49033, #95464, #4569, #65557, #66100, #1372, #31557, #92401, #44785, #39039, #22890, #72943, #50201, #32401, #5661, #25966, #96125, #88030, #91337, #58497, #30889, #22996, #88163, #21489, #31113, #73144, #63659, #79610, #9069, #78161, #56924, #83235, #56663, #26416, #27909, #88748, #42021, #15384, #90097, #70269, #95611, #19303, #44032, #66578, #68259, #97426, #68568, #48459, #69368, #36625, #24509, #35524, #68818, #25206, #90219, #10434, #48448, #2017, #29141, #42062, #62399, #1934, #8193, #46268, #55400, #61507, #45863, #42336, #67582, #14887, #67643, #2012, #45098, #78023, #58846, #38697, #77241, #20013, #20235, #44993, #72957, #99632, #84830, #16753, #35068, #69477, #25728, #32157, #8426, #66476, #58603, #98955, #51402, #10267, #75637, #90381, #58616, #33673, #34256, #40301, #81142, #13215, #91588, #60201, #78524, #6481, #76629, #52212, #76448, #44651, #8078, #4978, #42527, #26183, #85852, #75616, #97214, #44654, #100388, #16491, #47937, #100024, #96196, #65675, #25590, #66823, #59672, #56153, #6806, #35339, #59181, #66880, #45679, #8074, #87992, #53480, #56799, #37468, #42244, #5774, #63359, #9204, #22321, #85181, #80486, #82320, #730 ) ) ;
#82484=CARTESIAN_POINT ( 'NONE',  ( 30.32108885906865936, -6.376774720514426953, 3.274824222184972822 ) ) ;
#82489=CARTESIAN_POINT ( 'NONE',  ( 22.81105451610979173, -1.682774720514426114, -18.46691820600746681 ) ) ;
#82491=ORIENTED_EDGE ( 'NONE', *, *, #67647, .F. ) ;
#82512=CIRCLE ( 'NONE', #67970, 28.96799999999999642 ) ;
#82516=ORIENTED_EDGE ( 'NONE', *, *, #77506, .F. ) ;
#82538=CARTESIAN_POINT ( 'NONE',  ( -41.32836283488544638, -2.682774720514426559, 39.26872235229541985 ) ) ;
#82544=CARTESIAN_POINT ( 'NONE',  ( 33.69795529655567634, 6.475225279485573360, 20.86760796525322093 ) ) ;
#82555=CARTESIAN_POINT ( 'NONE',  ( -2.750773227259631692, -6.376774720514413630, 19.84584863393302001 ) ) ;
#82575=AXIS2_PLACEMENT_3D ( 'NONE', #33985, #72554, #73059 ) ;
#82588=FACE_OUTER_BOUND ( 'NONE', #28266, .T. ) ;
#82600=CARTESIAN_POINT ( 'NONE',  ( 3.128267882468583228, -6.376774720514424288, 21.08409277973916218 ) ) ;
#82609=DIRECTION ( 'NONE',  ( 1.000000000000000000, -0.000000000000000000, 0.000000000000000000 ) ) ;
#82612=ORIENTED_EDGE ( 'NONE', *, *, #45769, .T. ) ;
#82625=ORIENTED_EDGE ( 'NONE', *, *, #43491, .T. ) ;
#82631=ORIENTED_EDGE ( 'NONE', *, *, #35823, .T. ) ;
#82636=ORIENTED_EDGE ( 'NONE', *, *, #27938, .T. ) ;
#82640=EDGE_CURVE ( 'NONE', #26990, #36206, #13418, .T. ) ;
#82644=EDGE_CURVE ( 'NONE', #65974, #78100, #30210, .T. ) ;
#82646=CARTESIAN_POINT ( 'NONE',  ( 5.993553214355093139, -5.876774720514417183, 20.20316077874593930 ) ) ;
#82656=AXIS2_PLACEMENT_3D ( 'NONE', #14647, #90782, #7539 ) ;
#82665=CARTESIAN_POINT ( 'NONE',  ( -1.222978892338334012, -5.876774720514411854, 19.56655654527324373 ) ) ;
#82667=CARTESIAN_POINT ( 'NONE',  ( 0.000000000000000000, -2.056774720514426669, 0.000000000000000000 ) ) ;
#82671=FACE_OUTER_BOUND ( 'NONE', #13071, .T. ) ;
#82673=EDGE_CURVE ( 'NONE', #25591, #40969, #5814, .T. ) ;
#82682=CARTESIAN_POINT ( 'NONE',  ( 282.9764569301858046, -3.316774720514426900, 20.79159422840526616 ) ) ;
#82685=CARTESIAN_POINT ( 'NONE',  ( -0.4362980769230789257, -6.376774720514411854, 19.46153846153846345 ) ) ;
#82700=B_SPLINE_CURVE_WITH_KNOTS ( 'NONE', 3,
 ( #73810, #4311, #7283, #85918 ),
 .UNSPECIFIED., .F., .F.,
 ( 4, 4 ),
 ( 0.000000000000000000, 0.0002088004239042353695 ),
 .UNSPECIFIED. ) ;
#82704=EDGE_CURVE ( 'NONE', #18629, #24103, #62487, .T. ) ;
#82710=FACE_OUTER_BOUND ( 'NONE', #80936, .T. ) ;
#82719=DIRECTION ( 'NONE',  ( 0.7071067811865507924, 0.000000000000000000, 0.7071067811865442421 ) ) ;
#82721=CARTESIAN_POINT ( 'NONE',  ( -25.92875734969025814, -6.376774720514426953, 26.43402280011862615 ) ) ;
#82722=AXIS2_PLACEMENT_3D ( 'NONE', #67467, #98393, #75552 ) ;
#82738=EDGE_LOOP ( 'NONE', ( #82119, #3719, #15124, #67428 ) ) ;
#82743=CARTESIAN_POINT ( 'NONE',  ( 5.949073730962466833, 5.965225279485572685, -27.94053387008862188 ) ) ;
#82744=CARTESIAN_POINT ( 'NONE',  ( 3.050049012211247579, -5.876774720514426065, 21.53019692557248632 ) ) ;
#82751=CARTESIAN_POINT ( 'NONE',  ( 15.50761710536979798, -3.593805972274602301, -28.23039328495928046 ) ) ;
#82755=EDGE_CURVE ( 'NONE', #5079, #68195, #33534, .T. ) ;
#82760=EDGE_CURVE ( 'NONE', #12714, #98742, #17812, .T. ) ;
#82768=EDGE_LOOP ( 'NONE', ( #4262, #19, #87786, #78820 ) ) ;
#82769=VECTOR ( 'NONE', #38837, 1000.000000000000000 ) ;
#82770=CARTESIAN_POINT ( 'NONE',  ( 9.278253834636469577, -6.376774720514426953, 21.48128695274316158 ) ) ;
#82779=CARTESIAN_POINT ( 'NONE',  ( 8.667033081675079131, -3.316774720514425567, -27.07192531862967400 ) ) ;
#82782=ORIENTED_EDGE ( 'NONE', *, *, #54940, .F. ) ;
#82784=ADVANCED_FACE ( 'NONE', ( #93920 ), #1104, .F. ) ;
#82787=CIRCLE ( 'NONE', #39044, 3.349999999999998757 ) ;
#82815=LINE ( 'NONE', #51888, #75009 ) ;
#82824=DIRECTION ( 'NONE',  ( -0.000000000000000000, 1.000000000000000000, -0.000000000000000000 ) ) ;
#82827=DIRECTION ( 'NONE',  ( 0.7071067811865507924, 0.000000000000000000, -0.7071067811865442421 ) ) ;
#82828=CARTESIAN_POINT ( 'NONE',  ( 10.40220176116686979, -5.447062032237068863, -27.19353416079722763 ) ) ;
#82831=CARTESIAN_POINT ( 'NONE',  ( 0.3910256410256394144, -6.376774720514411854, 19.63681891025641235 ) ) ;
#82836=CARTESIAN_POINT ( 'NONE',  ( -1.359251851468251449, -5.876774720514419847, 20.71116975788854120 ) ) ;
#82847=DIRECTION ( 'NONE',  ( 0.000000000000000000, 0.000000000000000000, 1.000000000000000000 ) ) ;
#82860=CARTESIAN_POINT ( 'NONE',  ( -29.49875734969025842, 5.965225279485572685, 17.86602280011862476 ) ) ;
#82862=ORIENTED_EDGE ( 'NONE', *, *, #73571, .F. ) ;
#82864=CARTESIAN_POINT ( 'NONE',  ( 3.252401863874210264, 5.965225279485592225, -29.35688408629928858 ) ) ;
#82865=CARTESIAN_POINT ( 'NONE',  ( -1.358974358974355257, -5.876774720514426953, 21.75000000000000711 ) ) ;
#82871=CARTESIAN_POINT ( 'NONE',  ( -4.223504350552545361, -6.376774720514411854, 19.52341893546492813 ) ) ;
#82877=DIRECTION ( 'NONE',  ( 0.9872275723272646575, 0.000000000000000000, 0.1593164160933058515 ) ) ;
#82886=CIRCLE ( 'NONE', #16460, 1.325999999999943446 ) ;
#82889=VERTEX_POINT ( 'NONE', #94931 ) ;
#82894=CARTESIAN_POINT ( 'NONE',  ( 7.480769230769231726, -6.376774720514420736, 20.77403846153845635 ) ) ;
#82901=CYLINDRICAL_SURFACE ( 'NONE', #45979, 2.249999999999998668 ) ;
#82909=CARTESIAN_POINT ( 'NONE',  ( 29.71119274252842501, -4.341971045292455145, 27.93347042254709223 ) ) ;
#82917=ORIENTED_EDGE ( 'NONE', *, *, #22491, .T. ) ;
#82918=FACE_OUTER_BOUND ( 'NONE', #14777, .T. ) ;
#82948=DIRECTION ( 'NONE',  ( -0.1311553622875919756, -0.000000000000000000, -0.9913618264504692190 ) ) ;
#82951=CARTESIAN_POINT ( 'NONE',  ( 0.3910256410256441884, -6.376774720514427841, 21.75000000000000000 ) ) ;
#82982=CARTESIAN_POINT ( 'NONE',  ( 31.84105487026622683, -3.622774720514426949, -11.95870468328481984 ) ) ;
#82986=ORIENTED_EDGE ( 'NONE', *, *, #85630, .T. ) ;
#82988=EDGE_CURVE ( 'NONE', #87707, #51886, #64200, .T. ) ;
#82990=CARTESIAN_POINT ( 'NONE',  ( 0.3910256410256441884, -5.876774720514426953, 21.75000000000000000 ) ) ;
#82993=VERTEX_POINT ( 'NONE', #42170 ) ;
#82994=CARTESIAN_POINT ( 'NONE',  ( 13.91401389203221406, 5.965225279485572685, 158.0376437107427137 ) ) ;
#83007=ORIENTED_EDGE ( 'NONE', *, *, #81458, .F. ) ;
#83013=CARTESIAN_POINT ( 'NONE',  ( 14.15579980161844986, -3.316774720514426456, -28.31186755866361437 ) ) ;
#83024=ORIENTED_EDGE ( 'NONE', *, *, #22163, .T. ) ;
#83025=EDGE_LOOP ( 'NONE', ( #45143, #57311, #5289, #32721 ) ) ;
#83026=CARTESIAN_POINT ( 'NONE',  ( -10.26098930579144763, -5.972795536074636757, 28.98685178976001353 ) ) ;
#83030=DIRECTION ( 'NONE',  ( 0.000000000000000000, 0.000000000000000000, 1.000000000000000000 ) ) ;
#83035=CARTESIAN_POINT ( 'NONE',  ( -4.968349358974361252, -6.376774720514411854, 19.46153846153847056 ) ) ;
#83043=CARTESIAN_POINT ( 'NONE',  ( -2.702089344534958304, -5.876774720514411854, 19.72789237585158162 ) ) ;
#83077=VECTOR ( 'NONE', #28480, 1000.000000000000000 ) ;
#83093=CARTESIAN_POINT ( 'NONE',  ( 7.403636664866980688, -5.876774720514423400, 21.18544102487025782 ) ) ;
#83096=DIRECTION ( 'NONE',  ( 0.000000000000000000, -1.000000000000000000, 0.000000000000000000 ) ) ;
#83102=B_SPLINE_CURVE_WITH_KNOTS ( 'NONE', 3,
 ( #50446, #80394, #82383, #10884, #3783, #88510, #11875, #35225, #28108, #34719, #97116, #73776, #66696, #65200 ),
 .UNSPECIFIED., .F., .F.,
 ( 4, 2, 2, 2, 2, 2, 4 ),
 ( 3.469446951953614189E-18, 0.0003991292329371358004, 0.0007982584658742681314, 0.001197387698811397914, 0.001596516931748527806, 0.002394775397622781951, 0.003193033863497036530 ),
 .UNSPECIFIED. ) ;
#83104=ORIENTED_EDGE ( 'NONE', *, *, #97527, .F. ) ;
#83112=VERTEX_POINT ( 'NONE', #90815 ) ;
#83118=ORIENTED_EDGE ( 'NONE', *, *, #86593, .T. ) ;
#83128=CARTESIAN_POINT ( 'NONE',  ( 4.931982383686722926, -6.376774720514411854, 19.38944687450761961 ) ) ;
#83136=EDGE_CURVE ( 'NONE', #49712, #69249, #92801, .T. ) ;
#83137=CARTESIAN_POINT ( 'NONE',  ( -2.768609665556980293, -0.3587747205144057872, -29.41086200512614823 ) ) ;
#83140=DIRECTION ( 'NONE',  ( 0.000000000000000000, 0.000000000000000000, 1.000000000000000000 ) ) ;
#83145=EDGE_LOOP ( 'NONE', ( #42364, #99134, #32308, #64445 ) ) ;
#83146=ORIENTED_EDGE ( 'NONE', *, *, #8179, .F. ) ;
#83160=VECTOR ( 'NONE', #36351, 1000.000000000000114 ) ;
#83175=CARTESIAN_POINT ( 'NONE',  ( 14.43441819135929727, 5.965225279485572685, -28.36222020317710246 ) ) ;
#83179=CARTESIAN_POINT ( 'NONE',  ( -2.704906987277324593, 5.965225279485572685, -28.92935364444904067 ) ) ;
#83182=CIRCLE ( 'NONE', #75069, 0.3000000000000016542 ) ;
#83198=ORIENTED_EDGE ( 'NONE', *, *, #59759, .F. ) ;
#83200=CARTESIAN_POINT ( 'NONE',  ( 13.02968616431713578, -5.152774720514426754, -26.31186222701416000 ) ) ;
#83212=EDGE_CURVE ( 'NONE', #32836, #66793, #45643, .T. ) ;
#83213=VECTOR ( 'NONE', #45044, 1000.000000000000000 ) ;
#83217=CARTESIAN_POINT ( 'NONE',  ( -7.641025641025641413, -6.376774720514418959, 20.36458333333334636 ) ) ;
#83222=AXIS2_PLACEMENT_3D ( 'NONE', #4950, #19661, #4462 ) ;
#83227=EDGE_LOOP ( 'NONE', ( #74287, #89213, #8503, #13982 ) ) ;
#83232=ORIENTED_EDGE ( 'NONE', *, *, #79905, .T. ) ;
#83235=ADVANCED_FACE ( 'NONE', ( #85279 ), #7661, .F. ) ;
#83248=ORIENTED_EDGE ( 'NONE', *, *, #69722, .F. ) ;
#83263=B_SPLINE_CURVE_WITH_KNOTS ( 'NONE', 3,
 ( #215, #77325, #24546, #93550, #8831, #86453, #32162, #70232, #69737, #8327, #7826, #85954, #93053, #31160, #23029, #45904, #62130, #712, #54511 ),
 .UNSPECIFIED., .F., .F.,
 ( 4, 1, 1, 1, 1, 1, 1, 1, 1, 1, 1, 1, 1, 1, 1, 1, 4 ),
 ( 0.000000000000000000, 0.06867706841303485021, 0.1368709585090958636, 0.2061143571452989376, 0.2775381819697280150, 0.3497719775548984722, 0.4212508361555684644, 0.4929107569233693309, 0.5670265889927383895, 0.6066141532413351634, 0.6497039535189884640, 0.6973031504846843864, 0.7490856597091365421, 0.8048806474593092064, 0.8654850057023351084, 0.9302371271531362229, 1.000000000000000000 ),
 .UNSPECIFIED. ) ;
#83266=CIRCLE ( 'NONE', #55705, 12.65241003308275758 ) ;
#83274=CARTESIAN_POINT ( 'NONE',  ( 32.98733314340959311, 5.965225279485572685, 2.074222136288530027 ) ) ;
#83290=CARTESIAN_POINT ( 'NONE',  ( 28.20688450243646272, -14.82721238576461609, -7.073367244510395224 ) ) ;
#83291=DIRECTION ( 'NONE',  ( 0.7071067811865474617, 0.000000000000000000, 0.7071067811865474617 ) ) ;
#83307=DIRECTION ( 'NONE',  ( -1.333806637208504346E-15, 6.669033186042521139E-15, -1.000000000000000000 ) ) ;
#83308=DIRECTION ( 'NONE',  ( -0.7071067811865476838, 0.000000000000000000, 0.7071067811865474617 ) ) ;
#83316=CARTESIAN_POINT ( 'NONE',  ( -20.27875734969026311, 6.143225279485574397, 24.00402280011862288 ) ) ;
#83323=CIRCLE ( 'NONE', #67211, 1.399999999999998579 ) ;
#83327=ORIENTED_EDGE ( 'NONE', *, *, #40617, .F. ) ;
#83329=CARTESIAN_POINT ( 'NONE',  ( 22.81105451610979173, 8.475225279485572472, -18.46691820600746681 ) ) ;
#83330=EDGE_CURVE ( 'NONE', #46643, #18086, #4370, .T. ) ;
#83331=CARTESIAN_POINT ( 'NONE',  ( -4.993225604111835914, 5.965225279485592225, -29.11654937215278593 ) ) ;
#83333=DIRECTION ( 'NONE',  ( -0.000000000000000000, 1.000000000000000000, -0.000000000000000000 ) ) ;
#83340=ORIENTED_EDGE ( 'NONE', *, *, #93453, .T. ) ;
#83343=DIRECTION ( 'NONE',  ( 1.000000000000000000, 0.000000000000000000, -2.168404344971008868E-16 ) ) ;
#83350=VECTOR ( 'NONE', #46371, 1000.000000000000000 ) ;
#83357=DIRECTION ( 'NONE',  ( -0.000000000000000000, 1.000000000000000000, -0.000000000000000000 ) ) ;
#83374=DIRECTION ( 'NONE',  ( -0.000000000000000000, 1.000000000000000000, -0.000000000000000000 ) ) ;
#83384=VERTEX_POINT ( 'NONE', #63478 ) ;
#83388=EDGE_CURVE ( 'NONE', #88394, #69866, #61159, .T. ) ;
#83403=VERTEX_POINT ( 'NONE', #76653 ) ;
#83408=CARTESIAN_POINT ( 'NONE',  ( 32.42932432802503939, -6.376774720514426953, -0.2107846672978405389 ) ) ;
#83411=CARTESIAN_POINT ( 'NONE',  ( 6.274899854645557440, -5.876774720514428729, 21.83451738260096775 ) ) ;
#83418=CARTESIAN_POINT ( 'NONE',  ( 3.450324536843889067, -5.876774720514404748, 18.60429515659643229 ) ) ;
#83419=CARTESIAN_POINT ( 'NONE',  ( 3.398951772795901771, -5.876774720514403860, 18.23562605320997676 ) ) ;
#83428=CARTESIAN_POINT ( 'NONE',  ( 30.93860345374796594, -0.6647747205144264315, 19.84760796525321780 ) ) ;
#83435=CARTESIAN_POINT ( 'NONE',  ( 32.53135143123563466, 5.965225279485572685, 6.926385399448451885 ) ) ;
#83448=LINE ( 'NONE', #44912, #76681 ) ;
#83460=LINE ( 'NONE', #6838, #39752 ) ;
#83470=CARTESIAN_POINT ( 'NONE',  ( 0.3545156366401029935, -5.876774720514413630, 20.17598923696321478 ) ) ;
#83475=DIRECTION ( 'NONE',  ( -1.526034937513432889E-15, 7.121496375062686157E-15, -1.000000000000000000 ) ) ;
#83486=ORIENTED_EDGE ( 'NONE', *, *, #83931, .F. ) ;
#83497=CARTESIAN_POINT ( 'NONE',  ( -3.085512303079157359, -6.376774720514415407, 19.95084900476495093 ) ) ;
#83502=EDGE_LOOP ( 'NONE', ( #1698, #46839, #68512, #42004 ) ) ;
#83509=CARTESIAN_POINT ( 'NONE',  ( 4.653846153846159517, -6.376774720514415407, 19.99999999999999289 ) ) ;
#83511=CARTESIAN_POINT ( 'NONE',  ( 29.94037442937952065, -5.350967020813893527, 19.84760796525321425 ) ) ;
#83514=ORIENTED_EDGE ( 'NONE', *, *, #63667, .T. ) ;
#83521=ORIENTED_EDGE ( 'NONE', *, *, #26868, .F. ) ;
#83525=ORIENTED_EDGE ( 'NONE', *, *, #43030, .F. ) ;
#83527=ORIENTED_EDGE ( 'NONE', *, *, #86871, .F. ) ;
#83532=CIRCLE ( 'NONE', #98155, 11.85241003308275864 ) ;
#83543=DIRECTION ( 'NONE',  ( -0.000000000000000000, 1.000000000000000000, -0.000000000000000000 ) ) ;
#83544=FACE_OUTER_BOUND ( 'NONE', #1289, .T. ) ;
#83545=LINE ( 'NONE', #64991, #28757 ) ;
#83546=CIRCLE ( 'NONE', #2597, 2.249999999999998668 ) ;
#83560=LINE ( 'NONE', #61252, #78048 ) ;
#83564=CARTESIAN_POINT ( 'NONE',  ( 10.46399479596578175, -3.400839389856524342, -27.03001098546515735 ) ) ;
#83566=CARTESIAN_POINT ( 'NONE',  ( -0.02075734969026423599, -6.376774720514426953, -0.08597719988137648983 ) ) ;
#83574=CARTESIAN_POINT ( 'NONE',  ( 3.398286024651508530, -6.376774720514429617, 21.76255057507181334 ) ) ;
#83580=CARTESIAN_POINT ( 'NONE',  ( 31.48454476783385658, -4.132774720514426292, -1.134026763942596494 ) ) ;
#83585=ORIENTED_EDGE ( 'NONE', *, *, #84161, .T. ) ;
#83589=CARTESIAN_POINT ( 'NONE',  ( 3.165726958143470160, -6.376774720514422512, 21.14296526391294506 ) ) ;
#83595=DIRECTION ( 'NONE',  ( 0.1489078231574191002, 6.845827386180410961E-16, -0.9888510809027407644 ) ) ;
#83598=FACE_OUTER_BOUND ( 'NONE', #56943, .T. ) ;
#83601=DIRECTION ( 'NONE',  ( -0.000000000000000000, -1.000000000000000000, -0.000000000000000000 ) ) ;
#83603=EDGE_LOOP ( 'NONE', ( #31252, #73538, #96019, #49871 ) ) ;
#83604=VECTOR ( 'NONE', #49362, 1000.000000000000000 ) ;
#83607=AXIS2_PLACEMENT_3D ( 'NONE', #37642, #6191, #99519 ) ;
#83611=EDGE_CURVE ( 'NONE', #95824, #33670, #66063, .T. ) ;
#83632=EDGE_LOOP ( 'NONE', ( #89174, #84342, #6121, #13790, #25253, #16370, #18904, #53863, #71442 ) ) ;
#83635=VERTEX_POINT ( 'NONE', #83665 ) ;
#83636=CARTESIAN_POINT ( 'NONE',  ( 3.879812756903532556, -6.376774720514401196, 18.16163344421570969 ) ) ;
#83637=ORIENTED_EDGE ( 'NONE', *, *, #69069, .T. ) ;
#83644=PLANE ( 'NONE',  #49667 ) ;
#83646=CARTESIAN_POINT ( 'NONE',  ( 17.51792015816173986, 5.965225279485572685, 29.01255224319336889 ) ) ;
#83663=DIRECTION ( 'NONE',  ( 0.000000000000000000, 0.000000000000000000, -1.000000000000000000 ) ) ;
#83665=CARTESIAN_POINT ( 'NONE',  ( 30.09341516180546350, -2.682774720514426559, -13.89311774897855933 ) ) ;
#83679=VECTOR ( 'NONE', #44791, 1000.000000000000000 ) ;
#83680=VERTEX_POINT ( 'NONE', #1448 ) ;
#83684=VECTOR ( 'NONE', #61331, 1000.000000000000000 ) ;
#83700=ADVANCED_FACE ( 'NONE', ( #70958, #7047 ), #31385, .T. ) ;
#83713=DIRECTION ( 'NONE',  ( 0.000000000000000000, 0.000000000000000000, 1.000000000000000000 ) ) ;
#83716=EDGE_CURVE ( 'NONE', #881, #50095, #51372, .T. ) ;
#83721=VECTOR ( 'NONE', #48492, 1000.000000000000000 ) ;
#83722=CARTESIAN_POINT ( 'NONE',  ( 5.642884982650352654, -5.876774720514425177, 20.85668005806743608 ) ) ;
#83729=CARTESIAN_POINT ( 'NONE',  ( -28.98875734969026041, 5.965225279485572685, 17.86602280011862476 ) ) ;
#83737=VERTEX_POINT ( 'NONE', #16651 ) ;
#83741=ORIENTED_EDGE ( 'NONE', *, *, #27450, .F. ) ;
#83744=CARTESIAN_POINT ( 'NONE',  ( 2.627412086454235851, -5.876774720514419847, 20.59155478446653831 ) ) ;
#83746=AXIS2_PLACEMENT_3D ( 'NONE', #94634, #31739, #64215 ) ;
#83758=CARTESIAN_POINT ( 'NONE',  ( 32.95803010956177559, -3.605854314291305762, -13.01399263622904812 ) ) ;
#83759=ORIENTED_EDGE ( 'NONE', *, *, #51229, .F. ) ;
#83760=CARTESIAN_POINT ( 'NONE',  ( -10.54059822343757880, -5.876774720514426953, 22.82308057603841078 ) ) ;
#83763=ORIENTED_EDGE ( 'NONE', *, *, #40388, .T. ) ;
#83766=ADVANCED_FACE ( 'NONE', ( #84163 ), #38595, .F. ) ;
#83775=DIRECTION ( 'NONE',  ( 0.000000000000000000, -1.000000000000000000, 0.000000000000000000 ) ) ;
#83776=EDGE_LOOP ( 'NONE', ( #74653, #50675, #43968, #28762 ) ) ;
#83781=EDGE_CURVE ( 'NONE', #50554, #34695, #50119, .T. ) ;
#83785=AXIS2_PLACEMENT_3D ( 'NONE', #96907, #11175, #57375 ) ;
#83790=CARTESIAN_POINT ( 'NONE',  ( 15.31892417638225012, -3.658177093025726023, -28.50911884272268182 ) ) ;
#83811=ORIENTED_EDGE ( 'NONE', *, *, #52101, .F. ) ;
#83812=CARTESIAN_POINT ( 'NONE',  ( 33.40725018382580913, -3.504198967030887069, -12.51830322776342008 ) ) ;
#83819=LINE ( 'NONE', #93422, #95332 ) ;
#83827=ADVANCED_FACE ( 'NONE', ( #2952 ), #64870, .F. ) ;
#83835=CARTESIAN_POINT ( 'NONE',  ( 31.59111626279633711, -0.3587747205144265483, 16.27760796525321751 ) ) ;
#83840=CARTESIAN_POINT ( 'NONE',  ( 5.326923076923078426, -6.376774720514420736, 20.76772836538461320 ) ) ;
#83845=AXIS2_PLACEMENT_3D ( 'NONE', #62331, #54723, #38485 ) ;
#83858=CARTESIAN_POINT ( 'NONE',  ( -20.77875734969026311, -5.356774720514425603, 0.7300228001186309656 ) ) ;
#83860=LINE ( 'NONE', #76726, #28231 ) ;
#83862=DIRECTION ( 'NONE',  ( -0.000000000000000000, 1.000000000000000000, -0.000000000000000000 ) ) ;
#83864=ORIENTED_EDGE ( 'NONE', *, *, #97897, .T. ) ;
#83871=ORIENTED_EDGE ( 'NONE', *, *, #83896, .F. ) ;
#83873=DIRECTION ( 'NONE',  ( -0.000000000000000000, 1.000000000000000000, -0.000000000000000000 ) ) ;
#83875=VECTOR ( 'NONE', #22266, 1000.000000000000000 ) ;
#83880=CARTESIAN_POINT ( 'NONE',  ( 6.424528460793287543, -6.376774720514413630, 19.73230822599986212 ) ) ;
#83886=VERTEX_POINT ( 'NONE', #9545 ) ;
#83896=EDGE_CURVE ( 'NONE', #54031, #86922, #85436, .T. ) ;
#83899=CARTESIAN_POINT ( 'NONE',  ( -27.61845239340658154, 5.965225279485594001, -10.37513603161905351 ) ) ;
#83925=DIRECTION ( 'NONE',  ( 0.7512896232465891000, 0.000000000000000000, 0.6599726524652351767 ) ) ;
#83926=CARTESIAN_POINT ( 'NONE',  ( 3.052815417670126319, -6.376774720514406525, 18.46676085997033923 ) ) ;
#83927=VECTOR ( 'NONE', #50108, 1000.000000000000000 ) ;
#83931=EDGE_CURVE ( 'NONE', #33363, #74029, #43505, .T. ) ;
#83937=CARTESIAN_POINT ( 'NONE',  ( 26.73860345374794178, 1.477225279485574028, 19.84760796525321425 ) ) ;
#83948=FACE_OUTER_BOUND ( 'NONE', #46100, .T. ) ;
#83951=DIRECTION ( 'NONE',  ( 0.000000000000000000, 1.478457507934778393E-16, -1.000000000000000000 ) ) ;
#83953=CIRCLE ( 'NONE', #22364, 2.249999999999998668 ) ;
#83956=CARTESIAN_POINT ( 'NONE',  ( -0.6227173540047638012, -6.376774720514413630, 19.48351902941045211 ) ) ;
#83965=CARTESIAN_POINT ( 'NONE',  ( 3.421177667410919110, -6.376774720514426953, 28.69411518427638441 ) ) ;
#83973=CARTESIAN_POINT ( 'NONE',  ( -0.2112149364088803105, -5.876774720514410077, 19.49357334786886398 ) ) ;
#83977=AXIS2_PLACEMENT_3D ( 'NONE', #3608, #55899, #10712 ) ;
#83979=CARTESIAN_POINT ( 'NONE',  ( -23.24941632505786870, -6.376774720514426953, 27.45402280011862572 ) ) ;
#83986=ORIENTED_EDGE ( 'NONE', *, *, #85580, .F. ) ;
#83988=CARTESIAN_POINT ( 'NONE',  ( 4.740341618695937065, -6.376774720514404748, 18.75174579344860248 ) ) ;
#83993=VERTEX_POINT ( 'NONE', #52604 ) ;
#83995=CARTESIAN_POINT ( 'NONE',  ( -2.794871794871795156, -6.376774720514417183, 20.36318108974359475 ) ) ;
#84009=DIRECTION ( 'NONE',  ( -1.000000000000000000, 0.000000000000000000, 0.000000000000000000 ) ) ;
#84013=EDGE_LOOP ( 'NONE', ( #48108, #67595, #57963, #5870 ) ) ;
#84018=CARTESIAN_POINT ( 'NONE',  ( 14.43441819135929194, -3.316774720514426456, -28.36222020317710957 ) ) ;
#84025=ADVANCED_FACE ( 'NONE', ( #52110 ), #12537, .T. ) ;
#84060=FACE_OUTER_BOUND ( 'NONE', #53811, .T. ) ;
#84078=FACE_OUTER_BOUND ( 'NONE', #34526, .T. ) ;
#84084=CARTESIAN_POINT ( 'NONE',  ( 29.70220533433691301, 6.475225279485573360, 28.20564067601639735 ) ) ;
#84085=FACE_OUTER_BOUND ( 'NONE', #77073, .T. ) ;
#84089=CARTESIAN_POINT ( 'NONE',  ( 22.81105451610979173, -1.684774720501991618, -20.71691820600746681 ) ) ;
#84102=CARTESIAN_POINT ( 'NONE',  ( -5.824076695599092801, -5.876774720514411854, 19.72913074730691108 ) ) ;
#84114=ORIENTED_EDGE ( 'NONE', *, *, #37676, .F. ) ;
#84130=CYLINDRICAL_SURFACE ( 'NONE', #65318, 15.00000000000000178 ) ;
#84135=CARTESIAN_POINT ( 'NONE',  ( 4.948119756536996761, -6.376774720514410077, 19.52858994054604125 ) ) ;
#84142=B_SPLINE_CURVE_WITH_KNOTS ( 'NONE', 3,
 ( #46014, #76933, #62241, #40892, #77433, #7935, #48520, #16041, #38884, #2343, #86063, #24159, #55129, #25157, #56637, #78940, #39888, #16537, #93667 ),
 .UNSPECIFIED., .F., .F.,
 ( 4, 1, 1, 1, 1, 1, 1, 1, 1, 1, 1, 1, 1, 1, 1, 1, 4 ),
 ( 0.000000000000000000, 0.07834298519369982394, 0.1505633028794195749, 0.2161510566599787464, 0.2756797924514269305, 0.3287070503654637710, 0.3759044348322068685, 0.4173018977400307916, 0.4526927480535820614, 0.5172652917530110583, 0.5812165680623054831, 0.6453218939728019299, 0.7120244933797625908, 0.7801300447160447460, 0.8502182262116649847, 0.9226485217347383250, 1.000000000000000000 ),
 .UNSPECIFIED. ) ;
#84158=CARTESIAN_POINT ( 'NONE',  ( -0.8460708837923186509, -5.876774720514410966, 19.21968329462762526 ) ) ;
#84161=EDGE_CURVE ( 'NONE', #55189, #83112, #29763, .T. ) ;
#84163=FACE_OUTER_BOUND ( 'NONE', #76389, .T. ) ;
#84164=DIRECTION ( 'NONE',  ( -0.000000000000000000, 1.000000000000000000, -0.000000000000000000 ) ) ;
#84168=AXIS2_PLACEMENT_3D ( 'NONE', #27077, #12336, #43306 ) ;
#84184=CARTESIAN_POINT ( 'NONE',  ( -5.903826827417286260, -6.376774720514418959, 20.39230070883895252 ) ) ;
#84197=CARTESIAN_POINT ( 'NONE',  ( 33.63243172119919677, -3.340070231344590912, -11.49682753434936622 ) ) ;
#84198=ORIENTED_EDGE ( 'NONE', *, *, #37188, .T. ) ;
#84206=CARTESIAN_POINT ( 'NONE',  ( 15.97264540888996365, 5.965225279485572685, -27.93485543958161443 ) ) ;
#84214=CARTESIAN_POINT ( 'NONE',  ( 0.000000000000000000, -5.876774720514426953, -1.399999999999999911 ) ) ;
#84215=CIRCLE ( 'NONE', #24255, 91.74549126261079834 ) ;
#84219=CARTESIAN_POINT ( 'NONE',  ( 22.81105451610979173, -1.682774720514426114, -18.46691820600746681 ) ) ;
#84220=EDGE_LOOP ( 'NONE', ( #38158, #73397, #1134, #80316 ) ) ;
#84228=CIRCLE ( 'NONE', #85835, 1.836000000000000743 ) ;
#84234=ORIENTED_EDGE ( 'NONE', *, *, #28353, .T. ) ;
#84236=ORIENTED_EDGE ( 'NONE', *, *, #62191, .T. ) ;
#84247=CARTESIAN_POINT ( 'NONE',  ( -19.38764004357182813, -6.376774720514426953, -21.62823517627351322 ) ) ;
#84256=LINE ( 'NONE', #75638, #64414 ) ;
#84259=CARTESIAN_POINT ( 'NONE',  ( 5.471383689419965890, -0.3587747205144057872, -29.02273493113404612 ) ) ;
#84262=ORIENTED_EDGE ( 'NONE', *, *, #34486, .T. ) ;
#84265=ORIENTED_EDGE ( 'NONE', *, *, #74190, .F. ) ;
#84268=ADVANCED_FACE ( 'NONE', ( #79929 ), #40377, .F. ) ;
#84280=DIRECTION ( 'NONE',  ( -1.000000000000000000, -0.000000000000000000, -0.000000000000000000 ) ) ;
#84287=CARTESIAN_POINT ( 'NONE',  ( 15.30669619680802995, -3.489325088183165224, -28.51986054853846753 ) ) ;
#84291=ORIENTED_EDGE ( 'NONE', *, *, #72017, .F. ) ;
#84292=CARTESIAN_POINT ( 'NONE',  ( 30.53060340732035982, -6.376774720514426953, 20.86760796525322093 ) ) ;
#84295=CARTESIAN_POINT ( 'NONE',  ( -41.32836283488544638, -2.682774720514426559, 39.26872235229541985 ) ) ;
#84296=ORIENTED_EDGE ( 'NONE', *, *, #26293, .T. ) ;
#84317=CARTESIAN_POINT ( 'NONE',  ( -1.733151984336291695, -5.876774720514408301, 19.29154511076646017 ) ) ;
#84329=CARTESIAN_POINT ( 'NONE',  ( -1.955883090540335045, -5.876774720514411854, 19.49432735726521315 ) ) ;
#84330=EDGE_CURVE ( 'NONE', #70350, #99563, #9920, .T. ) ;
#84342=ORIENTED_EDGE ( 'NONE', *, *, #47805, .F. ) ;
#84357=CARTESIAN_POINT ( 'NONE',  ( -5.877732331298974877, -6.376774720514411854, 19.69174559449349005 ) ) ;
#84366=CARTESIAN_POINT ( 'NONE',  ( 0.09189959430841809773, -6.376774720514410077, 19.67013632031035542 ) ) ;
#84378=CARTESIAN_POINT ( 'NONE',  ( 32.69168087260868560, -4.943943141208723802, -11.74984035242545133 ) ) ;
#84391=EDGE_CURVE ( 'NONE', #98350, #33363, #79030, .T. ) ;
#84393=DIRECTION ( 'NONE',  ( 1.000000000000000000, 0.000000000000000000, 0.000000000000000000 ) ) ;
#84398=CARTESIAN_POINT ( 'NONE',  ( 7.402957069319889172, -6.376774720514418959, 20.34212842306459024 ) ) ;
#84403=CARTESIAN_POINT ( 'NONE',  ( -22.05275734969026047, -0.3587747205144262708, 31.02402280011862246 ) ) ;
#84404=CARTESIAN_POINT ( 'NONE',  ( 32.68381218857752657, -4.917472161913310380, -3.063707678755676511 ) ) ;
#84422=CARTESIAN_POINT ( 'NONE',  ( 22.02124265030973760, 6.143225279485574397, 16.20402280011862217 ) ) ;
#84424=CARTESIAN_POINT ( 'NONE',  ( 2.936453026386435017, -5.876774720514407413, 18.60215244312560401 ) ) ;
#84425=FACE_OUTER_BOUND ( 'NONE', #24084, .T. ) ;
#84444=CARTESIAN_POINT ( 'NONE',  ( -29.49875734969025842, 5.965225279485572685, 25.61802280011862720 ) ) ;
#84453=CARTESIAN_POINT ( 'NONE',  ( -1.488488975859286523, -6.376774720514411854, 19.49847411603315095 ) ) ;
#84459=EDGE_CURVE ( 'NONE', #40793, #72161, #99508, .T. ) ;
#84461=LINE ( 'NONE', #85965, #51666 ) ;
#84462=EDGE_CURVE ( 'NONE', #77005, #97841, #49870, .T. ) ;
#84473=CARTESIAN_POINT ( 'NONE',  ( 0.3791100739519297491, -5.876774720514418071, 20.35309744218306349 ) ) ;
#84477=LINE ( 'NONE', #15457, #43135 ) ;
#84480=EDGE_LOOP ( 'NONE', ( #9, #35456, #90604, #61881 ) ) ;
#84487=CARTESIAN_POINT ( 'NONE',  ( 4.931982383686722926, -6.376774720514411854, 19.38944687450761961 ) ) ;
#84495=CARTESIAN_POINT ( 'NONE',  ( -4.243469080022288509, -6.376774720514411854, 19.94806476610987644 ) ) ;
#84498=ORIENTED_EDGE ( 'NONE', *, *, #25363, .F. ) ;
#84499=CARTESIAN_POINT ( 'NONE',  ( -2.711489738547795625, -6.376774720514410077, 19.27798293355755632 ) ) ;
#84501=CARTESIAN_POINT ( 'NONE',  ( 22.74089357256066890, 1.477225279485574028, -19.20396252371061863 ) ) ;
#84504=CARTESIAN_POINT ( 'NONE',  ( 7.089543269230769162, -5.876774720514413630, 19.75741185897435415 ) ) ;
#84511=CARTESIAN_POINT ( 'NONE',  ( 4.653733606810938284, -6.376774720514411854, 19.95301661664751336 ) ) ;
#84512=EDGE_LOOP ( 'NONE', ( #51644, #537, #73778, #81899 ) ) ;
#84519=CARTESIAN_POINT ( 'NONE',  ( 22.02124265030973760, -6.376774720514428729, 19.20402280011862217 ) ) ;
#84528=ORIENTED_EDGE ( 'NONE', *, *, #96407, .T. ) ;
#84533=EDGE_CURVE ( 'NONE', #67210, #58474, #32015, .T. ) ;
#84540=ORIENTED_EDGE ( 'NONE', *, *, #80491, .F. ) ;
#84552=DIRECTION ( 'NONE',  ( -0.6599726524652352877, 0.000000000000000000, 0.7512896232465892110 ) ) ;
#84562=CARTESIAN_POINT ( 'NONE',  ( 4.468667172983064262, -5.876774720514401196, 18.40700896291420463 ) ) ;
#84574=CARTESIAN_POINT ( 'NONE',  ( 3.181132013147180970, -6.376774720514426065, 21.64201922499777808 ) ) ;
#84581=( LENGTH_UNIT ( ) NAMED_UNIT ( * ) SI_UNIT ( .MILLI., .METRE. ) );
#84590=EDGE_CURVE ( 'NONE', #94756, #70772, #49269, .T. ) ;
#84605=CARTESIAN_POINT ( 'NONE',  ( -5.205649524681222218, -6.376774720514408301, 19.16400979764067714 ) ) ;
#84607=DIRECTION ( 'NONE',  ( 0.000000000000000000, -1.000000000000000000, 0.000000000000000000 ) ) ;
#84633=VECTOR ( 'NONE', #3938, 1000.000000000000000 ) ;
#84638=CARTESIAN_POINT ( 'NONE',  ( 3.825381322105384285, -6.376774720514401196, 18.16071977647550995 ) ) ;
#84646=DIRECTION ( 'NONE',  ( 0.000000000000000000, -1.000000000000000000, 0.000000000000000000 ) ) ;
#84650=ORIENTED_EDGE ( 'NONE', *, *, #32369, .F. ) ;
#84655=DIRECTION ( 'NONE',  ( 0.000000000000000000, 0.000000000000000000, 1.000000000000000000 ) ) ;
#84687=CARTESIAN_POINT ( 'NONE',  ( 15.04337798821885208, -2.682774720514427003, -27.31760573472296016 ) ) ;
#84697=CARTESIAN_POINT ( 'NONE',  ( 22.02124265030973760, -7.835183881457444599, 17.60402280011862075 ) ) ;
#84700=ORIENTED_EDGE ( 'NONE', *, *, #32422, .F. ) ;
#84705=CARTESIAN_POINT ( 'NONE',  ( -0.5315124411682757843, -6.376774720514411854, 19.46509473978807847 ) ) ;
#84709=EDGE_CURVE ( 'NONE', #2149, #5650, #44111, .T. ) ;
#84716=DIRECTION ( 'NONE',  ( -0.000000000000000000, 1.000000000000000000, -0.000000000000000000 ) ) ;
#84718=EDGE_CURVE ( 'NONE', #81032, #8388, #45633, .T. ) ;
#84720=DIRECTION ( 'NONE',  ( -0.000000000000000000, 1.000000000000000000, -0.000000000000000000 ) ) ;
#84743=VERTEX_POINT ( 'NONE', #21768 ) ;
#84744=CIRCLE ( 'NONE', #3716, 3.349999999999998757 ) ;
#84747=CARTESIAN_POINT ( 'NONE',  ( 3.769931535195356620, -5.876774720514428729, 21.83933825178638699 ) ) ;
#84757=DIRECTION ( 'NONE',  ( 0.000000000000000000, 0.000000000000000000, 1.000000000000000000 ) ) ;
#84760=ADVANCED_FACE ( 'NONE', ( #97899 ), #46598, .T. ) ;
#84770=ORIENTED_EDGE ( 'NONE', *, *, #32938, .F. ) ;
#84774=LINE ( 'NONE', #92384, #75720 ) ;
#84781=CARTESIAN_POINT ( 'NONE',  ( 31.62401270459618630, -4.290926300276496796, 26.86768354919275836 ) ) ;
#84782=AXIS2_PLACEMENT_3D ( 'NONE', #20557, #90082, #66269 ) ;
#84800=ORIENTED_EDGE ( 'NONE', *, *, #67017, .T. ) ;
#84809=CARTESIAN_POINT ( 'NONE',  ( -28.84663072490566194, 5.965225279485572685, 28.73989617533406715 ) ) ;
#84810=AXIS2_PLACEMENT_3D ( 'NONE', #42797, #20926, #82827 ) ;
#84830=ADVANCED_FACE ( 'NONE', ( #14162 ), #76553, .F. ) ;
#84832=CARTESIAN_POINT ( 'NONE',  ( 4.712727796232553779, -3.316774720514426456, -25.55789472434992859 ) ) ;
#84845=DIRECTION ( 'NONE',  ( 0.000000000000000000, 0.000000000000000000, -1.000000000000000000 ) ) ;
#84851=DIRECTION ( 'NONE',  ( 1.334402673828313339E-16, 0.000000000000000000, -1.000000000000000000 ) ) ;
#84866=CARTESIAN_POINT ( 'NONE',  ( 0.3180806761505774460, -6.376774720514415407, 20.02963804100705403 ) ) ;
#84870=ORIENTED_EDGE ( 'NONE', *, *, #27114, .F. ) ;
#84887=VERTEX_POINT ( 'NONE', #83175 ) ;
#84891=CARTESIAN_POINT ( 'NONE',  ( -7.567681410454951241, -6.376774720514411854, 19.71630089903357330 ) ) ;
#84896=CARTESIAN_POINT ( 'NONE',  ( -0.5218785734906133955, -6.376774720514408301, 19.14848118821636547 ) ) ;
#84898=CARTESIAN_POINT ( 'NONE',  ( 7.480769230769231726, -5.876774720514430506, 20.77403846153845635 ) ) ;
#84903=ORIENTED_EDGE ( 'NONE', *, *, #48534, .F. ) ;
#84904=PLANE ( 'NONE',  #30260 ) ;
#84909=DIRECTION ( 'NONE',  ( 0.7512896232465892110, 0.000000000000000000, 0.6599726524652350657 ) ) ;
#84917=CARTESIAN_POINT ( 'NONE',  ( 14.52511747680497933, 5.965225279485572685, -27.86035006098926559 ) ) ;
#84918=ORIENTED_EDGE ( 'NONE', *, *, #32938, .T. ) ;
#84923=EDGE_CURVE ( 'NONE', #21553, #57117, #72529, .T. ) ;
#84932=CARTESIAN_POINT ( 'NONE',  ( -20.27875734969026311, -7.835183881457444599, 25.40402280011862146 ) ) ;
#84940=CARTESIAN_POINT ( 'NONE',  ( 5.641025641025643189, -5.876774720514419847, 20.78665865384615330 ) ) ;
#84946=CARTESIAN_POINT ( 'NONE',  ( -28.98875734969026041, 5.965225279485572685, 26.43402280011862615 ) ) ;
#84950=CARTESIAN_POINT ( 'NONE',  ( -5.576923076923074873, -6.376774720514427841, 21.75000000000000711 ) ) ;
#84967=CARTESIAN_POINT ( 'NONE',  ( 0.3545156366401029935, -6.376774720514413630, 20.17598923696321478 ) ) ;
#84982=CARTESIAN_POINT ( 'NONE',  ( 4.403244164709623654, -6.376774720514404748, 18.35516266052912826 ) ) ;
#84986=ORIENTED_EDGE ( 'NONE', *, *, #72694, .T. ) ;
#84987=ORIENTED_EDGE ( 'NONE', *, *, #61154, .F. ) ;
#84990=CARTESIAN_POINT ( 'NONE',  ( -4.533825836049095059, -6.376774720514411854, 19.59623724171353132 ) ) ;
#84993=ORIENTED_EDGE ( 'NONE', *, *, #6847, .T. ) ;
#84996=DIRECTION ( 'NONE',  ( 0.000000000000000000, 1.478457507934778393E-16, -1.000000000000000000 ) ) ;
#85005=DIRECTION ( 'NONE',  ( 0.000000000000000000, 0.000000000000000000, -1.000000000000000000 ) ) ;
#85006=ORIENTED_EDGE ( 'NONE', *, *, #27621, .T. ) ;
#85012=CARTESIAN_POINT ( 'NONE',  ( 6.948977015814011615, -5.356774720514426491, -25.20533573604597066 ) ) ;
#85019=ORIENTED_EDGE ( 'NONE', *, *, #53378, .T. ) ;
#85026=LINE ( 'NONE', #30747, #75806 ) ;
#85030=LINE ( 'NONE', #45989, #21381 ) ;
#85034=EDGE_LOOP ( 'NONE', ( #23939, #863, #1146, #77628 ) ) ;
#85037=CARTESIAN_POINT ( 'NONE',  ( -4.495793269230770939, -5.876774720514410077, 19.27714342948718595 ) ) ;
#85045=CARTESIAN_POINT ( 'NONE',  ( -5.706951327759631099, -5.876774720514412742, 19.48569229636961353 ) ) ;
#85046=EDGE_CURVE ( 'NONE', #97326, #45914, #43416, .T. ) ;
#85053=CIRCLE ( 'NONE', #16966, 0.3000000000000016542 ) ;
#85076=CARTESIAN_POINT ( 'NONE',  ( 2.880689065218799083, -6.376774720514426065, 21.31732089891691828 ) ) ;
#85080=DIRECTION ( 'NONE',  ( 0.000000000000000000, 0.000000000000000000, -1.000000000000000000 ) ) ;
#85092=CARTESIAN_POINT ( 'NONE',  ( 4.639502537026700679, -5.876774720514415407, 19.60647575951318800 ) ) ;
#85095=CIRCLE ( 'NONE', #78570, 4.080000000000000071 ) ;
#85097=ORIENTED_EDGE ( 'NONE', *, *, #31061, .T. ) ;
#85107=DIRECTION ( 'NONE',  ( 0.000000000000000000, 0.000000000000000000, 1.000000000000000000 ) ) ;
#85111=EDGE_LOOP ( 'NONE', ( #46988, #9745, #92096, #51598 ) ) ;
#85113=ORIENTED_EDGE ( 'NONE', *, *, #69722, .T. ) ;
#85115=DIRECTION ( 'NONE',  ( 0.000000000000000000, 0.000000000000000000, -1.000000000000000000 ) ) ;
#85124=ORIENTED_EDGE ( 'NONE', *, *, #77143, .T. ) ;
#85135=ORIENTED_EDGE ( 'NONE', *, *, #1726, .F. ) ;
#85137=CARTESIAN_POINT ( 'NONE',  ( 4.642799911345256270, -5.876774720514406525, 18.59646607068888713 ) ) ;
#85142=CARTESIAN_POINT ( 'NONE',  ( 6.044871794871792048, -6.376774720514401196, 18.16025641025640880 ) ) ;
#85144=CIRCLE ( 'NONE', #55979, 0.3000000000000016542 ) ;
#85147=ORIENTED_EDGE ( 'NONE', *, *, #53378, .F. ) ;
#85148=ORIENTED_EDGE ( 'NONE', *, *, #34486, .F. ) ;
#85163=PLANE ( 'NONE',  #7892 ) ;
#85170=DIRECTION ( 'NONE',  ( 1.000000000000000000, -0.000000000000000000, 2.417950247244706201E-16 ) ) ;
#85173=AXIS2_PLACEMENT_3D ( 'NONE', #58036, #50911, #65162 ) ;
#85181=ADVANCED_FACE ( 'NONE', ( #53633 ), #100257, .F. ) ;
#85201=CARTESIAN_POINT ( 'NONE',  ( -1.044871794871790938, -6.376774720514427841, 21.75000000000000355 ) ) ;
#85208=VECTOR ( 'NONE', #26665, 1000.000000000000000 ) ;
#85224=ADVANCED_FACE ( 'NONE', ( #826 ), #85557, .T. ) ;
#85246=DIRECTION ( 'NONE',  ( 0.7071067811865507924, 0.000000000000000000, 0.7071067811865442421 ) ) ;
#85252=B_SPLINE_CURVE_WITH_KNOTS ( 'NONE', 3,
 ( #87421, #48877, #57498, #79804, #80818, #55995, #1701, #11301, #10301, #33136 ),
 .UNSPECIFIED., .F., .F.,
 ( 4, 2, 2, 2, 4 ),
 ( 0.000000000000000000, 0.0004823517777971119314, 0.0009647035555942238627, 0.001447055333391335848, 0.001929407111188447725 ),
 .UNSPECIFIED. ) ;
#85253=CARTESIAN_POINT ( 'NONE',  ( 25.53174711415574194, -4.590565211979967586, -10.98894470817409363 ) ) ;
#85259=CARTESIAN_POINT ( 'NONE',  ( 4.736659488006659480, -5.876774720514420736, 21.25082490164487581 ) ) ;
#85263=AXIS2_PLACEMENT_3D ( 'NONE', #25322, #17209, #71011 ) ;
#85272=CARTESIAN_POINT ( 'NONE',  ( 2.911360383046243783, -6.376774720514417183, 20.24673073119071276 ) ) ;
#85274=CARTESIAN_POINT ( 'NONE',  ( 22.81105451610979173, 6.475225279485573360, -17.31691820600746823 ) ) ;
#85279=FACE_OUTER_BOUND ( 'NONE', #62968, .T. ) ;
#85283=CARTESIAN_POINT ( 'NONE',  ( 31.63284457977613684, -3.861502214243257125, 27.22238481897691287 ) ) ;
#85292=CARTESIAN_POINT ( 'NONE',  ( -5.314757719055156038, -5.876774720514411854, 19.55912026249540858 ) ) ;
#85298=DIRECTION ( 'NONE',  ( 0.06486421869277853025, 0.000000000000000000, -0.9978940991575085961 ) ) ;
#85299=PLANE ( 'NONE',  #78742 ) ;
#85337=VECTOR ( 'NONE', #76884, 1000.000000000000000 ) ;
#85339=EDGE_CURVE ( 'NONE', #881, #25949, #65263, .T. ) ;
#85341=AXIS2_PLACEMENT_3D ( 'NONE', #33414, #18197, #97319 ) ;
#85350=B_SPLINE_CURVE_WITH_KNOTS ( 'NONE', 3,
 ( #3412, #88635, #90124, #19106, #50077, #27729, #89626, #81018, #27235, #42965, #73901, #45460, #13983, #21590, #60687, #91114, #98724, #67805, #22576 ),
 .UNSPECIFIED., .F., .F.,
 ( 4, 1, 1, 1, 1, 1, 1, 1, 1, 1, 1, 1, 1, 1, 1, 1, 4 ),
 ( 0.000000000000000000, 0.08252970382206505084, 0.1587788549175693509, 0.2277380621151788020, 0.2899456527966750574, 0.3454988386981356352, 0.3938963373401225820, 0.4363737851900879039, 0.4721222744615228839, 0.5363836155048278265, 0.5990779017254967975, 0.6619482340244574603, 0.7263105423531552862, 0.7917711030502098124, 0.8586473037978579192, 0.9273053338076842067, 1.000000000000000000 ),
 .UNSPECIFIED. ) ;
#85355=CARTESIAN_POINT ( 'NONE',  ( -5.850750514176234596, -6.376774720514411854, 19.74039977944280366 ) ) ;
#85366=ORIENTED_EDGE ( 'NONE', *, *, #33751, .T. ) ;
#85368=CIRCLE ( 'NONE', #7592, 84.48086791635432746 ) ;
#85374=CARTESIAN_POINT ( 'NONE',  ( 33.00535138976593430, -3.570691370340898452, -12.97242311383974744 ) ) ;
#85391=CARTESIAN_POINT ( 'NONE',  ( 6.403846153846157740, -5.876774720514425177, 21.48076923076922995 ) ) ;
#85394=CARTESIAN_POINT ( 'NONE',  ( 7.234974673537251100, -5.876774720514416295, 19.99114326857715795 ) ) ;
#85403=DIRECTION ( 'NONE',  ( -0.000000000000000000, 1.000000000000000000, -0.000000000000000000 ) ) ;
#85418=EDGE_CURVE ( 'NONE', #75788, #77715, #71350, .T. ) ;
#85419=ORIENTED_EDGE ( 'NONE', *, *, #65393, .F. ) ;
#85420=CARTESIAN_POINT ( 'NONE',  ( 3.325015365150250535, -5.876774720514403860, 18.26971317031913955 ) ) ;
#85421=LINE ( 'NONE', #70207, #90319 ) ;
#85435=DIRECTION ( 'NONE',  ( 0.000000000000000000, 0.000000000000000000, -1.000000000000000000 ) ) ;
#85436=B_SPLINE_CURVE_WITH_KNOTS ( 'NONE', 3,
 ( #11541, #17157, #71963, #41504, #34389, #88679, #48123, #79052, #1949, #2444, #49131, #80058, #81564, #98764, #66357, #67844, #27279, #74922, #83035 ),
 .UNSPECIFIED., .F., .F.,
 ( 4, 1, 1, 1, 1, 1, 1, 1, 1, 1, 1, 1, 1, 1, 1, 1, 4 ),
 ( 0.000000000000000000, 0.08252970382206502309, 0.1587788549175692676, 0.2277380621151786910, 0.2899456527966748909, 0.3454988386981381332, 0.3938963373401223600, 0.4363737851900878484, 0.4721222744615228284, 0.5363836155048271603, 0.5990779017254961314, 0.6619482340244576823, 0.7263105423531555083, 0.7917711030502102565, 0.8586473037978576972, 0.9273053338076845398, 1.000000000000000000 ),
 .UNSPECIFIED. ) ;
#85443=VECTOR ( 'NONE', #659, 1000.000000000000000 ) ;
#85445=EDGE_CURVE ( 'NONE', #38147, #79658, #79950, .T. ) ;
#85447=CARTESIAN_POINT ( 'NONE',  ( 5.271800844967073907, -3.316774720514426456, -28.56638892015272191 ) ) ;
#85463=ORIENTED_EDGE ( 'NONE', *, *, #60245, .T. ) ;
#85475=VECTOR ( 'NONE', #13603, 1000.000000000000000 ) ;
#85478=ORIENTED_EDGE ( 'NONE', *, *, #82988, .T. ) ;
#85488=CARTESIAN_POINT ( 'NONE',  ( -4.440151687742864617, -6.376774720514411854, 19.67013632031035897 ) ) ;
#85490=ORIENTED_EDGE ( 'NONE', *, *, #66977, .T. ) ;
#85492=EDGE_CURVE ( 'NONE', #10968, #34973, #25664, .T. ) ;
#85496=EDGE_CURVE ( 'NONE', #17186, #65082, #10946, .T. ) ;
#85501=DIRECTION ( 'NONE',  ( 0.000000000000000000, 0.000000000000000000, 1.000000000000000000 ) ) ;
#85505=CARTESIAN_POINT ( 'NONE',  ( 4.127614219445591814, -6.376774720514408301, 18.60403502951120558 ) ) ;
#85513=CARTESIAN_POINT ( 'NONE',  ( 4.784292611721462585, -5.356774720514426491, -25.54547254883130947 ) ) ;
#85529=ADVANCED_FACE ( 'NONE', ( #72352 ), #100073, .F. ) ;
#85533=ORIENTED_EDGE ( 'NONE', *, *, #26355, .T. ) ;
#85534=LINE ( 'NONE', #16018, #19559 ) ;
#85557=CYLINDRICAL_SURFACE ( 'NONE', #80709, 28.45799999999999486 ) ;
#85561=DIRECTION ( 'NONE',  ( -0.000000000000000000, -1.000000000000000000, -0.000000000000000000 ) ) ;
#85563=CARTESIAN_POINT ( 'NONE',  ( 4.959895098850171102, -5.876774720514411854, 19.67755022954121813 ) ) ;
#85571=ADVANCED_FACE ( 'NONE', ( #97179 ), #66165, .F. ) ;
#85580=EDGE_CURVE ( 'NONE', #82409, #47215, #74339, .T. ) ;
#85581=ORIENTED_EDGE ( 'NONE', *, *, #41367, .T. ) ;
#85585=CARTESIAN_POINT ( 'NONE',  ( 14.99708669145757511, -3.499965418336752343, -27.33093470766933564 ) ) ;
#85593=CARTESIAN_POINT ( 'NONE',  ( -5.205649524681222218, -6.376774720514406525, 19.16400979764067714 ) ) ;
#85603=DIRECTION ( 'NONE',  ( -1.000000000000000000, 0.000000000000000000, 0.000000000000000000 ) ) ;
#85612=EDGE_LOOP ( 'NONE', ( #77028, #35476, #17856, #90608 ) ) ;
#85619=ADVANCED_FACE ( 'NONE', ( #90557 ), #66754, .F. ) ;
#85630=EDGE_CURVE ( 'NONE', #57287, #40266, #5820, .T. ) ;
#85634=DIRECTION ( 'NONE',  ( 0.000000000000000000, 0.000000000000000000, 1.000000000000000000 ) ) ;
#85641=B_SPLINE_CURVE_WITH_KNOTS ( 'NONE', 3,
 ( #73752, #97091, #67655, #4251, #43316, #13834 ),
 .UNSPECIFIED., .F., .F.,
 ( 4, 2, 4 ),
 ( 0.004212217532641997220, 0.005885052055372064564, 0.007557886578102131908 ),
 .UNSPECIFIED. ) ;
#85650=DIRECTION ( 'NONE',  ( 1.000000000000000000, 0.000000000000000000, 0.000000000000000000 ) ) ;
#85659=ADVANCED_FACE ( 'NONE', ( #98659 ), #52506, .T. ) ;
#85676=CARTESIAN_POINT ( 'NONE',  ( 13.91401389203221406, -6.376774720514426953, 158.0376437107427137 ) ) ;
#85677=CARTESIAN_POINT ( 'NONE',  ( 15.92621150404962016, 6.475225279485573360, -27.29681269571041824 ) ) ;
#85679=EDGE_CURVE ( 'NONE', #75373, #60109, #83953, .T. ) ;
#85694=CARTESIAN_POINT ( 'NONE',  ( -3.826923076923074429, -6.376774720514427841, 21.75000000000000355 ) ) ;
#85697=CARTESIAN_POINT ( 'NONE',  ( -5.988734693054777125, -6.376774720514415407, 19.95737465391042065 ) ) ;
#85708=DIRECTION ( 'NONE',  ( -0.000000000000000000, 1.000000000000000000, -0.000000000000000000 ) ) ;
#85716=CARTESIAN_POINT ( 'NONE',  ( -0.9078848932494473223, -6.376774720514411854, 19.67454710845354171 ) ) ;
#85719=ORIENTED_EDGE ( 'NONE', *, *, #20805, .T. ) ;
#85726=CARTESIAN_POINT ( 'NONE',  ( -24.97666371003640506, -0.3587747205143964613, -15.72894043976419454 ) ) ;
#85743=EDGE_CURVE ( 'NONE', #36332, #18512, #23970, .T. ) ;
#85752=CARTESIAN_POINT ( 'NONE',  ( -4.886549725601808447, -5.876774720514410077, 19.15251819062245175 ) ) ;
#85766=VECTOR ( 'NONE', #81773, 999.9999999999998863 ) ;
#85769=CARTESIAN_POINT ( 'NONE',  ( 3.797776442307698286, -5.876774720514427841, 21.83974358974358410 ) ) ;
#85773=CIRCLE ( 'NONE', #72829, 252.4458649670781085 ) ;
#85781=ORIENTED_EDGE ( 'NONE', *, *, #24326, .F. ) ;
#85789=ORIENTED_EDGE ( 'NONE', *, *, #11656, .T. ) ;
#85790=LINE ( 'NONE', #62969, #51655 ) ;
#85794=CARTESIAN_POINT ( 'NONE',  ( 29.61860529676591369, -5.187414344753652706, 28.58826086137218780 ) ) ;
#85810=CARTESIAN_POINT ( 'NONE',  ( 32.98733314340959311, 5.965225279485572685, 2.074222136288530027 ) ) ;
#85811=CARTESIAN_POINT ( 'NONE',  ( 14.75122623597949101, -4.701663563191170070, -27.79036425924725151 ) ) ;
#85814=CARTESIAN_POINT ( 'NONE',  ( 31.64143112576189765, 5.965225279485572685, 14.03360796525321774 ) ) ;
#85816=DIRECTION ( 'NONE',  ( 0.000000000000000000, 0.000000000000000000, 1.000000000000000000 ) ) ;
#85818=ORIENTED_EDGE ( 'NONE', *, *, #65393, .T. ) ;
#85820=CIRCLE ( 'NONE', #95596, 15.00000000000000178 ) ;
#85825=CARTESIAN_POINT ( 'NONE',  ( -4.568292318365942073, -0.3587747205144265483, 30.06720597538392425 ) ) ;
#85826=CARTESIAN_POINT ( 'NONE',  ( 32.29806486058159010, -4.575840390334028562, -4.131869215359018632 ) ) ;
#85827=CARTESIAN_POINT ( 'NONE',  ( 6.371704462700114924, -6.376774720514427841, 21.83798798526824214 ) ) ;
#85833=CARTESIAN_POINT ( 'NONE',  ( 31.55507366846311967, -4.132774720514426292, -2.076992067079099336 ) ) ;
#85835=AXIS2_PLACEMENT_3D ( 'NONE', #1801, #21734, #32738 ) ;
#85841=VECTOR ( 'NONE', #73266, 1000.000000000000000 ) ;
#85851=PLANE ( 'NONE',  #40435 ) ;
#85852=ADVANCED_FACE ( 'NONE', ( #10819 ), #76085, .T. ) ;
#85856=LINE ( 'NONE', #62523, #29110 ) ;
#85875=DIRECTION ( 'NONE',  ( -1.000000000000000000, 0.000000000000000000, 0.000000000000000000 ) ) ;
#85878=EDGE_LOOP ( 'NONE', ( #11703, #22941, #36831, #46069, #100101, #53573, #19129 ) ) ;
#85884=ORIENTED_EDGE ( 'NONE', *, *, #20439, .T. ) ;
#85885=CARTESIAN_POINT ( 'NONE',  ( 32.18888049830260911, -5.126885235861809775, -11.87322522691203908 ) ) ;
#85888=VECTOR ( 'NONE', #66806, 1000.000000000000000 ) ;
#85903=DIRECTION ( 'NONE',  ( 0.000000000000000000, 0.000000000000000000, 1.000000000000000000 ) ) ;
#85918=CARTESIAN_POINT ( 'NONE',  ( 16.15056352287345121, -3.622774720514426949, -27.77856273171767398 ) ) ;
#85925=AXIS2_PLACEMENT_3D ( 'NONE', #81079, #51127, #96303 ) ;
#85933=PLANE ( 'NONE',  #60719 ) ;
#85945=CARTESIAN_POINT ( 'NONE',  ( 3.787259615384621192, -6.376774720514426065, 21.48076923076922640 ) ) ;
#85954=CARTESIAN_POINT ( 'NONE',  ( 0.3376760108279234784, -5.876774720514417183, 20.09898898868105732 ) ) ;
#85959=B_SPLINE_CURVE_WITH_KNOTS ( 'NONE', 3,
 ( #37150, #99529, #58511, #50893, #74705, #54889, #77691, #61997, #24424, #14799, #100020, #62497, #92925, #85827, #55389 ),
 .UNSPECIFIED., .F., .F.,
 ( 4, 1, 1, 1, 1, 1, 1, 1, 1, 1, 1, 1, 4 ),
 ( 0.000000000000000000, 0.08594794314412859682, 0.1691252118806910454, 0.2503991071860492412, 0.3322897361388358339, 0.4133642879158805905, 0.4941722833711898466, 0.5760217353866382561, 0.6607569692540066209, 0.7457831259137440716, 0.8300435929752246755, 0.9140275458206831294, 1.000000000000000000 ),
 .UNSPECIFIED. ) ;
#85965=CARTESIAN_POINT ( 'NONE',  ( 27.86270917940689174, 5.965225279485572685, 29.49402280011862487 ) ) ;
#85975=AXIS2_PLACEMENT_3D ( 'NONE', #62478, #54367, #39125 ) ;
#85983=EDGE_CURVE ( 'NONE', #90358, #67210, #4210, .T. ) ;
#85987=DIRECTION ( 'NONE',  ( 0.000000000000000000, 0.000000000000000000, -1.000000000000000000 ) ) ;
#86007=CARTESIAN_POINT ( 'NONE',  ( -3.108974358974355923, -6.376774720514427841, 21.75000000000001066 ) ) ;
#86009=EDGE_LOOP ( 'NONE', ( #75027, #80529, #18455, #80022 ) ) ;
#86012=VERTEX_POINT ( 'NONE', #58507 ) ;
#86016=CARTESIAN_POINT ( 'NONE',  ( 22.81105451610979173, -1.682774720514426114, -18.46691820600746681 ) ) ;
#86018=CARTESIAN_POINT ( 'NONE',  ( 10.22011794243639038, -5.356774720516090937, -27.02313658038265132 ) ) ;
#86026=DIRECTION ( 'NONE',  ( 0.000000000000000000, 0.000000000000000000, -1.000000000000000000 ) ) ;
#86027=VERTEX_POINT ( 'NONE', #19920 ) ;
#86029=LINE ( 'NONE', #79413, #52252 ) ;
#86033=CARTESIAN_POINT ( 'NONE',  ( -24.90875734969025501, 6.475225279485573360, 30.00402280011862288 ) ) ;
#86039=CARTESIAN_POINT ( 'NONE',  ( 32.45853543194704116, 5.965225279485572685, 9.169203677920338080 ) ) ;
#86041=B_SPLINE_CURVE_WITH_KNOTS ( 'NONE', 3,
 ( #75973, #15085, #6482, #85593, #61778, #98818, #67895, #37927, #77964, #23186, #45552, #37433, #53167, #92205, #68383 ),
 .UNSPECIFIED., .F., .F.,
 ( 4, 1, 1, 1, 1, 1, 1, 1, 1, 1, 1, 1, 4 ),
 ( 0.000000000000000000, 0.08415201884431650070, 0.1665323202984589912, 0.2488363311465309202, 0.3312461454872611122, 0.4129571090216161422, 0.4904942776695665474, 0.5661557919819242279, 0.6399873346864671797, 0.7167654882718511589, 0.8021439047100994424, 0.8958332007101933447, 1.000000000000000000 ),
 .UNSPECIFIED. ) ;
#86043=VERTEX_POINT ( 'NONE', #5199 ) ;
#86051=CARTESIAN_POINT ( 'NONE',  ( -5.530932042872791499, -5.876774720514408301, 19.30497968945844534 ) ) ;
#86063=CARTESIAN_POINT ( 'NONE',  ( -2.702089344534958304, -5.876774720514413630, 19.72789237585158162 ) ) ;
#86069=ORIENTED_EDGE ( 'NONE', *, *, #75680, .T. ) ;
#86080=CARTESIAN_POINT ( 'NONE',  ( 3.902919446070569176, -6.376774720514427841, 21.47497695444087284 ) ) ;
#86092=DIRECTION ( 'NONE',  ( 2.168404344971008868E-16, 0.000000000000000000, 1.000000000000000000 ) ) ;
#86098=DIRECTION ( 'NONE',  ( 0.000000000000000000, -1.000000000000000000, 0.000000000000000000 ) ) ;
#86109=ORIENTED_EDGE ( 'NONE', *, *, #25925, .T. ) ;
#86115=ORIENTED_EDGE ( 'NONE', *, *, #3322, .F. ) ;
#86124=LINE ( 'NONE', #38945, #5612 ) ;
#86128=CARTESIAN_POINT ( 'NONE',  ( 4.518205171808153509, -6.376774720514406525, 19.05004583296150500 ) ) ;
#86134=ORIENTED_EDGE ( 'NONE', *, *, #28593, .F. ) ;
#86141=ORIENTED_EDGE ( 'NONE', *, *, #76602, .F. ) ;
#86155=CARTESIAN_POINT ( 'NONE',  ( 26.73860345374794178, 1.477225279485574028, 19.84760796525321425 ) ) ;
#86165=DIRECTION ( 'NONE',  ( 0.000000000000000000, -1.000000000000000000, 0.000000000000000000 ) ) ;
#86172=CYLINDRICAL_SURFACE ( 'NONE', #2590, 129.7684398600581517 ) ;
#86186=DIRECTION ( 'NONE',  ( -0.000000000000000000, -1.000000000000000000, -0.000000000000000000 ) ) ;
#86197=EDGE_CURVE ( 'NONE', #10968, #57696, #92425, .T. ) ;
#86200=EDGE_CURVE ( 'NONE', #27315, #95233, #83819, .T. ) ;
#86208=CARTESIAN_POINT ( 'NONE',  ( 5.184553252003285984, 6.475225279485573360, -28.06387035751381731 ) ) ;
#86213=CARTESIAN_POINT ( 'NONE',  ( 10.54059822343757880, -5.876774720514426953, 23.12308057603841149 ) ) ;
#86217=LINE ( 'NONE', #61894, #71095 ) ;
#86237=CARTESIAN_POINT ( 'NONE',  ( -1.438454482798693146, -5.876774720514409189, 19.55848054040323092 ) ) ;
#86254=CARTESIAN_POINT ( 'NONE',  ( -5.023036858974361252, -5.876774720514410077, 19.14743589743590846 ) ) ;
#86256=ORIENTED_EDGE ( 'NONE', *, *, #88764, .F. ) ;
#86258=EDGE_LOOP ( 'NONE', ( #6514, #33490, #38283, #1267, #78605, #89753, #16700, #3885 ) ) ;
#86262=CARTESIAN_POINT ( 'NONE',  ( 25.03841014571435508, -5.082747618816810586, -9.367571460246121973 ) ) ;
#86266=CARTESIAN_POINT ( 'NONE',  ( 30.32108885906865936, -4.540774720514427543, 3.274824222184972822 ) ) ;
#86268=CARTESIAN_POINT ( 'NONE',  ( 4.332134589405623792, -5.876774720514426953, 21.69242924468134959 ) ) ;
#86271=ORIENTED_EDGE ( 'NONE', *, *, #28014, .T. ) ;
#86296=CARTESIAN_POINT ( 'NONE',  ( -5.568927889719891944, -5.876774720514417183, 20.14881673916291760 ) ) ;
#86300=DIRECTION ( 'NONE',  ( 1.000000000000000000, 0.000000000000000000, -2.504262461560503878E-15 ) ) ;
#86304=CARTESIAN_POINT ( 'NONE',  ( 2.905472630834636139, -6.376774720514415407, 19.87563926270137671 ) ) ;
#86315=DIRECTION ( 'NONE',  ( -0.000000000000000000, 0.000000000000000000, -1.000000000000000000 ) ) ;
#86328=CARTESIAN_POINT ( 'NONE',  ( -1.967852706420949005, -5.876774720514409189, 19.18381548539530357 ) ) ;
#86337=AXIS2_PLACEMENT_3D ( 'NONE', #69349, #64136, #76941 ) ;
#86346=EDGE_CURVE ( 'NONE', #95277, #8989, #96994, .T. ) ;
#86347=CARTESIAN_POINT ( 'NONE',  ( -19.80875734969026425, 5.965225279485572685, 30.51402280011862089 ) ) ;
#86350=ORIENTED_EDGE ( 'NONE', *, *, #66405, .T. ) ;
#86355=ADVANCED_FACE ( 'NONE', ( #19675 ), #56776, .F. ) ;
#86363=CARTESIAN_POINT ( 'NONE',  ( 7.164812103570541879, -5.876774720514421624, 20.85668272347560404 ) ) ;
#86368=CARTESIAN_POINT ( 'NONE',  ( -23.29179552176161749, 5.965225279485594001, -17.29637630388738501 ) ) ;
#86373=CARTESIAN_POINT ( 'NONE',  ( 7.165897526731081157, -5.876774720514419847, 20.76279523443833597 ) ) ;
#86374=FACE_OUTER_BOUND ( 'NONE', #8655, .T. ) ;
#86416=DIRECTION ( 'NONE',  ( -0.000000000000000000, -1.000000000000000000, -0.000000000000000000 ) ) ;
#86420=ORIENTED_EDGE ( 'NONE', *, *, #36592, .F. ) ;
#86423=PLANE ( 'NONE',  #64938 ) ;
#86441=CARTESIAN_POINT ( 'NONE',  ( 3.557932825399831689, -6.376774720514429617, 21.44518044978141091 ) ) ;
#86444=LINE ( 'NONE', #9308, #41855 ) ;
#86453=CARTESIAN_POINT ( 'NONE',  ( -0.001774553997815280816, -5.876774720514414518, 19.59623724171353487 ) ) ;
#86456=LINE ( 'NONE', #93057, #57300 ) ;
#86458=CARTESIAN_POINT ( 'NONE',  ( 0.000000000000000000, -4.056774720514426669, 0.000000000000000000 ) ) ;
#86470=ORIENTED_EDGE ( 'NONE', *, *, #16424, .F. ) ;
#86473=CARTESIAN_POINT ( 'NONE',  ( -13.89275734969026388, -0.3587747205144262708, 30.51402280011862089 ) ) ;
#86486=FACE_BOUND ( 'NONE', #86702, .T. ) ;
#86488=CARTESIAN_POINT ( 'NONE',  ( 2.677564053859940341, -6.376774720514406525, 19.16116138973293559 ) ) ;
#86494=CARTESIAN_POINT ( 'NONE',  ( -4.177535645411178500, -5.876774720514415407, 20.17598923696320767 ) ) ;
#86499=PLANE ( 'NONE',  #74204 ) ;
#86503=ORIENTED_EDGE ( 'NONE', *, *, #26743, .T. ) ;
#86509=ORIENTED_EDGE ( 'NONE', *, *, #58112, .T. ) ;
#86515=DIRECTION ( 'NONE',  ( -0.000000000000000000, 1.000000000000000000, -0.000000000000000000 ) ) ;
#86516=CARTESIAN_POINT ( 'NONE',  ( 5.101312121039179637, -3.305285905532577839, -27.56070534847060571 ) ) ;
#86517=CARTESIAN_POINT ( 'NONE',  ( 10.77631500667670572, -5.356774720514423827, -24.99100794736120434 ) ) ;
#86518=PLANE ( 'NONE',  #42054 ) ;
#86532=VECTOR ( 'NONE', #60674, 1000.000000000000000 ) ;
#86534=CARTESIAN_POINT ( 'NONE',  ( 31.27821779315964790, -4.116118814799345493, -3.972734673865978117 ) ) ;
#86542=ORIENTED_EDGE ( 'NONE', *, *, #46224, .F. ) ;
#86548=EDGE_CURVE ( 'NONE', #46432, #11836, #13560, .T. ) ;
#86552=DIRECTION ( 'NONE',  ( -0.000000000000000000, -1.000000000000000000, -0.000000000000000000 ) ) ;
#86563=CARTESIAN_POINT ( 'NONE',  ( 5.271800844963591359, -3.316774720514426456, -28.56638892015329034 ) ) ;
#86566=CARTESIAN_POINT ( 'NONE',  ( 15.14080536460164517, -5.152774720514427642, -26.62908960815038384 ) ) ;
#86569=LINE ( 'NONE', #48020, #99048 ) ;
#86571=LINE ( 'NONE', #24166, #798 ) ;
#86578=CARTESIAN_POINT ( 'NONE',  ( 2.627412086454235851, -5.876774720514420736, 20.59155478446653831 ) ) ;
#86588=CARTESIAN_POINT ( 'NONE',  ( 15.13694198098060717, -3.544954394834232581, -27.27417057618865570 ) ) ;
#86593=EDGE_CURVE ( 'NONE', #36415, #25694, #45037, .T. ) ;
#86597=CARTESIAN_POINT ( 'NONE',  ( 4.214857194124448370, -5.876774720514402972, 18.65898740197609840 ) ) ;
#86601=ORIENTED_EDGE ( 'NONE', *, *, #71716, .F. ) ;
#86606=B_SPLINE_CURVE_WITH_KNOTS ( 'NONE', 3,
 ( #90985, #52434, #44825, #75746, #6246, #1142, #84366, #7237, #8753, #55435, #84866, #93470, #93977, #61553, #24469, #8251, #22452, #53437, #7744 ),
 .UNSPECIFIED., .F., .F.,
 ( 4, 1, 1, 1, 1, 1, 1, 1, 1, 1, 1, 1, 1, 1, 1, 1, 4 ),
 ( 0.000000000000000000, 0.06867706841303485021, 0.1368709585090958636, 0.2061143571452989376, 0.2775381819697280150, 0.3497719775548984722, 0.4212508361555684644, 0.4929107569233693309, 0.5670265889927383895, 0.6066141532413351634, 0.6497039535189884640, 0.6973031504846843864, 0.7490856597091365421, 0.8048806474593092064, 0.8654850057023351084, 0.9302371271531362229, 1.000000000000000000 ),
 .UNSPECIFIED. ) ;
#86617=ORIENTED_EDGE ( 'NONE', *, *, #13901, .T. ) ;
#86622=EDGE_CURVE ( 'NONE', #90525, #12265, #15064, .T. ) ;
#86624=CARTESIAN_POINT ( 'NONE',  ( -6.741682653110981249, 5.965225279485572685, 30.62569541381301619 ) ) ;
#86638=ORIENTED_EDGE ( 'NONE', *, *, #99760, .T. ) ;
#86652=ORIENTED_EDGE ( 'NONE', *, *, #66400, .T. ) ;
#86654=LINE ( 'NONE', #11531, #83927 ) ;
#86662=CARTESIAN_POINT ( 'NONE',  ( -6.720452724358975338, -6.376774720514411854, 19.46153846153846700 ) ) ;
#86679=EDGE_CURVE ( 'NONE', #16727, #60162, #8458, .T. ) ;
#86687=CARTESIAN_POINT ( 'NONE',  ( 22.02124265030973760, -5.356774720514425603, 19.55402280011862004 ) ) ;
#86690=EDGE_CURVE ( 'NONE', #6469, #97458, #54642, .T. ) ;
#86702=EDGE_LOOP ( 'NONE', ( #69363, #59950, #24744, #42102 ) ) ;
#86705=CARTESIAN_POINT ( 'NONE',  ( 7.275731542451676859, -6.376774720514415407, 20.06332870126568224 ) ) ;
#86706=( BOUNDED_SURFACE ( )  B_SPLINE_SURFACE ( 3, 2, ( 
 ( #91513, #15381, #30614 ),
 ( #53477, #100100, #6776 ),
 ( #22980, #6283, #75785 ),
 ( #29616, #14385, #40614 ),
 ( #94886, #63467, #77276 ),
 ( #94389, #84404, #53970 ),
 ( #71569, #2062, #55847 ),
 ( #99119, #37731, #24871 ) ),
 .UNSPECIFIED., .F., .F., .F. ) 
 B_SPLINE_SURFACE_WITH_KNOTS ( ( 4, 2, 2, 4 ),
 ( 3, 3 ),
 ( 0.04217399329892001364, 0.04593451325143335651, 0.04781477322769002447, 0.04969503320394669937 ),
 ( 0.000000000000000000, 1.000000000000000000 ),
 .UNSPECIFIED. ) 
 GEOMETRIC_REPRESENTATION_ITEM ( )  RATIONAL_B_SPLINE_SURFACE ( (
 ( 1.000000000000000000, 0.7071067811865475727, 1.000000000000000000),
 ( 1.000000000000000000, 0.7337798844374378016, 1.000000000000000000),
 ( 1.000000000000000000, 0.7590275050786486899, 1.000000000000000000),
 ( 1.000000000000000000, 0.7948576648490734975, 1.000000000000000000),
 ( 1.000000000000000000, 0.8064603411375558251, 1.000000000000000000),
 ( 1.000000000000000000, 0.8289835611541060967, 1.000000000000000000),
 ( 1.000000000000000000, 0.8399042809640585583, 1.000000000000000000),
 ( 1.000000000000000000, 0.8504728678901986028, 1.000000000000000000) ) ) 
 REPRESENTATION_ITEM ( '' )  SURFACE ( )  );
#86711=DIRECTION ( 'NONE',  ( 0.7512896232465891000, 1.109416176496794925E-16, 0.6599726524652351767 ) ) ;
#86721=DIRECTION ( 'NONE',  ( 0.1489078231574191002, 6.845827386180410961E-16, -0.9888510809027407644 ) ) ;
#86734=CARTESIAN_POINT ( 'NONE',  ( -1.595974963000059477, -6.376774720514408301, 19.39236848396478408 ) ) ;
#86736=VERTEX_POINT ( 'NONE', #8955 ) ;
#86744=EDGE_LOOP ( 'NONE', ( #55820, #59813, #88787, #22845, #74672, #81120, #47281, #78256, #45440, #80518, #36156, #35117, #31319, #37349, #21208 ) ) ;
#86754=CARTESIAN_POINT ( 'NONE',  ( 5.271800844963591359, -3.316774720514426456, -28.56638892015329745 ) ) ;
#86755=CARTESIAN_POINT ( 'NONE',  ( 6.044871794871792048, -6.376774720514401196, 18.16025641025640880 ) ) ;
#86758=CARTESIAN_POINT ( 'NONE',  ( 25.42782340596018287, -5.181097800357524541, -8.121040708313532974 ) ) ;
#86759=CARTESIAN_POINT ( 'NONE',  ( 5.090559816868301724, -3.309281602496330521, -27.56260619295190040 ) ) ;
#86771=VERTEX_POINT ( 'NONE', #42431 ) ;
#86782=VERTEX_POINT ( 'NONE', #71369 ) ;
#86785=DIRECTION ( 'NONE',  ( 0.000000000000000000, 0.000000000000000000, 1.000000000000000000 ) ) ;
#86787=CARTESIAN_POINT ( 'NONE',  ( 31.67769140193634314, -4.988134948533209823, 28.98636546410035564 ) ) ;
#86812=AXIS2_PLACEMENT_3D ( 'NONE', #11245, #57940, #94476 ) ;
#86817=ORIENTED_EDGE ( 'NONE', *, *, #70573, .T. ) ;
#86819=CARTESIAN_POINT ( 'NONE',  ( -6.775140224358976226, -5.876774720514409189, 19.14743589743590846 ) ) ;
#86820=ORIENTED_EDGE ( 'NONE', *, *, #99589, .T. ) ;
#86821=LINE ( 'NONE', #45762, #49116 ) ;
#86822=DIRECTION ( 'NONE',  ( 0.000000000000000000, 1.000000000000000000, 0.000000000000000000 ) ) ;
#86823=CARTESIAN_POINT ( 'NONE',  ( -10.24059822343757986, -5.876774720514426953, 22.82308057603840368 ) ) ;
#86836=PLANE ( 'NONE',  #43747 ) ;
#86845=ORIENTED_EDGE ( 'NONE', *, *, #83212, .T. ) ;
#86854=ORIENTED_EDGE ( 'NONE', *, *, #96521, .T. ) ;
#86856=ORIENTED_EDGE ( 'NONE', *, *, #17910, .T. ) ;
#86871=EDGE_CURVE ( 'NONE', #18354, #73552, #2582, .T. ) ;
#86875=EDGE_CURVE ( 'NONE', #34853, #8365, #43420, .T. ) ;
#86877=ADVANCED_FACE ( 'NONE', ( #27690 ), #75338, .F. ) ;
#86896=FACE_OUTER_BOUND ( 'NONE', #21475, .T. ) ;
#86899=VERTEX_POINT ( 'NONE', #82460 ) ;
#86922=VERTEX_POINT ( 'NONE', #35797 ) ;
#86924=CARTESIAN_POINT ( 'NONE',  ( 4.689770114687411784, -6.376774720514424288, 21.33175327469028915 ) ) ;
#86926=CARTESIAN_POINT ( 'NONE',  ( -7.326923076923074873, -5.876774720514426953, 21.75000000000001066 ) ) ;
#86934=AXIS2_PLACEMENT_3D ( 'NONE', #71258, #55544, #78846 ) ;
#86936=CARTESIAN_POINT ( 'NONE',  ( 3.094204744773375815, -5.876774720514421624, 21.02053020447315745 ) ) ;
#86941=VECTOR ( 'NONE', #65440, 1000.000000000000000 ) ;
#86942=CIRCLE ( 'NONE', #44798, 251.4258649670780699 ) ;
#86943=CARTESIAN_POINT ( 'NONE',  ( 6.377880655330028681, -5.876774720514423400, 21.48000012937543346 ) ) ;
#86944=CARTESIAN_POINT ( 'NONE',  ( 31.31283134548411340, -4.772774720514425972, -10.20862453625735178 ) ) ;
#86952=LINE ( 'NONE', #27062, #99374 ) ;
#86961=CARTESIAN_POINT ( 'NONE',  ( 0.000000000000000000, -4.056774720514426669, 0.000000000000000000 ) ) ;
#86962=ORIENTED_EDGE ( 'NONE', *, *, #39920, .T. ) ;
#86964=FACE_OUTER_BOUND ( 'NONE', #19515, .T. ) ;
#86973=AXIS2_PLACEMENT_3D ( 'NONE', #38728, #15891, #45370 ) ;
#86974=CARTESIAN_POINT ( 'NONE',  ( 15.63605935613269438, 5.965225279485572685, -27.55169773172585934 ) ) ;
#86982=ORIENTED_EDGE ( 'NONE', *, *, #53927, .F. ) ;
#86989=LINE ( 'NONE', #33714, #76167 ) ;
#86998=EDGE_CURVE ( 'NONE', #50083, #65105, #67889, .T. ) ;
#87000=EDGE_CURVE ( 'NONE', #70182, #5644, #70234, .T. ) ;
#87007=EDGE_LOOP ( 'NONE', ( #4392, #2554, #16599, #40949 ) ) ;
#87046=AXIS2_PLACEMENT_3D ( 'NONE', #40728, #10278, #1170 ) ;
#87070=FACE_OUTER_BOUND ( 'NONE', #9360, .T. ) ;
#87073=DIRECTION ( 'NONE',  ( -0.000000000000000000, 1.000000000000000000, -0.000000000000000000 ) ) ;
#87075=AXIS2_PLACEMENT_3D ( 'NONE', #81442, #76665, #11921 ) ;
#87093=LINE ( 'NONE', #95211, #99826 ) ;
#87109=CARTESIAN_POINT ( 'NONE',  ( -20.27875734969026311, 6.143225279485574397, 24.00402280011862288 ) ) ;
#87115=VERTEX_POINT ( 'NONE', #33166 ) ;
#87123=CARTESIAN_POINT ( 'NONE',  ( -65.05438548721848235, -3.316774720514426456, 27.45402280011862572 ) ) ;
#87127=CARTESIAN_POINT ( 'NONE',  ( 3.787259615384621192, -5.876774720514405637, 18.51923076923076295 ) ) ;
#87139=B_SPLINE_SURFACE_WITH_KNOTS ( 'NONE', 3, 1, ( 
 ( #35244, #74297 ),
 ( #11402, #51467 ),
 ( #97625, #35744 ),
 ( #50973, #96627 ),
 ( #42376, #82401 ),
 ( #67202, #4789 ),
 ( #28129, #3803 ),
 ( #34741, #5778 ),
 ( #92999, #99112 ),
 ( #84398, #7264 ),
 ( #29608, #14377 ),
 ( #46338, #98618 ),
 ( #36733, #61079 ),
 ( #53469, #69174 ),
 ( #82894, #92503 ) ),
 .UNSPECIFIED., .F., .F., .F.,
 ( 4, 1, 1, 1, 1, 1, 1, 1, 1, 1, 1, 1, 4 ),
 ( 2, 2 ),
 ( 0.000000000000000000, 0.08762222184221857280, 0.1714015232428990343, 0.2501655146837731269, 0.3257011369098756770, 0.3963425794403447888, 0.4627261202239039140, 0.5255277688564403693, 0.5841885094617105256, 0.6947236425220619793, 0.8002739465981734135, 0.9021818103852868864, 1.000000000000000000 ),
 ( 0.000000000000000000, 1.000000000000000000 ),
 .UNSPECIFIED. ) ;
#87141=CARTESIAN_POINT ( 'NONE',  ( -28.98875734969026041, 5.965225279485572685, -0.08597719988137116076 ) ) ;
#87144=CARTESIAN_POINT ( 'NONE',  ( -6.265203266387573855, -5.876774720514408301, 19.29154511076646017 ) ) ;
#87149=VERTEX_POINT ( 'NONE', #72746 ) ;
#87164=CIRCLE ( 'NONE', #61250, 84.48086791635431325 ) ;
#87172=CARTESIAN_POINT ( 'NONE',  ( 13.43165536947796213, -3.316774720514427344, -28.18099828186571187 ) ) ;
#87176=DIRECTION ( 'NONE',  ( 0.000000000000000000, 1.000000000000000000, 0.000000000000000000 ) ) ;
#87180=CARTESIAN_POINT ( 'NONE',  ( 0.000000000000000000, -2.056774720514426669, 0.000000000000000000 ) ) ;
#87189=CARTESIAN_POINT ( 'NONE',  ( 5.963731207934512391, -6.376774720514413630, 19.80418863844947097 ) ) ;
#87192=EDGE_LOOP ( 'NONE', ( #36377, #43292, #568, #4121 ) ) ;
#87193=PLANE ( 'NONE',  #91458 ) ;
#87200=DIRECTION ( 'NONE',  ( 0.000000000000000000, 1.000000000000000000, 0.000000000000000000 ) ) ;
#87206=ORIENTED_EDGE ( 'NONE', *, *, #60330, .T. ) ;
#87210=FACE_OUTER_BOUND ( 'NONE', #54692, .T. ) ;
#87211=CARTESIAN_POINT ( 'NONE',  ( -1.036876607668611117, -6.376774720514417183, 20.14881673916291405 ) ) ;
#87213=ORIENTED_EDGE ( 'NONE', *, *, #14388, .T. ) ;
#87215=VECTOR ( 'NONE', #97672, 1000.000000000000000 ) ;
#87226=CARTESIAN_POINT ( 'NONE',  ( 22.02124265030973760, -6.376774720514428729, 16.20402280011862217 ) ) ;
#87227=CARTESIAN_POINT ( 'NONE',  ( 30.43908124610670285, 1.477225279485574028, -13.86910542224428866 ) ) ;
#87231=VERTEX_POINT ( 'NONE', #87458 ) ;
#87255=PLANE ( 'NONE',  #61737 ) ;
#87257=EDGE_CURVE ( 'NONE', #18015, #53541, #75161, .T. ) ;
#87259=DIRECTION ( 'NONE',  ( 0.000000000000000000, 1.000000000000000000, -0.000000000000000000 ) ) ;
#87264=DIRECTION ( 'NONE',  ( 0.9976052577199501226, 0.000000000000000000, 0.06916465693916179491 ) ) ;
#87265=CARTESIAN_POINT ( 'NONE',  ( 4.465438306463536122, -5.876774720514426065, 21.59631214011467293 ) ) ;
#87268=ORIENTED_EDGE ( 'NONE', *, *, #45236, .T. ) ;
#87273=VERTEX_POINT ( 'NONE', #96861 ) ;
#87293=CARTESIAN_POINT ( 'NONE',  ( 30.09341516180546350, -1.682774720514426114, -11.39311774897855933 ) ) ;
#87297=CARTESIAN_POINT ( 'NONE',  ( -5.382328594919684406, -5.876774720514414518, 19.61227901093090864 ) ) ;
#87299=DIRECTION ( 'NONE',  ( -2.504262461560503878E-15, -0.000000000000000000, -1.000000000000000000 ) ) ;
#87302=CARTESIAN_POINT ( 'NONE',  ( 0.000000000000000000, -4.056774720514426669, -1.399999999999999911 ) ) ;
#87308=ORIENTED_EDGE ( 'NONE', *, *, #56908, .F. ) ;
#87310=DIRECTION ( 'NONE',  ( 0.000000000000000000, 0.000000000000000000, -1.000000000000000000 ) ) ;
#87322=LINE ( 'NONE', #34549, #483 ) ;
#87326=CARTESIAN_POINT ( 'NONE',  ( 10.75273025779354796, -5.876774720514426953, 23.03521261039436752 ) ) ;
#87329=LINE ( 'NONE', #9201, #80725 ) ;
#87340=ORIENTED_EDGE ( 'NONE', *, *, #53927, .T. ) ;
#87344=EDGE_CURVE ( 'NONE', #47463, #73040, #24956, .T. ) ;
#87359=ORIENTED_EDGE ( 'NONE', *, *, #38789, .T. ) ;
#87371=CARTESIAN_POINT ( 'NONE',  ( 5.329826657887789310, -5.876774720514418071, 20.66144943787464783 ) ) ;
#87377=DIRECTION ( 'NONE',  ( -0.000000000000000000, 1.000000000000000000, -0.000000000000000000 ) ) ;
#87386=ORIENTED_EDGE ( 'NONE', *, *, #38154, .F. ) ;
#87393=ORIENTED_EDGE ( 'NONE', *, *, #73723, .F. ) ;
#87421=CARTESIAN_POINT ( 'NONE',  ( 31.60706529141452137, -4.540774720514427543, 26.12024523944105070 ) ) ;
#87425=CARTESIAN_POINT ( 'NONE',  ( 4.527536911777373163, -6.376774720514422512, 21.53954785142818196 ) ) ;
#87427=AXIS2_PLACEMENT_3D ( 'NONE', #83760, #37594, #14241 ) ;
#87431=AXIS2_PLACEMENT_3D ( 'NONE', #90115, #27223, #66298 ) ;
#87433=CIRCLE ( 'NONE', #56678, 6.000000000000000888 ) ;
#87440=CARTESIAN_POINT ( 'NONE',  ( 3.748501943728875574, -5.876774720514425177, 21.47917144995767558 ) ) ;
#87458=CARTESIAN_POINT ( 'NONE',  ( 11.22434917415779054, -4.132774715458839232, -26.87660878605755599 ) ) ;
#87466=CARTESIAN_POINT ( 'NONE',  ( 7.480769230769231726, -5.876774720514430506, 20.77403846153845635 ) ) ;
#87471=CARTESIAN_POINT ( 'NONE',  ( 7.480769230769231726, -5.876774720514420736, 20.77403846153845635 ) ) ;
#87473=LINE ( 'NONE', #96095, #42792 ) ;
#87480=CARTESIAN_POINT ( 'NONE',  ( 10.40578984036287302, 5.965225279485572685, -28.04626194901324965 ) ) ;
#87484=EDGE_CURVE ( 'NONE', #83384, #6469, #98846, .T. ) ;
#87490=DIRECTION ( 'NONE',  ( 0.000000000000000000, 1.000000000000000000, -0.000000000000000000 ) ) ;
#87492=CARTESIAN_POINT ( 'NONE',  ( 3.252808283508203058, -6.376774720514402972, 18.30939203766361345 ) ) ;
#87495=ORIENTED_EDGE ( 'NONE', *, *, #28593, .T. ) ;
#87498=DIRECTION ( 'NONE',  ( -0.000000000000000000, 0.000000000000000000, -1.000000000000000000 ) ) ;
#87504=FACE_OUTER_BOUND ( 'NONE', #27578, .T. ) ;
#87509=CARTESIAN_POINT ( 'NONE',  ( -2.148731487934370410, -5.876774720514411854, 19.46295461892501422 ) ) ;
#87510=ORIENTED_EDGE ( 'NONE', *, *, #13909, .T. ) ;
#87512=DIRECTION ( 'NONE',  ( 1.000000000000000000, 0.000000000000000000, 0.000000000000000000 ) ) ;
#87515=AXIS2_PLACEMENT_3D ( 'NONE', #49802, #11218, #42193 ) ;
#87528=CARTESIAN_POINT ( 'NONE',  ( -7.326923076923074873, -6.376774720514427841, 21.75000000000001066 ) ) ;
#87530=FACE_OUTER_BOUND ( 'NONE', #57237, .T. ) ;
#87533=FACE_OUTER_BOUND ( 'NONE', #70512, .T. ) ;
#87540=VERTEX_POINT ( 'NONE', #77000 ) ;
#87541=ORIENTED_EDGE ( 'NONE', *, *, #38426, .F. ) ;
#87544=CARTESIAN_POINT ( 'NONE',  ( 33.61456970919601872, -6.376774720514426953, -11.35828564741663627 ) ) ;
#87552=DIRECTION ( 'NONE',  ( -0.7512896232465891000, -0.000000000000000000, -0.6599726524652351767 ) ) ;
#87553=DIRECTION ( 'NONE',  ( -2.417950247244706201E-16, 0.000000000000000000, 1.000000000000000000 ) ) ;
#87562=CIRCLE ( 'NONE', #61643, 0.3000000000000016542 ) ;
#87581=DIRECTION ( 'NONE',  ( 1.000000000000000000, -0.000000000000000000, 2.417950247244706201E-16 ) ) ;
#87591=CARTESIAN_POINT ( 'NONE',  ( 4.373554412633047228, -5.876774720514421624, 21.19197260575996822 ) ) ;
#87604=EDGE_CURVE ( 'NONE', #97072, #17304, #22509, .T. ) ;
#87617=DIRECTION ( 'NONE',  ( 1.000000000000000000, 0.000000000000000000, 0.000000000000000000 ) ) ;
#87624=ORIENTED_EDGE ( 'NONE', *, *, #85492, .T. ) ;
#87633=LINE ( 'NONE', #39951, #12059 ) ;
#87635=EDGE_CURVE ( 'NONE', #56601, #31048, #34353, .T. ) ;
#87640=DIRECTION ( 'NONE',  ( 1.000000000000000000, 0.000000000000000000, 0.000000000000000000 ) ) ;
#87647=EDGE_LOOP ( 'NONE', ( #10460, #76345, #68515, #91352, #51771, #78205, #85781, #41852 ) ) ;
#87653=DIRECTION ( 'NONE',  ( -0.000000000000000000, 1.000000000000000000, -0.000000000000000000 ) ) ;
#87667=ORIENTED_EDGE ( 'NONE', *, *, #60770, .F. ) ;
#87670=CARTESIAN_POINT ( 'NONE',  ( 30.61643171255909479, -3.477635932356431869, 27.37433006808820579 ) ) ;
#87677=LINE ( 'NONE', #56746, #54104 ) ;
#87700=DIRECTION ( 'NONE',  ( -0.000000000000000000, 0.000000000000000000, -1.000000000000000000 ) ) ;
#87707=VERTEX_POINT ( 'NONE', #5886 ) ;
#87713=B_SPLINE_CURVE_WITH_KNOTS ( 'NONE', 3,
 ( #35872, #75914, #58709, #97764, #83026, #60223, #73936, #91145, #36870, #21623, #6419, #68319, #66841, #59214, #4436, #35382 ),
 .UNSPECIFIED., .F., .F.,
 ( 4, 2, 2, 2, 2, 2, 2, 4 ),
 ( -2.611475609838436325E-05, 0.001181507984664241897, 0.001785319355045555511, 0.002389130725426869776, 0.002992942095808183173, 0.003596753466189497005, 0.004200564836570811270, 0.004804376206952124667 ),
 .UNSPECIFIED. ) ;
#87716=ORIENTED_EDGE ( 'NONE', *, *, #79350, .T. ) ;
#87720=CARTESIAN_POINT ( 'NONE',  ( -41.32836283488544638, -6.376774720514426953, 39.26872235229541985 ) ) ;
#87732=CARTESIAN_POINT ( 'NONE',  ( -29.49875734969026198, 5.965225279485572685, 7.870022800118625206 ) ) ;
#87738=DIRECTION ( 'NONE',  ( -0.000000000000000000, -1.000000000000000000, -0.000000000000000000 ) ) ;
#87742=EDGE_LOOP ( 'NONE', ( #12006, #46823, #81419, #79649 ) ) ;
#87745=CARTESIAN_POINT ( 'NONE',  ( 14.87948092214613283, -4.970807589639874458, -27.40745209048265352 ) ) ;
#87753=ORIENTED_EDGE ( 'NONE', *, *, #19314, .T. ) ;
#87758=ORIENTED_EDGE ( 'NONE', *, *, #25121, .T. ) ;
#87759=CARTESIAN_POINT ( 'NONE',  ( -6.775140224358976226, -6.376774720514408301, 19.14743589743590846 ) ) ;
#87760=AXIS2_PLACEMENT_3D ( 'NONE', #66722, #90030, #98625 ) ;
#87762=CARTESIAN_POINT ( 'NONE',  ( 2.949406532984364393, -5.876774720514410966, 19.42899254576129664 ) ) ;
#87766=CARTESIAN_POINT ( 'NONE',  ( 8.205893897551582938, -3.316774720514426456, -27.11136772256261196 ) ) ;
#87781=DIRECTION ( 'NONE',  ( 0.000000000000000000, -1.000000000000000000, 0.000000000000000000 ) ) ;
#87786=ORIENTED_EDGE ( 'NONE', *, *, #44159, .T. ) ;
#87809=FACE_OUTER_BOUND ( 'NONE', #73635, .T. ) ;
#87810=ORIENTED_EDGE ( 'NONE', *, *, #84459, .T. ) ;
#87833=AXIS2_PLACEMENT_3D ( 'NONE', #67332, #28260, #90162 ) ;
#87836=CARTESIAN_POINT ( 'NONE',  ( -24.90875734969025501, -3.316774720514426456, 29.49402280011862487 ) ) ;
#87838=LINE ( 'NONE', #96443, #62930 ) ;
#87855=VERTEX_POINT ( 'NONE', #29226 ) ;
#87860=DIRECTION ( 'NONE',  ( 2.504262461560503484E-15, -6.886721769291384876E-15, 1.000000000000000000 ) ) ;
#87861=ADVANCED_FACE ( 'NONE', ( #28734 ), #43955, .T. ) ;
#87867=EDGE_CURVE ( 'NONE', #36332, #67804, #37837, .T. ) ;
#87872=DIRECTION ( 'NONE',  ( -0.2488812114211667037, 0.000000000000000000, -0.9685340172660599212 ) ) ;
#87873=CARTESIAN_POINT ( 'NONE',  ( 2.590395174287518643, -5.876774720514416295, 20.05492615153064762 ) ) ;
#87875=ORIENTED_EDGE ( 'NONE', *, *, #38789, .F. ) ;
#87879=CARTESIAN_POINT ( 'NONE',  ( 7.166666666666668739, -5.876774720514419847, 20.78665865384614975 ) ) ;
#87880=CARTESIAN_POINT ( 'NONE',  ( 6.259688558337090036, -6.376774720514413630, 19.73360741988579292 ) ) ;
#87885=CARTESIAN_POINT ( 'NONE',  ( 2.598318274922708060, -5.876774720514413630, 19.68966562063331693 ) ) ;
#87889=ORIENTED_EDGE ( 'NONE', *, *, #92413, .F. ) ;
#87900=CARTESIAN_POINT ( 'NONE',  ( -24.90875734969025501, 5.965225279485572685, 26.43402280011862615 ) ) ;
#87907=CARTESIAN_POINT ( 'NONE',  ( 6.420673076923079314, -6.376774720514427841, 21.83974358974358765 ) ) ;
#87910=CARTESIAN_POINT ( 'NONE',  ( 6.555906488453394410, -5.876774720514425177, 21.46941147007026274 ) ) ;
#87912=CARTESIAN_POINT ( 'NONE',  ( 6.727764423076923350, -6.376774720514413630, 19.76442307692307665 ) ) ;
#87913=CARTESIAN_POINT ( 'NONE',  ( -9.940598223437577374, -6.376774720514426953, 22.08128695274315945 ) ) ;
#87930=CARTESIAN_POINT ( 'NONE',  ( -5.154768636056045850, -6.376774720514413630, 19.48351902941045921 ) ) ;
#87934=CARTESIAN_POINT ( 'NONE',  ( 4.931367317174526477, -5.876774720514419847, 20.61012727089847019 ) ) ;
#87935=CARTESIAN_POINT ( 'NONE',  ( 25.61870917940689552, 5.965225279485572685, 28.79814474876421926 ) ) ;
#87950=CARTESIAN_POINT ( 'NONE',  ( -2.148731487934370410, -6.376774720514411854, 19.46295461892501422 ) ) ;
#87962=LINE ( 'NONE', #9829, #5372 ) ;
#87979=CARTESIAN_POINT ( 'NONE',  ( 5.184553252003285984, 6.475225279485573360, -28.06387035751381731 ) ) ;
#87981=PLANE ( 'NONE',  #44380 ) ;
#87982=ORIENTED_EDGE ( 'NONE', *, *, #72932, .T. ) ;
#87992=ADVANCED_FACE ( 'NONE', ( #78379 ), #1777, .F. ) ;
#88000=ORIENTED_EDGE ( 'NONE', *, *, #98205, .F. ) ;
#88011=CARTESIAN_POINT ( 'NONE',  ( 32.48725517365867432, -4.170878844625590887, -0.8993273505261454304 ) ) ;
#88030=ADVANCED_FACE ( 'NONE', ( #77378, #62186 ), #54079, .F. ) ;
#88041=ORIENTED_EDGE ( 'NONE', *, *, #9570, .F. ) ;
#88044=CARTESIAN_POINT ( 'NONE',  ( -5.988734693054777125, -6.376774720514415407, 19.95737465391042065 ) ) ;
#88058=DIRECTION ( 'NONE',  ( 0.000000000000000000, 0.000000000000000000, -1.000000000000000000 ) ) ;
#88059=LINE ( 'NONE', #18034, #34488 ) ;
#88069=FACE_OUTER_BOUND ( 'NONE', #65233, .T. ) ;
#88070=CARTESIAN_POINT ( 'NONE',  ( -10.24059822343757808, -5.876774720514426953, 17.91871304725684766 ) ) ;
#88072=EDGE_CURVE ( 'NONE', #54059, #12135, #25610, .T. ) ;
#88084=CARTESIAN_POINT ( 'NONE',  ( -27.96875734969026084, -6.376774720514426953, 0.7300228001186309656 ) ) ;
#88090=EDGE_CURVE ( 'NONE', #32327, #39562, #14593, .T. ) ;
#88093=DIRECTION ( 'NONE',  ( 0.000000000000000000, 0.000000000000000000, -1.000000000000000000 ) ) ;
#88099=CIRCLE ( 'NONE', #29776, 2.249999999999998668 ) ;
#88105=VECTOR ( 'NONE', #84909, 1000.000000000000227 ) ;
#88108=VERTEX_POINT ( 'NONE', #42850 ) ;
#88112=DIRECTION ( 'NONE',  ( 1.252131230780251742E-15, -6.886721769291384876E-15, 1.000000000000000000 ) ) ;
#88113=LINE ( 'NONE', #32818, #74386 ) ;
#88115=ORIENTED_EDGE ( 'NONE', *, *, #64627, .T. ) ;
#88122=VERTEX_POINT ( 'NONE', #72293 ) ;
#88124=CARTESIAN_POINT ( 'NONE',  ( -0.08860454909227881426, -6.376774720514410077, 19.21747685089457036 ) ) ;
#88163=ADVANCED_FACE ( 'NONE', ( #26614 ), #2787, .T. ) ;
#88167=EDGE_LOOP ( 'NONE', ( #6285, #47910, #18622, #17451, #13486, #89933, #39358, #63361, #56020, #69918, #4432, #49456 ) ) ;
#88171=ORIENTED_EDGE ( 'NONE', *, *, #86998, .T. ) ;
#88173=CARTESIAN_POINT ( 'NONE',  ( 30.61752088227329693, -5.013017886559611114, 27.44065105897852419 ) ) ;
#88174=CARTESIAN_POINT ( 'NONE',  ( -7.326923076923076650, -6.376774720514417183, 20.36318108974359831 ) ) ;
#88188=DIRECTION ( 'NONE',  ( -1.000000000000000000, 0.000000000000000000, 1.895872651340772790E-16 ) ) ;
#88189=CARTESIAN_POINT ( 'NONE',  ( -1.267404104715736279, -6.376774720514413630, 19.66076420632889921 ) ) ;
#88205=EDGE_CURVE ( 'NONE', #67306, #58916, #42043, .T. ) ;
#88212=VERTEX_POINT ( 'NONE', #19989 ) ;
#88218=EDGE_CURVE ( 'NONE', #95881, #95239, #50956, .T. ) ;
#88223=DIRECTION ( 'NONE',  ( 1.257682986112628661E-16, 0.000000000000000000, 1.000000000000000000 ) ) ;
#88228=DIRECTION ( 'NONE',  ( -0.000000000000000000, 1.000000000000000000, -0.000000000000000000 ) ) ;
#88242=ORIENTED_EDGE ( 'NONE', *, *, #47543, .F. ) ;
#88244=EDGE_LOOP ( 'NONE', ( #41590, #56077, #87206, #38685, #48065, #46322, #98211, #60076 ) ) ;
#88245=ORIENTED_EDGE ( 'NONE', *, *, #51393, .F. ) ;
#88247=CARTESIAN_POINT ( 'NONE',  ( 14.92791587776674334, -5.037605299509789525, -27.26084882802267373 ) ) ;
#88249=B_SPLINE_CURVE_WITH_KNOTS ( 'NONE', 3,
 ( #15822, #68130, #76707, #45786, #68624, #31552, #62016 ),
 .UNSPECIFIED., .F., .F.,
 ( 4, 1, 1, 1, 4 ),
 ( 0.000000000000000000, 0.2835948081386937547, 0.5433948405759735367, 0.7806456291745620391, 1.000000000000000000 ),
 .UNSPECIFIED. ) ;
#88250=LINE ( 'NONE', #11116, #70371 ) ;
#88256=ORIENTED_EDGE ( 'NONE', *, *, #79308, .T. ) ;
#88259=ORIENTED_EDGE ( 'NONE', *, *, #65140, .T. ) ;
#88260=CARTESIAN_POINT ( 'NONE',  ( -6.265203266387573855, -6.376774720514408301, 19.29154511076646017 ) ) ;
#88262=ORIENTED_EDGE ( 'NONE', *, *, #98026, .F. ) ;
#88266=CARTESIAN_POINT ( 'NONE',  ( 12.90232279286373185, -3.316774720514426456, -28.14923833570356493 ) ) ;
#88273=CARTESIAN_POINT ( 'NONE',  ( 5.095029512766671154, -3.302735871364486098, -27.56177443937556859 ) ) ;
#88283=CARTESIAN_POINT ( 'NONE',  ( 31.93426202889373400, -6.376774720514426953, 6.907000118922836940 ) ) ;
#88291=CARTESIAN_POINT ( 'NONE',  ( 3.632573734185411851, -6.376774720514429617, 21.82795992345630509 ) ) ;
#88293=DIRECTION ( 'NONE',  ( -0.8264557562326033668, 6.845827386180409975E-16, -0.5630016722799281448 ) ) ;
#88307=LINE ( 'NONE', #19770, #31676 ) ;
#88317=DIRECTION ( 'NONE',  ( -0.000000000000000000, -1.000000000000000000, -0.000000000000000000 ) ) ;
#88329=VERTEX_POINT ( 'NONE', #89505 ) ;
#88331=CARTESIAN_POINT ( 'NONE',  ( -7.586742644780859912, -5.876774720514413630, 19.78730719034165020 ) ) ;
#88336=DIRECTION ( 'NONE',  ( 0.000000000000000000, -1.000000000000000000, 0.000000000000000000 ) ) ;
#88338=CARTESIAN_POINT ( 'NONE',  ( 12.53797248504841910, -0.3587747205144256601, -28.12591401903467059 ) ) ;
#88345=AXIS2_PLACEMENT_3D ( 'NONE', #48060, #63807, #94721 ) ;
#88371=CARTESIAN_POINT ( 'NONE',  ( 7.041152093163508319, -6.376774720514424288, 21.17127001373575368 ) ) ;
#88388=CARTESIAN_POINT ( 'NONE',  ( -29.49875734969025842, -0.3587747205144265483, 25.61802280011862720 ) ) ;
#88394=VERTEX_POINT ( 'NONE', #36718 ) ;
#88400=ORIENTED_EDGE ( 'NONE', *, *, #65875, .F. ) ;
#88412=EDGE_LOOP ( 'NONE', ( #54560, #17524, #54676, #90599 ) ) ;
#88418=ORIENTED_EDGE ( 'NONE', *, *, #55746, .T. ) ;
#88426=DIRECTION ( 'NONE',  ( 2.000709955812756815E-15, 0.000000000000000000, 1.000000000000000000 ) ) ;
#88434=ADVANCED_FACE ( 'NONE', ( #62558 ), #30396, .T. ) ;
#88436=CARTESIAN_POINT ( 'NONE',  ( 4.038745349937860496, -6.376774720514429617, 21.81354843764681206 ) ) ;
#88438=B_SPLINE_CURVE_WITH_KNOTS ( 'NONE', 3,
 ( #17320, #93432, #85833, #71621, #73991, #39654, #58276, #24429, #27313, #16317 ),
 .UNSPECIFIED., .F., .F.,
 ( 4, 2, 2, 2, 4 ),
 ( 1.734723475976807094E-18, 0.001417051740733931559, 0.002125577611100896037, 0.002479840546284378926, 0.002834103481467860949 ),
 .UNSPECIFIED. ) ;
#88446=CARTESIAN_POINT ( 'NONE',  ( 30.61004588589006659, -4.070814610512477394, 27.12580813198458785 ) ) ;
#88455=CARTESIAN_POINT ( 'NONE',  ( 31.79364159983995464, -1.682774720514426114, -11.59305536555894278 ) ) ;
#88465=CARTESIAN_POINT ( 'NONE',  ( 13.25751441563444999, -6.376774720514426065, -25.10777837594209672 ) ) ;
#88467=DIRECTION ( 'NONE',  ( 0.7071067811865507924, 0.000000000000000000, 0.7071067811865442421 ) ) ;
#88473=CARTESIAN_POINT ( 'NONE',  ( 0.7051282051282083962, -6.376774720514427841, 21.75000000000000000 ) ) ;
#88477=VECTOR ( 'NONE', #6054, 1000.000000000000000 ) ;
#88480=VECTOR ( 'NONE', #22257, 1000.000000000000000 ) ;
#88481=DIRECTION ( 'NONE',  ( -0.000000000000000000, 1.000000000000000000, -0.000000000000000000 ) ) ;
#88483=CARTESIAN_POINT ( 'NONE',  ( 32.66876533700882845, 5.965225279485572685, -12.58926540598385557 ) ) ;
#88500=DIRECTION ( 'NONE',  ( 0.000000000000000000, 0.000000000000000000, 1.000000000000000000 ) ) ;
#88502=CARTESIAN_POINT ( 'NONE',  ( -4.968349358974360364, -6.376774720514411854, 19.46153846153846700 ) ) ;
#88505=DIRECTION ( 'NONE',  ( -2.338552693767719605E-15, 0.000000000000000000, 1.000000000000000000 ) ) ;
#88510=CARTESIAN_POINT ( 'NONE',  ( 29.70906083364843653, -4.222256839740661682, 27.99786980188468277 ) ) ;
#88512=ORIENTED_EDGE ( 'NONE', *, *, #42476, .T. ) ;
#88514=CARTESIAN_POINT ( 'NONE',  ( 3.249631081431332280, -5.876774720514423400, 21.24682042713427776 ) ) ;
#88515=EDGE_CURVE ( 'NONE', #5644, #50554, #56957, .T. ) ;
#88519=CARTESIAN_POINT ( 'NONE',  ( -0.02075734969026423599, 6.475225279485573360, -28.03397719988137382 ) ) ;
#88536=CARTESIAN_POINT ( 'NONE',  ( -11.64875734969026233, -0.3587747205144265483, 31.02402280011862246 ) ) ;
#88537=CARTESIAN_POINT ( 'NONE',  ( 4.762431091568566366, -6.376774720514422512, 21.19858511215680608 ) ) ;
#88544=CARTESIAN_POINT ( 'NONE',  ( 31.21773176006472283, -5.300046855345732943, 2.139914057118826651 ) ) ;
#88546=VECTOR ( 'NONE', #23905, 1000.000000000000000 ) ;
#88547=CARTESIAN_POINT ( 'NONE',  ( 13.91401389203221406, 5.965225279485572685, 28.26920385068457264 ) ) ;
#88558=CARTESIAN_POINT ( 'NONE',  ( -4.495793269230770939, -5.876774720514410077, 19.27714342948718595 ) ) ;
#88564=EDGE_LOOP ( 'NONE', ( #91769, #13407, #9299, #33710 ) ) ;
#88577=DIRECTION ( 'NONE',  ( 0.000000000000000000, 1.000000000000000000, 0.000000000000000000 ) ) ;
#88590=CARTESIAN_POINT ( 'NONE',  ( 3.749014282529493869, -6.376774720514404748, 18.52125941707705792 ) ) ;
#88601=CARTESIAN_POINT ( 'NONE',  ( -2.373828433815573735, -6.376774720514410077, 19.48240003225459915 ) ) ;
#88603=AXIS2_PLACEMENT_3D ( 'NONE', #15793, #28658, #85816 ) ;
#88605=CARTESIAN_POINT ( 'NONE',  ( -4.968349358974361252, -5.876774720514412742, 19.46153846153847056 ) ) ;
#88616=CYLINDRICAL_SURFACE ( 'NONE', #77077, 2.249999999999998668 ) ;
#88619=PLANE ( 'NONE',  #39532 ) ;
#88622=AXIS2_PLACEMENT_3D ( 'NONE', #22722, #38968, #14626 ) ;
#88626=AXIS2_PLACEMENT_3D ( 'NONE', #25750, #11516, #10519 ) ;
#88630=CARTESIAN_POINT ( 'NONE',  ( 3.036358173076929123, -6.376774720514420736, 20.87990785256409865 ) ) ;
#88634=ORIENTED_EDGE ( 'NONE', *, *, #48438, .T. ) ;
#88635=CARTESIAN_POINT ( 'NONE',  ( -1.044792363895550302, -5.876774720514418071, 20.41272575174754422 ) ) ;
#88671=DIRECTION ( 'NONE',  ( 0.000000000000000000, -1.000000000000000000, 0.000000000000000000 ) ) ;
#88674=CARTESIAN_POINT ( 'NONE',  ( -7.294102189209645815, -6.376774720514413630, 19.89644244529368677 ) ) ;
#88678=ORIENTED_EDGE ( 'NONE', *, *, #68009, .F. ) ;
#88679=CARTESIAN_POINT ( 'NONE',  ( -5.563047341353722253, -6.376774720514413630, 20.06599527532950589 ) ) ;
#88680=PLANE ( 'NONE',  #50836 ) ;
#88684=EDGE_CURVE ( 'NONE', #65705, #54440, #5641, .T. ) ;
#88699=AXIS2_PLACEMENT_3D ( 'NONE', #62851, #40496, #94770 ) ;
#88702=DIRECTION ( 'NONE',  ( -0.000000000000000000, 1.000000000000000000, 0.000000000000000000 ) ) ;
#88710=DIRECTION ( 'NONE',  ( 0.000000000000000000, 1.000000000000000000, 1.155373159085149695E-17 ) ) ;
#88713=DIRECTION ( 'NONE',  ( 0.000000000000000000, -1.000000000000000000, 0.000000000000000000 ) ) ;
#88716=PLANE ( 'NONE',  #94518 ) ;
#88721=ADVANCED_FACE ( 'NONE', ( #96998 ), #44713, .F. ) ;
#88722=DIRECTION ( 'NONE',  ( 0.000000000000000000, 0.000000000000000000, 1.000000000000000000 ) ) ;
#88729=CARTESIAN_POINT ( 'NONE',  ( 4.959846025536391423, -6.376774720514417183, 20.32314756232572250 ) ) ;
#88745=ORIENTED_EDGE ( 'NONE', *, *, #26195, .F. ) ;
#88748=ADVANCED_FACE ( 'NONE', ( #54332 ), #92373, .F. ) ;
#88760=CARTESIAN_POINT ( 'NONE',  ( 6.887358010905132666, -5.876774720514425177, 21.32574817943157086 ) ) ;
#88764=EDGE_CURVE ( 'NONE', #83886, #93143, #61942, .T. ) ;
#88766=ORIENTED_EDGE ( 'NONE', *, *, #7647, .F. ) ;
#88767=CARTESIAN_POINT ( 'NONE',  ( 3.202571139211427553, -5.876774720514407413, 18.81074098386681470 ) ) ;
#88781=CARTESIAN_POINT ( 'NONE',  ( 6.059061188053544988, -5.876774720514417183, 20.16803580207560742 ) ) ;
#88783=CARTESIAN_POINT ( 'NONE',  ( -53.01255352321339842, -2.682774720514426559, 35.59556822165056644 ) ) ;
#88786=ORIENTED_EDGE ( 'NONE', *, *, #27309, .F. ) ;
#88787=ORIENTED_EDGE ( 'NONE', *, *, #24930, .T. ) ;
#88795=DIRECTION ( 'NONE',  ( -0.000000000000000000, -1.000000000000000000, -0.000000000000000000 ) ) ;
#88820=DIRECTION ( 'NONE',  ( 0.000000000000000000, 0.000000000000000000, 1.000000000000000000 ) ) ;
#88822=B_SPLINE_CURVE_WITH_KNOTS ( 'NONE', 3,
 ( #5127, #82743, #13727, #76127, #13226, #43695, #36080 ),
 .UNSPECIFIED., .F., .F.,
 ( 4, 1, 1, 1, 4 ),
 ( 0.3452202732246780759, 0.4949101844912719983, 0.6446000957578658097, 0.7942900070244596211, 0.9439799182910535436 ),
 .UNSPECIFIED. ) ;
#88832=CARTESIAN_POINT ( 'NONE',  ( 26.37445894957760117, -1.682774720514426114, -11.69480419648520986 ) ) ;
#88838=EDGE_CURVE ( 'NONE', #89557, #87707, #53830, .T. ) ;
#88840=DIRECTION ( 'NONE',  ( 0.000000000000000000, -1.000000000000000000, 0.000000000000000000 ) ) ;
#88846=EDGE_CURVE ( 'NONE', #14525, #90882, #7137, .T. ) ;
#88859=CARTESIAN_POINT ( 'NONE',  ( -24.90875734969025501, -3.316774720514426456, 30.51402280011862089 ) ) ;
#88872=CYLINDRICAL_SURFACE ( 'NONE', #73990, 129.7684398600581517 ) ;
#88876=ORIENTED_EDGE ( 'NONE', *, *, #34073, .F. ) ;
#88880=DIRECTION ( 'NONE',  ( -0.000000000000000000, 1.000000000000000000, -0.000000000000000000 ) ) ;
#88882=EDGE_LOOP ( 'NONE', ( #6993, #96615, #67403, #50631 ) ) ;
#88907=CARTESIAN_POINT ( 'NONE',  ( 22.81105451610979173, -4.772774720514425972, -18.46691820600746681 ) ) ;
#88914=CARTESIAN_POINT ( 'NONE',  ( 7.166666666666669627, -5.876774720514419847, 20.78665865384615330 ) ) ;
#88915=ORIENTED_EDGE ( 'NONE', *, *, #71874, .F. ) ;
#88923=LINE ( 'NONE', #29001, #18964 ) ;
#88942=CARTESIAN_POINT ( 'NONE',  ( -15.82668884360736961, 6.475225279485576024, 42.07822029717483758 ) ) ;
#88947=DIRECTION ( 'NONE',  ( -5.238131417152343399E-15, 0.000000000000000000, -1.000000000000000000 ) ) ;
#88954=DIRECTION ( 'NONE',  ( 0.000000000000000000, 1.000000000000000000, 0.000000000000000000 ) ) ;
#88965=ADVANCED_FACE ( 'NONE', ( #2048 ), #95381, .F. ) ;
#88966=CARTESIAN_POINT ( 'NONE',  ( 0.03625801282051022839, -6.376774720514410077, 19.27714342948718240 ) ) ;
#88967=CARTESIAN_POINT ( 'NONE',  ( 8.159923944583882260, -6.376774720514430506, -28.14238247108524149 ) ) ;
#88969=PLANE ( 'NONE',  #33794 ) ;
#88980=DIRECTION ( 'NONE',  ( 0.000000000000000000, -1.000000000000000000, 0.000000000000000000 ) ) ;
#88985=DIRECTION ( 'NONE',  ( -0.000000000000000000, 1.000000000000000000, -0.000000000000000000 ) ) ;
#88988=CARTESIAN_POINT ( 'NONE',  ( 6.303825520940272042, 5.965225279485572685, -28.39893233836329856 ) ) ;
#88994=CARTESIAN_POINT ( 'NONE',  ( -2.794871794871791604, -6.376774720514427841, 21.75000000000001066 ) ) ;
#88995=CARTESIAN_POINT ( 'NONE',  ( -2.701720430790311767, 5.965225279485594001, -28.90526747363640681 ) ) ;
#88996=CARTESIAN_POINT ( 'NONE',  ( -10.54059822343757702, -5.876774720514426953, 17.17691942396159988 ) ) ;
#89007=DIRECTION ( 'NONE',  ( -0.000000000000000000, 1.000000000000000000, -0.000000000000000000 ) ) ;
#89017=EDGE_CURVE ( 'NONE', #8499, #66329, #25938, .T. ) ;
#89018=CARTESIAN_POINT ( 'NONE',  ( 15.10352928271630724, -2.682774720514426559, -27.29968155418892195 ) ) ;
#89038=VECTOR ( 'NONE', #39086, 1000.000000000000114 ) ;
#89047=VECTOR ( 'NONE', #16496, 1000.000000000000000 ) ;
#89064=CARTESIAN_POINT ( 'NONE',  ( 15.98182857103851795, -3.492575169077971609, -27.92678846288758976 ) ) ;
#89070=DIRECTION ( 'NONE',  ( 0.9685340172660599212, 0.000000000000000000, -0.2488812114211667037 ) ) ;
#89074=CARTESIAN_POINT ( 'NONE',  ( -9.940598223437573822, -6.376774720514426953, 21.78128695274315874 ) ) ;
#89089=CIRCLE ( 'NONE', #16139, 1.399999999999999911 ) ;
#89098=CARTESIAN_POINT ( 'NONE',  ( -2.532641601674031850, -6.376774720514410077, 19.55266968305501507 ) ) ;
#89099=AXIS2_PLACEMENT_3D ( 'NONE', #63592, #7777, #85903 ) ;
#89113=PLANE ( 'NONE',  #70796 ) ;
#89116=CARTESIAN_POINT ( 'NONE',  ( -10.54059822343757702, -5.876774720514426953, 17.17691942396159988 ) ) ;
#89127=PLANE ( 'NONE',  #27592 ) ;
#89136=ORIENTED_EDGE ( 'NONE', *, *, #64222, .F. ) ;
#89151=LINE ( 'NONE', #12017, #12490 ) ;
#89161=LINE ( 'NONE', #58221, #27234 ) ;
#89162=AXIS2_PLACEMENT_3D ( 'NONE', #13979, #75879, #73897 ) ;
#89166=ORIENTED_EDGE ( 'NONE', *, *, #769, .T. ) ;
#89168=AXIS2_PLACEMENT_3D ( 'NONE', #80884, #36208, #98082 ) ;
#89174=ORIENTED_EDGE ( 'NONE', *, *, #67886, .T. ) ;
#89189=VECTOR ( 'NONE', #70071, 1000.000000000000000 ) ;
#89191=DIRECTION ( 'NONE',  ( -0.000000000000000000, -0.000000000000000000, -1.000000000000000000 ) ) ;
#89213=ORIENTED_EDGE ( 'NONE', *, *, #89894, .F. ) ;
#89220=CARTESIAN_POINT ( 'NONE',  ( 5.697397333356354565, -6.376774720514418959, 20.51730809691671809 ) ) ;
#89223=CARTESIAN_POINT ( 'NONE',  ( 4.261846905714947731, -6.376774720514427841, 21.73176331363731251 ) ) ;
#89225=CARTESIAN_POINT ( 'NONE',  ( 32.66876533700883556, 6.475225279485573360, -12.58926540598386445 ) ) ;
#89228=AXIS2_PLACEMENT_3D ( 'NONE', #24601, #1287, #16486 ) ;
#89236=ORIENTED_EDGE ( 'NONE', *, *, #60888, .F. ) ;
#89237=ORIENTED_EDGE ( 'NONE', *, *, #12443, .T. ) ;
#89238=ORIENTED_EDGE ( 'NONE', *, *, #65954, .T. ) ;
#89246=VECTOR ( 'NONE', #85298, 999.9999999999998863 ) ;
#89257=EDGE_CURVE ( 'NONE', #60099, #67166, #64794, .T. ) ;
#89262=CARTESIAN_POINT ( 'NONE',  ( 9.422519371942208011, -3.316774720514425567, -27.03574706870085720 ) ) ;
#89269=CARTESIAN_POINT ( 'NONE',  ( 5.817949855437939632, -5.876774720514417183, 20.34349022145623209 ) ) ;
#89272=ORIENTED_EDGE ( 'NONE', *, *, #77697, .T. ) ;
#89282=VERTEX_POINT ( 'NONE', #39351 ) ;
#89289=DIRECTION ( 'NONE',  ( -1.000000000000000000, 0.000000000000000000, 0.000000000000000000 ) ) ;
#89291=ORIENTED_EDGE ( 'NONE', *, *, #66534, .F. ) ;
#89298=EDGE_CURVE ( 'NONE', #3028, #87115, #24615, .T. ) ;
#89303=CIRCLE ( 'NONE', #45557, 28.96799999999999642 ) ;
#89315=VERTEX_POINT ( 'NONE', #32234 ) ;
#89349=DIRECTION ( 'NONE',  ( 0.000000000000000000, 0.000000000000000000, 1.000000000000000000 ) ) ;
#89352=ORIENTED_EDGE ( 'NONE', *, *, #87000, .F. ) ;
#89354=EDGE_LOOP ( 'NONE', ( #75643, #43937, #17626, #76623 ) ) ;
#89367=ORIENTED_EDGE ( 'NONE', *, *, #32936, .F. ) ;
#89372=APPLICATION_CONTEXT ( 'configuration controlled 3d designs of mechanical parts and assemblies' ) ;
#89376=CARTESIAN_POINT ( 'NONE',  ( 14.43441819133292370, -3.316774720514429120, -28.36222020317234183 ) ) ;
#89390=ORIENTED_EDGE ( 'NONE', *, *, #86593, .F. ) ;
#89398=EDGE_CURVE ( 'NONE', #31070, #7198, #84228, .T. ) ;
#89400=CARTESIAN_POINT ( 'NONE',  ( 0.7051282051282083962, -6.376774720514427841, 21.75000000000000000 ) ) ;
#89402=CARTESIAN_POINT ( 'NONE',  ( 7.478911390063968767, -6.376774720514422512, 20.82112274756839199 ) ) ;
#89403=CARTESIAN_POINT ( 'NONE',  ( 5.443272695963705665, -5.876774720514418071, 20.27301970143225418 ) ) ;
#89405=CARTESIAN_POINT ( 'NONE',  ( 6.627987042499408510, -5.876774720514423400, 21.45334999081212146 ) ) ;
#89414=LINE ( 'NONE', #50861, #18397 ) ;
#89421=DIRECTION ( 'NONE',  ( 0.000000000000000000, 0.000000000000000000, 1.000000000000000000 ) ) ;
#89422=VECTOR ( 'NONE', #22239, 1000.000000000000000 ) ;
#89431=CARTESIAN_POINT ( 'NONE',  ( 4.115044103975469270, -5.876774720514426953, 21.79213183355573946 ) ) ;
#89443=ORIENTED_EDGE ( 'NONE', *, *, #6468, .F. ) ;
#89448=CARTESIAN_POINT ( 'NONE',  ( -7.064692883725313344, -6.376774720514411854, 19.55266968305501862 ) ) ;
#89455=PLANE ( 'NONE',  #84810 ) ;
#89456=CARTESIAN_POINT ( 'NONE',  ( 4.329581153495547063, -5.876774720514421624, 21.24220543808225869 ) ) ;
#89462=CARTESIAN_POINT ( 'NONE',  ( 10.16119454606143435, -6.376774720514430506, -28.04611093484508899 ) ) ;
#89464=CARTESIAN_POINT ( 'NONE',  ( -7.024122139145243082, -5.876774720514408301, 19.17707164986947532 ) ) ;
#89466=DIRECTION ( 'NONE',  ( 1.000000000000000000, 8.673617379884028076E-17, 6.938893903907222461E-16 ) ) ;
#89468=CARTESIAN_POINT ( 'NONE',  ( 33.13288845015618023, 5.965225279485572685, -0.1650522222209214185 ) ) ;
#89475=ORIENTED_EDGE ( 'NONE', *, *, #2595, .T. ) ;
#89477=CARTESIAN_POINT ( 'NONE',  ( -1.653359744423585465, -6.376774720514413630, 19.34586827028017098 ) ) ;
#89493=DIRECTION ( 'NONE',  ( 0.000000000000000000, 0.000000000000000000, 1.000000000000000000 ) ) ;
#89502=CARTESIAN_POINT ( 'NONE',  ( 9.278253834636469577, -5.876774720514426953, 21.48128695274316158 ) ) ;
#89505=CARTESIAN_POINT ( 'NONE',  ( 11.62916340711181284, 5.965225279485572685, 28.75961759920349792 ) ) ;
#89512=EDGE_LOOP ( 'NONE', ( #29842, #22490, #20142, #26838 ) ) ;
#89517=CARTESIAN_POINT ( 'NONE',  ( -6.741682653110981249, 5.965225279485572685, 30.62569541381301619 ) ) ;
#89524=DIRECTION ( 'NONE',  ( -0.000000000000000000, 1.000000000000000000, -0.000000000000000000 ) ) ;
#89530=ORIENTED_EDGE ( 'NONE', *, *, #58949, .F. ) ;
#89534=ORIENTED_EDGE ( 'NONE', *, *, #13901, .F. ) ;
#89536=ORIENTED_EDGE ( 'NONE', *, *, #51188, .T. ) ;
#89539=FACE_OUTER_BOUND ( 'NONE', #9649, .T. ) ;
#89549=EDGE_LOOP ( 'NONE', ( #50158, #72068, #54838, #67521 ) ) ;
#89551=CARTESIAN_POINT ( 'NONE',  ( 2.610950917001260141, -5.876774720514412742, 19.54489930512155027 ) ) ;
#89552=FACE_OUTER_BOUND ( 'NONE', #62212, .T. ) ;
#89557=VERTEX_POINT ( 'NONE', #4795 ) ;
#89559=CARTESIAN_POINT ( 'NONE',  ( 5.109298100548420152, -3.316774720514426456, -27.55941679637948383 ) ) ;
#89573=CARTESIAN_POINT ( 'NONE',  ( -4.533825836049095059, -5.876774720514412742, 19.59623724171353132 ) ) ;
#89586=EDGE_CURVE ( 'NONE', #53085, #1756, #35749, .T. ) ;
#89597=AXIS2_PLACEMENT_3D ( 'NONE', #9705, #71111, #24422 ) ;
#89615=ORIENTED_EDGE ( 'NONE', *, *, #99037, .F. ) ;
#89626=CARTESIAN_POINT ( 'NONE',  ( -1.022535880784302353, -5.876774720514415407, 19.99258394656883908 ) ) ;
#89636=ORIENTED_EDGE ( 'NONE', *, *, #38154, .T. ) ;
#89639=B_SPLINE_SURFACE_WITH_KNOTS ( 'NONE', 3, 1, ( 
 ( #23296, #16695 ),
 ( #78580, #55281 ),
 ( #84705, #15196 ),
 ( #54282, #39037 ),
 ( #46159, #22293 ),
 ( #45658, #77087 ),
 ( #93315, #7587 ),
 ( #85716, #69495 ),
 ( #47162, #15698 ),
 ( #62385, #40041 ),
 ( #100411, #29924 ),
 ( #8593, #70495 ),
 ( #980, #31932 ),
 ( #62901, #60891 ),
 ( #87211, #4365 ),
 ( #17704, #72005 ),
 ( #59148, #64410 ),
 ( #10090, #20564 ),
 ( #51534, #32429 ) ),
 .UNSPECIFIED., .F., .F., .F.,
 ( 4, 1, 1, 1, 1, 1, 1, 1, 1, 1, 1, 1, 1, 1, 1, 1, 4 ),
 ( 2, 2 ),
 ( 0.000000000000000000, 0.07269466619231579330, 0.1413526962021420808, 0.2082288969497901876, 0.2736894576468447138, 0.3380517659755425397, 0.4009220982745032025, 0.4636163844951721735, 0.5278777255384771161, 0.5636262148099120406, 0.6061036626598774735, 0.6545011613018643093, 0.7100543472033249426, 0.7722619378848212257, 0.8412211450824306214, 0.9174702961779349630, 1.000000000000000000 ),
 ( 0.000000000000000000, 1.000000000000000000 ),
 .UNSPECIFIED. ) ;
#89642=ORIENTED_EDGE ( 'NONE', *, *, #93018, .F. ) ;
#89643=EDGE_LOOP ( 'NONE', ( #81983, #46679, #53042, #50578 ) ) ;
#89652=CIRCLE ( 'NONE', #18307, 2.500000000000000444 ) ;
#89667=CYLINDRICAL_SURFACE ( 'NONE', #45435, 4.080000000000000071 ) ;
#89669=DIRECTION ( 'NONE',  ( 0.000000000000000000, 0.000000000000000000, 1.000000000000000000 ) ) ;
#89689=CIRCLE ( 'NONE', #36238, 1.020000000000000018 ) ;
#89693=VERTEX_POINT ( 'NONE', #38723 ) ;
#89694=LINE ( 'NONE', #81587, #49417 ) ;
#89703=EDGE_CURVE ( 'NONE', #87231, #35025, #1040, .T. ) ;
#89714=PLANE ( 'NONE',  #29934 ) ;
#89716=EDGE_CURVE ( 'NONE', #96004, #57696, #76145, .T. ) ;
#89718=AXIS2_PLACEMENT_3D ( 'NONE', #88536, #31365, #80417 ) ;
#89719=VERTEX_POINT ( 'NONE', #39221 ) ;
#89724=AXIS2_PLACEMENT_3D ( 'NONE', #81565, #73454, #34890 ) ;
#89746=CARTESIAN_POINT ( 'NONE',  ( -5.837039262820512775, -6.376774720514413630, 19.76512419871795245 ) ) ;
#89753=ORIENTED_EDGE ( 'NONE', *, *, #86690, .T. ) ;
#89756=VECTOR ( 'NONE', #80571, 1000.000000000000000 ) ;
#89757=EDGE_LOOP ( 'NONE', ( #12295, #82862, #6125, #60678 ) ) ;
#89758=CARTESIAN_POINT ( 'NONE',  ( 2.904396343079095111, -5.876774720514415407, 19.95793242748194984 ) ) ;
#89759=ORIENTED_EDGE ( 'NONE', *, *, #19206, .T. ) ;
#89764=ADVANCED_FACE ( 'NONE', ( #94514 ), #31610, .T. ) ;
#89770=CARTESIAN_POINT ( 'NONE',  ( -12.84880425037203011, 5.965225279485592225, -26.59900746623528534 ) ) ;
#89772=DIRECTION ( 'NONE',  ( 1.000000000000000000, 0.000000000000000000, 5.238131417152343399E-15 ) ) ;
#89775=ORIENTED_EDGE ( 'NONE', *, *, #91449, .T. ) ;
#89788=DIRECTION ( 'NONE',  ( 0.7512896232465891000, 1.109416176496795172E-16, 0.6599726524652352877 ) ) ;
#89792=AXIS2_PLACEMENT_3D ( 'NONE', #35194, #97083, #58532 ) ;
#89795=DIRECTION ( 'NONE',  ( 1.000000000000000000, -4.089440751051245812E-15, 0.000000000000000000 ) ) ;
#89798=CARTESIAN_POINT ( 'NONE',  ( 22.02124265030973760, -6.376774720514428729, 13.20402280011862395 ) ) ;
#89816=CARTESIAN_POINT ( 'NONE',  ( -10.30858931494281450, -5.088649829473331110, 28.47370074478044444 ) ) ;
#89825=CARTESIAN_POINT ( 'NONE',  ( 5.920986267150416538, -5.876774720514421624, 21.32549308339960348 ) ) ;
#89851=CIRCLE ( 'NONE', #54237, 28.96799999999999642 ) ;
#89860=EDGE_LOOP ( 'NONE', ( #8343, #34634, #10148, #51111 ) ) ;
#89864=EDGE_LOOP ( 'NONE', ( #67578, #81624, #22590, #46700 ) ) ;
#89865=CARTESIAN_POINT ( 'NONE',  ( 6.826756808399247589, -6.376774720514424288, 21.36722843294932161 ) ) ;
#89866=CARTESIAN_POINT ( 'NONE',  ( -1.358974358974357921, -5.876774720514419847, 20.75510817307693046 ) ) ;
#89867=ORIENTED_EDGE ( 'NONE', *, *, #56543, .F. ) ;
#89872=CARTESIAN_POINT ( 'NONE',  ( 32.59332756141814258, 1.477225279485574028, -11.41404606144462086 ) ) ;
#89874=EDGE_CURVE ( 'NONE', #75373, #78258, #57977, .T. ) ;
#89894=EDGE_CURVE ( 'NONE', #75557, #86771, #41239, .T. ) ;
#89900=CARTESIAN_POINT ( 'NONE',  ( 7.475222833218381879, -6.376774720514418959, 20.91460388675487891 ) ) ;
#89901=CARTESIAN_POINT ( 'NONE',  ( 5.327901167172695907, -5.876774720514418959, 20.73192761314082233 ) ) ;
#89903=CARTESIAN_POINT ( 'NONE',  ( 7.166040305186291093, -5.876774720514419847, 20.81030863372915718 ) ) ;
#89905=CARTESIAN_POINT ( 'NONE',  ( 29.65385891689261655, -5.748374461104726940, 28.02705487427158104 ) ) ;
#89907=EDGE_CURVE ( 'NONE', #31070, #98531, #25099, .T. ) ;
#89908=EDGE_CURVE ( 'NONE', #12714, #38118, #6657, .T. ) ;
#89911=CARTESIAN_POINT ( 'NONE',  ( -27.15721599100127648, 5.965225279485572685, -10.22292133548836546 ) ) ;
#89918=DIRECTION ( 'NONE',  ( 0.000000000000000000, -1.000000000000000000, 0.000000000000000000 ) ) ;
#89933=ORIENTED_EDGE ( 'NONE', *, *, #43189, .T. ) ;
#89934=CARTESIAN_POINT ( 'NONE',  ( -28.84663072490566194, 5.965225279485572685, 28.73989617533406715 ) ) ;
#89942=CARTESIAN_POINT ( 'NONE',  ( -19.69812919673063689, -0.3587747205143964613, -22.00173861453436430 ) ) ;
#89950=CARTESIAN_POINT ( 'NONE',  ( 10.70203014590133783, -5.295085572968130094, -27.33604350180555187 ) ) ;
#89952=CIRCLE ( 'NONE', #94810, 1.399999999999998579 ) ;
#89953=CARTESIAN_POINT ( 'NONE',  ( 11.40529837384167777, -3.316774720514342967, -28.07356074712937044 ) ) ;
#89972=EDGE_LOOP ( 'NONE', ( #88915, #31112, #69419, #75917 ) ) ;
#89974=CARTESIAN_POINT ( 'NONE',  ( -29.49975734969026320, 6.475225279485573360, 25.41160796525321430 ) ) ;
#89978=DIRECTION ( 'NONE',  ( -1.000000000000000000, 0.000000000000000000, 0.000000000000000000 ) ) ;
#89982=LINE ( 'NONE', #12842, #13841 ) ;
#89985=ORIENTED_EDGE ( 'NONE', *, *, #72697, .F. ) ;
#89988=ORIENTED_EDGE ( 'NONE', *, *, #58807, .F. ) ;
#89991=DIRECTION ( 'NONE',  ( 0.000000000000000000, 0.000000000000000000, -1.000000000000000000 ) ) ;
#89997=ORIENTED_EDGE ( 'NONE', *, *, #60696, .T. ) ;
#90006=EDGE_LOOP ( 'NONE', ( #44647, #50818, #74530, #33852 ) ) ;
#90008=B_SPLINE_CURVE_WITH_KNOTS ( 'NONE', 3,
 ( #99741, #22621, #45991, #47990, #94144, #31756, #7915, #62724, #1314, #69821 ),
 .UNSPECIFIED., .F., .F.,
 ( 4, 2, 2, 2, 4 ),
 ( 0.000000000000000000, 0.0004275315936953677531, 0.0008550631873907355062, 0.001282594781086103313, 0.001710126374781471012 ),
 .UNSPECIFIED. ) ;
#90009=CARTESIAN_POINT ( 'NONE',  ( 3.094204744773375815, -5.876774720514422512, 21.02053020447315745 ) ) ;
#90011=ORIENTED_EDGE ( 'NONE', *, *, #32773, .F. ) ;
#90018=VERTEX_POINT ( 'NONE', #99984 ) ;
#90029=CARTESIAN_POINT ( 'NONE',  ( 7.116579217368891541, -6.376774720514415407, 20.51774267661129869 ) ) ;
#90030=DIRECTION ( 'NONE',  ( 0.000000000000000000, -1.000000000000000000, 0.000000000000000000 ) ) ;
#90034=EDGE_LOOP ( 'NONE', ( #80118, #71816, #67662, #20470, #47351 ) ) ;
#90045=ORIENTED_EDGE ( 'NONE', *, *, #83136, .T. ) ;
#90048=ORIENTED_EDGE ( 'NONE', *, *, #38775, .F. ) ;
#90049=CARTESIAN_POINT ( 'NONE',  ( 3.020285327128866992, -6.376774720514406525, 19.15473963397401391 ) ) ;
#90050=CARTESIAN_POINT ( 'NONE',  ( 2.710830299132254595, -6.376774720514410077, 19.05039662921485544 ) ) ;
#90073=DIRECTION ( 'NONE',  ( 0.000000000000000000, 0.000000000000000000, -1.000000000000000000 ) ) ;
#90075=AXIS2_PLACEMENT_3D ( 'NONE', #59343, #35999, #89795 ) ;
#90078=AXIS2_PLACEMENT_3D ( 'NONE', #32937, #63913, #79601 ) ;
#90080=B_SPLINE_CURVE_WITH_KNOTS ( 'NONE', 3,
 ( #57013, #87950, #80329, #49402, #10820, #72730, #34166, #65136, #57515, #21405, #66633, #97548, #68602, #44772, #99526, #13797, #75696, #36158, #30024 ),
 .UNSPECIFIED., .F., .F.,
 ( 4, 1, 1, 1, 1, 1, 1, 1, 1, 1, 1, 1, 1, 1, 1, 1, 4 ),
 ( 0.000000000000000000, 0.06815824415599749941, 0.1347066022023570842, 0.2018649976035983007, 0.2707882662774625526, 0.3400242943604910306, 0.4080827390537214439, 0.4768131952581447508, 0.5473460643070945375, 0.5856397954238962145, 0.6288649531777642521, 0.6771532033637908121, 0.7308028113651056090, 0.7898066155325017546, 0.8543250087420143357, 0.9243651340575425035, 1.000000000000000000 ),
 .UNSPECIFIED. ) ;
#90081=CARTESIAN_POINT ( 'NONE',  ( -1.001577508147789342, -6.376774720514411854, 19.87297243748311004 ) ) ;
#90082=DIRECTION ( 'NONE',  ( 0.000000000000000000, 1.000000000000000000, 0.000000000000000000 ) ) ;
#90090=EDGE_CURVE ( 'NONE', #32852, #11983, #85790, .T. ) ;
#90094=CYLINDRICAL_SURFACE ( 'NONE', #33429, 0.3000000000000016542 ) ;
#90097=ADVANCED_FACE ( 'NONE', ( #47735 ), #99496, .F. ) ;
#90112=CARTESIAN_POINT ( 'NONE',  ( 0.000000000000000000, -5.876774720514426953, 0.000000000000000000 ) ) ;
#90113=CYLINDRICAL_SURFACE ( 'NONE', #78608, 0.3000000000000016542 ) ;
#90115=CARTESIAN_POINT ( 'NONE',  ( -41.32836283488544638, -5.356774720514427379, 39.26872235229541985 ) ) ;
#90116=ORIENTED_EDGE ( 'NONE', *, *, #79169, .T. ) ;
#90124=CARTESIAN_POINT ( 'NONE',  ( -1.044639546681034536, -5.876774720514417183, 20.34213149456667580 ) ) ;
#90130=VERTEX_POINT ( 'NONE', #17783 ) ;
#90138=VECTOR ( 'NONE', #75471, 1000.000000000000000 ) ;
#90150=ORIENTED_EDGE ( 'NONE', *, *, #20612, .T. ) ;
#90156=ORIENTED_EDGE ( 'NONE', *, *, #50341, .T. ) ;
#90161=B_SPLINE_CURVE_WITH_KNOTS ( 'NONE', 3,
 ( #87907, #94509, #80288, #94004, #10782, #63587, #72687, #24990, #62572, #9773, #12760, #42745, #89900, #89402, #19382 ),
 .UNSPECIFIED., .F., .F.,
 ( 4, 1, 1, 1, 1, 1, 1, 1, 1, 1, 1, 1, 4 ),
 ( 0.000000000000000000, 0.08433472199262730118, 0.1670523184160740138, 0.2495660772409658001, 0.3327404818018465660, 0.4159148863627275539, 0.4978280095399964522, 0.5803725886080518537, 0.6646001210565030126, 0.7494666931126164888, 0.8325102339401410090, 0.9156392816681726554, 1.000000000000000000 ),
 .UNSPECIFIED. ) ;
#90162=DIRECTION ( 'NONE',  ( 0.000000000000000000, 0.000000000000000000, -1.000000000000000000 ) ) ;
#90167=VERTEX_POINT ( 'NONE', #75046 ) ;
#90171=AXIS2_PLACEMENT_3D ( 'NONE', #37755, #68714, #62601 ) ;
#90177=DIRECTION ( 'NONE',  ( -0.000000000000000000, 1.000000000000000000, -0.000000000000000000 ) ) ;
#90178=FACE_BOUND ( 'NONE', #27835, .T. ) ;
#90195=EDGE_LOOP ( 'NONE', ( #83741, #9715, #99823, #69585 ) ) ;
#90209=VECTOR ( 'NONE', #44977, 1000.000000000000000 ) ;
#90212=ORIENTED_EDGE ( 'NONE', *, *, #83716, .T. ) ;
#90213=CARTESIAN_POINT ( 'NONE',  ( 5.641575934020636396, -6.376774720514420736, 20.76276410292889096 ) ) ;
#90219=ADVANCED_FACE ( 'NONE', ( #35512 ), #43619, .T. ) ;
#90230=ORIENTED_EDGE ( 'NONE', *, *, #56433, .T. ) ;
#90232=ORIENTED_EDGE ( 'NONE', *, *, #45929, .F. ) ;
#90239=ORIENTED_EDGE ( 'NONE', *, *, #61831, .T. ) ;
#90256=VERTEX_POINT ( 'NONE', #67960 ) ;
#90265=DIRECTION ( 'NONE',  ( 0.9161084732596777025, 7.885106708985488048E-16, -0.4009304992412306978 ) ) ;
#90268=CARTESIAN_POINT ( 'NONE',  ( 5.654014271574485662, -6.376774720514420736, 20.92503208403226722 ) ) ;
#90288=EDGE_CURVE ( 'NONE', #67166, #60099, #37078, .T. ) ;
#90300=EDGE_LOOP ( 'NONE', ( #70814, #9118, #46851, #37378, #69647, #18530, #45303, #50064, #18619, #89475, #1890, #67525, #20633, #11761, #95364, #90859, #34492, #62065, #13402, #17475, #32727, #2631, #7621, #66, #62492, #36102, #63972 ) ) ;
#90312=AXIS2_PLACEMENT_3D ( 'NONE', #36114, #95514, #75166 ) ;
#90313=CARTESIAN_POINT ( 'NONE',  ( 30.45304879119406039, -4.772774720514425972, -10.07140455160086390 ) ) ;
#90319=VECTOR ( 'NONE', #24020, 1000.000000000000000 ) ;
#90322=DIRECTION ( 'NONE',  ( 0.000000000000000000, 0.000000000000000000, 1.000000000000000000 ) ) ;
#90327=CARTESIAN_POINT ( 'NONE',  ( 22.81105451610979173, -2.682774720514426559, -18.46691820600746681 ) ) ;
#90328=PLANE ( 'NONE',  #72222 ) ;
#90342=LINE ( 'NONE', #5604, #73755 ) ;
#90348=EDGE_LOOP ( 'NONE', ( #27071, #89636, #5918, #6746 ) ) ;
#90358=VERTEX_POINT ( 'NONE', #31382 ) ;
#90366=VERTEX_POINT ( 'NONE', #23255 ) ;
#90367=VERTEX_POINT ( 'NONE', #16150 ) ;
#90375=CARTESIAN_POINT ( 'NONE',  ( 27.53860345374771867, -5.356774720514425603, -9.482392034746242260 ) ) ;
#90379=DIRECTION ( 'NONE',  ( -0.9161084732596779245, -5.365801633547208359E-16, 0.4009304992412300872 ) ) ;
#90381=ADVANCED_FACE ( 'NONE', ( #47121 ), #85163, .F. ) ;
#90394=DIRECTION ( 'NONE',  ( -0.000000000000000000, -1.000000000000000000, -0.000000000000000000 ) ) ;
#90400=CARTESIAN_POINT ( 'NONE',  ( 10.46399479596398052, -3.316774720514422903, -27.03001098546561209 ) ) ;
#90404=CARTESIAN_POINT ( 'NONE',  ( 29.72131469344797239, -6.278265095287072661, 26.95488797742164877 ) ) ;
#90414=AXIS2_PLACEMENT_3D ( 'NONE', #79381, #27103, #40824 ) ;
#90422=ORIENTED_EDGE ( 'NONE', *, *, #78158, .T. ) ;
#90426=CARTESIAN_POINT ( 'NONE',  ( -9.278253834636473130, -6.376774720514426953, 21.78128695274316229 ) ) ;
#90429=ORIENTED_EDGE ( 'NONE', *, *, #73998, .F. ) ;
#90431=CARTESIAN_POINT ( 'NONE',  ( 33.00535138976592719, -3.570691370340881576, -12.97242311383975988 ) ) ;
#90433=B_SPLINE_CURVE_WITH_KNOTS ( 'NONE', 3,
 ( #19480, #2282, #41846, #9873, #42842, #18982, #56066, #50443, #35221, #95615, #17487, #34716, #95113, #49961, #73772, #33212, #58073, #72288, #18487 ),
 .UNSPECIFIED., .F., .F.,
 ( 4, 1, 1, 1, 1, 1, 1, 1, 1, 1, 1, 1, 1, 1, 1, 1, 4 ),
 ( 0.000000000000000000, 0.07059928943359200515, 0.1379009210036200861, 0.2031961978097334975, 0.2667897246502631270, 0.3291063872214231578, 0.3906535452348600668, 0.4526530569344815458, 0.5157480403003722458, 0.5779263408004527980, 0.6389300116184465361, 0.6983507176418213280, 0.7572960374442707643, 0.8163937673501530101, 0.8762669096141296743, 0.9368171089060820522, 1.000000000000000000 ),
 .UNSPECIFIED. ) ;
#90438=DIRECTION ( 'NONE',  ( 0.000000000000000000, -1.000000000000000000, 0.000000000000000000 ) ) ;
#90440=CARTESIAN_POINT ( 'NONE',  ( -7.326845193947049140, -6.376774720514417183, 20.33046051580616265 ) ) ;
#90449=CARTESIAN_POINT ( 'NONE',  ( -1.358974358974357921, -5.876774720514419847, 20.75510817307693046 ) ) ;
#90451=LINE ( 'NONE', #6208, #39463 ) ;
#90459=CARTESIAN_POINT ( 'NONE',  ( -29.49875734969026198, 5.965225279485572685, 10.11402280011862587 ) ) ;
#90461=ORIENTED_EDGE ( 'NONE', *, *, #67491, .F. ) ;
#90465=CARTESIAN_POINT ( 'NONE',  ( -24.90875734969025501, -3.316774720514426456, 27.45402280011862572 ) ) ;
#90467=EDGE_CURVE ( 'NONE', #92450, #26965, #65364, .T. ) ;
#90475=DIRECTION ( 'NONE',  ( 0.000000000000000000, 0.000000000000000000, -1.000000000000000000 ) ) ;
#90485=CYLINDRICAL_SURFACE ( 'NONE', #40516, 0.3000000000000016542 ) ;
#90487=EDGE_LOOP ( 'NONE', ( #3936, #29245, #43138, #75181 ) ) ;
#90499=ORIENTED_EDGE ( 'NONE', *, *, #51458, .F. ) ;
#90501=CARTESIAN_POINT ( 'NONE',  ( 3.045412351277957175, -5.876774720514421624, 20.90433128744512814 ) ) ;
#90506=ORIENTED_EDGE ( 'NONE', *, *, #65954, .F. ) ;
#90513=DIRECTION ( 'NONE',  ( -1.000000000000000000, 0.000000000000000000, 0.000000000000000000 ) ) ;
#90519=ORIENTED_EDGE ( 'NONE', *, *, #25063, .T. ) ;
#90525=VERTEX_POINT ( 'NONE', #73947 ) ;
#90528=CARTESIAN_POINT ( 'NONE',  ( 30.63256949310621735, -4.401217678701063285, 28.01131607762999565 ) ) ;
#90538=CARTESIAN_POINT ( 'NONE',  ( -16.22218391600152643, -6.376774720514426953, -54.85883559227303863 ) ) ;
#90557=FACE_OUTER_BOUND ( 'NONE', #91372, .T. ) ;
#90564=DIRECTION ( 'NONE',  ( -0.000000000000000000, 1.000000000000000000, -0.000000000000000000 ) ) ;
#90570=CARTESIAN_POINT ( 'NONE',  ( 33.13288845015618023, 5.965225279485572685, -0.1650522222209214185 ) ) ;
#90572=CARTESIAN_POINT ( 'NONE',  ( -1.022535880784302353, -6.376774720514415407, 19.99258394656883908 ) ) ;
#90576=ADVANCED_FACE ( 'NONE', ( #20640 ), #35394, .T. ) ;
#90582=CARTESIAN_POINT ( 'NONE',  ( -0.4909855769230799249, -5.876774720514410077, 19.14743589743590491 ) ) ;
#90583=EDGE_CURVE ( 'NONE', #29990, #14292, #93798, .T. ) ;
#90586=EDGE_CURVE ( 'NONE', #18471, #46432, #98258, .T. ) ;
#90596=LINE ( 'NONE', #21075, #4231 ) ;
#90599=ORIENTED_EDGE ( 'NONE', *, *, #73822, .F. ) ;
#90604=ORIENTED_EDGE ( 'NONE', *, *, #27244, .T. ) ;
#90606=DIRECTION ( 'NONE',  ( 0.000000000000000000, -1.000000000000000000, 0.000000000000000000 ) ) ;
#90608=ORIENTED_EDGE ( 'NONE', *, *, #98918, .F. ) ;
#90610=VECTOR ( 'NONE', #28706, 1000.000000000000000 ) ;
#90624=EDGE_LOOP ( 'NONE', ( #77911, #68810, #32586, #109, #46817, #94595, #2938, #79728 ) ) ;
#90626=CIRCLE ( 'NONE', #35581, 252.4458649670781085 ) ;
#90630=VERTEX_POINT ( 'NONE', #40316 ) ;
#90631=CARTESIAN_POINT ( 'NONE',  ( 30.09341516180546350, -4.772774720514425972, -11.39311774897855933 ) ) ;
#90633=CARTESIAN_POINT ( 'NONE',  ( 0.000000000000000000, -5.356774720514425603, 0.000000000000000000 ) ) ;
#90648=CARTESIAN_POINT ( 'NONE',  ( 26.73860345374794534, 1.477225279485574028, -7.113848178280766099 ) ) ;
#90649=VECTOR ( 'NONE', #30534, 1000.000000000000000 ) ;
#90653=CARTESIAN_POINT ( 'NONE',  ( 28.30015606816038698, -1.682774720514426114, -13.13501953239208930 ) ) ;
#90673=CARTESIAN_POINT ( 'NONE',  ( -0.4909855769230799249, -6.376774720514410077, 19.14743589743590491 ) ) ;
#90684=ORIENTED_EDGE ( 'NONE', *, *, #54052, .F. ) ;
#90692=CARTESIAN_POINT ( 'NONE',  ( 32.66876533700882845, 6.475225279485573360, -12.58926540598385557 ) ) ;
#90697=VECTOR ( 'NONE', #12179, 1000.000000000000114 ) ;
#90699=CARTESIAN_POINT ( 'NONE',  ( 2.677468215678941110, -6.376774720514418959, 20.83735685176740304 ) ) ;
#90702=EDGE_CURVE ( 'NONE', #65855, #98879, #1466, .T. ) ;
#90707=DIRECTION ( 'NONE',  ( -0.000000000000000000, 1.000000000000000000, -0.000000000000000000 ) ) ;
#90711=CARTESIAN_POINT ( 'NONE',  ( 5.993553214355093139, -6.376774720514417183, 20.20316077874593930 ) ) ;
#90724=CARTESIAN_POINT ( 'NONE',  ( 7.176111537430461595, -5.876774720514424288, 21.53668079471899333 ) ) ;
#90727=LINE ( 'NONE', #50176, #50897 ) ;
#90729=FACE_OUTER_BOUND ( 'NONE', #30617, .T. ) ;
#90730=ORIENTED_EDGE ( 'NONE', *, *, #68506, .F. ) ;
#90750=CIRCLE ( 'NONE', #29175, 251.9358649670780892 ) ;
#90763=CARTESIAN_POINT ( 'NONE',  ( 6.404294203292168142, -6.376774720514415407, 20.09052689972686423 ) ) ;
#90765=CARTESIAN_POINT ( 'NONE',  ( 14.98985047787450320, -3.577630190450212577, -26.76169638709854226 ) ) ;
#90769=ORIENTED_EDGE ( 'NONE', *, *, #47715, .F. ) ;
#90770=CIRCLE ( 'NONE', #64877, 1.020000000000000018 ) ;
#90771=ORIENTED_EDGE ( 'NONE', *, *, #16312, .F. ) ;
#90782=DIRECTION ( 'NONE',  ( 0.7512896232465892110, 0.000000000000000000, 0.6599726524652352877 ) ) ;
#90788=EDGE_CURVE ( 'NONE', #51587, #534, #40352, .T. ) ;
#90809=CARTESIAN_POINT ( 'NONE',  ( -5.891837592278976743, -6.376774720514418959, 20.62654306927474934 ) ) ;
#90810=DIRECTION ( 'NONE',  ( -0.000000000000000000, 1.000000000000000000, -0.000000000000000000 ) ) ;
#90811=CARTESIAN_POINT ( 'NONE',  ( -7.347880794884120722E-16, -5.356774720514425603, -6.000000000000000888 ) ) ;
#90815=CARTESIAN_POINT ( 'NONE',  ( 15.32643653063177958, -3.577630190450218350, -27.14485409495429380 ) ) ;
#90816=CARTESIAN_POINT ( 'NONE',  ( 282.9764569301858046, 5.965225279485572685, 20.79159422840526616 ) ) ;
#90821=AXIS2_PLACEMENT_3D ( 'NONE', #59199, #59702, #37358 ) ;
#90822=DIRECTION ( 'NONE',  ( -1.000000000000000000, 0.000000000000000000, 0.000000000000000000 ) ) ;
#90828=DIRECTION ( 'NONE',  ( 0.000000000000000000, 0.000000000000000000, -1.000000000000000000 ) ) ;
#90843=EDGE_CURVE ( 'NONE', #49731, #53050, #95397, .T. ) ;
#90849=LINE ( 'NONE', #83729, #48561 ) ;
#90855=ORIENTED_EDGE ( 'NONE', *, *, #74447, .F. ) ;
#90859=ORIENTED_EDGE ( 'NONE', *, *, #59922, .T. ) ;
#90874=DIRECTION ( 'NONE',  ( 0.000000000000000000, 0.000000000000000000, 1.000000000000000000 ) ) ;
#90882=VERTEX_POINT ( 'NONE', #21445 ) ;
#90888=CARTESIAN_POINT ( 'NONE',  ( -6.275748223059703257, -5.876774720514411854, 19.59984006504824805 ) ) ;
#90890=FACE_OUTER_BOUND ( 'NONE', #53697, .T. ) ;
#90895=DIRECTION ( 'NONE',  ( -0.1311553622875919756, 6.845827386180409975E-16, -0.9913618264504692190 ) ) ;
#90898=ORIENTED_EDGE ( 'NONE', *, *, #2762, .F. ) ;
#90913=LINE ( 'NONE', #60483, #79977 ) ;
#90919=CARTESIAN_POINT ( 'NONE',  ( 10.27515206207115739, -5.152774720514427642, -28.04856579873300149 ) ) ;
#90923=DIRECTION ( 'NONE',  ( 0.000000000000000000, 0.000000000000000000, 1.000000000000000000 ) ) ;
#90928=LINE ( 'NONE', #89934, #61880 ) ;
#90933=CARTESIAN_POINT ( 'NONE',  ( 33.96422015159436114, 5.965225279485572685, -7.233236000911337449 ) ) ;
#90943=ORIENTED_EDGE ( 'NONE', *, *, #54831, .T. ) ;
#90944=FACE_OUTER_BOUND ( 'NONE', #9889, .T. ) ;
#90945=DIRECTION ( 'NONE',  ( -1.000000000000000000, -0.000000000000000000, 0.000000000000000000 ) ) ;
#90952=EDGE_CURVE ( 'NONE', #13162, #98350, #37192, .T. ) ;
#90957=CARTESIAN_POINT ( 'NONE',  ( 5.864177746775673050, -6.376774720514426065, 21.69926562011473337 ) ) ;
#90979=LINE ( 'NONE', #12847, #94850 ) ;
#90984=FACE_OUTER_BOUND ( 'NONE', #52131, .T. ) ;
#90985=CARTESIAN_POINT ( 'NONE',  ( -0.4362980769230789257, -6.376774720514411854, 19.46153846153846345 ) ) ;
#90990=CARTESIAN_POINT ( 'NONE',  ( 282.9764569301858046, -4.540774720514427543, 20.79159422840526616 ) ) ;
#90998=ORIENTED_EDGE ( 'NONE', *, *, #79217, .F. ) ;
#91005=EDGE_LOOP ( 'NONE', ( #95345, #48209, #82029, #9034 ) ) ;
#91006=CARTESIAN_POINT ( 'NONE',  ( -4.141025641025638748, -6.376774720514427841, 21.75000000000000355 ) ) ;
#91011=DIRECTION ( 'NONE',  ( -4.448048651795319837E-16, -1.000000000000000000, -7.118365844322522408E-16 ) ) ;
#91022=EDGE_LOOP ( 'NONE', ( #59901, #41324, #90156, #34356, #79286, #76207, #20099, #40790 ) ) ;
#91025=FACE_OUTER_BOUND ( 'NONE', #55789, .T. ) ;
#91029=CARTESIAN_POINT ( 'NONE',  ( 30.59070867143730155, -4.540774708561928108, 26.30292506078689385 ) ) ;
#91036=EDGE_CURVE ( 'NONE', #83384, #90167, #70135, .T. ) ;
#91038=DIRECTION ( 'NONE',  ( -0.6599726524652352877, 0.000000000000000000, 0.7512896232465892110 ) ) ;
#91049=DIRECTION ( 'NONE',  ( 0.1489078231574191002, 6.845827386180410961E-16, -0.9888510809027407644 ) ) ;
#91050=DIRECTION ( 'NONE',  ( -0.000000000000000000, -1.000000000000000000, -0.000000000000000000 ) ) ;
#91060=CARTESIAN_POINT ( 'NONE',  ( -4.194375271223358403, -5.876774720514417183, 20.09898898868106087 ) ) ;
#91070=CARTESIAN_POINT ( 'NONE',  ( -1.318699232124953324, -6.376774720514411854, 19.74039977944280722 ) ) ;
#91074=LINE ( 'NONE', #76336, #68435 ) ;
#91083=DIRECTION ( 'NONE',  ( 0.000000000000000000, -1.000000000000000000, 0.000000000000000000 ) ) ;
#91095=VECTOR ( 'NONE', #52385, 1000.000000000000000 ) ;
#91098=EDGE_CURVE ( 'NONE', #45069, #90256, #42034, .T. ) ;
#91102=CARTESIAN_POINT ( 'NONE',  ( 4.692776824272364422, -6.376774720514406525, 18.67160386110882442 ) ) ;
#91104=VERTEX_POINT ( 'NONE', #26893 ) ;
#91106=EDGE_CURVE ( 'NONE', #20975, #64208, #97402, .T. ) ;
#91108=VERTEX_POINT ( 'NONE', #18282 ) ;
#91114=CARTESIAN_POINT ( 'NONE',  ( -0.6227173540047638012, -5.876774720514413630, 19.48351902941045211 ) ) ;
#91119=CARTESIAN_POINT ( 'NONE',  ( -4.968349358974361252, -6.376774720514411854, 19.46153846153847056 ) ) ;
#91127=CARTESIAN_POINT ( 'NONE',  ( 4.572862496014544753, -6.376774720514408301, 19.20224321281611068 ) ) ;
#91129=CARTESIAN_POINT ( 'NONE',  ( 30.53060340732035982, -4.594240983522013266, 19.84760796525321425 ) ) ;
#91139=ORIENTED_EDGE ( 'NONE', *, *, #862, .F. ) ;
#91145=CARTESIAN_POINT ( 'NONE',  ( -10.18932761084327865, -5.341047792237469949, 29.75743496038930758 ) ) ;
#91146=EDGE_CURVE ( 'NONE', #74381, #26531, #91287, .T. ) ;
#91150=CARTESIAN_POINT ( 'NONE',  ( 32.66876533700883556, 5.965225279485572685, -12.58926540598386445 ) ) ;
#91151=VERTEX_POINT ( 'NONE', #44618 ) ;
#91166=DIRECTION ( 'NONE',  ( 1.000000000000000000, -4.015954566446630556E-15, 0.000000000000000000 ) ) ;
#91170=LINE ( 'NONE', #90673, #2272 ) ;
#91180=DIRECTION ( 'NONE',  ( -0.000000000000000000, 1.000000000000000000, -0.000000000000000000 ) ) ;
#91186=ORIENTED_EDGE ( 'NONE', *, *, #98501, .T. ) ;
#91188=PRODUCT_DEFINITION_FORMATION_WITH_SPECIFIED_SOURCE ( 'ANY', '', #51515, .NOT_KNOWN. ) ;
#91193=B_SPLINE_CURVE_WITH_KNOTS ( 'NONE', 3,
 ( #68187, #84896, #76277, #14379, #30108, #45355, #61081, #92010, #61585, #78769, #39719, #9269, #16380, #40234, #55464 ),
 .UNSPECIFIED., .F., .F.,
 ( 4, 1, 1, 1, 1, 1, 1, 1, 1, 1, 1, 1, 4 ),
 ( 0.000000000000000000, 0.08415201884431637580, 0.1665323202984579920, 0.2488363311465297822, 0.3312461454872601685, 0.4129571090216147544, 0.4904942776695643825, 0.5661557919819225626, 0.6399873346864677348, 0.7167654882718510478, 0.8021439047100968889, 0.8958332007101900141, 1.000000000000000000 ),
 .UNSPECIFIED. ) ;
#91195=CIRCLE ( 'NONE', #97717, 253.2618649670780826 ) ;
#91206=CARTESIAN_POINT ( 'NONE',  ( 3.249631081431332280, -6.376774720514424288, 21.24682042713427776 ) ) ;
#91214=ADVANCED_FACE ( 'NONE', ( #82671 ), #14150, .F. ) ;
#91219=CARTESIAN_POINT ( 'NONE',  ( -4.223504350552545361, -5.876774720514412742, 19.52341893546492813 ) ) ;
#91229=CIRCLE ( 'NONE', #34535, 1.399999999999988143 ) ;
#91235=EDGE_CURVE ( 'NONE', #38539, #64573, #45274, .T. ) ;
#91243=EDGE_CURVE ( 'NONE', #90256, #31553, #44342, .T. ) ;
#91250=CARTESIAN_POINT ( 'NONE',  ( 4.403244164709623654, -5.876774720514402972, 18.35516266052912826 ) ) ;
#91260=AXIS2_PLACEMENT_3D ( 'NONE', #74109, #88336, #72617 ) ;
#91267=EDGE_LOOP ( 'NONE', ( #71498, #38336, #91976, #45110 ) ) ;
#91268=DIRECTION ( 'NONE',  ( 1.000000000000000000, 0.000000000000000000, 0.000000000000000000 ) ) ;
#91271=VECTOR ( 'NONE', #67754, 1000.000000000000000 ) ;
#91281=AXIS2_PLACEMENT_3D ( 'NONE', #32125, #678, #63098 ) ;
#91285=CARTESIAN_POINT ( 'NONE',  ( -2.959136224476847765, -6.376774720514413630, 19.53857357749110335 ) ) ;
#91287=LINE ( 'NONE', #98385, #80909 ) ;
#91303=ORIENTED_EDGE ( 'NONE', *, *, #89874, .F. ) ;
#91306=CARTESIAN_POINT ( 'NONE',  ( 27.53860345374808105, 1.477225279485574028, 19.84760796525321425 ) ) ;
#91314=AXIS2_PLACEMENT_3D ( 'NONE', #82982, #99205, #69771 ) ;
#91317=CARTESIAN_POINT ( 'NONE',  ( 33.64270623324222953, -3.650451339955370855, -11.69061897474703571 ) ) ;
#91325=LINE ( 'NONE', #21799, #24058 ) ;
#91332=CARTESIAN_POINT ( 'NONE',  ( 5.766314450391940127, -5.876774720514423400, 21.17177008079512035 ) ) ;
#91334=VECTOR ( 'NONE', #99404, 1000.000000000000000 ) ;
#91337=ADVANCED_FACE ( 'NONE', ( #16653, #78544 ), #77047, .T. ) ;
#91348=DIRECTION ( 'NONE',  ( -0.000000000000000000, 1.000000000000000000, -0.000000000000000000 ) ) ;
#91352=ORIENTED_EDGE ( 'NONE', *, *, #23414, .T. ) ;
#91355=EDGE_LOOP ( 'NONE', ( #13714, #22100, #57208, #20208 ) ) ;
#91359=CARTESIAN_POINT ( 'NONE',  ( 3.113719597313231002, -5.876774720514426065, 21.58936759753562029 ) ) ;
#91372=EDGE_LOOP ( 'NONE', ( #36742, #720, #68653, #8301 ) ) ;
#91378=CARTESIAN_POINT ( 'NONE',  ( 15.29947330337543754, -6.376774720514426953, -27.16854002387008649 ) ) ;
#91382=LINE ( 'NONE', #65421, #56039 ) ;
#91407=FACE_OUTER_BOUND ( 'NONE', #16263, .T. ) ;
#91426=CARTESIAN_POINT ( 'NONE',  ( -1.358974358974355257, -6.376774720514427841, 21.75000000000000711 ) ) ;
#91433=CARTESIAN_POINT ( 'NONE',  ( 4.653726706778644306, -6.376774720514415407, 20.04674869880385302 ) ) ;
#91437=CARTESIAN_POINT ( 'NONE',  ( 1.140932434931746582E-13, -6.376774720514426953, 21.78128695274321203 ) ) ;
#91439=DIRECTION ( 'NONE',  ( -0.000000000000000000, 0.000000000000000000, -1.000000000000000000 ) ) ;
#91440=CARTESIAN_POINT ( 'NONE',  ( -1.845912073933368536, -5.876774720514408301, 19.53740760792477360 ) ) ;
#91441=DIRECTION ( 'NONE',  ( -0.000000000000000000, 1.000000000000000000, -0.000000000000000000 ) ) ;
#91449=EDGE_CURVE ( 'NONE', #19254, #52189, #10470, .T. ) ;
#91450=DIRECTION ( 'NONE',  ( 0.000000000000000000, 0.000000000000000000, -1.000000000000000000 ) ) ;
#91458=AXIS2_PLACEMENT_3D ( 'NONE', #25290, #79579, #452 ) ;
#91459=DIRECTION ( 'NONE',  ( 0.000000000000000000, 1.000000000000000000, 0.000000000000000000 ) ) ;
#91476=PLANE ( 'NONE',  #63345 ) ;
#91498=ORIENTED_EDGE ( 'NONE', *, *, #73318, .F. ) ;
#91508=ORIENTED_EDGE ( 'NONE', *, *, #75096, .F. ) ;
#91509=CARTESIAN_POINT ( 'NONE',  ( 0.3910256410256418014, -6.376774720514418959, 20.67377804487179915 ) ) ;
#91513=CARTESIAN_POINT ( 'NONE',  ( 30.32108885906865936, -6.376774720514427841, 3.274824222184972822 ) ) ;
#91528=EDGE_CURVE ( 'NONE', #79185, #38725, #13457, .T. ) ;
#91535=CARTESIAN_POINT ( 'NONE',  ( 2.909586618535765723, -6.376774720514411854, 19.75512108203924200 ) ) ;
#91536=CARTESIAN_POINT ( 'NONE',  ( 3.116263380642223968, -5.876774720514402084, 18.40799819116699609 ) ) ;
#91560=DIRECTION ( 'NONE',  ( -0.000000000000000000, -1.000000000000000000, -0.000000000000000000 ) ) ;
#91563=CARTESIAN_POINT ( 'NONE',  ( -0.7067007548136460260, -6.376774720514410077, 19.51517878119693350 ) ) ;
#91564=CARTESIAN_POINT ( 'NONE',  ( -2.196420576317535289, -6.376774720514410077, 19.14926908420044782 ) ) ;
#91577=VECTOR ( 'NONE', #80407, 1000.000000000000000 ) ;
#91581=VERTEX_POINT ( 'NONE', #88605 ) ;
#91588=ADVANCED_FACE ( 'NONE', ( #81491 ), #67997, .T. ) ;
#91600=DIRECTION ( 'NONE',  ( 0.000000000000000000, -1.000000000000000000, 0.000000000000000000 ) ) ;
#91609=CARTESIAN_POINT ( 'NONE',  ( -2.806649551956928335, -6.376774720514411854, 19.35116211686183618 ) ) ;
#91613=ORIENTED_EDGE ( 'NONE', *, *, #52799, .F. ) ;
#91616=VECTOR ( 'NONE', #42807, 1000.000000000000114 ) ;
#91618=ORIENTED_EDGE ( 'NONE', *, *, #417, .T. ) ;
#91628=DIRECTION ( 'NONE',  ( -7.185047449708836111E-16, -0.000000000000000000, -1.000000000000000000 ) ) ;
#91634=CARTESIAN_POINT ( 'NONE',  ( -20.27875734969026311, -4.776774720514394446, 24.00402280011862288 ) ) ;
#91640=EDGE_CURVE ( 'NONE', #92630, #1389, #76348, .T. ) ;
#91661=CARTESIAN_POINT ( 'NONE',  ( -2.188401442307694289, -5.876774720514410077, 19.46153846153846700 ) ) ;
#91677=CYLINDRICAL_SURFACE ( 'NONE', #10738, 3.060000000000000053 ) ;
#91680=ORIENTED_EDGE ( 'NONE', *, *, #9226, .T. ) ;
#91682=DIRECTION ( 'NONE',  ( -0.000000000000000000, 1.000000000000000000, -0.000000000000000000 ) ) ;
#91683=CARTESIAN_POINT ( 'NONE',  ( 2.933277810221831761, -5.876774720514424288, 21.39432064584807947 ) ) ;
#91689=CARTESIAN_POINT ( 'NONE',  ( 31.18725089179298138, -4.540774720514433760, 2.579558749741450718 ) ) ;
#91694=DIRECTION ( 'NONE',  ( 0.000000000000000000, -1.000000000000000000, 0.000000000000000000 ) ) ;
#91698=CARTESIAN_POINT ( 'NONE',  ( 10.54059822343757702, -6.376774720514426953, 17.17691942396159988 ) ) ;
#91704=EDGE_CURVE ( 'NONE', #69556, #15899, #97132, .T. ) ;
#91706=AXIS2_PLACEMENT_3D ( 'NONE', #36317, #59666, #67277 ) ;
#91710=CARTESIAN_POINT ( 'NONE',  ( -28.98875734969026396, -3.316774720514426456, -0.08597719988137648983 ) ) ;
#91726=ORIENTED_EDGE ( 'NONE', *, *, #25014, .T. ) ;
#91741=CARTESIAN_POINT ( 'NONE',  ( -29.49875734969026198, -0.3587747205144265483, 2.362022800118626531 ) ) ;
#91743=CARTESIAN_POINT ( 'NONE',  ( 4.967620699791259753, -5.876774720514413630, 19.94530485585548973 ) ) ;
#91745=B_SPLINE_CURVE_WITH_KNOTS ( 'NONE', 3,
 ( #38973, #41361, #77026, #412, #39482, #920, #31872, #50472, #35750, #73314, #59591, #36247, #35252, #90029, #74304, #3810, #58100, #12394, #20501 ),
 .UNSPECIFIED., .F., .F.,
 ( 4, 1, 1, 1, 1, 1, 1, 1, 1, 1, 1, 1, 1, 1, 1, 1, 4 ),
 ( 0.000000000000000000, 0.07059928943359200515, 0.1379009210036200861, 0.2031961978097334975, 0.2667897246502631270, 0.3291063872214231578, 0.3906535452348600668, 0.4526530569344815458, 0.5157480403003722458, 0.5779263408004527980, 0.6389300116184465361, 0.6983507176418213280, 0.7572960374442707643, 0.8163937673501530101, 0.8762669096141296743, 0.9368171089060820522, 1.000000000000000000 ),
 .UNSPECIFIED. ) ;
#91758=ADVANCED_FACE ( 'NONE', ( #70753 ), #79354, .T. ) ;
#91759=CARTESIAN_POINT ( 'NONE',  ( 0.3910256410256418014, -5.876774720514418959, 20.67377804487179915 ) ) ;
#91760=ORIENTED_EDGE ( 'NONE', *, *, #23112, .T. ) ;
#91769=ORIENTED_EDGE ( 'NONE', *, *, #58309, .F. ) ;
#91774=LINE ( 'NONE', #6050, #88480 ) ;
#91812=FACE_OUTER_BOUND ( 'NONE', #1408, .T. ) ;
#91820=EDGE_CURVE ( 'NONE', #65974, #50219, #7962, .T. ) ;
#91828=DIRECTION ( 'NONE',  ( 0.000000000000000000, -1.000000000000000000, 0.000000000000000000 ) ) ;
#91840=EDGE_CURVE ( 'NONE', #23326, #95426, #25574, .T. ) ;
#91847=EDGE_CURVE ( 'NONE', #64651, #9578, #14472, .T. ) ;
#91851=ORIENTED_EDGE ( 'NONE', *, *, #4906, .F. ) ;
#91855=ORIENTED_EDGE ( 'NONE', *, *, #11907, .F. ) ;
#91864=CARTESIAN_POINT ( 'NONE',  ( 30.57258140252915979, 5.759614247572967471, 25.39586761113762137 ) ) ;
#91871=FACE_OUTER_BOUND ( 'NONE', #15677, .T. ) ;
#91884=CARTESIAN_POINT ( 'NONE',  ( 8.219458839706481612, -3.316774720514422015, -27.11006393991256758 ) ) ;
#91889=VECTOR ( 'NONE', #65462, 1000.000000000000000 ) ;
#91898=CARTESIAN_POINT ( 'NONE',  ( 14.43441819135840376, -3.316774720514426456, -28.36222020317694970 ) ) ;
#91902=B_SPLINE_SURFACE_WITH_KNOTS ( 'NONE', 3, 1, ( 
 ( #10661, #27876 ),
 ( #72075, #26882 ),
 ( #4555, #73070 ),
 ( #41621, #34500 ),
 ( #27385, #97391 ),
 ( #25883, #18759 ),
 ( #11153, #57852 ) ),
 .UNSPECIFIED., .F., .F., .F.,
 ( 4, 1, 1, 1, 4 ),
 ( 2, 2 ),
 ( 0.000000000000000000, 0.2193543708254379609, 0.4566051594240264633, 0.7164051918613062453, 1.000000000000000000 ),
 ( 0.000000000000000000, 1.000000000000000000 ),
 .UNSPECIFIED. ) ;
#91911=EDGE_LOOP ( 'NONE', ( #50448, #53296, #10818, #45344 ) ) ;
#91917=VECTOR ( 'NONE', #81060, 1000.000000000000000 ) ;
#91933=CARTESIAN_POINT ( 'NONE',  ( -1.345681049247692940, -5.876774720514410077, 19.69174559449348294 ) ) ;
#91943=EDGE_CURVE ( 'NONE', #17321, #31540, #13830, .T. ) ;
#91944=CARTESIAN_POINT ( 'NONE',  ( 7.155387812436688755, -5.321161431766062044, -25.57627477809911198 ) ) ;
#91976=ORIENTED_EDGE ( 'NONE', *, *, #98789, .T. ) ;
#91979=DIRECTION ( 'NONE',  ( -0.2488812114211667037, 0.000000000000000000, -0.9685340172660599212 ) ) ;
#91991=CARTESIAN_POINT ( 'NONE',  ( 31.84105487026594261, -5.152774720514426754, -11.95870468328485003 ) ) ;
#91997=CIRCLE ( 'NONE', #57991, 84.48086791635432746 ) ;
#92001=VERTEX_POINT ( 'NONE', #22432 ) ;
#92005=CARTESIAN_POINT ( 'NONE',  ( -7.243541020599075786, -6.376774720514408301, 19.27798293355755632 ) ) ;
#92006=AXIS2_PLACEMENT_3D ( 'NONE', #34142, #49373, #11788 ) ;
#92007=CARTESIAN_POINT ( 'NONE',  ( 5.314386400780318986, -0.3587747205143965723, -28.55951656536880989 ) ) ;
#92010=CARTESIAN_POINT ( 'NONE',  ( -0.9988807608215116707, -6.376774720514410077, 19.30497968945844889 ) ) ;
#92015=CARTESIAN_POINT ( 'NONE',  ( 31.41423154468143153, -2.682774720514426559, -0.3119954678742140053 ) ) ;
#92032=CARTESIAN_POINT ( 'NONE',  ( 22.81105451610979173, 8.475225279485572472, -18.46691820600746681 ) ) ;
#92035=CARTESIAN_POINT ( 'NONE',  ( 2.834823996951755465, -5.876774720514407413, 18.76222163777333307 ) ) ;
#92048=DIRECTION ( 'NONE',  ( -0.000000000000000000, 1.000000000000000000, -0.000000000000000000 ) ) ;
#92074=CARTESIAN_POINT ( 'NONE',  ( 29.73828978136053891, -5.356774720514425603, -4.021765098496561386 ) ) ;
#92075=CIRCLE ( 'NONE', #82371, 2.499999999999995115 ) ;
#92081=CARTESIAN_POINT ( 'NONE',  ( -0.001774553997815280816, -5.876774720514413630, 19.59623724171353487 ) ) ;
#92085=AXIS2_PLACEMENT_3D ( 'NONE', #86458, #222, #40289 ) ;
#92096=ORIENTED_EDGE ( 'NONE', *, *, #14221, .T. ) ;
#92097=CARTESIAN_POINT ( 'NONE',  ( 4.959895098850171102, -6.376774720514411854, 19.67755022954121813 ) ) ;
#92101=FACE_OUTER_BOUND ( 'NONE', #12868, .T. ) ;
#92103=VERTEX_POINT ( 'NONE', #99059 ) ;
#92109=CARTESIAN_POINT ( 'NONE',  ( -3.095730855174848362, -5.876774720514412742, 20.04377961306771638 ) ) ;
#92125=ORIENTED_EDGE ( 'NONE', *, *, #98205, .T. ) ;
#92129=CARTESIAN_POINT ( 'NONE',  ( 6.190876379491990988, -5.356774720513713284, -27.38145113946987408 ) ) ;
#92140=ORIENTED_EDGE ( 'NONE', *, *, #91840, .T. ) ;
#92141=CARTESIAN_POINT ( 'NONE',  ( 5.802984775641024662, -6.376774720514402972, 18.35026041666666430 ) ) ;
#92161=EDGE_CURVE ( 'NONE', #83403, #73995, #645, .T. ) ;
#92170=DIRECTION ( 'NONE',  ( 0.000000000000000000, 0.000000000000000000, 1.000000000000000000 ) ) ;
#92185=CARTESIAN_POINT ( 'NONE',  ( -28.98875734969026041, -0.3587747205144265483, 25.61802280011862720 ) ) ;
#92189=DIRECTION ( 'NONE',  ( -0.000000000000000000, 0.000000000000000000, 1.000000000000000000 ) ) ;
#92205=CARTESIAN_POINT ( 'NONE',  ( -5.824076695599092801, -6.376774720514411854, 19.72913074730691108 ) ) ;
#92214=CARTESIAN_POINT ( 'NONE',  ( -5.799455386767018439, -6.376774720514415407, 19.66076420632890276 ) ) ;
#92218=DIRECTION ( 'NONE',  ( 0.000000000000000000, -1.000000000000000000, 0.000000000000000000 ) ) ;
#92222=ORIENTED_EDGE ( 'NONE', *, *, #21906, .T. ) ;
#92223=ORIENTED_EDGE ( 'NONE', *, *, #95878, .T. ) ;
#92224=VERTEX_POINT ( 'NONE', #62026 ) ;
#92243=VECTOR ( 'NONE', #68232, 1000.000000000000000 ) ;
#92248=ORIENTED_EDGE ( 'NONE', *, *, #8796, .F. ) ;
#92249=CARTESIAN_POINT ( 'NONE',  ( 4.039061187531148178, -6.376774720514401196, 18.18637930035166761 ) ) ;
#92257=CARTESIAN_POINT ( 'NONE',  ( 9.940598223437577374, -5.876774720514426953, 22.08128695274315945 ) ) ;
#92264=ORIENTED_EDGE ( 'NONE', *, *, #88218, .T. ) ;
#92284=VECTOR ( 'NONE', #53290, 1000.000000000000000 ) ;
#92289=EDGE_CURVE ( 'NONE', #79731, #97458, #85856, .T. ) ;
#92291=FACE_OUTER_BOUND ( 'NONE', #42714, .T. ) ;
#92297=CARTESIAN_POINT ( 'NONE',  ( 15.32643653063177958, -2.682774720514426559, -27.14485409495429380 ) ) ;
#92321=DIRECTION ( 'NONE',  ( -1.000000000000000000, -0.000000000000000000, -5.238131417152343399E-15 ) ) ;
#92329=CARTESIAN_POINT ( 'NONE',  ( -17.97250661212648026, 5.965225279485594001, -23.43622901028613015 ) ) ;
#92334=ORIENTED_EDGE ( 'NONE', *, *, #32240, .F. ) ;
#92353=CIRCLE ( 'NONE', #27549, 15.00000000000000178 ) ;
#92359=LINE ( 'NONE', #93355, #52628 ) ;
#92361=ORIENTED_EDGE ( 'NONE', *, *, #16891, .T. ) ;
#92366=CARTESIAN_POINT ( 'NONE',  ( 26.51161204093744317, -5.098805221225331863, -7.190516857961198660 ) ) ;
#92369=EDGE_CURVE ( 'NONE', #52199, #67682, #11724, .T. ) ;
#92371=CARTESIAN_POINT ( 'NONE',  ( -9.543201319291914093E-14, -5.876774720514426953, 18.21871304725679508 ) ) ;
#92373=CYLINDRICAL_SURFACE ( 'NONE', #87427, 0.3000000000000016542 ) ;
#92384=CARTESIAN_POINT ( 'NONE',  ( -29.49875734969025842, 5.965225279485572685, 25.61802280011862720 ) ) ;
#92388=DIRECTION ( 'NONE',  ( 0.6599726524652352877, 0.000000000000000000, -0.7512896232465891000 ) ) ;
#92401=ADVANCED_FACE ( 'NONE', ( #37063 ), #22320, .F. ) ;
#92413=EDGE_CURVE ( 'NONE', #95239, #22543, #61502, .T. ) ;
#92425=LINE ( 'NONE', #100016, #37025 ) ;
#92428=CARTESIAN_POINT ( 'NONE',  ( -1.044871794871790938, -6.376774720514427841, 21.75000000000000355 ) ) ;
#92429=CARTESIAN_POINT ( 'NONE',  ( -1.390986686320385468, -5.876774720514414518, 19.62288733224860948 ) ) ;
#92440=LINE ( 'NONE', #61520, #83679 ) ;
#92442=LINE ( 'NONE', #24936, #35637 ) ;
#92445=VERTEX_POINT ( 'NONE', #76113 ) ;
#92448=LINE ( 'NONE', #15322, #93880 ) ;
#92449=CARTESIAN_POINT ( 'NONE',  ( 282.9764569301858046, 5.965225279485572685, 20.79159422840526616 ) ) ;
#92450=VERTEX_POINT ( 'NONE', #5115 ) ;
#92456=AXIS2_PLACEMENT_3D ( 'NONE', #58693, #97747, #98741 ) ;
#92467=VERTEX_POINT ( 'NONE', #22817 ) ;
#92477=CARTESIAN_POINT ( 'NONE',  ( 3.475076759263674209, -5.876774720514402084, 18.20843037655054530 ) ) ;
#92480=EDGE_CURVE ( 'NONE', #66723, #3925, #93737, .T. ) ;
#92483=ORIENTED_EDGE ( 'NONE', *, *, #40878, .T. ) ;
#92486=VECTOR ( 'NONE', #43383, 1000.000000000000000 ) ;
#92489=ADVANCED_FACE ( 'NONE', ( #69522 ), #2395, .T. ) ;
#92502=CARTESIAN_POINT ( 'NONE',  ( 0.000000000000000000, -4.132774720514426292, 0.000000000000000000 ) ) ;
#92503=CARTESIAN_POINT ( 'NONE',  ( 7.480769230769231726, -5.876774720514419847, 20.77403846153845635 ) ) ;
#92510=CARTESIAN_POINT ( 'NONE',  ( 30.93860345374796594, 6.475225279485573360, 20.86760796525322093 ) ) ;
#92519=EDGE_CURVE ( 'NONE', #5151, #38725, #77611, .T. ) ;
#92528=CARTESIAN_POINT ( 'NONE',  ( -24.55517127435777169, 5.965225279485592225, -15.44180958690142802 ) ) ;
#92548=CARTESIAN_POINT ( 'NONE',  ( 4.329581153495547063, -6.376774720514422512, 21.24220543808225869 ) ) ;
#92550=CARTESIAN_POINT ( 'NONE',  ( -29.49975734969026320, 6.475225279485571583, 13.17908622612278435 ) ) ;
#92552=CARTESIAN_POINT ( 'NONE',  ( 32.88562546571908740, -6.376774720514426953, -5.083907541707153754 ) ) ;
#92560=PLANE ( 'NONE',  #36194 ) ;
#92573=ORIENTED_EDGE ( 'NONE', *, *, #25317, .T. ) ;
#92574=CARTESIAN_POINT ( 'NONE',  ( 0.09189959430841809773, -6.376774720514410077, 19.67013632031035542 ) ) ;
#92587=DIRECTION ( 'NONE',  ( -1.334402673828313093E-16, 0.000000000000000000, -1.000000000000000000 ) ) ;
#92594=ORIENTED_EDGE ( 'NONE', *, *, #27030, .F. ) ;
#92600=ORIENTED_EDGE ( 'NONE', *, *, #73662, .F. ) ;
#92614=CARTESIAN_POINT ( 'NONE',  ( 4.593956459244529889, -6.376774720514410077, 19.29001220640957115 ) ) ;
#92615=ORIENTED_EDGE ( 'NONE', *, *, #26163, .T. ) ;
#92619=ORIENTED_EDGE ( 'NONE', *, *, #2081, .F. ) ;
#92621=CARTESIAN_POINT ( 'NONE',  ( 3.797776442307698286, -6.376774720514427841, 21.83974358974358410 ) ) ;
#92625=CARTESIAN_POINT ( 'NONE',  ( 30.00738719773716667, 1.477225279485574028, -9.049252915307089751 ) ) ;
#92626=DIRECTION ( 'NONE',  ( 0.000000000000000000, -0.7071067811865525687, 0.7071067811865425767 ) ) ;
#92630=VERTEX_POINT ( 'NONE', #59176 ) ;
#92656=CARTESIAN_POINT ( 'NONE',  ( -2.732037236150805626, -5.876774720514410077, 19.78976258633487717 ) ) ;
#92670=FACE_BOUND ( 'NONE', #67043, .T. ) ;
#92684=VECTOR ( 'NONE', #56518, 1000.000000000000000 ) ;
#92706=FACE_OUTER_BOUND ( 'NONE', #94987, .T. ) ;
#92711=EDGE_CURVE ( 'NONE', #83737, #80766, #60184, .T. ) ;
#92713=ORIENTED_EDGE ( 'NONE', *, *, #37752, .F. ) ;
#92721=ORIENTED_EDGE ( 'NONE', *, *, #34992, .F. ) ;
#92781=LINE ( 'NONE', #38506, #43430 ) ;
#92783=DIRECTION ( 'NONE',  ( 0.000000000000000000, 0.000000000000000000, 1.000000000000000000 ) ) ;
#92786=AXIS2_PLACEMENT_3D ( 'NONE', #47653, #87200, #16183 ) ;
#92799=CARTESIAN_POINT ( 'NONE',  ( 6.044871794871792048, -5.876774720514402084, 18.16025641025640880 ) ) ;
#92801=LINE ( 'NONE', #53763, #41608 ) ;
#92808=CARTESIAN_POINT ( 'NONE',  ( -26.91814428177455909, -6.376774720514426953, 29.98490496616818746 ) ) ;
#92810=ORIENTED_EDGE ( 'NONE', *, *, #16198, .T. ) ;
#92812=DIRECTION ( 'NONE',  ( -1.000000000000000000, -0.000000000000000000, 0.000000000000000000 ) ) ;
#92832=ORIENTED_EDGE ( 'NONE', *, *, #98096, .T. ) ;
#92853=AXIS2_PLACEMENT_3D ( 'NONE', #34764, #35273, #88058 ) ;
#92855=CARTESIAN_POINT ( 'NONE',  ( -5.023036858974361252, -6.376774720514410077, 19.14743589743590846 ) ) ;
#92866=CARTESIAN_POINT ( 'NONE',  ( 26.29690453849245912, -5.126799159439001663, -7.299189467990571778 ) ) ;
#92867=FACE_OUTER_BOUND ( 'NONE', #2786, .T. ) ;
#92872=DIRECTION ( 'NONE',  ( -0.6599726524652352877, 0.000000000000000000, 0.7512896232465891000 ) ) ;
#92873=B_SPLINE_SURFACE_WITH_KNOTS ( 'NONE', 3, 1, ( 
 ( #19933, #39410 ),
 ( #27567, #24177 ),
 ( #86080, #97065 ),
 ( #78958, #17066 ),
 ( #33290, #50902 ),
 ( #58519, #47533 ),
 ( #2868, #78455 ),
 ( #64277, #89456 ),
 ( #33800, #87591 ),
 ( #18071, #48543 ),
 ( #49041, #81842 ),
 ( #32296, #8958 ),
 ( #70871, #63267 ),
 ( #40416, #55652 ),
 ( #71372, #32796 ),
 ( #17571, #79469 ),
 ( #5214, #98547 ),
 ( #43294, #82336 ),
 ( #21416, #29043 ),
 ( #44783, #67136 ),
 ( #51900, #35674 ),
 ( #91433, #28542 ),
 ( #52393, #59511 ) ),
 .UNSPECIFIED., .F., .F., .F.,
 ( 4, 1, 1, 1, 1, 1, 1, 1, 1, 1, 1, 1, 1, 1, 1, 1, 1, 1, 1, 1, 4 ),
 ( 2, 2 ),
 ( 0.000000000000000000, 0.06003444026901250119, 0.1202779235945630187, 0.1823475613976146548, 0.2479191353524036190, 0.2816410472276386079, 0.3157005399103620658, 0.3503217567352117090, 0.3857031347924850806, 0.4218194746720334010, 0.4591956847073521697, 0.4978664178964332665, 0.5383012713842354469, 0.5812102302905466367, 0.6281834969011891312, 0.6794027672860705191, 0.7346986428153930992, 0.7940735398291317582, 0.8584163058134541835, 0.9270489341241319181, 1.000000000000000000 ),
 ( 0.000000000000000000, 1.000000000000000000 ),
 .UNSPECIFIED. ) ;
#92882=CARTESIAN_POINT ( 'NONE',  ( 2.905029696106983916, -5.876774720514415407, 20.12486936895525957 ) ) ;
#92885=EDGE_LOOP ( 'NONE', ( #29621, #68888, #93940, #25969 ) ) ;
#92887=AXIS2_PLACEMENT_3D ( 'NONE', #63085, #94011, #18395 ) ;
#92925=CARTESIAN_POINT ( 'NONE',  ( 6.274899854645557440, -6.376774720514429617, 21.83451738260096775 ) ) ;
#92940=CARTESIAN_POINT ( 'NONE',  ( -19.69812919673063689, -0.3587747205143964613, -22.00173861453436430 ) ) ;
#92941=B_SPLINE_SURFACE_WITH_KNOTS ( 'NONE', 3, 1, ( 
 ( #67726, #5804 ),
 ( #29139, #36761 ),
 ( #39123, #74324 ),
 ( #76299, #12910 ),
 ( #60114, #83418 ),
 ( #13905, #93403 ),
 ( #98140, #43876 ),
 ( #28154, #52993 ),
 ( #51490, #44381 ),
 ( #74809, #4815 ),
 ( #35769, #14405 ),
 ( #82426, #31513 ),
 ( #5305, #44884 ),
 ( #90049, #75804 ),
 ( #62476, #54867 ),
 ( #59607, #43386 ),
 ( #29640, #13408 ),
 ( #36264, #66738 ),
 ( #6306, #37262 ),
 ( #91535, #49270 ),
 ( #86304, #47250 ),
 ( #9684, #80197 ),
 ( #25908, #93911 ) ),
 .UNSPECIFIED., .F., .F., .F.,
 ( 4, 1, 1, 1, 1, 1, 1, 1, 1, 1, 1, 1, 1, 1, 1, 1, 1, 1, 1, 1, 4 ),
 ( 2, 2 ),
 ( 0.000000000000000000, 0.05968866615394263775, 0.1195065383498360445, 0.1810745839532865720, 0.2461623370263499311, 0.2798942139317999178, 0.3144679584461503863, 0.3504028635546707626, 0.3874736882805470684, 0.4261472450317768113, 0.4666236557295641019, 0.5087454666265019965, 0.5533282563676282795, 0.6000583194662235664, 0.6491770639906175866, 0.7005515754705256004, 0.7548938693300147884, 0.8118248696719926327, 0.8715135358259358256, 0.9343188020093610158, 1.000000000000000000 ),
 ( 0.000000000000000000, 1.000000000000000000 ),
 .UNSPECIFIED. ) ;
#92942=LINE ( 'NONE', #23418, #944 ) ;
#92946=EDGE_CURVE ( 'NONE', #50658, #84887, #51140, .T. ) ;
#92950=ORIENTED_EDGE ( 'NONE', *, *, #94861, .F. ) ;
#92973=EDGE_CURVE ( 'NONE', #1282, #47230, #78862, .T. ) ;
#92981=LINE ( 'NONE', #8260, #12487 ) ;
#92984=CARTESIAN_POINT ( 'NONE',  ( 6.365284455128204399, -5.876774720514413630, 19.73076923076922640 ) ) ;
#92987=VERTEX_POINT ( 'NONE', #25595 ) ;
#92993=ORIENTED_EDGE ( 'NONE', *, *, #92480, .F. ) ;
#92999=CARTESIAN_POINT ( 'NONE',  ( 7.370931459274800090, -6.376774720514417183, 20.26286690110499578 ) ) ;
#93018=EDGE_CURVE ( 'NONE', #404, #81766, #14548, .T. ) ;
#93022=DIRECTION ( 'NONE',  ( -0.9888510809027408754, -5.365801633547210331E-16, -0.1489078231574191558 ) ) ;
#93023=DIRECTION ( 'NONE',  ( -0.000000000000000000, 1.000000000000000000, -0.000000000000000000 ) ) ;
#93024=VERTEX_POINT ( 'NONE', #93592 ) ;
#93026=CARTESIAN_POINT ( 'NONE',  ( 3.714584954927674154, -5.876774720514403860, 18.16171433633635246 ) ) ;
#93028=CARTESIAN_POINT ( 'NONE',  ( -0.4909855769230799249, -6.376774720514410077, 19.14743589743590491 ) ) ;
#93029=DIRECTION ( 'NONE',  ( -1.000000000000000000, -0.000000000000000000, 0.000000000000000000 ) ) ;
#93033=VERTEX_POINT ( 'NONE', #24584 ) ;
#93053=CARTESIAN_POINT ( 'NONE',  ( 0.3545156366401029935, -5.876774720514414518, 20.17598923696321478 ) ) ;
#93055=EDGE_CURVE ( 'NONE', #65803, #27638, #2275, .T. ) ;
#93057=CARTESIAN_POINT ( 'NONE',  ( 5.802984775641024662, -5.876774720514403860, 18.35026041666666430 ) ) ;
#93059=CARTESIAN_POINT ( 'NONE',  ( 10.24059822343752479, -5.876774720514426953, -2.394817856121274864E-14 ) ) ;
#93064=CARTESIAN_POINT ( 'NONE',  ( -16.22218391600152643, 6.475225279485573360, -54.85883559227303863 ) ) ;
#93074=ADVANCED_FACE ( 'NONE', ( #35213 ), #13350, .T. ) ;
#93086=DIRECTION ( 'NONE',  ( 0.000000000000000000, 0.000000000000000000, 1.000000000000000000 ) ) ;
#93088=ORIENTED_EDGE ( 'NONE', *, *, #45668, .F. ) ;
#93089=CARTESIAN_POINT ( 'NONE',  ( 3.797776442307698286, -6.376774720514401196, 18.16025641025640525 ) ) ;
#93090=FACE_OUTER_BOUND ( 'NONE', #75895, .T. ) ;
#93099=EDGE_CURVE ( 'NONE', #35481, #58114, #73277, .T. ) ;
#93111=DIRECTION ( 'NONE',  ( 1.000000000000000000, -0.000000000000000000, 1.286817348990133655E-16 ) ) ;
#93115=CARTESIAN_POINT ( 'NONE',  ( 3.903461913076534451, -6.376774720514404748, 18.52532880998198905 ) ) ;
#93122=FACE_OUTER_BOUND ( 'NONE', #68059, .T. ) ;
#93143=VERTEX_POINT ( 'NONE', #51436 ) ;
#93180=EDGE_CURVE ( 'NONE', #83886, #93325, #65684, .T. ) ;
#93195=ADVANCED_FACE ( 'NONE', ( #58552 ), #26601, .T. ) ;
#93201=CARTESIAN_POINT ( 'NONE',  ( 4.572862496014544753, -5.876774720514408301, 19.20224321281611068 ) ) ;
#93208=LINE ( 'NONE', #39930, #54646 ) ;
#93215=CARTESIAN_POINT ( 'NONE',  ( 14.76093561896379214, 5.965225279485572685, -26.55548769130089681 ) ) ;
#93220=ORIENTED_EDGE ( 'NONE', *, *, #44517, .F. ) ;
#93225=ORIENTED_EDGE ( 'NONE', *, *, #93099, .T. ) ;
#93226=LINE ( 'NONE', #23716, #26641 ) ;
#93230=CARTESIAN_POINT ( 'NONE',  ( 4.486687842132109694, -5.876774720514410966, 18.98221446873611029 ) ) ;
#93235=ORIENTED_EDGE ( 'NONE', *, *, #98789, .F. ) ;
#93241=DIRECTION ( 'NONE',  ( 0.000000000000000000, 0.000000000000000000, -1.000000000000000000 ) ) ;
#93242=ORIENTED_EDGE ( 'NONE', *, *, #16638, .T. ) ;
#93243=CIRCLE ( 'NONE', #47909, 0.3000000000000016542 ) ;
#93245=DIRECTION ( 'NONE',  ( 7.726610339123061470E-14, 0.000000000000000000, -1.000000000000000000 ) ) ;
#93248=CARTESIAN_POINT ( 'NONE',  ( 4.782775879418006859, -6.376774720514406525, 18.83817099474236656 ) ) ;
#93258=EDGE_LOOP ( 'NONE', ( #98119, #98481, #97962, #26489 ) ) ;
#93259=VERTEX_POINT ( 'NONE', #22942 ) ;
#93262=ORIENTED_EDGE ( 'NONE', *, *, #92369, .T. ) ;
#93268=DIRECTION ( 'NONE',  ( -0.000000000000000000, -1.000000000000000000, -0.000000000000000000 ) ) ;
#93276=CARTESIAN_POINT ( 'NONE',  ( 10.46399479596396453, -2.682774720514426559, -27.03001098546561920 ) ) ;
#93286=PLANE ( 'NONE',  #8704 ) ;
#93290=PLANE ( 'NONE',  #50617 ) ;
#93291=VERTEX_POINT ( 'NONE', #7742 ) ;
#93305=EDGE_CURVE ( 'NONE', #54440, #42578, #75744, .T. ) ;
#93308=ORIENTED_EDGE ( 'NONE', *, *, #31345, .F. ) ;
#93315=CARTESIAN_POINT ( 'NONE',  ( -0.8502773128684013582, -6.376774720514413630, 19.61227901093089798 ) ) ;
#93325=VERTEX_POINT ( 'NONE', #6244 ) ;
#93327=CARTESIAN_POINT ( 'NONE',  ( 9.940598223437573822, -6.376774720514426953, 18.21871304725684837 ) ) ;
#93332=ORIENTED_EDGE ( 'NONE', *, *, #19602, .T. ) ;
#93343=ORIENTED_EDGE ( 'NONE', *, *, #7420, .F. ) ;
#93355=CARTESIAN_POINT ( 'NONE',  ( -3.106028565906091998, -6.376774720514426953, 3.106028565906120864 ) ) ;
#93365=CIRCLE ( 'NONE', #52893, 28.96799999999999642 ) ;
#93366=DIRECTION ( 'NONE',  ( -5.238131417152343399E-15, 0.000000000000000000, 1.000000000000000000 ) ) ;
#93368=DIRECTION ( 'NONE',  ( 0.000000000000000000, 0.000000000000000000, -1.000000000000000000 ) ) ;
#93372=ORIENTED_EDGE ( 'NONE', *, *, #79217, .T. ) ;
#93376=VECTOR ( 'NONE', #27733, 1000.000000000000000 ) ;
#93382=CARTESIAN_POINT ( 'NONE',  ( 9.278253834636473130, -5.876774720514426953, 21.78128695274316229 ) ) ;
#93390=VECTOR ( 'NONE', #11954, 1000.000000000000000 ) ;
#93391=CARTESIAN_POINT ( 'NONE',  ( 29.74624769612771402, -6.376774720514427841, 26.55905195464798396 ) ) ;
#93398=CARTESIAN_POINT ( 'NONE',  ( -5.063563723219555612, -5.876774720514409189, 19.46509473978807847 ) ) ;
#93403=CARTESIAN_POINT ( 'NONE',  ( 3.362850247043494001, -5.876774720514404748, 18.65880685207958223 ) ) ;
#93412=VECTOR ( 'NONE', #95118, 1000.000000000000114 ) ;
#93422=CARTESIAN_POINT ( 'NONE',  ( 30.93860345374796594, 5.965225279485572685, 28.07639619989136293 ) ) ;
#93432=CARTESIAN_POINT ( 'NONE',  ( 31.52563388547018874, -4.132774720514424516, -1.605328387144967728 ) ) ;
#93433=EDGE_LOOP ( 'NONE', ( #74309, #44139, #20126, #72177 ) ) ;
#93435=CARTESIAN_POINT ( 'NONE',  ( 8.090164212199763227, -5.215366374113139081, -25.84881406240220869 ) ) ;
#93453=EDGE_CURVE ( 'NONE', #98127, #20122, #131, .T. ) ;
#93463=CARTESIAN_POINT ( 'NONE',  ( -6.775140224358976226, -6.376774720514408301, 19.14743589743590846 ) ) ;
#93464=DIRECTION ( 'NONE',  ( -0.8264557562326033668, 6.845827386180409975E-16, -0.5630016722799281448 ) ) ;
#93467=ORIENTED_EDGE ( 'NONE', *, *, #21128, .T. ) ;
#93470=CARTESIAN_POINT ( 'NONE',  ( 0.3376760108279234784, -6.376774720514417183, 20.09898898868105732 ) ) ;
#93475=VECTOR ( 'NONE', #38085, 999.9999999999998863 ) ;
#93480=ORIENTED_EDGE ( 'NONE', *, *, #96911, .T. ) ;
#93481=CARTESIAN_POINT ( 'NONE',  ( 32.52533654608641456, -5.023480152701085721, -11.79063777444543781 ) ) ;
#93486=EDGE_CURVE ( 'NONE', #54063, #25694, #77734, .T. ) ;
#93490=B_SPLINE_CURVE_WITH_KNOTS ( 'NONE', 3,
 ( #13004, #43970, #83013, #84018 ),
 .UNSPECIFIED., .F., .F.,
 ( 4, 4 ),
 ( 0.008354480413380572026, 0.009203042238611652825 ),
 .UNSPECIFIED. ) ;
#93496=CARTESIAN_POINT ( 'NONE',  ( -6.901944873432418248, -6.376774720514410077, 19.15221817653406688 ) ) ;
#93500=CARTESIAN_POINT ( 'NONE',  ( 3.176458874063926352, 5.965225279485592225, -28.85257003503889095 ) ) ;
#93502=CARTESIAN_POINT ( 'NONE',  ( 7.477175500793984853, -5.876774720514417183, 20.66439772633092176 ) ) ;
#93503=DIRECTION ( 'NONE',  ( -0.000000000000000000, 1.000000000000000000, -0.000000000000000000 ) ) ;
#93515=DIRECTION ( 'NONE',  ( 0.000000000000000000, 0.000000000000000000, -1.000000000000000000 ) ) ;
#93520=LINE ( 'NONE', #100115, #17969 ) ;
#93521=CIRCLE ( 'NONE', #35242, 251.4258649670780699 ) ;
#93524=ORIENTED_EDGE ( 'NONE', *, *, #24946, .F. ) ;
#93525=CARTESIAN_POINT ( 'NONE',  ( -27.96875734969026084, -3.316774720514426456, 0.7300228001186309656 ) ) ;
#93549=VECTOR ( 'NONE', #25622, 1000.000000000000000 ) ;
#93550=CARTESIAN_POINT ( 'NONE',  ( -0.2112149364088803105, -5.876774720514410077, 19.49357334786886398 ) ) ;
#93556=CARTESIAN_POINT ( 'NONE',  ( -7.627782137226129855, -5.876774720514413630, 20.04377961306771994 ) ) ;
#93567=ORIENTED_EDGE ( 'NONE', *, *, #87604, .F. ) ;
#93568=AXIS2_PLACEMENT_3D ( 'NONE', #82682, #60375, #53250 ) ;
#93580=CIRCLE ( 'NONE', #25521, 27.94799999999999685 ) ;
#93585=DIRECTION ( 'NONE',  ( 0.000000000000000000, -1.000000000000000000, 0.000000000000000000 ) ) ;
#93588=CARTESIAN_POINT ( 'NONE',  ( 3.552794897967157528, -6.376774720514401196, 18.18650940196788568 ) ) ;
#93592=CARTESIAN_POINT ( 'NONE',  ( 26.73860345374794534, -5.058662225110310828, -7.113848178280766099 ) ) ;
#93618=LINE ( 'NONE', #62702, #17225 ) ;
#93619=CARTESIAN_POINT ( 'NONE',  ( -29.49875734969025842, -0.3587747205144265483, 17.86602280011862476 ) ) ;
#93624=ORIENTED_EDGE ( 'NONE', *, *, #49137, .F. ) ;
#93636=DIRECTION ( 'NONE',  ( 0.000000000000000000, 1.000000000000000000, 0.000000000000000000 ) ) ;
#93658=DIRECTION ( 'NONE',  ( 0.000000000000000000, 1.000000000000000000, 0.000000000000000000 ) ) ;
#93660=CARTESIAN_POINT ( 'NONE',  ( -4.929522925832171332, -6.376774720514426953, -28.63504101147569614 ) ) ;
#93667=CARTESIAN_POINT ( 'NONE',  ( -2.188401442307694289, -5.876774720514411854, 19.46153846153846700 ) ) ;
#93673=CARTESIAN_POINT ( 'NONE',  ( 13.91401389203221406, 6.475225279485573360, 27.24920385068457662 ) ) ;
#93676=EDGE_CURVE ( 'NONE', #1756, #13745, #42226, .T. ) ;
#93688=DIRECTION ( 'NONE',  ( -0.03244919754393515293, 0.000000000000000000, 0.9994733861282923959 ) ) ;
#93691=VERTEX_POINT ( 'NONE', #12731 ) ;
#93698=CARTESIAN_POINT ( 'NONE',  ( -2.762050907158362989, -6.376774720514415407, 19.89644244529369033 ) ) ;
#93702=CARTESIAN_POINT ( 'NONE',  ( 4.647383884978952828, -5.876774720514412742, 19.72975307774251164 ) ) ;
#93715=LINE ( 'NONE', #57189, #26567 ) ;
#93716=CARTESIAN_POINT ( 'NONE',  ( 9.543201319291914093E-14, -6.376774720514426953, 18.21871304725679508 ) ) ;
#93721=ORIENTED_EDGE ( 'NONE', *, *, #55776, .F. ) ;
#93727=FACE_OUTER_BOUND ( 'NONE', #20393, .T. ) ;
#93731=CARTESIAN_POINT ( 'NONE',  ( 4.653733606810938284, -6.376774720514411854, 19.95301661664751336 ) ) ;
#93736=ORIENTED_EDGE ( 'NONE', *, *, #86197, .T. ) ;
#93737=B_SPLINE_CURVE_WITH_KNOTS ( 'NONE', 3,
 ( #88630, #25719, #46691, #70013, #72909, #19099, #48582, #57198, #57685, #23832, #77110 ),
 .UNSPECIFIED., .F., .F.,
 ( 4, 1, 1, 1, 1, 1, 1, 1, 4 ),
 ( 0.000000000000000000, 0.1105883385953350950, 0.2245417540535963874, 0.3425034940501046066, 0.4643240984173571118, 0.5907560327017662427, 0.7222274753555133486, 0.8588428362087243695, 1.000000000000000000 ),
 .UNSPECIFIED. ) ;
#93739=ORIENTED_EDGE ( 'NONE', *, *, #12968, .F. ) ;
#93740=CARTESIAN_POINT ( 'NONE',  ( -28.98875734969026041, 5.965225279485572685, 25.61802280011862720 ) ) ;
#93748=ADVANCED_FACE ( 'NONE', ( #35598 ), #26484, .F. ) ;
#93768=ORIENTED_EDGE ( 'NONE', *, *, #29018, .T. ) ;
#93779=DIRECTION ( 'NONE',  ( 0.000000000000000000, 0.000000000000000000, -1.000000000000000000 ) ) ;
#93783=CARTESIAN_POINT ( 'NONE',  ( 11.19917779851249939, -2.682774720514424782, -27.04477526052296099 ) ) ;
#93798=CIRCLE ( 'NONE', #82423, 4.080000000000000071 ) ;
#93826=B_SPLINE_CURVE_WITH_KNOTS ( 'NONE', 3,
 ( #83580, #28305, #28803, #52147, #91689, #68372 ),
 .UNSPECIFIED., .F., .F.,
 ( 4, 2, 4 ),
 ( 0.002936590050694640099, 0.005175337996430707382, 0.007414085942166775967 ),
 .UNSPECIFIED. ) ;
#93827=EDGE_CURVE ( 'NONE', #28958, #40199, #30469, .T. ) ;
#93840=DIRECTION ( 'NONE',  ( 0.000000000000000000, 1.000000000000000000, 0.000000000000000000 ) ) ;
#93846=DIRECTION ( 'NONE',  ( -0.000000000000000000, 1.000000000000000000, -0.000000000000000000 ) ) ;
#93861=EDGE_CURVE ( 'NONE', #17304, #41475, #53484, .T. ) ;
#93872=DIRECTION ( 'NONE',  ( -0.4725087886537609472, 0.000000000000000000, -0.8813259582271223413 ) ) ;
#93876=PLANE ( 'NONE',  #2830 ) ;
#93880=VECTOR ( 'NONE', #13325, 1000.000000000000000 ) ;
#93887=ORIENTED_EDGE ( 'NONE', *, *, #64854, .F. ) ;
#93899=CARTESIAN_POINT ( 'NONE',  ( 31.61557479013570315, -6.410763075590560689, 26.52166531862750176 ) ) ;
#93904=DIRECTION ( 'NONE',  ( 1.000000000000000000, 0.000000000000000000, 0.000000000000000000 ) ) ;
#93911=CARTESIAN_POINT ( 'NONE',  ( 2.903846153846159517, -5.876774720514415407, 19.99999999999999289 ) ) ;
#93920=FACE_OUTER_BOUND ( 'NONE', #38531, .T. ) ;
#93933=LINE ( 'NONE', #16309, #17721 ) ;
#93940=ORIENTED_EDGE ( 'NONE', *, *, #76950, .T. ) ;
#93943=CARTESIAN_POINT ( 'NONE',  ( 8.524890150443020786, -5.131488666162827172, -25.99302514158824096 ) ) ;
#93947=AXIS2_PLACEMENT_3D ( 'NONE', #69996, #84716, #32437 ) ;
#93951=CARTESIAN_POINT ( 'NONE',  ( -2.806649551956928335, -5.876774720514411854, 19.35116211686183618 ) ) ;
#93957=ORIENTED_EDGE ( 'NONE', *, *, #14833, .F. ) ;
#93972=EDGE_CURVE ( 'NONE', #82993, #48082, #9635, .T. ) ;
#93977=CARTESIAN_POINT ( 'NONE',  ( 0.3545156366401029935, -6.376774720514413630, 20.17598923696321478 ) ) ;
#93991=EDGE_CURVE ( 'NONE', #6499, #57568, #71626, .T. ) ;
#93995=EDGE_LOOP ( 'NONE', ( #47592, #34957, #12782, #55200 ) ) ;
#93999=VERTEX_POINT ( 'NONE', #81652 ) ;
#94002=CARTESIAN_POINT ( 'NONE',  ( -7.640838998533831194, -6.376774720514417183, 20.32624910079993086 ) ) ;
#94003=AXIS2_PLACEMENT_3D ( 'NONE', #67054, #57448, #50322 ) ;
#94004=CARTESIAN_POINT ( 'NONE',  ( 6.698292889820671725, -6.376774720514424288, 21.80822233811499444 ) ) ;
#94009=ADVANCED_FACE ( 'NONE', ( #64957 ), #20140, .T. ) ;
#94010=CARTESIAN_POINT ( 'NONE',  ( 7.190659024148910561, -5.876774720514414518, 19.91543959911579620 ) ) ;
#94011=DIRECTION ( 'NONE',  ( 0.000000000000000000, 0.000000000000000000, 1.000000000000000000 ) ) ;
#94016=VECTOR ( 'NONE', #3923, 1000.000000000000000 ) ;
#94035=CARTESIAN_POINT ( 'NONE',  ( 4.931367317174526477, -6.376774720514420736, 20.61012727089847019 ) ) ;
#94038=EDGE_CURVE ( 'NONE', #32327, #99093, #44784, .T. ) ;
#94049=CARTESIAN_POINT ( 'NONE',  ( 3.206569032998081603, -6.376774720514424288, 21.19686455982786200 ) ) ;
#94065=AXIS2_PLACEMENT_3D ( 'NONE', #24486, #49352, #33108 ) ;
#94066=PRODUCT_DEFINITION ( 'UNKNOWN', '', #91188, #5341 ) ;
#94086=CARTESIAN_POINT ( 'NONE',  ( -4.312370003044874167, -5.876774720514409189, 19.42522865122897358 ) ) ;
#94092=CARTESIAN_POINT ( 'NONE',  ( 9.402885806365684829, 5.965225279485572685, 29.04108526060719342 ) ) ;
#94099=DIRECTION ( 'NONE',  ( 1.000000000000000000, -0.000000000000000000, 2.417950247244706201E-16 ) ) ;
#94105=FACE_OUTER_BOUND ( 'NONE', #12676, .T. ) ;
#94108=CARTESIAN_POINT ( 'NONE',  ( -28.98875734969026396, -0.3587747205144265483, 2.362022800118626531 ) ) ;
#94109=VERTEX_POINT ( 'NONE', #97427 ) ;
#94113=EDGE_CURVE ( 'NONE', #17980, #22949, #21777, .T. ) ;
#94119=ORIENTED_EDGE ( 'NONE', *, *, #95836, .T. ) ;
#94122=VERTEX_POINT ( 'NONE', #75570 ) ;
#94124=CARTESIAN_POINT ( 'NONE',  ( -65.05438548721848235, -6.376774720514426953, 29.49402280011861777 ) ) ;
#94125=CARTESIAN_POINT ( 'NONE',  ( 5.325188327271017208, -5.356774720514426491, -25.45818409267644711 ) ) ;
#94131=EDGE_CURVE ( 'NONE', #77609, #6499, #93365, .T. ) ;
#94134=ORIENTED_EDGE ( 'NONE', *, *, #91449, .F. ) ;
#94136=DIRECTION ( 'NONE',  ( 0.000000000000000000, 0.000000000000000000, -1.000000000000000000 ) ) ;
#94137=VERTEX_POINT ( 'NONE', #43645 ) ;
#94144=CARTESIAN_POINT ( 'NONE',  ( 15.38791554121732119, -3.579805417253313138, -28.27843079449244357 ) ) ;
#94160=CARTESIAN_POINT ( 'NONE',  ( -2.794871794871795156, -6.376774720514417183, 20.36318108974359475 ) ) ;
#94162=CARTESIAN_POINT ( 'NONE',  ( -65.05438548721848235, -6.376774720514426953, 0.7300228001186309656 ) ) ;
#94171=CARTESIAN_POINT ( 'NONE',  ( 12.40597316965629560, -5.152774720514427642, -26.28458722401733993 ) ) ;
#94173=CARTESIAN_POINT ( 'NONE',  ( 4.948119756536996761, -5.876774720514410077, 19.52858994054604125 ) ) ;
#94183=CYLINDRICAL_SURFACE ( 'NONE', #99347, 2.500000000000000444 ) ;
#94185=CARTESIAN_POINT ( 'NONE',  ( -27.15721599100127648, -0.3587747205144061757, -10.22292133548836723 ) ) ;
#94203=CARTESIAN_POINT ( 'NONE',  ( 282.9764569301858046, -6.376774720514426953, 20.79159422840526616 ) ) ;
#94222=VERTEX_POINT ( 'NONE', #62369 ) ;
#94228=ORIENTED_EDGE ( 'NONE', *, *, #68739, .T. ) ;
#94232=VECTOR ( 'NONE', #25808, 1000.000000000000000 ) ;
#94234=CARTESIAN_POINT ( 'NONE',  ( 4.413617546364139166, -5.876774720514407413, 18.86076033669171181 ) ) ;
#94236=ORIENTED_EDGE ( 'NONE', *, *, #77590, .F. ) ;
#94245=ORIENTED_EDGE ( 'NONE', *, *, #6926, .T. ) ;
#94249=VERTEX_POINT ( 'NONE', #61874 ) ;
#94251=CARTESIAN_POINT ( 'NONE',  ( -6.636054160061366503, -5.876774720514411854, 19.15289935703627933 ) ) ;
#94255=EDGE_CURVE ( 'NONE', #14282, #12529, #15682, .T. ) ;
#94256=DIRECTION ( 'NONE',  ( 0.000000000000000000, -1.000000000000000000, 0.000000000000000000 ) ) ;
#94264=VECTOR ( 'NONE', #9659, 1000.000000000000000 ) ;
#94265=DIRECTION ( 'NONE',  ( -0.9997753877537054468, 0.000000000000000000, 0.02119372647572819943 ) ) ;
#94272=CARTESIAN_POINT ( 'NONE',  ( -29.49875734969025842, -0.3587747205144262708, 23.37402280011862743 ) ) ;
#94285=FACE_OUTER_BOUND ( 'NONE', #58547, .T. ) ;
#94290=CARTESIAN_POINT ( 'NONE',  ( -0.02075734969026423599, 6.475225279485573360, -0.08597719988137648983 ) ) ;
#94293=CARTESIAN_POINT ( 'NONE',  ( 5.443272695963705665, -6.376774720514417183, 20.27301970143225418 ) ) ;
#94296=EDGE_LOOP ( 'NONE', ( #16968, #28613, #16684, #26994 ) ) ;
#94298=CARTESIAN_POINT ( 'NONE',  ( -5.988734693054777125, -5.876774720514415407, 19.95737465391042065 ) ) ;
#94311=DIRECTION ( 'NONE',  ( -0.000000000000000000, 1.000000000000000000, -0.000000000000000000 ) ) ;
#94316=CARTESIAN_POINT ( 'NONE',  ( 7.141559373243376641, -6.376774720514415407, 19.83742167145384983 ) ) ;
#94338=LINE ( 'NONE', #87227, #64739 ) ;
#94339=VERTEX_POINT ( 'NONE', #72987 ) ;
#94345=ORIENTED_EDGE ( 'NONE', *, *, #58807, .T. ) ;
#94347=FACE_OUTER_BOUND ( 'NONE', #52549, .T. ) ;
#94359=EDGE_CURVE ( 'NONE', #2589, #12603, #12061, .T. ) ;
#94361=CARTESIAN_POINT ( 'NONE',  ( 0.3085469314987323020, -6.376774720514413630, 19.52341893546493523 ) ) ;
#94389=CARTESIAN_POINT ( 'NONE',  ( 31.55302460176084978, -5.360765615368469739, -3.312397695011010335 ) ) ;
#94394=CARTESIAN_POINT ( 'NONE',  ( 2.976770017179964700, -6.376774720514420736, 20.68690469677381927 ) ) ;
#94402=CARTESIAN_POINT ( 'NONE',  ( 29.57907552799942508, -3.316774720514426456, 29.21818156447044501 ) ) ;
#94419=CARTESIAN_POINT ( 'NONE',  ( 30.93860345374796594, -0.6647747205144264315, 19.84760796525321780 ) ) ;
#94422=PLANE ( 'NONE',  #96646 ) ;
#94437=ADVANCED_FACE ( 'NONE', ( #5453 ), #59757, .F. ) ;
#94438=LINE ( 'NONE', #30536, #38090 ) ;
#94447=AXIS2_PLACEMENT_3D ( 'NONE', #53142, #91180, #67364 ) ;
#94468=EDGE_CURVE ( 'NONE', #41242, #23326, #19490, .T. ) ;
#94476=DIRECTION ( 'NONE',  ( -0.9976052577199500115, 0.000000000000000000, -0.06916465693916190594 ) ) ;
#94477=CARTESIAN_POINT ( 'NONE',  ( 4.653846153846159517, -6.376774720514415407, 19.99999999999999289 ) ) ;
#94483=CARTESIAN_POINT ( 'NONE',  ( 5.705253819860196529, -5.876774720514415407, 19.95963554344900714 ) ) ;
#94492=FACE_OUTER_BOUND ( 'NONE', #86744, .T. ) ;
#94498=EDGE_LOOP ( 'NONE', ( #18019, #19193, #32942, #17638, #50414, #34650, #73332, #7027, #69782, #27259, #21291, #81999, #62017, #90422, #63051, #57562, #91139, #18916, #67842, #54929 ) ) ;
#94500=EDGE_CURVE ( 'NONE', #11983, #42816, #66381, .T. ) ;
#94509=CARTESIAN_POINT ( 'NONE',  ( 6.467769777575680834, -6.376774720514427841, 21.83821538399986650 ) ) ;
#94510=CARTESIAN_POINT ( 'NONE',  ( 6.329711958793041049, -5.876774720514412742, 19.73172534246499765 ) ) ;
#94514=FACE_OUTER_BOUND ( 'NONE', #26378, .T. ) ;
#94518=AXIS2_PLACEMENT_3D ( 'NONE', #80594, #65406, #58274 ) ;
#94527=AXIS2_PLACEMENT_3D ( 'NONE', #90570, #66267, #12447 ) ;
#94532=CARTESIAN_POINT ( 'NONE',  ( -5.238752036864926964, -6.376774720514410077, 19.51517878119694061 ) ) ;
#94546=CARTESIAN_POINT ( 'NONE',  ( 3.296548071537245495, -6.376774720514426065, 21.29143507544719682 ) ) ;
#94552=CARTESIAN_POINT ( 'NONE',  ( 5.671135738765417322, -6.376774720514422512, 20.99074880795119924 ) ) ;
#94553=DIRECTION ( 'NONE',  ( -0.000000000000000000, 1.000000000000000000, -0.000000000000000000 ) ) ;
#94560=ORIENTED_EDGE ( 'NONE', *, *, #99520, .F. ) ;
#94563=AXIS2_PLACEMENT_3D ( 'NONE', #38993, #94780, #95289 ) ;
#94566=CARTESIAN_POINT ( 'NONE',  ( 5.271800844967073907, -6.376774720514426953, -28.56638892015272546 ) ) ;
#94580=CARTESIAN_POINT ( 'NONE',  ( 6.561060095583167495, -5.876774720514427841, 21.83518827598938117 ) ) ;
#94595=ORIENTED_EDGE ( 'NONE', *, *, #94500, .F. ) ;
#94600=CARTESIAN_POINT ( 'NONE',  ( 2.610950917001260141, -6.376774720514411854, 19.54489930512155027 ) ) ;
#94602=AXIS2_PLACEMENT_3D ( 'NONE', #94162, #62236, #17042 ) ;
#94612=CARTESIAN_POINT ( 'NONE',  ( 33.61456970919604714, 5.965225279485572685, -11.35828564741647462 ) ) ;
#94622=ORIENTED_EDGE ( 'NONE', *, *, #79461, .F. ) ;
#94627=ORIENTED_EDGE ( 'NONE', *, *, #52774, .T. ) ;
#94634=CARTESIAN_POINT ( 'NONE',  ( 29.80070917940689412, 6.475225279485573360, 27.39560796525321607 ) ) ;
#94643=CARTESIAN_POINT ( 'NONE',  ( -6.275748223059703257, -6.376774720514411854, 19.59984006504824805 ) ) ;
#94647=CARTESIAN_POINT ( 'NONE',  ( 0.7051282051282027341, -6.376774720514408301, 19.19230769230768985 ) ) ;
#94651=VERTEX_POINT ( 'NONE', #22653 ) ;
#94656=ORIENTED_EDGE ( 'NONE', *, *, #7752, .T. ) ;
#94672=DIRECTION ( 'NONE',  ( 0.000000000000000000, -1.000000000000000000, 0.000000000000000000 ) ) ;
#94684=PLANE ( 'NONE',  #10296 ) ;
#94689=CARTESIAN_POINT ( 'NONE',  ( 30.09341516180546350, 1.477225279485574028, -11.39311774897855933 ) ) ;
#94692=ADVANCED_FACE ( 'NONE', ( #32286 ), #91677, .F. ) ;
#94720=DIRECTION ( 'NONE',  ( 1.000000000000000000, 0.000000000000000000, 0.000000000000000000 ) ) ;
#94721=DIRECTION ( 'NONE',  ( 0.000000000000000000, 0.000000000000000000, -1.000000000000000000 ) ) ;
#94727=ORIENTED_EDGE ( 'NONE', *, *, #13673, .F. ) ;
#94729=CARTESIAN_POINT ( 'NONE',  ( -10.24059822343757808, -6.376774720514426953, 0.000000000000000000 ) ) ;
#94732=FACE_OUTER_BOUND ( 'NONE', #43832, .T. ) ;
#94736=CARTESIAN_POINT ( 'NONE',  ( 4.518205171808153509, -5.876774720514407413, 19.05004583296150500 ) ) ;
#94744=ORIENTED_EDGE ( 'NONE', *, *, #37643, .F. ) ;
#94748=DIRECTION ( 'NONE',  ( 1.000000000000000000, 0.000000000000000000, 0.000000000000000000 ) ) ;
#94749=DIRECTION ( 'NONE',  ( 0.000000000000000000, 1.000000000000000000, 0.000000000000000000 ) ) ;
#94751=ORIENTED_EDGE ( 'NONE', *, *, #667, .T. ) ;
#94756=VERTEX_POINT ( 'NONE', #7441 ) ;
#94763=DIRECTION ( 'NONE',  ( -0.000000000000000000, 1.000000000000000000, -0.000000000000000000 ) ) ;
#94764=AXIS2_PLACEMENT_3D ( 'NONE', #79476, #17073, #63783 ) ;
#94770=DIRECTION ( 'NONE',  ( 0.000000000000000000, 0.000000000000000000, -1.000000000000000000 ) ) ;
#94779=CARTESIAN_POINT ( 'NONE',  ( -25.92875734969025814, -3.316774720514426456, 0.7300228001186309656 ) ) ;
#94780=DIRECTION ( 'NONE',  ( -0.000000000000000000, -1.000000000000000000, -0.000000000000000000 ) ) ;
#94784=LINE ( 'NONE', #85677, #63161 ) ;
#94796=CARTESIAN_POINT ( 'NONE',  ( 5.329826657887789310, -6.376774720514418959, 20.66144943787464783 ) ) ;
#94798=FACE_OUTER_BOUND ( 'NONE', #79802, .T. ) ;
#94803=LINE ( 'NONE', #15679, #3782 ) ;
#94810=AXIS2_PLACEMENT_3D ( 'NONE', #42426, #27181, #73358 ) ;
#94815=CARTESIAN_POINT ( 'NONE',  ( 7.462166178408539352, 6.475225279485573360, -27.67315496249664974 ) ) ;
#94816=EDGE_CURVE ( 'NONE', #77603, #32014, #63768, .T. ) ;
#94821=DIRECTION ( 'NONE',  ( 0.000000000000000000, -1.000000000000000000, 0.000000000000000000 ) ) ;
#94822=CARTESIAN_POINT ( 'NONE',  ( 29.73860345376319003, 1.477225279485574028, -1.272392034746785860 ) ) ;
#94842=VERTEX_POINT ( 'NONE', #3364 ) ;
#94846=AXIS2_PLACEMENT_3D ( 'NONE', #88907, #11271, #64595 ) ;
#94848=DIRECTION ( 'NONE',  ( -0.9161084732596777025, 0.000000000000000000, 0.4009304992412306978 ) ) ;
#94850=VECTOR ( 'NONE', #83862, 1000.000000000000000 ) ;
#94861=EDGE_CURVE ( 'NONE', #41242, #28943, #40407, .T. ) ;
#94865=ORIENTED_EDGE ( 'NONE', *, *, #26195, .T. ) ;
#94874=CARTESIAN_POINT ( 'NONE',  ( 3.960462906497916435, -5.876774720514426953, 21.82884394085917279 ) ) ;
#94886=CARTESIAN_POINT ( 'NONE',  ( 31.29611288755342002, -5.755914996345237178, -2.011851919325042370 ) ) ;
#94891=LINE ( 'NONE', #26390, #6970 ) ;
#94896=EDGE_CURVE ( 'NONE', #90018, #7123, #65274, .T. ) ;
#94909=CARTESIAN_POINT ( 'NONE',  ( -4.993225604111834137, -0.3587747205143964613, -29.11654937215279304 ) ) ;
#94911=AXIS2_PLACEMENT_3D ( 'NONE', #22072, #76848, #5370 ) ;
#94920=EDGE_CURVE ( 'NONE', #40199, #4283, #34796, .T. ) ;
#94922=ORIENTED_EDGE ( 'NONE', *, *, #87867, .T. ) ;
#94923=VECTOR ( 'NONE', #93023, 1000.000000000000000 ) ;
#94925=DIRECTION ( 'NONE',  ( -1.000000000000000000, 0.000000000000000000, -0.000000000000000000 ) ) ;
#94928=VECTOR ( 'NONE', #65649, 1000.000000000000000 ) ;
#94931=CARTESIAN_POINT ( 'NONE',  ( 31.41423154468143153, -4.132774720514426292, -0.3119954678742140053 ) ) ;
#94938=VERTEX_POINT ( 'NONE', #74349 ) ;
#94939=LINE ( 'NONE', #42178, #5416 ) ;
#94942=CARTESIAN_POINT ( 'NONE',  ( 13.10664265030973930, -0.3587747205144256601, -28.18129937523770678 ) ) ;
#94950=ADVANCED_FACE ( 'NONE', ( #12444 ), #51022, .F. ) ;
#94957=PLANE ( 'NONE',  #44581 ) ;
#94971=VERTEX_POINT ( 'NONE', #84946 ) ;
#94982=CARTESIAN_POINT ( 'NONE',  ( 7.139069293134643779, -5.876774720514421624, 20.58118917620081945 ) ) ;
#94983=CARTESIAN_POINT ( 'NONE',  ( 5.627902640648289712, -5.876774720514413630, 20.02890049923285787 ) ) ;
#94987=EDGE_LOOP ( 'NONE', ( #123, #64066, #23727, #54602 ) ) ;
#95002=EDGE_CURVE ( 'NONE', #76045, #32852, #45902, .T. ) ;
#95019=CIRCLE ( 'NONE', #39899, 3.060000000000000497 ) ;
#95030=LINE ( 'NONE', #9282, #76124 ) ;
#95036=CARTESIAN_POINT ( 'NONE',  ( -5.382328594919684406, -5.876774720514411854, 19.61227901093090864 ) ) ;
#95038=EDGE_CURVE ( 'NONE', #79658, #8748, #38770, .T. ) ;
#95039=ORIENTED_EDGE ( 'NONE', *, *, #8668, .T. ) ;
#95040=CARTESIAN_POINT ( 'NONE',  ( 4.736659488006659480, -5.876774720514419847, 21.25082490164487581 ) ) ;
#95041=CARTESIAN_POINT ( 'NONE',  ( 31.79364159983995464, -6.376774720514426953, -11.59305536555894278 ) ) ;
#95042=VECTOR ( 'NONE', #21523, 1000.000000000000000 ) ;
#95046=ADVANCED_FACE ( 'NONE', ( #24041 ), #6331, .T. ) ;
#95061=CARTESIAN_POINT ( 'NONE',  ( 6.326958800731953048, -6.376774720514426065, 21.47849181751607972 ) ) ;
#95063=B_SPLINE_CURVE_WITH_KNOTS ( 'NONE', 3,
 ( #86566, #7937, #63247, #94171 ),
 .UNSPECIFIED., .F., .F.,
 ( 4, 4 ),
 ( 1.734723475976806902E-18, 0.002763707449907618768 ),
 .UNSPECIFIED. ) ;
#95069=CIRCLE ( 'NONE', #5908, 129.7684398600581517 ) ;
#95084=CARTESIAN_POINT ( 'NONE',  ( 7.475222833218381879, -5.876774720514418959, 20.91460388675487891 ) ) ;
#95095=CARTESIAN_POINT ( 'NONE',  ( 8.573524122111766843, 5.965225279485574461, -28.10203366675327175 ) ) ;
#95104=CARTESIAN_POINT ( 'NONE',  ( 2.628295812946869425, -6.376774720514411854, 19.40849182188139110 ) ) ;
#95109=CARTESIAN_POINT ( 'NONE',  ( -11.64875734969026233, 5.965225279485572685, 31.02402280011862246 ) ) ;
#95111=ORIENTED_EDGE ( 'NONE', *, *, #46604, .T. ) ;
#95113=CARTESIAN_POINT ( 'NONE',  ( 7.087697398486194622, -5.876774720514418959, 20.45710073441444621 ) ) ;
#95118=DIRECTION ( 'NONE',  ( -0.3133898629642186684, 4.164321980682960499E-15, 0.9496245541219267006 ) ) ;
#95119=CARTESIAN_POINT ( 'NONE',  ( -2.070328576748420524, -5.876774720514410966, 19.46575348430201657 ) ) ;
#95132=VECTOR ( 'NONE', #49463, 1000.000000000000000 ) ;
#95134=DIRECTION ( 'NONE',  ( 0.000000000000000000, 1.000000000000000000, 0.000000000000000000 ) ) ;
#95154=CARTESIAN_POINT ( 'NONE',  ( 31.73616390345410920, -3.909076239803030539, -3.851095480477756627 ) ) ;
#95192=VECTOR ( 'NONE', #50254, 1000.000000000000000 ) ;
#95197=CARTESIAN_POINT ( 'NONE',  ( 2.598243466966731585, -5.876774720514414518, 20.31174627870924709 ) ) ;
#95203=ORIENTED_EDGE ( 'NONE', *, *, #14542, .T. ) ;
#95208=DIRECTION ( 'NONE',  ( 0.000000000000000000, 1.000000000000000000, 0.000000000000000000 ) ) ;
#95209=VECTOR ( 'NONE', #59597, 1000.000000000000000 ) ;
#95211=CARTESIAN_POINT ( 'NONE',  ( 1.305682803664691249, 5.965225279485572685, 29.57950906855421991 ) ) ;
#95232=ORIENTED_EDGE ( 'NONE', *, *, #14721, .T. ) ;
#95233=VERTEX_POINT ( 'NONE', #60016 ) ;
#95234=ORIENTED_EDGE ( 'NONE', *, *, #66535, .T. ) ;
#95235=DIRECTION ( 'NONE',  ( 0.000000000000000000, 0.000000000000000000, -1.000000000000000000 ) ) ;
#95239=VERTEX_POINT ( 'NONE', #80845 ) ;
#95243=CARTESIAN_POINT ( 'NONE',  ( 4.281720980632043094, -5.876774720514409189, 18.71132571341777151 ) ) ;
#95247=CARTESIAN_POINT ( 'NONE',  ( 32.16024265030974050, 5.965225279485572685, 14.03360796525321774 ) ) ;
#95256=ORIENTED_EDGE ( 'NONE', *, *, #9570, .T. ) ;
#95257=EDGE_LOOP ( 'NONE', ( #2291, #40117, #26350, #73785, #24134, #60659, #89367, #70793, #17725, #61070 ) ) ;
#95260=CARTESIAN_POINT ( 'NONE',  ( 29.73860345376319358, -3.356774720514427379, 1.647607965253213180 ) ) ;
#95267=VECTOR ( 'NONE', #94672, 1000.000000000000000 ) ;
#95277=VERTEX_POINT ( 'NONE', #31037 ) ;
#95280=CARTESIAN_POINT ( 'NONE',  ( 30.61317826727886526, -3.861502214243257125, 27.24847364799711613 ) ) ;
#95282=CARTESIAN_POINT ( 'NONE',  ( -7.264088518202086675, -6.376774720514411854, 19.78976258633487717 ) ) ;
#95287=ORIENTED_EDGE ( 'NONE', *, *, #5015, .F. ) ;
#95288=CARTESIAN_POINT ( 'NONE',  ( 14.43441819135927950, 5.965225279485592225, -28.36222020317712378 ) ) ;
#95289=DIRECTION ( 'NONE',  ( 0.000000000000000000, 0.000000000000000000, -1.000000000000000000 ) ) ;
#95292=DIRECTION ( 'NONE',  ( -5.939352905686045343E-16, 0.000000000000000000, 1.000000000000000000 ) ) ;
#95295=DIRECTION ( 'NONE',  ( -0.4009304992412300317, -0.000000000000000000, -0.9161084732596779245 ) ) ;
#95302=DIRECTION ( 'NONE',  ( 0.000000000000000000, 0.000000000000000000, -1.000000000000000000 ) ) ;
#95324=DIRECTION ( 'NONE',  ( -0.1311553622875919756, 6.845827386180409975E-16, -0.9913618264504692190 ) ) ;
#95326=CARTESIAN_POINT ( 'NONE',  ( 7.402957069319889172, -6.376774720514418959, 20.34212842306459024 ) ) ;
#95328=LINE ( 'NONE', #12458, #44623 ) ;
#95329=LINE ( 'NONE', #49177, #77582 ) ;
#95330=ORIENTED_EDGE ( 'NONE', *, *, #84709, .F. ) ;
#95332=VECTOR ( 'NONE', #30530, 1000.000000000000000 ) ;
#95335=CARTESIAN_POINT ( 'NONE',  ( 4.885870204371583370, -6.376774720514420736, 20.85936027411790405 ) ) ;
#95343=LINE ( 'NONE', #22426, #95484 ) ;
#95345=ORIENTED_EDGE ( 'NONE', *, *, #21469, .T. ) ;
#95356=CARTESIAN_POINT ( 'NONE',  ( -19.80875734969026425, -0.3587747205144265483, 31.02402280011862246 ) ) ;
#95364=ORIENTED_EDGE ( 'NONE', *, *, #46115, .T. ) ;
#95365=CARTESIAN_POINT ( 'NONE',  ( -6.128026245051341192, -5.876774720514410077, 19.39236848396478763 ) ) ;
#95366=CARTESIAN_POINT ( 'NONE',  ( 3.248328688408994580, -5.876774720514406525, 18.75910638930973917 ) ) ;
#95371=CARTESIAN_POINT ( 'NONE',  ( 13.80377080874918150, -3.316774720514426900, -27.21172484903264532 ) ) ;
#95374=EDGE_CURVE ( 'NONE', #18993, #70394, #88438, .T. ) ;
#95381=PLANE ( 'NONE',  #82575 ) ;
#95382=CARTESIAN_POINT ( 'NONE',  ( -9.543201319291914093E-14, -6.376774720514426953, 18.21871304725679508 ) ) ;
#95383=EDGE_LOOP ( 'NONE', ( #94656, #84870, #75397, #761 ) ) ;
#95384=EDGE_CURVE ( 'NONE', #61485, #55194, #48285, .T. ) ;
#95397=CIRCLE ( 'NONE', #16223, 0.3000000000000016542 ) ;
#95401=ORIENTED_EDGE ( 'NONE', *, *, #18937, .T. ) ;
#95419=CARTESIAN_POINT ( 'NONE',  ( -1.358974358974357921, -6.376774720514420736, 20.75510817307693046 ) ) ;
#95423=CIRCLE ( 'NONE', #72686, 130.7884398600581335 ) ;
#95425=ADVANCED_FACE ( 'NONE', ( #81602 ), #12072, .F. ) ;
#95426=VERTEX_POINT ( 'NONE', #63017 ) ;
#95436=CARTESIAN_POINT ( 'NONE',  ( -7.635352852713973348, -5.876774720514416295, 20.14409848895066091 ) ) ;
#95437=VECTOR ( 'NONE', #96190, 1000.000000000000000 ) ;
#95447=DIRECTION ( 'NONE',  ( -6.267148949376405333E-16, 1.000000000000000000, 5.583826031377241668E-16 ) ) ;
#95451=DIRECTION ( 'NONE',  ( 0.000000000000000000, 0.000000000000000000, -1.000000000000000000 ) ) ;
#95455=DIRECTION ( 'NONE',  ( 0.000000000000000000, 0.000000000000000000, 1.000000000000000000 ) ) ;
#95464=ADVANCED_FACE ( 'NONE', ( #97323, #84085 ), #36917, .T. ) ;
#95484=VECTOR ( 'NONE', #72022, 1000.000000000000000 ) ;
#95487=CARTESIAN_POINT ( 'NONE',  ( 7.165897526731081157, -6.376774720514420736, 20.76279523443833597 ) ) ;
#95488=CARTESIAN_POINT ( 'NONE',  ( 5.495499487697820484, -5.876774720514418071, 20.18701882043406926 ) ) ;
#95492=ORIENTED_EDGE ( 'NONE', *, *, #11715, .T. ) ;
#95494=CARTESIAN_POINT ( 'NONE',  ( 2.589743589743596086, -5.876774720514419847, 20.00140224358974095 ) ) ;
#95500=CARTESIAN_POINT ( 'NONE',  ( 11.92750898180832131, -4.915819049120522699, -27.17522536519172860 ) ) ;
#95514=DIRECTION ( 'NONE',  ( -0.000000000000000000, 1.000000000000000000, -0.000000000000000000 ) ) ;
#95526=CARTESIAN_POINT ( 'NONE',  ( 13.03371494964462407, 6.475225279485575136, -27.13839018153349869 ) ) ;
#95537=DIRECTION ( 'NONE',  ( 0.000000000000000000, 1.000000000000000000, 0.000000000000000000 ) ) ;
#95541=ORIENTED_EDGE ( 'NONE', *, *, #44159, .F. ) ;
#95542=CARTESIAN_POINT ( 'NONE',  ( 4.638796026491669444, -5.876774720514423400, 21.40644651702305268 ) ) ;
#95548=VECTOR ( 'NONE', #7122, 1000.000000000000000 ) ;
#95550=AXIS2_PLACEMENT_3D ( 'NONE', #24073, #70761, #78353 ) ;
#95553=VECTOR ( 'NONE', #75401, 1000.000000000000000 ) ;
#95557=DIRECTION ( 'NONE',  ( -0.9952638024365005887, -0.000000000000000000, -0.09721092304694053943 ) ) ;
#95561=CARTESIAN_POINT ( 'NONE',  ( -41.32836283488544638, -2.682774720514426559, 39.26872235229541985 ) ) ;
#95570=CARTESIAN_POINT ( 'NONE',  ( 6.310942340984578180, -6.376774720514426953, -25.29254520177807208 ) ) ;
#95581=CARTESIAN_POINT ( 'NONE',  ( 7.403636664866980688, -6.376774720514424288, 21.18544102487025782 ) ) ;
#95585=CARTESIAN_POINT ( 'NONE',  ( -27.13414387080440093, 5.965225279485594001, -10.21530720150730254 ) ) ;
#95596=AXIS2_PLACEMENT_3D ( 'NONE', #106, #31045, #23935 ) ;
#95611=ADVANCED_FACE ( 'NONE', ( #30805 ), #47540, .F. ) ;
#95615=CARTESIAN_POINT ( 'NONE',  ( 6.963174204274080736, -5.876774720514416295, 20.29202897614545975 ) ) ;
#95616=CARTESIAN_POINT ( 'NONE',  ( 9.278253834636469577, -5.876774720514426953, 21.48128695274316158 ) ) ;
#95620=EDGE_CURVE ( 'NONE', #31086, #1896, #54160, .T. ) ;
#95625=VECTOR ( 'NONE', #65172, 1000.000000000000000 ) ;
#95628=PLANE ( 'NONE',  #89228 ) ;
#95632=AXIS2_PLACEMENT_3D ( 'NONE', #69698, #39236, #37252 ) ;
#95692=CARTESIAN_POINT ( 'NONE',  ( 16.15056352287343699, -5.152774720514406326, -27.77856273171769530 ) ) ;
#95695=CIRCLE ( 'NONE', #51951, 1.149999999999998135 ) ;
#95709=ADVANCED_FACE ( 'NONE', ( #72878 ), #19571, .F. ) ;
#95712=ORIENTED_EDGE ( 'NONE', *, *, #80065, .F. ) ;
#95725=ORIENTED_EDGE ( 'NONE', *, *, #12968, .T. ) ;
#95729=EDGE_LOOP ( 'NONE', ( #59447, #96133, #88262, #68600, #100088, #34216 ) ) ;
#95752=VERTEX_POINT ( 'NONE', #21555 ) ;
#95761=ORIENTED_EDGE ( 'NONE', *, *, #12155, .T. ) ;
#95777=CARTESIAN_POINT ( 'NONE',  ( 30.63451081005166543, -4.279369518130740069, 28.08236555530620038 ) ) ;
#95778=CARTESIAN_POINT ( 'NONE',  ( -6.905879715866854340, -6.376774720514411854, 19.48240003225459560 ) ) ;
#95781=DIRECTION ( 'NONE',  ( -0.9994733861282923959, 0.000000000000000000, -0.03244919754393515293 ) ) ;
#95782=VERTEX_POINT ( 'NONE', #35315 ) ;
#95783=CARTESIAN_POINT ( 'NONE',  ( 13.43165536947796213, 5.965225279485592225, -28.18099828186571187 ) ) ;
#95784=PLANE ( 'NONE',  #10332 ) ;
#95815=CARTESIAN_POINT ( 'NONE',  ( -2.794871794871795156, -5.876774720514418071, 20.36318108974359475 ) ) ;
#95816=ORIENTED_EDGE ( 'NONE', *, *, #1204, .F. ) ;
#95824=VERTEX_POINT ( 'NONE', #99182 ) ;
#95825=DIRECTION ( 'NONE',  ( -0.000000000000000000, 1.000000000000000000, -0.000000000000000000 ) ) ;
#95827=VECTOR ( 'NONE', #8436, 1000.000000000000000 ) ;
#95830=CARTESIAN_POINT ( 'NONE',  ( 4.966987340572156739, -6.376774720514417183, 20.16530235339958210 ) ) ;
#95836=EDGE_CURVE ( 'NONE', #8339, #81218, #100159, .T. ) ;
#95842=DIRECTION ( 'NONE',  ( -0.000000000000000000, -1.000000000000000000, -0.000000000000000000 ) ) ;
#95847=VERTEX_POINT ( 'NONE', #92074 ) ;
#95849=EDGE_CURVE ( 'NONE', #27638, #23749, #723, .T. ) ;
#95855=DIRECTION ( 'NONE',  ( -0.000000000000000000, 0.000000000000000000, -1.000000000000000000 ) ) ;
#95862=VERTEX_POINT ( 'NONE', #22545 ) ;
#95872=EDGE_CURVE ( 'NONE', #33316, #15357, #30678, .T. ) ;
#95878=EDGE_CURVE ( 'NONE', #75528, #40241, #84461, .T. ) ;
#95881=VERTEX_POINT ( 'NONE', #1242 ) ;
#95882=ORIENTED_EDGE ( 'NONE', *, *, #51660, .F. ) ;
#95883=ORIENTED_EDGE ( 'NONE', *, *, #53489, .T. ) ;
#95884=VECTOR ( 'NONE', #53018, 1000.000000000000000 ) ;
#95888=EDGE_CURVE ( 'NONE', #93691, #78770, #53036, .T. ) ;
#95893=CARTESIAN_POINT ( 'NONE',  ( 2.745953332610513442, -6.376774720514418959, 21.05053573504278575 ) ) ;
#95896=FACE_OUTER_BOUND ( 'NONE', #40282, .T. ) ;
#95902=DIRECTION ( 'NONE',  ( 0.000000000000000000, 1.000000000000000000, 0.000000000000000000 ) ) ;
#95908=CARTESIAN_POINT ( 'NONE',  ( 11.98973536156539943, -2.682774720514426559, -26.26140391504922178 ) ) ;
#95936=CARTESIAN_POINT ( 'NONE',  ( -7.491187506528125262, -5.876774720514410966, 19.53857357749109980 ) ) ;
#95959=B_SPLINE_CURVE_WITH_KNOTS ( 'NONE', 3,
 ( #25748, #910, #56215, #1920, #64341, #64847, #16622, #24736, #25240, #87144, #10518, #55215, #94251, #17633, #2420 ),
 .UNSPECIFIED., .F., .F.,
 ( 4, 1, 1, 1, 1, 1, 1, 1, 1, 1, 1, 1, 4 ),
 ( 0.000000000000000000, 0.07176606415833990116, 0.1412255357663689537, 0.2091158524974625343, 0.2748396534685271231, 0.3394829303752209260, 0.4024762667353996570, 0.4649418891713271162, 0.5268326406463837985, 0.6474148160608227398, 0.7655615117859490004, 0.8816150870393316685, 1.000000000000000000 ),
 .UNSPECIFIED. ) ;
#95985=AXIS2_PLACEMENT_3D ( 'NONE', #6906, #15508, #46473 ) ;
#95990=B_SPLINE_CURVE_WITH_KNOTS ( 'NONE', 3,
 ( #59267, #90213, #19686, #66404, #50166, #89220, #43051, #4490, #35437, #51154, #13073, #90711, #20189, #19194, #97327, #74971, #27814, #82103, #34930 ),
 .UNSPECIFIED., .F., .F.,
 ( 4, 1, 1, 1, 1, 1, 1, 1, 1, 1, 1, 1, 1, 1, 1, 1, 4 ),
 ( 0.000000000000000000, 0.06113791491562318298, 0.1199938438512138800, 0.1782253215076183839, 0.2362564202618999687, 0.2949293769549112820, 0.3547157488097555933, 0.4167296639241647727, 0.4806644084708298625, 0.5458317702108677061, 0.6097581054261674849, 0.6729712284742227490, 0.7360168691676642894, 0.7998393981920319806, 0.8647753566655687063, 0.9310876232725688872, 1.000000000000000000 ),
 .UNSPECIFIED. ) ;
#96004=VERTEX_POINT ( 'NONE', #87466 ) ;
#96005=ORIENTED_EDGE ( 'NONE', *, *, #52866, .F. ) ;
#96006=DIRECTION ( 'NONE',  ( -1.000000000000000000, 0.000000000000000000, 0.000000000000000000 ) ) ;
#96015=CARTESIAN_POINT ( 'NONE',  ( -12.65407072091355722, -6.376774720514426953, -26.15404995688569301 ) ) ;
#96018=CARTESIAN_POINT ( 'NONE',  ( 7.111284305517425075, -6.376774720514422512, 21.05363841023157434 ) ) ;
#96019=ORIENTED_EDGE ( 'NONE', *, *, #28187, .T. ) ;
#96026=LINE ( 'NONE', #58478, #62151 ) ;
#96039=CARTESIAN_POINT ( 'NONE',  ( -5.576843645946834016, -5.876774720514417183, 20.41272575174755133 ) ) ;
#96046=CARTESIAN_POINT ( 'NONE',  ( 0.000000000000000000, -2.056774720514426669, 0.000000000000000000 ) ) ;
#96050=ADVANCED_FACE ( 'NONE', ( #79847 ), #10848, .F. ) ;
#96059=CARTESIAN_POINT ( 'NONE',  ( 3.557932825399831689, -5.876774720514428729, 21.44518044978141091 ) ) ;
#96075=CARTESIAN_POINT ( 'NONE',  ( 10.16466294932649106, -6.376774720514429617, -24.98589889747637116 ) ) ;
#96082=AXIS2_PLACEMENT_3D ( 'NONE', #96176, #73340, #11929 ) ;
#96084=B_SPLINE_SURFACE_WITH_KNOTS ( 'NONE', 3, 1, ( 
 ( #16583, #39437 ),
 ( #70385, #84102 ),
 ( #92214, #22687 ),
 ( #99804, #68880 ),
 ( #54179, #100303 ),
 ( #77973, #30312 ),
 ( #53673, #875 ),
 ( #1386, #69885 ),
 ( #32320, #61787 ),
 ( #7472, #70895 ),
 ( #62286, #76478 ),
 ( #84605, #6984 ),
 ( #15092, #46059 ),
 ( #54670, #38432 ),
 ( #8487, #47059 ) ),
 .UNSPECIFIED., .F., .F., .F.,
 ( 4, 1, 1, 1, 1, 1, 1, 1, 1, 1, 1, 1, 4 ),
 ( 2, 2 ),
 ( 0.000000000000000000, 0.1041667992898066553, 0.1978560952899005576, 0.2832345117281488411, 0.3600126653135328203, 0.4338442080180757721, 0.5095057223304334526, 0.5870428909783838023, 0.6687538545127389433, 0.7511636688534690798, 0.8334676797015410088, 0.9158479811556834438, 1.000000000000000000 ),
 ( 0.000000000000000000, 1.000000000000000000 ),
 .UNSPECIFIED. ) ;
#96093=VECTOR ( 'NONE', #81399, 1000.000000000000000 ) ;
#96095=CARTESIAN_POINT ( 'NONE',  ( -28.98875734969026396, 5.965225279485572685, 7.870022800118625206 ) ) ;
#96102=CARTESIAN_POINT ( 'NONE',  ( 7.207151257207165429, 5.965225279485574461, -28.24477140324590252 ) ) ;
#96103=DIRECTION ( 'NONE',  ( -1.000000000000000000, -0.000000000000000000, 0.000000000000000000 ) ) ;
#96108=CARTESIAN_POINT ( 'NONE',  ( 33.12653832968937451, -6.376774720514426953, -7.315055336576590683 ) ) ;
#96118=CARTESIAN_POINT ( 'NONE',  ( -10.24059822343752479, -6.376774720514426953, -2.394817856121274864E-14 ) ) ;
#96122=AXIS2_PLACEMENT_3D ( 'NONE', #11695, #88840, #80217 ) ;
#96125=ADVANCED_FACE ( 'NONE', ( #41295 ), #2745, .T. ) ;
#96127=CARTESIAN_POINT ( 'NONE',  ( 33.28704981706498955, -4.441298812401576868, -11.58844794911118647 ) ) ;
#96132=CARTESIAN_POINT ( 'NONE',  ( 14.85834502026402681, -2.682774720514426559, -27.37203305628894867 ) ) ;
#96133=ORIENTED_EDGE ( 'NONE', *, *, #38917, .T. ) ;
#96134=VERTEX_POINT ( 'NONE', #64157 ) ;
#96140=LINE ( 'NONE', #97129, #91577 ) ;
#96151=FACE_OUTER_BOUND ( 'NONE', #75513, .T. ) ;
#96152=FACE_BOUND ( 'NONE', #2108, .T. ) ;
#96155=VERTEX_POINT ( 'NONE', #75228 ) ;
#96156=ORIENTED_EDGE ( 'NONE', *, *, #6382, .T. ) ;
#96166=VECTOR ( 'NONE', #16632, 1000.000000000000000 ) ;
#96167=FACE_OUTER_BOUND ( 'NONE', #55895, .T. ) ;
#96176=CARTESIAN_POINT ( 'NONE',  ( -29.49875734969026198, -0.3587747205144265483, 10.11402280011862587 ) ) ;
#96180=LINE ( 'NONE', #57625, #13930 ) ;
#96190=DIRECTION ( 'NONE',  ( 0.000000000000000000, 0.000000000000000000, -1.000000000000000000 ) ) ;
#96193=FACE_OUTER_BOUND ( 'NONE', #87647, .T. ) ;
#96196=ADVANCED_FACE ( 'NONE', ( #50912 ), #44490, .T. ) ;
#96201=VECTOR ( 'NONE', #67877, 1000.000000000000000 ) ;
#96204=CARTESIAN_POINT ( 'NONE',  ( 2.993365552154886089, -6.376774720514413630, 19.24059921568563425 ) ) ;
#96214=FACE_OUTER_BOUND ( 'NONE', #35615, .T. ) ;
#96217=EDGE_CURVE ( 'NONE', #58474, #99423, #88249, .T. ) ;
#96218=EDGE_LOOP ( 'NONE', ( #59425, #17239, #88634, #22251 ) ) ;
#96227=CARTESIAN_POINT ( 'NONE',  ( -5.891025641025639636, -6.376774720514420736, 20.75510817307693046 ) ) ;
#96253=CIRCLE ( 'NONE', #91314, 1.529999999999998916 ) ;
#96254=ORIENTED_EDGE ( 'NONE', *, *, #57243, .T. ) ;
#96272=ORIENTED_EDGE ( 'NONE', *, *, #57243, .F. ) ;
#96273=ORIENTED_EDGE ( 'NONE', *, *, #33751, .F. ) ;
#96295=CARTESIAN_POINT ( 'NONE',  ( -0.5218785734906133955, -6.376774720514410077, 19.14848118821636547 ) ) ;
#96301=LINE ( 'NONE', #49641, #89756 ) ;
#96303=DIRECTION ( 'NONE',  ( 0.000000000000000000, 0.000000000000000000, -1.000000000000000000 ) ) ;
#96328=CARTESIAN_POINT ( 'NONE',  ( 13.91401389203221406, -3.316774720514426456, 158.0376437107427137 ) ) ;
#96332=CARTESIAN_POINT ( 'NONE',  ( 3.825380556292953482, -6.376774720514427841, 21.83927723428477208 ) ) ;
#96335=VECTOR ( 'NONE', #27791, 1000.000000000000000 ) ;
#96340=B_SPLINE_CURVE_WITH_KNOTS ( 'NONE', 3,
 ( #71058, #13877, #1548, #61576, #15371, #53960 ),
 .UNSPECIFIED., .F., .F.,
 ( 4, 2, 4 ),
 ( 0.001731663773559744077, 0.004550964303235547140, 0.007370264832911350636 ),
 .UNSPECIFIED. ) ;
#96350=ORIENTED_EDGE ( 'NONE', *, *, #78709, .T. ) ;
#96358=CARTESIAN_POINT ( 'NONE',  ( -28.98875734969026041, -0.3587747205144265483, 17.86602280011862476 ) ) ;
#96362=CARTESIAN_POINT ( 'NONE',  ( 6.627987042499408510, -5.876774720514424288, 21.45334999081212146 ) ) ;
#96371=ORIENTED_EDGE ( 'NONE', *, *, #37515, .T. ) ;
#96380=CARTESIAN_POINT ( 'NONE',  ( 5.817949855437939632, -6.376774720514417183, 20.34349022145623209 ) ) ;
#96404=DIRECTION ( 'NONE',  ( 8.719066383522879804E-15, 0.000000000000000000, -1.000000000000000000 ) ) ;
#96407=EDGE_CURVE ( 'NONE', #65127, #70560, #3624, .T. ) ;
#96409=AXIS2_PLACEMENT_3D ( 'NONE', #17434, #25041, #31156 ) ;
#96440=ORIENTED_EDGE ( 'NONE', *, *, #70156, .F. ) ;
#96443=CARTESIAN_POINT ( 'NONE',  ( -5.576923076923074873, -6.376774720514427841, 21.75000000000000711 ) ) ;
#96450=AXIS2_PLACEMENT_3D ( 'NONE', #19592, #50553, #42954 ) ;
#96474=VERTEX_POINT ( 'NONE', #82226 ) ;
#96476=VERTEX_POINT ( 'NONE', #67518 ) ;
#96481=( BOUNDED_SURFACE ( )  B_SPLINE_SURFACE ( 3, 2, ( 
 ( #23102, #69801, #85513 ),
 ( #54091, #15004, #94125 ),
 ( #78892, #92129, #24113 ),
 ( #32226, #32730, #85012 ),
 ( #15997, #55085, #9391 ),
 ( #281, #23604, #70805 ),
 ( #15496, #55588, #31230 ),
 ( #46461, #54577, #24609 ),
 ( #40351, #62703, #45972 ),
 ( #77391, #86018, #46967 ),
 ( #70304, #63202, #86517 ),
 ( #78394, #39343, #784 ) ),
 .UNSPECIFIED., .F., .F., .T. ) 
 B_SPLINE_SURFACE_WITH_KNOTS ( ( 4, 2, 2, 2, 2, 4 ),
 ( 3, 3 ),
 ( -3.428680950268159222E-15, 0.001642567453077259246, 0.003285134906157947173, 0.004106418632698291028, 0.004927702359238635317, 0.006570269812319323027 ),
 ( 0.000000000000000000, 1.000000000000000000 ),
 .UNSPECIFIED. ) 
 GEOMETRIC_REPRESENTATION_ITEM ( )  RATIONAL_B_SPLINE_SURFACE ( (
 ( 1.000000000000000000, 0.7071067811865476838, 1.000000000000000000),
 ( 1.000000000000000000, 0.7071067811865476838, 1.000000000000000000),
 ( 1.000000000000000000, 0.7071067811865476838, 1.000000000000000000),
 ( 1.000000000000000000, 0.7071067811865476838, 1.000000000000000000),
 ( 1.000000000000000000, 0.7071067811865476838, 1.000000000000000000),
 ( 1.000000000000000000, 0.7071067811865476838, 1.000000000000000000),
 ( 1.000000000000000000, 0.7071067811865476838, 1.000000000000000000),
 ( 1.000000000000000000, 0.7071067811865476838, 1.000000000000000000),
 ( 1.000000000000000000, 0.7071067811865476838, 1.000000000000000000),
 ( 1.000000000000000000, 0.7071067811865476838, 1.000000000000000000),
 ( 1.000000000000000000, 0.7071067811865476838, 1.000000000000000000),
 ( 1.000000000000000000, 0.7071067811865476838, 1.000000000000000000) ) ) 
 REPRESENTATION_ITEM ( '' )  SURFACE ( )  );
#96482=ORIENTED_EDGE ( 'NONE', *, *, #81083, .T. ) ;
#96485=CARTESIAN_POINT ( 'NONE',  ( 5.327901167172695907, -6.376774720514418959, 20.73192761314082233 ) ) ;
#96489=CARTESIAN_POINT ( 'NONE',  ( 4.878909776184770742E-15, -5.876774720514426953, 22.50000000000000355 ) ) ;
#96511=DIRECTION ( 'NONE',  ( 0.000000000000000000, 0.000000000000000000, 1.000000000000000000 ) ) ;
#96513=CARTESIAN_POINT ( 'NONE',  ( -23.59123376470063960, 6.143225279485574397, 23.50402280011862288 ) ) ;
#96514=ORIENTED_EDGE ( 'NONE', *, *, #88072, .F. ) ;
#96520=ORIENTED_EDGE ( 'NONE', *, *, #52291, .F. ) ;
#96521=EDGE_CURVE ( 'NONE', #62694, #40793, #85773, .T. ) ;
#96530=B_SPLINE_CURVE_WITH_KNOTS ( 'NONE', 3,
 ( #12742, #97975, #83758, #44711 ),
 .UNSPECIFIED., .F., .F.,
 ( 4, 4 ),
 ( 1.788112030672749005E-18, 0.0002127494369525745788 ),
 .UNSPECIFIED. ) ;
#96534=CARTESIAN_POINT ( 'NONE',  ( -5.514838905578028694, -6.376774720514410077, 19.81240905262003338 ) ) ;
#96540=FACE_OUTER_BOUND ( 'NONE', #11190, .T. ) ;
#96541=CARTESIAN_POINT ( 'NONE',  ( 13.96165483782453087, -2.682774720514426114, -27.24025806393558824 ) ) ;
#96543=VERTEX_POINT ( 'NONE', #13202 ) ;
#96550=FACE_OUTER_BOUND ( 'NONE', #28655, .T. ) ;
#96554=CARTESIAN_POINT ( 'NONE',  ( 9.150000000000000355, -6.376774720514426953, -15.70000000000000284 ) ) ;
#96563=CARTESIAN_POINT ( 'NONE',  ( 8.159923944623203695, -3.316774720514428232, -28.14238247154670347 ) ) ;
#96565=CARTESIAN_POINT ( 'NONE',  ( -6.775140224358976226, -6.376774720514408301, 19.14743589743590846 ) ) ;
#96573=CIRCLE ( 'NONE', #46305, 2.500000000000000444 ) ;
#96577=FACE_OUTER_BOUND ( 'NONE', #89860, .T. ) ;
#96579=PLANE ( 'NONE',  #84168 ) ;
#96593=LINE ( 'NONE', #74260, #29809 ) ;
#96602=ORIENTED_EDGE ( 'NONE', *, *, #76504, .F. ) ;
#96607=DIRECTION ( 'NONE',  ( 0.000000000000000000, 0.000000000000000000, 1.000000000000000000 ) ) ;
#96609=CARTESIAN_POINT ( 'NONE',  ( -19.80875734969026425, -0.3587747205144265483, 31.02402280011862246 ) ) ;
#96615=ORIENTED_EDGE ( 'NONE', *, *, #43718, .F. ) ;
#96618=ORIENTED_EDGE ( 'NONE', *, *, #71139, .T. ) ;
#96627=CARTESIAN_POINT ( 'NONE',  ( 7.190659024148910561, -5.876774720514413630, 19.91543959911579620 ) ) ;
#96636=ORIENTED_EDGE ( 'NONE', *, *, #76342, .F. ) ;
#96642=CARTESIAN_POINT ( 'NONE',  ( 28.30015606816038698, -2.682774720514426559, -13.13501953239208930 ) ) ;
#96646=AXIS2_PLACEMENT_3D ( 'NONE', #70590, #1590, #40651 ) ;
#96649=VERTEX_POINT ( 'NONE', #38051 ) ;
#96653=AXIS2_PLACEMENT_3D ( 'NONE', #17488, #78870, #72789 ) ;
#96658=CARTESIAN_POINT ( 'NONE',  ( 2.598318274922708060, -6.376774720514413630, 19.68966562063331693 ) ) ;
#96676=DIRECTION ( 'NONE',  ( 0.000000000000000000, 0.000000000000000000, 1.000000000000000000 ) ) ;
#96677=LINE ( 'NONE', #19550, #95437 ) ;
#96681=CARTESIAN_POINT ( 'NONE',  ( -19.37210865224160017, -0.3587747205143967943, -21.60955166348796297 ) ) ;
#96685=CARTESIAN_POINT ( 'NONE',  ( 15.63775912259811918, -4.567193422985928564, -28.22903731538494299 ) ) ;
#96705=CARTESIAN_POINT ( 'NONE',  ( -29.49875734969026198, -0.3587747205144265483, 2.362022800118626531 ) ) ;
#96720=ORIENTED_EDGE ( 'NONE', *, *, #88684, .T. ) ;
#96721=VECTOR ( 'NONE', #77249, 1000.000000000000000 ) ;
#96722=CARTESIAN_POINT ( 'NONE',  ( -20.27875734969026311, -6.376774720514428729, 27.00402280011862288 ) ) ;
#96726=CIRCLE ( 'NONE', #88626, 130.2784398600581710 ) ;
#96738=AXIS2_PLACEMENT_3D ( 'NONE', #60972, #99502, #69578 ) ;
#96744=LINE ( 'NONE', #20609, #49109 ) ;
#96745=EDGE_CURVE ( 'NONE', #66223, #8977, #87433, .T. ) ;
#96767=VERTEX_POINT ( 'NONE', #42546 ) ;
#96772=DIRECTION ( 'NONE',  ( 0.000000000000000000, 0.000000000000000000, 1.000000000000000000 ) ) ;
#96775=CARTESIAN_POINT ( 'NONE',  ( -7.326695514711824231, -5.876774720514417183, 20.26757654895259719 ) ) ;
#96779=EDGE_CURVE ( 'NONE', #35328, #75907, #6605, .T. ) ;
#96780=ORIENTED_EDGE ( 'NONE', *, *, #57979, .T. ) ;
#96786=DIRECTION ( 'NONE',  ( 0.000000000000000000, 0.000000000000000000, 1.000000000000000000 ) ) ;
#96787=EDGE_CURVE ( 'NONE', #26613, #39625, #80926, .T. ) ;
#96801=CIRCLE ( 'NONE', #44952, 3.500000000000000000 ) ;
#96807=CARTESIAN_POINT ( 'NONE',  ( 9.940598223437573822, -5.876774720514426953, 21.78128695274315874 ) ) ;
#96823=DIRECTION ( 'NONE',  ( 0.000000000000000000, 0.000000000000000000, 1.000000000000000000 ) ) ;
#96841=EDGE_CURVE ( 'NONE', #33323, #76880, #94338, .T. ) ;
#96844=ORIENTED_EDGE ( 'NONE', *, *, #78757, .F. ) ;
#96853=EDGE_CURVE ( 'NONE', #95824, #33348, #55802, .T. ) ;
#96857=DIRECTION ( 'NONE',  ( 0.000000000000000000, 1.478457507934778393E-16, -1.000000000000000000 ) ) ;
#96858=LINE ( 'NONE', #97845, #86941 ) ;
#96861=CARTESIAN_POINT ( 'NONE',  ( 1.305682803664691249, -0.3587747205144265483, 29.57950906855421991 ) ) ;
#96868=CARTESIAN_POINT ( 'NONE',  ( 2.968164339864655332, -5.876774720514408301, 19.33154224050496595 ) ) ;
#96873=CARTESIAN_POINT ( 'NONE',  ( 12.20502328318355545, -3.316774720514426011, -28.10533714397569582 ) ) ;
#96881=CARTESIAN_POINT ( 'NONE',  ( 6.059061188053544988, -6.376774720514417183, 20.16803580207560742 ) ) ;
#96896=CARTESIAN_POINT ( 'NONE',  ( 2.708118538500707828, -6.376774720514424288, 20.94830092343283212 ) ) ;
#96907=CARTESIAN_POINT ( 'NONE',  ( 33.74607884027702909, -0.3587747205144265483, -4.999864028243830916 ) ) ;
#96911=EDGE_CURVE ( 'NONE', #40199, #63330, #54998, .T. ) ;
#96919=CARTESIAN_POINT ( 'NONE',  ( 4.653494883475234545, -5.876774720514415407, 20.13747874360300116 ) ) ;
#96924=ORIENTED_EDGE ( 'NONE', *, *, #99121, .T. ) ;
#96931=AXIS2_PLACEMENT_3D ( 'NONE', #86563, #75822, #42904 ) ;
#96940=CARTESIAN_POINT ( 'NONE',  ( 5.864225667603142789, -6.376774720514424288, 21.27837265517432996 ) ) ;
#96943=DIRECTION ( 'NONE',  ( 0.000000000000000000, -1.000000000000000000, 0.000000000000000000 ) ) ;
#96951=DIRECTION ( 'NONE',  ( 0.000000000000000000, 0.000000000000000000, 1.000000000000000000 ) ) ;
#96954=DIRECTION ( 'NONE',  ( 0.000000000000000000, -1.000000000000000000, 0.000000000000000000 ) ) ;
#96956=DIRECTION ( 'NONE',  ( 0.000000000000000000, 0.000000000000000000, -1.000000000000000000 ) ) ;
#96958=EDGE_LOOP ( 'NONE', ( #83340, #54583, #23066, #94134, #70441 ) ) ;
#96959=EDGE_CURVE ( 'NONE', #52438, #97248, #82512, .T. ) ;
#96965=EDGE_CURVE ( 'NONE', #26990, #62214, #19209, .T. ) ;
#96971=DIRECTION ( 'NONE',  ( -0.000000000000000000, 1.000000000000000000, -0.000000000000000000 ) ) ;
#96981=ORIENTED_EDGE ( 'NONE', *, *, #73318, .T. ) ;
#96987=CARTESIAN_POINT ( 'NONE',  ( 14.43441819133144044, -3.316774720514426900, -28.36222020317207182 ) ) ;
#96994=CIRCLE ( 'NONE', #32161, 1.836000000000000743 ) ;
#96998=FACE_OUTER_BOUND ( 'NONE', #99615, .T. ) ;
#97030=CARTESIAN_POINT ( 'NONE',  ( 32.50838937279095120, -1.682774720514426114, -10.74666623472941218 ) ) ;
#97035=ORIENTED_EDGE ( 'NONE', *, *, #30695, .F. ) ;
#97046=CARTESIAN_POINT ( 'NONE',  ( 33.65278273286722310, -3.366611878523314783, -11.65467467704458393 ) ) ;
#97047=CARTESIAN_POINT ( 'NONE',  ( 2.935461252226840401, -5.876774720514419847, 20.47627681611744777 ) ) ;
#97064=CARTESIAN_POINT ( 'NONE',  ( 15.97264540888995299, -3.316774720514426456, -27.93485543958162154 ) ) ;
#97065=CARTESIAN_POINT ( 'NONE',  ( 3.902919446070569176, -5.876774720514426953, 21.47497695444087284 ) ) ;
#97068=CARTESIAN_POINT ( 'NONE',  ( 7.460719433876314532, -6.376774720514426953, -25.14146935902945046 ) ) ;
#97070=CARTESIAN_POINT ( 'NONE',  ( -7.603582339867426043, -6.376774720514417183, 19.86545874326176175 ) ) ;
#97072=VERTEX_POINT ( 'NONE', #43561 ) ;
#97077=VECTOR ( 'NONE', #16094, 1000.000000000000000 ) ;
#97081=CARTESIAN_POINT ( 'NONE',  ( 9.843544857143434967, 5.965225279485572685, -27.49819965379373343 ) ) ;
#97083=DIRECTION ( 'NONE',  ( 7.994117400814786717E-16, 0.000000000000000000, -1.000000000000000000 ) ) ;
#97085=ORIENTED_EDGE ( 'NONE', *, *, #74532, .T. ) ;
#97087=CARTESIAN_POINT ( 'NONE',  ( -1.733151984336291695, -6.376774720514408301, 19.29154511076646017 ) ) ;
#97091=CARTESIAN_POINT ( 'NONE',  ( 30.55775998287478856, 1.765878758506263635, 24.49934028559108157 ) ) ;
#97112=DIRECTION ( 'NONE',  ( 0.000000000000000000, 0.000000000000000000, -1.000000000000000000 ) ) ;
#97116=CARTESIAN_POINT ( 'NONE',  ( 29.73612274945269718, -5.099749465620300626, 27.18845636319765191 ) ) ;
#97120=DIRECTION ( 'NONE',  ( 0.000000000000000000, 0.000000000000000000, 1.000000000000000000 ) ) ;
#97123=DIRECTION ( 'NONE',  ( -0.000000000000000000, 1.000000000000000000, -0.000000000000000000 ) ) ;
#97128=ORIENTED_EDGE ( 'NONE', *, *, #9557, .T. ) ;
#97129=CARTESIAN_POINT ( 'NONE',  ( -20.27875734969026311, 7.743225279485574042, 26.25402280011862288 ) ) ;
#97130=PLANE ( 'NONE',  #7721 ) ;
#97132=CIRCLE ( 'NONE', #11226, 0.3000000000000016542 ) ;
#97152=LINE ( 'NONE', #9036, #46535 ) ;
#97154=CIRCLE ( 'NONE', #1550, 3.349999999999998757 ) ;
#97172=CARTESIAN_POINT ( 'NONE',  ( -2.704906987277317931, -6.376774720514425177, -28.92935364444904778 ) ) ;
#97179=FACE_OUTER_BOUND ( 'NONE', #8153, .T. ) ;
#97195=DIRECTION ( 'NONE',  ( 0.000000000000000000, -1.000000000000000000, 0.000000000000000000 ) ) ;
#97209=CARTESIAN_POINT ( 'NONE',  ( 29.77147767949874435, -6.376774720514426953, 26.15915692125051706 ) ) ;
#97213=CARTESIAN_POINT ( 'NONE',  ( -3.826923076923074429, -5.876774720514426953, 21.75000000000000355 ) ) ;
#97214=ADVANCED_FACE ( 'NONE', ( #90729 ), #67907, .T. ) ;
#97222=VECTOR ( 'NONE', #28639, 1000.000000000000000 ) ;
#97226=DIRECTION ( 'NONE',  ( -0.06283980576413537855, 0.000000000000000000, -0.9980236263794188822 ) ) ;
#97231=ORIENTED_EDGE ( 'NONE', *, *, #27341, .T. ) ;
#97234=DIRECTION ( 'NONE',  ( 0.000000000000000000, 1.000000000000000000, 0.000000000000000000 ) ) ;
#97236=EDGE_CURVE ( 'NONE', #67798, #28943, #36121, .T. ) ;
#97242=LINE ( 'NONE', #57695, #93376 ) ;
#97243=ORIENTED_EDGE ( 'NONE', *, *, #85339, .T. ) ;
#97244=DIRECTION ( 'NONE',  ( 0.000000000000000000, -1.000000000000000000, 0.000000000000000000 ) ) ;
#97248=VERTEX_POINT ( 'NONE', #10354 ) ;
#97250=ORIENTED_EDGE ( 'NONE', *, *, #22863, .F. ) ;
#97251=CARTESIAN_POINT ( 'NONE',  ( 30.13760268648183782, -5.267913728810161622, 19.84760796525321425 ) ) ;
#97257=CARTESIAN_POINT ( 'NONE',  ( -27.96875734969026084, 6.143225279485573509, 0.7300228001186309656 ) ) ;
#97259=EDGE_CURVE ( 'NONE', #18022, #8339, #64677, .T. ) ;
#97273=EDGE_CURVE ( 'NONE', #11836, #99971, #51807, .T. ) ;
#97277=CARTESIAN_POINT ( 'NONE',  ( 32.66876533700882845, 5.965225279485572685, -12.58926540598385557 ) ) ;
#97280=DIRECTION ( 'NONE',  ( 1.000000000000000000, 0.000000000000000000, 0.000000000000000000 ) ) ;
#97306=CARTESIAN_POINT ( 'NONE',  ( 30.09341516180546350, 1.477225279485574028, -13.89311774897855933 ) ) ;
#97310=CARTESIAN_POINT ( 'NONE',  ( 32.73857899460460175, 6.475225279485576024, -13.20677013500359820 ) ) ;
#97312=EDGE_CURVE ( 'NONE', #96476, #79708, #64011, .T. ) ;
#97319=DIRECTION ( 'NONE',  ( -1.000000000000000000, -0.000000000000000000, -5.238131417152343399E-15 ) ) ;
#97320=ORIENTED_EDGE ( 'NONE', *, *, #9441, .T. ) ;
#97322=DIRECTION ( 'NONE',  ( -0.5473052603538086647, -0.000000000000000000, -0.8369330630277725946 ) ) ;
#97323=FACE_BOUND ( 'NONE', #3037, .T. ) ;
#97326=VERTEX_POINT ( 'NONE', #34206 ) ;
#97327=CARTESIAN_POINT ( 'NONE',  ( 6.199338013146583393, -6.376774720514415407, 20.11757922567734980 ) ) ;
#97333=DIRECTION ( 'NONE',  ( -0.9496245541219264785, 6.845827386180410961E-16, -0.3133898629642195011 ) ) ;
#97337=EDGE_CURVE ( 'NONE', #56850, #24103, #26590, .T. ) ;
#97339=EDGE_CURVE ( 'NONE', #37998, #16727, #35201, .T. ) ;
#97348=ORIENTED_EDGE ( 'NONE', *, *, #79386, .F. ) ;
#97352=EDGE_CURVE ( 'NONE', #36415, #2798, #40518, .T. ) ;
#97361=LINE ( 'NONE', #34465, #20435 ) ;
#97363=ORIENTED_EDGE ( 'NONE', *, *, #57005, .F. ) ;
#97366=EDGE_LOOP ( 'NONE', ( #11644, #22353, #39326, #13611, #36943, #75352, #94345, #69168 ) ) ;
#97381=LINE ( 'NONE', #89770, #46385 ) ;
#97391=CARTESIAN_POINT ( 'NONE',  ( 0.3085469314987323020, -5.876774720514413630, 19.52341893546493523 ) ) ;
#97392=ORIENTED_EDGE ( 'NONE', *, *, #70799, .F. ) ;
#97395=DIRECTION ( 'NONE',  ( -0.000000000000000000, -1.000000000000000000, -0.000000000000000000 ) ) ;
#97402=LINE ( 'NONE', #27888, #22505 ) ;
#97407=CARTESIAN_POINT ( 'NONE',  ( 32.16024265030974050, 5.965225279485572685, 16.27760796525321751 ) ) ;
#97415=DIRECTION ( 'NONE',  ( -1.611864046919725738E-15, -0.000000000000000000, -1.000000000000000000 ) ) ;
#97424=EDGE_CURVE ( 'NONE', #41475, #62694, #85641, .T. ) ;
#97426=ADVANCED_FACE ( 'NONE', ( #28086 ), #59039, .T. ) ;
#97427=CARTESIAN_POINT ( 'NONE',  ( 3.797776442307698286, -6.376774720514401196, 18.16025641025640525 ) ) ;
#97430=CARTESIAN_POINT ( 'NONE',  ( -10.31943567505730996, -5.151096386430394247, 28.35664311630200984 ) ) ;
#97434=ORIENTED_EDGE ( 'NONE', *, *, #77697, .F. ) ;
#97442=CYLINDRICAL_SURFACE ( 'NONE', #15953, 2.249999999999998668 ) ;
#97448=ORIENTED_EDGE ( 'NONE', *, *, #1936, .F. ) ;
#97451=CARTESIAN_POINT ( 'NONE',  ( 8.978253834636468866, -6.376774720514426953, 21.48128695274316158 ) ) ;
#97452=CARTESIAN_POINT ( 'NONE',  ( 30.57287095715020087, 6.475225279485571583, 25.41160796525326404 ) ) ;
#97458=VERTEX_POINT ( 'NONE', #11681 ) ;
#97460=VERTEX_POINT ( 'NONE', #56890 ) ;
#97489=CARTESIAN_POINT ( 'NONE',  ( 28.20688450243646272, -5.356774720514425603, -7.073367244510395224 ) ) ;
#97498=ORIENTED_EDGE ( 'NONE', *, *, #62267, .F. ) ;
#97499=VERTEX_POINT ( 'NONE', #58383 ) ;
#97504=CARTESIAN_POINT ( 'NONE',  ( -6.033988668995577065, -5.876774720514413630, 19.86422795159478483 ) ) ;
#97511=CARTESIAN_POINT ( 'NONE',  ( 7.041152093163508319, -5.876774720514423400, 21.17127001373575368 ) ) ;
#97513=CARTESIAN_POINT ( 'NONE',  ( 29.77147767949874435, -6.376774720514426953, 26.15915692125051706 ) ) ;
#97515=ORIENTED_EDGE ( 'NONE', *, *, #93991, .T. ) ;
#97517=CARTESIAN_POINT ( 'NONE',  ( 10.24966870126729646, 6.475225279485571583, -27.02528057709740850 ) ) ;
#97527=EDGE_CURVE ( 'NONE', #3028, #92001, #19789, .T. ) ;
#97534=CARTESIAN_POINT ( 'NONE',  ( 4.115044103975469270, -6.376774720514427841, 21.79213183355573946 ) ) ;
#97541=ORIENTED_EDGE ( 'NONE', *, *, #43781, .T. ) ;
#97544=CARTESIAN_POINT ( 'NONE',  ( 3.036358173076929123, -5.876774720514420736, 20.87990785256409865 ) ) ;
#97548=CARTESIAN_POINT ( 'NONE',  ( -1.409217194013772101, -6.376774720514417183, 20.11414146978959749 ) ) ;
#97550=DIRECTION ( 'NONE',  ( -0.000000000000000000, -1.000000000000000000, -0.000000000000000000 ) ) ;
#97551=DIRECTION ( 'NONE',  ( -0.000000000000000000, -1.000000000000000000, -0.000000000000000000 ) ) ;
#97553=CARTESIAN_POINT ( 'NONE',  ( 14.76093561896379214, 6.475225279485573360, -26.55548769130089681 ) ) ;
#97565=CARTESIAN_POINT ( 'NONE',  ( 12.30588647384254841, -6.376774720514765349, -28.11066263748569227 ) ) ;
#97577=CARTESIAN_POINT ( 'NONE',  ( 14.52511747680497933, 5.965225279485572685, -27.86035006098926559 ) ) ;
#97580=DIRECTION ( 'NONE',  ( -0.000000000000000000, -1.000000000000000000, -0.000000000000000000 ) ) ;
#97597=DIRECTION ( 'NONE',  ( 0.9888510809027409865, 7.885106708985486076E-16, 0.1489078231574183231 ) ) ;
#97607=DIRECTION ( 'NONE',  ( 0.000000000000000000, 0.000000000000000000, -1.000000000000000000 ) ) ;
#97608=DIRECTION ( 'NONE',  ( 0.000000000000000000, 0.000000000000000000, 1.000000000000000000 ) ) ;
#97621=CARTESIAN_POINT ( 'NONE',  ( 9.278253834636473130, -5.876774720514426953, 18.21871304725684482 ) ) ;
#97625=CARTESIAN_POINT ( 'NONE',  ( 7.141559373243376641, -6.376774720514415407, 19.83742167145384983 ) ) ;
#97641=CARTESIAN_POINT ( 'NONE',  ( 29.71903944837828604, -4.668615314384465087, 27.69752233256919993 ) ) ;
#97654=CARTESIAN_POINT ( 'NONE',  ( 2.590388488674697953, -5.876774720514416295, 19.94764386045124027 ) ) ;
#97666=DIRECTION ( 'NONE',  ( 0.000000000000000000, -1.000000000000000000, 0.000000000000000000 ) ) ;
#97672=DIRECTION ( 'NONE',  ( -0.000000000000000000, 1.000000000000000000, -0.000000000000000000 ) ) ;
#97678=LINE ( 'NONE', #34295, #5123 ) ;
#97679=EDGE_CURVE ( 'NONE', #35661, #93691, #30034, .T. ) ;
#97687=VECTOR ( 'NONE', #98533, 1000.000000000000000 ) ;
#97689=CARTESIAN_POINT ( 'NONE',  ( 3.559170184186323915, -6.376774720514402972, 18.55412939673608719 ) ) ;
#97691=CARTESIAN_POINT ( 'NONE',  ( 7.344278919687202922, -6.376774720514417183, 20.19896341048075783 ) ) ;
#97699=CARTESIAN_POINT ( 'NONE',  ( -2.457093156980370452, -6.376774720514411854, 19.51167604195716976 ) ) ;
#97703=CARTESIAN_POINT ( 'NONE',  ( 0.3908843598833069422, -5.876774720514419847, 20.63520656483649773 ) ) ;
#97717=AXIS2_PLACEMENT_3D ( 'NONE', #51262, #19794, #35544 ) ;
#97720=EDGE_CURVE ( 'NONE', #17929, #87231, #100160, .T. ) ;
#97733=DIRECTION ( 'NONE',  ( 0.000000000000000000, 0.000000000000000000, -1.000000000000000000 ) ) ;
#97747=DIRECTION ( 'NONE',  ( -0.000000000000000000, 1.000000000000000000, -0.000000000000000000 ) ) ;
#97763=EDGE_LOOP ( 'NONE', ( #29053, #40977, #57100 ) ) ;
#97764=CARTESIAN_POINT ( 'NONE',  ( -10.27747606359964117, -6.067502657846070235, 28.80925224784997596 ) ) ;
#97766=FACE_OUTER_BOUND ( 'NONE', #80799, .T. ) ;
#97767=ORIENTED_EDGE ( 'NONE', *, *, #34030, .F. ) ;
#97774=LINE ( 'NONE', #84917, #94923 ) ;
#97776=CIRCLE ( 'NONE', #13530, 28.96799999999999287 ) ;
#97780=CARTESIAN_POINT ( 'NONE',  ( -1.222978892338334012, -5.876774720514411854, 19.56655654527324373 ) ) ;
#97791=VECTOR ( 'NONE', #83291, 1000.000000000000114 ) ;
#97796=DIRECTION ( 'NONE',  ( 0.000000000000000000, 0.000000000000000000, -1.000000000000000000 ) ) ;
#97807=DIRECTION ( 'NONE',  ( 0.7071067811865474617, 0.000000000000000000, 0.7071067811865474617 ) ) ;
#97818=ADVANCED_FACE ( 'NONE', ( #48288 ), #54394, .F. ) ;
#97828=CARTESIAN_POINT ( 'NONE',  ( 6.467769777575680834, -5.876774720514426953, 21.83821538399986650 ) ) ;
#97832=EDGE_LOOP ( 'NONE', ( #30751, #88745, #36101, #77119 ) ) ;
#97834=ORIENTED_EDGE ( 'NONE', *, *, #46571, .T. ) ;
#97841=VERTEX_POINT ( 'NONE', #62506 ) ;
#97845=CARTESIAN_POINT ( 'NONE',  ( -27.83739072329610664, -0.3587747205143967943, -8.084349702057700426 ) ) ;
#97849=ORIENTED_EDGE ( 'NONE', *, *, #34428, .F. ) ;
#97873=ORIENTED_EDGE ( 'NONE', *, *, #74757, .F. ) ;
#97879=CARTESIAN_POINT ( 'NONE',  ( -1.064504969004270052, -5.876774720514408301, 19.35667676486395905 ) ) ;
#97897=EDGE_CURVE ( 'NONE', #2798, #64622, #69693, .T. ) ;
#97899=FACE_OUTER_BOUND ( 'NONE', #18198, .T. ) ;
#97912=ADVANCED_FACE ( 'NONE', ( #57910 ), #43178, .F. ) ;
#97916=ORIENTED_EDGE ( 'NONE', *, *, #91235, .F. ) ;
#97924=CARTESIAN_POINT ( 'NONE',  ( -10.79305683637731228, -0.3587747205144057872, -27.49869550653261285 ) ) ;
#97929=VERTEX_POINT ( 'NONE', #97451 ) ;
#97933=CARTESIAN_POINT ( 'NONE',  ( -11.64875734969026233, 5.965225279485572685, 31.02402280011862246 ) ) ;
#97937=EDGE_CURVE ( 'NONE', #32607, #27420, #66537, .T. ) ;
#97949=CARTESIAN_POINT ( 'NONE',  ( 3.794707603699265519E-15, -6.376774720514426953, 17.50000000000000000 ) ) ;
#97956=ORIENTED_EDGE ( 'NONE', *, *, #34194, .F. ) ;
#97958=CARTESIAN_POINT ( 'NONE',  ( 32.53346577320679245, -0.6027747205144262654, -11.93731717363830747 ) ) ;
#97960=ORIENTED_EDGE ( 'NONE', *, *, #42796, .F. ) ;
#97962=ORIENTED_EDGE ( 'NONE', *, *, #68126, .T. ) ;
#97965=CARTESIAN_POINT ( 'NONE',  ( 14.58759568486751235, -3.520387117353680484, -28.38990263572715733 ) ) ;
#97974=ADVANCED_FACE ( 'NONE', ( #56911 ), #18820, .T. ) ;
#97975=CARTESIAN_POINT ( 'NONE',  ( 32.90495245295455362, -3.622774720514437607, -13.06061886496134861 ) ) ;
#97984=LINE ( 'NONE', #91378, #83077 ) ;
#97985=ORIENTED_EDGE ( 'NONE', *, *, #24513, .T. ) ;
#97988=CARTESIAN_POINT ( 'NONE',  ( 0.000000000000000000, 1.477225279485574028, 19.84760796525321425 ) ) ;
#97993=PLANE ( 'NONE',  #44911 ) ;
#97997=DIRECTION ( 'NONE',  ( -0.000000000000000000, 1.000000000000000000, -0.000000000000000000 ) ) ;
#98005=DIRECTION ( 'NONE',  ( -1.000000000000000000, -8.334928612639484546E-17, 0.000000000000000000 ) ) ;
#98011=CARTESIAN_POINT ( 'NONE',  ( -29.49875734969025842, 5.965225279485572685, 15.62202280011862321 ) ) ;
#98015=DIRECTION ( 'NONE',  ( -0.000000000000000000, 1.000000000000000000, -0.000000000000000000 ) ) ;
#98020=DIRECTION ( 'NONE',  ( 0.000000000000000000, 0.000000000000000000, 1.000000000000000000 ) ) ;
#98026=EDGE_CURVE ( 'NONE', #35495, #63790, #36543, .T. ) ;
#98043=DIRECTION ( 'NONE',  ( -6.938893903907241788E-15, 0.000000000000000000, 1.000000000000000000 ) ) ;
#98047=FACE_OUTER_BOUND ( 'NONE', #83025, .T. ) ;
#98050=DIRECTION ( 'NONE',  ( 1.000000000000000000, 0.000000000000000000, 0.000000000000000000 ) ) ;
#98055=ORIENTED_EDGE ( 'NONE', *, *, #64696, .T. ) ;
#98057=CARTESIAN_POINT ( 'NONE',  ( 5.994920710892026605, -6.376774720514429617, 21.76186867112717138 ) ) ;
#98062=CYLINDRICAL_SURFACE ( 'NONE', #49252, 2.249999999999998668 ) ;
#98082=DIRECTION ( 'NONE',  ( 0.000000000000000000, 0.000000000000000000, -1.000000000000000000 ) ) ;
#98086=VECTOR ( 'NONE', #42861, 1000.000000000000000 ) ;
#98089=ORIENTED_EDGE ( 'NONE', *, *, #23752, .F. ) ;
#98096=EDGE_CURVE ( 'NONE', #67044, #67306, #38831, .T. ) ;
#98097=DIRECTION ( 'NONE',  ( -0.000000000000000000, -1.000000000000000000, -0.000000000000000000 ) ) ;
#98099=ORIENTED_EDGE ( 'NONE', *, *, #49029, .T. ) ;
#98119=ORIENTED_EDGE ( 'NONE', *, *, #45259, .F. ) ;
#98123=DIRECTION ( 'NONE',  ( -0.000000000000000000, -1.000000000000000000, -0.000000000000000000 ) ) ;
#98124=ORIENTED_EDGE ( 'NONE', *, *, #26435, .F. ) ;
#98127=VERTEX_POINT ( 'NONE', #46672 ) ;
#98131=CARTESIAN_POINT ( 'NONE',  ( 30.64109438017208120, -3.316774720514426456, 28.31981406664616330 ) ) ;
#98140=CARTESIAN_POINT ( 'NONE',  ( 3.296033061219842519, -6.376774720514406525, 18.71226942120119574 ) ) ;
#98152=EDGE_CURVE ( 'NONE', #67539, #86043, #27505, .T. ) ;
#98155=AXIS2_PLACEMENT_3D ( 'NONE', #6234, #29570, #60548 ) ;
#98158=DIRECTION ( 'NONE',  ( -0.7682573101345352429, 0.000000000000000000, 0.6401411605457412168 ) ) ;
#98159=CARTESIAN_POINT ( 'NONE',  ( 4.653846153846159517, -6.376774720514415407, 19.99999999999999289 ) ) ;
#98162=DIRECTION ( 'NONE',  ( 1.000000000000000000, 0.000000000000000000, 0.000000000000000000 ) ) ;
#98181=DIRECTION ( 'NONE',  ( 0.6599726524652352877, 0.000000000000000000, -0.7512896232465891000 ) ) ;
#98182=CARTESIAN_POINT ( 'NONE',  ( -2.243088942307695177, -5.876774720514409189, 19.14743589743590491 ) ) ;
#98188=DIRECTION ( 'NONE',  ( -0.000000000000000000, -1.000000000000000000, -0.000000000000000000 ) ) ;
#98205=EDGE_CURVE ( 'NONE', #35967, #99333, #4873, .T. ) ;
#98206=CARTESIAN_POINT ( 'NONE',  ( -9.278253834636469577, -5.876774720514426953, 18.51871304725684553 ) ) ;
#98211=ORIENTED_EDGE ( 'NONE', *, *, #79267, .F. ) ;
#98217=ORIENTED_EDGE ( 'NONE', *, *, #6718, .F. ) ;
#98218=CARTESIAN_POINT ( 'NONE',  ( -2.492070857093962921, -6.376774720514408301, 19.17707164986947177 ) ) ;
#98220=EDGE_CURVE ( 'NONE', #68551, #66723, #37191, .T. ) ;
#98225=DIRECTION ( 'NONE',  ( -0.000000000000000000, -1.000000000000000000, -0.000000000000000000 ) ) ;
#98235=ORIENTED_EDGE ( 'NONE', *, *, #35823, .F. ) ;
#98238=CARTESIAN_POINT ( 'NONE',  ( 31.50024378385495893, -5.449202613762975211, -3.047402719862319032 ) ) ;
#98241=CARTESIAN_POINT ( 'NONE',  ( 32.16024265030974050, 5.965225279485572685, 16.27760796525321751 ) ) ;
#98244=VERTEX_POINT ( 'NONE', #59270 ) ;
#98248=CIRCLE ( 'NONE', #18800, 1.325999999999969647 ) ;
#98253=FACE_OUTER_BOUND ( 'NONE', #83502, .T. ) ;
#98254=VERTEX_POINT ( 'NONE', #98816 ) ;
#98258=LINE ( 'NONE', #20146, #50069 ) ;
#98269=DIRECTION ( 'NONE',  ( 0.000000000000000000, -0.7071067811865513475, -0.7071067811865436870 ) ) ;
#98295=VECTOR ( 'NONE', #25944, 1000.000000000000000 ) ;
#98306=DIRECTION ( 'NONE',  ( 0.000000000000000000, -1.000000000000000000, 0.000000000000000000 ) ) ;
#98310=EDGE_CURVE ( 'NONE', #15278, #2149, #49266, .T. ) ;
#98314=CARTESIAN_POINT ( 'NONE',  ( 6.184520403203631389, -5.356774720514425603, -25.32021290018218451 ) ) ;
#98322=DIRECTION ( 'NONE',  ( 5.328431011793917330E-15, 0.000000000000000000, 1.000000000000000000 ) ) ;
#98348=ADVANCED_FACE ( 'NONE', ( #2884 ), #79487, .F. ) ;
#98350=VERTEX_POINT ( 'NONE', #26203 ) ;
#98365=CARTESIAN_POINT ( 'NONE',  ( 5.642884982650352654, -6.376774720514426065, 20.85668005806743608 ) ) ;
#98367=ORIENTED_EDGE ( 'NONE', *, *, #54940, .T. ) ;
#98372=CARTESIAN_POINT ( 'NONE',  ( -11.64875734969026233, -0.3587747205144265483, 30.51402280011862089 ) ) ;
#98385=CARTESIAN_POINT ( 'NONE',  ( 31.88667425545053291, 1.477225279485574028, -9.651215965565024035 ) ) ;
#98393=DIRECTION ( 'NONE',  ( 1.000000000000000000, 0.000000000000000000, 0.000000000000000000 ) ) ;
#98407=AXIS2_PLACEMENT_3D ( 'NONE', #49984, #58094, #36241 ) ;
#98408=DIRECTION ( 'NONE',  ( 0.000000000000000000, -1.000000000000000000, 0.000000000000000000 ) ) ;
#98418=CARTESIAN_POINT ( 'NONE',  ( 33.61456970919608978, -3.316774720514426900, -11.35828564741662738 ) ) ;
#98423=DIRECTION ( 'NONE',  ( -1.607395343451207646E-13, 0.000000000000000000, -1.000000000000000000 ) ) ;
#98428=CARTESIAN_POINT ( 'NONE',  ( -5.576923076923076650, -6.376774720514418959, 20.44941907051282470 ) ) ;
#98446=DIRECTION ( 'NONE',  ( 0.000000000000000000, 0.000000000000000000, 1.000000000000000000 ) ) ;
#98449=CARTESIAN_POINT ( 'NONE',  ( 282.9764569301858046, 5.965225279485572685, 20.79159422840526616 ) ) ;
#98461=CARTESIAN_POINT ( 'NONE',  ( 2.880689065218799083, -5.876774720514425177, 21.31732089891691828 ) ) ;
#98464=CARTESIAN_POINT ( 'NONE',  ( 30.56422633351845519, 2.967394884211873585, 24.91953760856571520 ) ) ;
#98481=ORIENTED_EDGE ( 'NONE', *, *, #20955, .F. ) ;
#98487=CARTESIAN_POINT ( 'NONE',  ( -5.988734693054777125, -5.876774720514416295, 19.95737465391042065 ) ) ;
#98489=DIRECTION ( 'NONE',  ( 0.000000000000000000, 0.000000000000000000, 1.000000000000000000 ) ) ;
#98491=CARTESIAN_POINT ( 'NONE',  ( 14.61581676225028126, -3.316774720514426456, -27.35847991880135766 ) ) ;
#98501=EDGE_CURVE ( 'NONE', #46605, #97072, #32816, .T. ) ;
#98525=AXIS2_PLACEMENT_3D ( 'NONE', #38264, #55507, #69222 ) ;
#98531=VERTEX_POINT ( 'NONE', #97209 ) ;
#98533=DIRECTION ( 'NONE',  ( -0.000000000000000000, 1.000000000000000000, -0.000000000000000000 ) ) ;
#98547=CARTESIAN_POINT ( 'NONE',  ( 4.612744205187371271, -5.876774720514418071, 20.61169588237105188 ) ) ;
#98550=LINE ( 'NONE', #53401, #45905 ) ;
#98565=VECTOR ( 'NONE', #5838, 1000.000000000000000 ) ;
#98586=CIRCLE ( 'NONE', #32174, 2.999999999999999112 ) ;
#98589=CARTESIAN_POINT ( 'NONE',  ( 7.480769230769231726, -6.376774720514420736, 20.77403846153845635 ) ) ;
#98605=CIRCLE ( 'NONE', #54878, 1.149999999999998135 ) ;
#98617=CARTESIAN_POINT ( 'NONE',  ( -17.66201745896767505, 5.965225279485572685, -23.06272557202527906 ) ) ;
#98618=CARTESIAN_POINT ( 'NONE',  ( 7.460332110455646593, -5.876774720514418071, 20.55293369838740247 ) ) ;
#98624=CARTESIAN_POINT ( 'NONE',  ( -9.278253834636473130, -6.376774720514426953, 18.21871304725684482 ) ) ;
#98625=DIRECTION ( 'NONE',  ( 0.000000000000000000, 0.000000000000000000, 1.000000000000000000 ) ) ;
#98637=CARTESIAN_POINT ( 'NONE',  ( -0.02075734969026423599, 5.965225279485572685, -0.08597719988137648983 ) ) ;
#98642=CARTESIAN_POINT ( 'NONE',  ( 3.632744579681756569, -5.876774720514403860, 18.17103827887095946 ) ) ;
#98659=FACE_OUTER_BOUND ( 'NONE', #2705, .T. ) ;
#98663=CYLINDRICAL_SURFACE ( 'NONE', #43441, 130.2784398600581710 ) ;
#98664=AXIS2_PLACEMENT_3D ( 'NONE', #44054, #61293, #67401 ) ;
#98675=UNCERTAINTY_MEASURE_WITH_UNIT (LENGTH_MEASURE( 1.000000000000000082E-05 ), #84581, 'distance_accuracy_value', 'NONE');
#98678=DIRECTION ( 'NONE',  ( -1.000000000000000000, 0.000000000000000000, 1.333806637208504346E-15 ) ) ;
#98685=ORIENTED_EDGE ( 'NONE', *, *, #73662, .T. ) ;
#98702=CARTESIAN_POINT ( 'NONE',  ( -3.108974358974355923, -6.376774720514427841, 21.75000000000001066 ) ) ;
#98711=CARTESIAN_POINT ( 'NONE',  ( 4.782775879418006859, -6.376774720514406525, 18.83817099474236656 ) ) ;
#98715=ORIENTED_EDGE ( 'NONE', *, *, #70596, .F. ) ;
#98716=VECTOR ( 'NONE', #45803, 1000.000000000000000 ) ;
#98722=EDGE_CURVE ( 'NONE', #20944, #55041, #40799, .T. ) ;
#98724=CARTESIAN_POINT ( 'NONE',  ( -0.5315124411682757843, -5.876774720514411854, 19.46509473978807847 ) ) ;
#98725=VECTOR ( 'NONE', #99969, 1000.000000000000000 ) ;
#98733=CARTESIAN_POINT ( 'NONE',  ( 12.40597316965629560, -5.152774720514427642, -26.28458722401733993 ) ) ;
#98736=EDGE_CURVE ( 'NONE', #93999, #98531, #22733, .T. ) ;
#98737=ORIENTED_EDGE ( 'NONE', *, *, #82755, .T. ) ;
#98738=CARTESIAN_POINT ( 'NONE',  ( 4.547289707988324103, -6.376774720514410077, 19.12266226838056582 ) ) ;
#98741=DIRECTION ( 'NONE',  ( 0.000000000000000000, 0.000000000000000000, 1.000000000000000000 ) ) ;
#98742=VERTEX_POINT ( 'NONE', #86473 ) ;
#98750=CARTESIAN_POINT ( 'NONE',  ( 30.93860345374796594, -0.6647747205144264315, 20.86760796525322093 ) ) ;
#98754=ORIENTED_EDGE ( 'NONE', *, *, #60696, .F. ) ;
#98758=LINE ( 'NONE', #29250, #3603 ) ;
#98764=CARTESIAN_POINT ( 'NONE',  ( -5.314757719055156038, -6.376774720514411854, 19.55912026249540858 ) ) ;
#98789=EDGE_CURVE ( 'NONE', #9886, #84887, #56548, .T. ) ;
#98792=VECTOR ( 'NONE', #53474, 1000.000000000000000 ) ;
#98801=CARTESIAN_POINT ( 'NONE',  ( 3.552327343495968570, -6.376774720514427841, 21.81288606793570395 ) ) ;
#98811=CARTESIAN_POINT ( 'NONE',  ( 27.53860345374808105, -5.356774720496559894, 19.84760796525321425 ) ) ;
#98816=CARTESIAN_POINT ( 'NONE',  ( 32.45853543194704116, -0.3587747205144265483, 9.169203677920338080 ) ) ;
#98818=CARTESIAN_POINT ( 'NONE',  ( -5.378122165843598701, -6.376774720514410077, 19.21968329462762526 ) ) ;
#98825=CARTESIAN_POINT ( 'NONE',  ( 8.978253834636468866, -5.876774720514426953, 21.48128695274316158 ) ) ;
#98834=ORIENTED_EDGE ( 'NONE', *, *, #98918, .T. ) ;
#98845=ORIENTED_EDGE ( 'NONE', *, *, #80426, .T. ) ;
#98846=LINE ( 'NONE', #14108, #33840 ) ;
#98851=EDGE_CURVE ( 'NONE', #61485, #79708, #81863, .T. ) ;
#98853=ORIENTED_EDGE ( 'NONE', *, *, #55536, .T. ) ;
#98855=ORIENTED_EDGE ( 'NONE', *, *, #60820, .F. ) ;
#98856=CARTESIAN_POINT ( 'NONE',  ( 4.263585034174699473, -6.376774720514402972, 18.26968045024142739 ) ) ;
#98858=ORIENTED_EDGE ( 'NONE', *, *, #80758, .T. ) ;
#98867=CARTESIAN_POINT ( 'NONE',  ( 6.251785340501501587, -6.376774720514424288, 21.46941214867599612 ) ) ;
#98869=AXIS2_PLACEMENT_3D ( 'NONE', #18765, #89289, #47855 ) ;
#98877=AXIS2_PLACEMENT_3D ( 'NONE', #40446, #85603, #62288 ) ;
#98879=VERTEX_POINT ( 'NONE', #43804 ) ;
#98881=DIRECTION ( 'NONE',  ( 0.000000000000000000, -1.000000000000000000, 0.000000000000000000 ) ) ;
#98888=EDGE_LOOP ( 'NONE', ( #88786, #79040, #19616, #92334 ) ) ;
#98901=CARTESIAN_POINT ( 'NONE',  ( 27.53860345374808105, -5.356774720514427379, 1.647607965253214291 ) ) ;
#98907=LINE ( 'NONE', #14168, #21495 ) ;
#98913=EDGE_CURVE ( 'NONE', #54223, #50219, #90770, .T. ) ;
#98917=ORIENTED_EDGE ( 'NONE', *, *, #68126, .F. ) ;
#98918=EDGE_CURVE ( 'NONE', #63342, #17304, #19953, .T. ) ;
#98923=CARTESIAN_POINT ( 'NONE',  ( 33.50227909998848475, -4.005981270903656188, -11.48786002470558643 ) ) ;
#98924=EDGE_LOOP ( 'NONE', ( #36477, #23219, #69085, #93736 ) ) ;
#98927=CARTESIAN_POINT ( 'NONE',  ( 0.000000000000000000, -2.056774720514426669, 4.299999999999999822 ) ) ;
#98934=EDGE_CURVE ( 'NONE', #1756, #12639, #29065, .T. ) ;
#98935=DIRECTION ( 'NONE',  ( 6.220620959342031946E-15, 0.000000000000000000, -1.000000000000000000 ) ) ;
#98942=CARTESIAN_POINT ( 'NONE',  ( 6.179707021866671646, -5.876774720514425177, 21.45334750074374242 ) ) ;
#98943=VECTOR ( 'NONE', #31506, 1000.000000000000000 ) ;
#98955=ADVANCED_FACE ( 'NONE', ( #51420 ), #5586, .T. ) ;
#98959=ORIENTED_EDGE ( 'NONE', *, *, #50843, .T. ) ;
#98963=VERTEX_POINT ( 'NONE', #99062 ) ;
#98964=CARTESIAN_POINT ( 'NONE',  ( 6.429811694900724461, -6.376774720514426065, 21.48000018967326596 ) ) ;
#98969=CARTESIAN_POINT ( 'NONE',  ( 30.56047832681635867, 2.297196155479663826, 24.67598410064777070 ) ) ;
#98989=CARTESIAN_POINT ( 'NONE',  ( 0.000000000000000000, -4.056774720514426669, 0.000000000000000000 ) ) ;
#98992=CARTESIAN_POINT ( 'NONE',  ( 15.32675665358028283, -3.579156900695799060, -27.14457288197743878 ) ) ;
#99033=CARTESIAN_POINT ( 'NONE',  ( -22.05275734969026047, 5.965225279485572685, 30.51402280011862089 ) ) ;
#99035=DIRECTION ( 'NONE',  ( 0.000000000000000000, 0.000000000000000000, -1.000000000000000000 ) ) ;
#99037=EDGE_CURVE ( 'NONE', #41750, #37181, #3299, .T. ) ;
#99042=DIRECTION ( 'NONE',  ( 0.000000000000000000, 0.000000000000000000, -1.000000000000000000 ) ) ;
#99048=VECTOR ( 'NONE', #35298, 1000.000000000000000 ) ;
#99050=CARTESIAN_POINT ( 'NONE',  ( -1.568769572606061535, -6.376774720514415407, 19.76359802465961835 ) ) ;
#99056=CARTESIAN_POINT ( 'NONE',  ( -7.999999999999996447, -6.376774720514426953, 17.50000000000000000 ) ) ;
#99059=CARTESIAN_POINT ( 'NONE',  ( 25.83488407601163672, -4.132774720514426292, -11.31196583263650091 ) ) ;
#99060=EDGE_CURVE ( 'NONE', #100399, #7123, #78140, .T. ) ;
#99062=CARTESIAN_POINT ( 'NONE',  ( -9.940598223437573822, -5.876774720514426953, 18.21871304725684837 ) ) ;
#99067=DIRECTION ( 'NONE',  ( 0.000000000000000000, 0.000000000000000000, -1.000000000000000000 ) ) ;
#99072=EDGE_CURVE ( 'NONE', #16621, #39794, #35460, .T. ) ;
#99079=ORIENTED_EDGE ( 'NONE', *, *, #22491, .F. ) ;
#99080=ORIENTED_EDGE ( 'NONE', *, *, #46440, .T. ) ;
#99093=VERTEX_POINT ( 'NONE', #25837 ) ;
#99112=CARTESIAN_POINT ( 'NONE',  ( 7.370931459274800090, -5.876774720514417183, 20.26286690110499578 ) ) ;
#99119=CARTESIAN_POINT ( 'NONE',  ( 31.81388842165050335, -4.825737335974109143, -4.598239840489335428 ) ) ;
#99121=EDGE_CURVE ( 'NONE', #96155, #100313, #29817, .T. ) ;
#99131=CARTESIAN_POINT ( 'NONE',  ( 5.331146515430939203, -5.876774720514419847, 20.91308853528358469 ) ) ;
#99134=ORIENTED_EDGE ( 'NONE', *, *, #100163, .T. ) ;
#99140=CARTESIAN_POINT ( 'NONE',  ( -20.77875734969026311, 6.143225279485574397, 29.49402280011862487 ) ) ;
#99142=CARTESIAN_POINT ( 'NONE',  ( 26.73860345374794889, -5.236829402159759894, -5.783717876163293248 ) ) ;
#99145=CARTESIAN_POINT ( 'NONE',  ( 3.421177667410919110, -0.3587747205144265483, 28.69411518427638441 ) ) ;
#99164=DIRECTION ( 'NONE',  ( 0.000000000000000000, -1.000000000000000000, 0.000000000000000000 ) ) ;
#99171=CARTESIAN_POINT ( 'NONE',  ( -1.036876607668611117, -6.376774720514417183, 20.14881673916291405 ) ) ;
#99172=FACE_OUTER_BOUND ( 'NONE', #53640, .T. ) ;
#99178=AXIS2_PLACEMENT_3D ( 'NONE', #78025, #48111, #94265 ) ;
#99182=CARTESIAN_POINT ( 'NONE',  ( -2.243088942307695177, -6.376774720514408301, 19.14743589743590491 ) ) ;
#99205=DIRECTION ( 'NONE',  ( 0.7512896232465894331, 0.000000000000000000, 0.6599726524652348436 ) ) ;
#99216=CARTESIAN_POINT ( 'NONE',  ( -2.243088942307695621, -5.876774720514409189, 19.14743589743590846 ) ) ;
#99236=DIRECTION ( 'NONE',  ( 0.000000000000000000, -1.000000000000000000, 0.000000000000000000 ) ) ;
#99240=CARTESIAN_POINT ( 'NONE',  ( 0.7051282051282083962, -6.376774720514427841, 21.75000000000000000 ) ) ;
#99242=ORIENTED_EDGE ( 'NONE', *, *, #63430, .T. ) ;
#99271=CIRCLE ( 'NONE', #58803, 3.349999999999998757 ) ;
#99301=CARTESIAN_POINT ( 'NONE',  ( 2.989331223418256744, -5.876774720514424288, 21.46569930292093886 ) ) ;
#99304=CARTESIAN_POINT ( 'NONE',  ( -10.75273025779354263, -6.376774720514426953, 16.96478738960562893 ) ) ;
#99308=CARTESIAN_POINT ( 'NONE',  ( 15.97264540888995299, -3.316774720514426456, -27.93485543958162154 ) ) ;
#99317=CARTESIAN_POINT ( 'NONE',  ( 30.45304879119406039, -4.772774720514425972, -10.07140455160086390 ) ) ;
#99322=CARTESIAN_POINT ( 'NONE',  ( 7.343377932919765705, -5.876774720514422512, 21.31293098237466310 ) ) ;
#99324=DIRECTION ( 'NONE',  ( -0.000000000000000000, 1.000000000000000000, -0.000000000000000000 ) ) ;
#99326=DIRECTION ( 'NONE',  ( 0.000000000000000000, 0.000000000000000000, -1.000000000000000000 ) ) ;
#99332=ORIENTED_EDGE ( 'NONE', *, *, #71874, .T. ) ;
#99333=VERTEX_POINT ( 'NONE', #70908 ) ;
#99337=CIRCLE ( 'NONE', #73436, 129.7684398600581517 ) ;
#99347=AXIS2_PLACEMENT_3D ( 'NONE', #94689, #24669, #71869 ) ;
#99350=CARTESIAN_POINT ( 'NONE',  ( 22.81105451610979173, 1.477225279485574028, -18.46691820600746681 ) ) ;
#99355=EDGE_CURVE ( 'NONE', #74013, #8750, #32334, .T. ) ;
#99356=CARTESIAN_POINT ( 'NONE',  ( 4.782775879418006859, -5.876774720514404748, 18.83817099474236656 ) ) ;
#99370=ORIENTED_EDGE ( 'NONE', *, *, #17258, .T. ) ;
#99374=VECTOR ( 'NONE', #64147, 1000.000000000000114 ) ;
#99378=DIRECTION ( 'NONE',  ( -1.000000000000000000, 0.000000000000000000, 0.000000000000000000 ) ) ;
#99404=DIRECTION ( 'NONE',  ( 1.000000000000000000, 0.000000000000000000, 0.000000000000000000 ) ) ;
#99415=EDGE_CURVE ( 'NONE', #15961, #46809, #3408, .T. ) ;
#99423=VERTEX_POINT ( 'NONE', #58185 ) ;
#99425=CARTESIAN_POINT ( 'NONE',  ( 30.93860345374796594, 5.515143950957555496, 14.99689261510125249 ) ) ;
#99431=DIRECTION ( 'NONE',  ( -0.000000000000000000, 1.000000000000000000, -0.000000000000000000 ) ) ;
#99444=VECTOR ( 'NONE', #45514, 1000.000000000000000 ) ;
#99453=ORIENTED_EDGE ( 'NONE', *, *, #63162, .F. ) ;
#99479=CIRCLE ( 'NONE', #15026, 1.835999999999931465 ) ;
#99487=EDGE_LOOP ( 'NONE', ( #33956, #22568, #18043, #97448 ) ) ;
#99488=CARTESIAN_POINT ( 'NONE',  ( -5.941268476065055815, -5.876774720514417183, 20.11414146978959749 ) ) ;
#99492=DIRECTION ( 'NONE',  ( -0.7682573101345366862, 0.000000000000000000, 0.6401411605457395515 ) ) ;
#99496=PLANE ( 'NONE',  #80841 ) ;
#99502=DIRECTION ( 'NONE',  ( -0.6559908753439240847, -0.4874460344622444929, -0.5762571777883070956 ) ) ;
#99508=LINE ( 'NONE', #84292, #32024 ) ;
#99519=DIRECTION ( 'NONE',  ( 0.000000000000000000, 0.000000000000000000, -1.000000000000000000 ) ) ;
#99520=EDGE_CURVE ( 'NONE', #54808, #75788, #43459, .T. ) ;
#99526=CARTESIAN_POINT ( 'NONE',  ( -1.371775545366004545, -6.376774720514413630, 20.39230070883894186 ) ) ;
#99529=CARTESIAN_POINT ( 'NONE',  ( 5.328346181807287252, -6.376774720514418959, 20.81670806933143680 ) ) ;
#99530=DIRECTION ( 'NONE',  ( 1.046287966022745640E-14, 0.000000000000000000, -1.000000000000000000 ) ) ;
#99537=CARTESIAN_POINT ( 'NONE',  ( 6.431460800610004469, -5.356774720514426491, -25.38187206382939465 ) ) ;
#99543=CARTESIAN_POINT ( 'NONE',  ( -2.070328576748420524, -5.876774720514410077, 19.46575348430201657 ) ) ;
#99551=DIRECTION ( 'NONE',  ( 0.000000000000000000, -1.000000000000000000, 0.000000000000000000 ) ) ;
#99554=DIRECTION ( 'NONE',  ( 0.000000000000000000, 0.000000000000000000, 1.000000000000000000 ) ) ;
#99563=VERTEX_POINT ( 'NONE', #44452 ) ;
#99571=ORIENTED_EDGE ( 'NONE', *, *, #97937, .T. ) ;
#99586=CARTESIAN_POINT ( 'NONE',  ( 6.727764423076923350, -6.376774720514413630, 19.76442307692307665 ) ) ;
#99589=EDGE_CURVE ( 'NONE', #52189, #50219, #32200, .T. ) ;
#99613=B_SPLINE_CURVE_WITH_KNOTS ( 'NONE', 3,
 ( #54617, #15536, #24647, #8934 ),
 .UNSPECIFIED., .F., .F.,
 ( 4, 4 ),
 ( 0.000000000000000000, 0.001096191829319139886 ),
 .UNSPECIFIED. ) ;
#99615=EDGE_LOOP ( 'NONE', ( #2391, #76745, #1226, #22265 ) ) ;
#99628=ORIENTED_EDGE ( 'NONE', *, *, #417, .F. ) ;
#99630=PLANE ( 'NONE',  #54696 ) ;
#99632=ADVANCED_FACE ( 'NONE', ( #9365 ), #61546, .T. ) ;
#99636=AXIS2_PLACEMENT_3D ( 'NONE', #65763, #65271, #4838 ) ;
#99640=DIRECTION ( 'NONE',  ( -0.000000000000000000, 1.000000000000000000, -0.000000000000000000 ) ) ;
#99665=ORIENTED_EDGE ( 'NONE', *, *, #85496, .T. ) ;
#99670=VECTOR ( 'NONE', #49477, 1000.000000000000000 ) ;
#99680=CARTESIAN_POINT ( 'NONE',  ( -1.044871794871793602, -6.376774720514418959, 20.44941907051282115 ) ) ;
#99688=ORIENTED_EDGE ( 'NONE', *, *, #58068, .T. ) ;
#99689=CARTESIAN_POINT ( 'NONE',  ( 4.115763745420833786, -6.376774720514402972, 18.20859014712428348 ) ) ;
#99691=ORIENTED_EDGE ( 'NONE', *, *, #98026, .T. ) ;
#99693=ORIENTED_EDGE ( 'NONE', *, *, #62081, .F. ) ;
#99700=ORIENTED_EDGE ( 'NONE', *, *, #84459, .F. ) ;
#99701=CARTESIAN_POINT ( 'NONE',  ( -3.108425644221024520, -6.376774720514415407, 20.25188360057253334 ) ) ;
#99705=DIRECTION ( 'NONE',  ( 0.000000000000000000, -1.000000000000000000, 0.000000000000000000 ) ) ;
#99714=ORIENTED_EDGE ( 'NONE', *, *, #6286, .T. ) ;
#99724=DIRECTION ( 'NONE',  ( 0.000000000000000000, 0.000000000000000000, 1.000000000000000000 ) ) ;
#99727=CARTESIAN_POINT ( 'NONE',  ( 26.37445894957760473, -2.682774720514426559, -11.69480419648520986 ) ) ;
#99737=VECTOR ( 'NONE', #26347, 1000.000000000000000 ) ;
#99741=CARTESIAN_POINT ( 'NONE',  ( 15.99960863614631101, -3.577630190450212577, -27.91116951066581819 ) ) ;
#99743=AXIS2_PLACEMENT_3D ( 'NONE', #59470, #67100, #98005 ) ;
#99744=VECTOR ( 'NONE', #23001, 1000.000000000000114 ) ;
#99745=ORIENTED_EDGE ( 'NONE', *, *, #34686, .F. ) ;
#99751=CIRCLE ( 'NONE', #21962, 7.652410033082760243 ) ;
#99756=CARTESIAN_POINT ( 'NONE',  ( -2.220741593810419801, -5.876774720514410077, 19.46247113826587238 ) ) ;
#99760=EDGE_CURVE ( 'NONE', #2589, #64840, #71782, .T. ) ;
#99768=ORIENTED_EDGE ( 'NONE', *, *, #91640, .F. ) ;
#99778=CARTESIAN_POINT ( 'NONE',  ( 2.880689065218799083, -5.876774720514426065, 21.31732089891691828 ) ) ;
#99794=VECTOR ( 'NONE', #78124, 1000.000000000000000 ) ;
#99804=CARTESIAN_POINT ( 'NONE',  ( -5.755030174389611730, -6.376774720514411854, 19.56655654527324728 ) ) ;
#99810=EDGE_LOOP ( 'NONE', ( #9878, #73064, #33344, #55339, #76120 ) ) ;
#99814=AXIS2_PLACEMENT_3D ( 'NONE', #84809, #30020, #83308 ) ;
#99823=ORIENTED_EDGE ( 'NONE', *, *, #93055, .T. ) ;
#99826=VECTOR ( 'NONE', #79481, 1000.000000000000000 ) ;
#99838=DIRECTION ( 'NONE',  ( 0.000000000000000000, -1.000000000000000000, 0.000000000000000000 ) ) ;
#99842=EDGE_LOOP ( 'NONE', ( #45600, #33177, #93524, #666 ) ) ;
#99847=LINE ( 'NONE', #61328, #28488 ) ;
#99849=VECTOR ( 'NONE', #45876, 1000.000000000000000 ) ;
#99854=CARTESIAN_POINT ( 'NONE',  ( 6.110660513271839456, -6.376774720514422512, 21.43053473047838509 ) ) ;
#99856=ADVANCED_FACE ( 'NONE', ( #58554 ), #91476, .F. ) ;
#99864=CARTESIAN_POINT ( 'NONE',  ( 10.75273025779354263, -5.876774720514426953, 16.96478738960562893 ) ) ;
#99865=CARTESIAN_POINT ( 'NONE',  ( 7.089543269230769162, -5.876774720514413630, 19.75741185897435415 ) ) ;
#99880=CARTESIAN_POINT ( 'NONE',  ( 0.3910256410256394144, -5.876774720514412742, 19.63681891025641235 ) ) ;
#99892=FACE_OUTER_BOUND ( 'NONE', #53591, .T. ) ;
#99897=AXIS2_PLACEMENT_3D ( 'NONE', #4482, #88713, #20182 ) ;
#99904=CARTESIAN_POINT ( 'NONE',  ( 33.55975867735808293, -4.270419025147598191, -12.32584534477734728 ) ) ;
#99909=CARTESIAN_POINT ( 'NONE',  ( 22.81105451610979173, 6.475225279485573360, -19.61691820600746539 ) ) ;
#99918=EDGE_CURVE ( 'NONE', #73552, #53085, #86606, .T. ) ;
#99926=CIRCLE ( 'NONE', #86973, 2.249999999999998668 ) ;
#99927=CARTESIAN_POINT ( 'NONE',  ( 5.696197030082937651, -5.876774720514422512, 21.05387829558662816 ) ) ;
#99929=CARTESIAN_POINT ( 'NONE',  ( 6.431189903846153300, -5.876774720514424288, 20.08974358974358765 ) ) ;
#99936=DIRECTION ( 'NONE',  ( 0.000000000000000000, -1.000000000000000000, 0.000000000000000000 ) ) ;
#99939=AXIS2_PLACEMENT_3D ( 'NONE', #9160, #69061, #16273 ) ;
#99944=EDGE_LOOP ( 'NONE', ( #21754, #17888, #53930, #69636, #7582 ) ) ;
#99954=VERTEX_POINT ( 'NONE', #62045 ) ;
#99955=AXIS2_PLACEMENT_3D ( 'NONE', #35724, #66697, #97608 ) ;
#99966=EDGE_CURVE ( 'NONE', #89557, #63566, #24415, .T. ) ;
#99969=DIRECTION ( 'NONE',  ( 1.000000000000000000, 0.000000000000000000, 0.000000000000000000 ) ) ;
#99971=VERTEX_POINT ( 'NONE', #30582 ) ;
#99974=VERTEX_POINT ( 'NONE', #1648 ) ;
#99983=VERTEX_POINT ( 'NONE', #24967 ) ;
#99984=CARTESIAN_POINT ( 'NONE',  ( -6.720452724358975338, -6.376774720514411854, 19.46153846153846700 ) ) ;
#99986=CIRCLE ( 'NONE', #90312, 1.399999999999988143 ) ;
#100016=CARTESIAN_POINT ( 'NONE',  ( 7.089543269230769162, -6.376774720514413630, 19.75741185897435415 ) ) ;
#100019=CARTESIAN_POINT ( 'NONE',  ( 32.74291612378888061, -3.662501476888925467, -3.918438066536008346 ) ) ;
#100020=CARTESIAN_POINT ( 'NONE',  ( 5.994920710892026605, -6.376774720514429617, 21.76186867112717138 ) ) ;
#100023=CARTESIAN_POINT ( 'NONE',  ( -10.16634758543296613, 6.475225279485573360, 30.00402280011862288 ) ) ;
#100024=ADVANCED_FACE ( 'NONE', ( #86374 ), #36371, .T. ) ;
#100025=CARTESIAN_POINT ( 'NONE',  ( -29.49875734969026198, -0.3587747205144265483, 2.362022800118626531 ) ) ;
#100037=CARTESIAN_POINT ( 'NONE',  ( -1.649669150391666506, -6.376774720514411854, 19.67464842890028365 ) ) ;
#100059=CARTESIAN_POINT ( 'NONE',  ( -6.128026245051341192, -6.376774720514410077, 19.39236848396478763 ) ) ;
#100069=VERTEX_POINT ( 'NONE', #5134 ) ;
#100070=CARTESIAN_POINT ( 'NONE',  ( -41.32836283488544638, -2.682774720514426559, 39.26872235229541985 ) ) ;
#100073=TOROIDAL_SURFACE ( 'NONE', #96931, 3.060000000000000053, 2.040000000000000036 ) ;
#100077=CARTESIAN_POINT ( 'NONE',  ( 32.85081302853803464, -3.622774720514426949, -13.10817780685209577 ) ) ;
#100088=ORIENTED_EDGE ( 'NONE', *, *, #93055, .F. ) ;
#100097=ORIENTED_EDGE ( 'NONE', *, *, #4122, .F. ) ;
#100100=CARTESIAN_POINT ( 'NONE',  ( 32.24176898385614720, -6.243294140736224129, 2.116998906223432453 ) ) ;
#100101=ORIENTED_EDGE ( 'NONE', *, *, #34042, .F. ) ;
#100105=DIRECTION ( 'NONE',  ( -2.338552693767719605E-15, 0.000000000000000000, 1.000000000000000000 ) ) ;
#100109=CARTESIAN_POINT ( 'NONE',  ( 20.84838633257991347, -4.362234729430479518, -17.34205791096968241 ) ) ;
#100115=CARTESIAN_POINT ( 'NONE',  ( 33.13288845015618023, -0.3587747205144265483, -0.1650522222209214185 ) ) ;
#100119=DIRECTION ( 'NONE',  ( -0.06283980576413539243, -0.000000000000000000, -0.9980236263794188822 ) ) ;
#100124=B_SPLINE_SURFACE_WITH_KNOTS ( 'NONE', 3, 1, ( 
 ( #36514, #68967 ),
 ( #67480, #29902 ),
 ( #90809, #22272 ),
 ( #21280, #53256 ),
 ( #84184, #14675 ),
 ( #9070, #69469 ),
 ( #56271, #8577 ),
 ( #39016, #9569 ),
 ( #47647, #30904 ),
 ( #85697, #94298 ),
 ( #79073, #77565 ),
 ( #40023, #46645 ),
 ( #17178, #7569 ),
 ( #40535, #39523 ),
 ( #61870, #78562 ),
 ( #24786, #55765 ),
 ( #8068, #48149 ),
 ( #32412, #31912 ),
 ( #70980, #960 ) ),
 .UNSPECIFIED., .F., .F., .F.,
 ( 4, 1, 1, 1, 1, 1, 1, 1, 1, 1, 1, 1, 1, 1, 1, 1, 4 ),
 ( 2, 2 ),
 ( 0.000000000000000000, 0.07563486594245749650, 0.1456749912579857753, 0.2101933844674984675, 0.2691971886348948351, 0.3228467966362095209, 0.3711350468222360810, 0.4143602045761041186, 0.4526539356929057956, 0.5231868047418553047, 0.5919172609462788337, 0.6599757056395081367, 0.7292117337225374474, 0.7981350023964017826, 0.8652933977976435820, 0.9318417558440023063, 1.000000000000000000 ),
 ( 0.000000000000000000, 1.000000000000000000 ),
 .UNSPECIFIED. ) ;
#100128=CARTESIAN_POINT ( 'NONE',  ( 5.326923076923078426, -5.876774720514419847, 20.76772836538461320 ) ) ;
#100134=LINE ( 'NONE', #74828, #81477 ) ;
#100148=EDGE_CURVE ( 'NONE', #1588, #7066, #95695, .T. ) ;
#100149=ADVANCED_FACE ( 'NONE', ( #68046 ), #23273, .T. ) ;
#100157=ORIENTED_EDGE ( 'NONE', *, *, #22363, .T. ) ;
#100159=LINE ( 'NONE', #38285, #25738 ) ;
#100160=B_SPLINE_CURVE_WITH_KNOTS ( 'NONE', 3,
 ( #52897, #99537, #61011, #91944, #53400, #93435, #93943, #71623, #17323, #15815, #1613, #2121 ),
 .UNSPECIFIED., .F., .F.,
 ( 4, 2, 2, 2, 2, 4 ),
 ( 0.000000000000000000, 0.08114505568447454020, 0.1622901113689490804, 0.3245802227378981608, 0.4868703341068472135, 0.6491604454757963216 ),
 .UNSPECIFIED. ) ;
#100163=EDGE_CURVE ( 'NONE', #64365, #71450, #58930, .T. ) ;
#100165=FACE_OUTER_BOUND ( 'NONE', #12955, .T. ) ;
#100168=DIRECTION ( 'NONE',  ( -0.000000000000000000, 1.000000000000000000, -0.000000000000000000 ) ) ;
#100172=AXIS2_PLACEMENT_3D ( 'NONE', #12693, #75091, #20799 ) ;
#100182=CARTESIAN_POINT ( 'NONE',  ( 4.588387839717440464, -6.376774720514401196, 18.52756237589653665 ) ) ;
#100183=DIRECTION ( 'NONE',  ( 0.000000000000000000, 0.000000000000000000, -1.000000000000000000 ) ) ;
#100190=CARTESIAN_POINT ( 'NONE',  ( -4.141166922167975883, -6.376774720514420736, 20.63520656483649063 ) ) ;
#100194=DIRECTION ( 'NONE',  ( 0.000000000000000000, 0.000000000000000000, 1.000000000000000000 ) ) ;
#100195=LINE ( 'NONE', #70283, #32032 ) ;
#100201=VERTEX_POINT ( 'NONE', #37584 ) ;
#100207=CARTESIAN_POINT ( 'NONE',  ( 33.69795529655567634, -0.6647747205144264315, 23.11160796525322070 ) ) ;
#100209=B_SPLINE_SURFACE_WITH_KNOTS ( 'NONE', 3, 1, ( 
 ( #12985, #61189 ),
 ( #52565, #37344 ),
 ( #99701, #44959 ),
 ( #37830, #68784 ),
 ( #43950, #92109 ),
 ( #83497, #5880 ),
 ( #36842, #7366 ),
 ( #59688, #53574 ),
 ( #29221, #21098 ),
 ( #76865, #53072 ),
 ( #67297, #52066 ),
 ( #51571, #75884 ),
 ( #91609, #20602 ),
 ( #84499, #38319 ),
 ( #30206, #36341 ),
 ( #98218, #5386 ),
 ( #6384, #69279 ),
 ( #60189, #68287 ),
 ( #44456, #99216 ) ),
 .UNSPECIFIED., .F., .F., .F.,
 ( 4, 1, 1, 1, 1, 1, 1, 1, 1, 1, 1, 1, 1, 1, 1, 1, 4 ),
 ( 2, 2 ),
 ( 0.000000000000000000, 0.06761452606740225857, 0.1311670463014497079, 0.1902933887105121569, 0.2450610151831991157, 0.2960272302790619703, 0.3428447301738881681, 0.3860527037713289422, 0.4255709801320508578, 0.4995034801514162126, 0.5702922612469554231, 0.6402757819125015626, 0.7105295546786241090, 0.7812030014762990637, 0.8520349845172640046, 0.9243956695042545579, 1.000000000000000000 ),
 ( 0.000000000000000000, 1.000000000000000000 ),
 .UNSPECIFIED. ) ;
#100212=EDGE_LOOP ( 'NONE', ( #61532, #30982 ) ) ;
#100228=DIRECTION ( 'NONE',  ( -0.000000000000000000, 1.000000000000000000, -0.000000000000000000 ) ) ;
#100240=ORIENTED_EDGE ( 'NONE', *, *, #93180, .T. ) ;
#100243=LINE ( 'NONE', #38868, #18336 ) ;
#100248=CARTESIAN_POINT ( 'NONE',  ( 30.09341516180546350, -1.682774720514426114, -11.39311774897855933 ) ) ;
#100257=CYLINDRICAL_SURFACE ( 'NONE', #7751, 91.74549126261076992 ) ;
#100276=CARTESIAN_POINT ( 'NONE',  ( 3.797776442307698286, -5.876774720514427841, 21.83974358974358410 ) ) ;
#100281=ORIENTED_EDGE ( 'NONE', *, *, #57873, .T. ) ;
#100287=AXIS2_PLACEMENT_3D ( 'NONE', #71760, #2252, #48927 ) ;
#100291=VECTOR ( 'NONE', #31663, 1000.000000000000000 ) ;
#100303=CARTESIAN_POINT ( 'NONE',  ( -5.706951327759631099, -5.876774720514411854, 19.48569229636961353 ) ) ;
#100306=CARTESIAN_POINT ( 'NONE',  ( 11.62916340711181284, 5.965225279485572685, 28.75961759920349792 ) ) ;
#100307=DIRECTION ( 'NONE',  ( 0.000000000000000000, 0.000000000000000000, -1.000000000000000000 ) ) ;
#100309=AXIS2_PLACEMENT_3D ( 'NONE', #93215, #77483, #78486 ) ;
#100313=VERTEX_POINT ( 'NONE', #76132 ) ;
#100314=ORIENTED_EDGE ( 'NONE', *, *, #2514, .F. ) ;
#100319=ORIENTED_EDGE ( 'NONE', *, *, #89894, .T. ) ;
#100329=ORIENTED_EDGE ( 'NONE', *, *, #34498, .T. ) ;
#100333=DIRECTION ( 'NONE',  ( 0.000000000000000000, -1.000000000000000000, 0.000000000000000000 ) ) ;
#100339=CARTESIAN_POINT ( 'NONE',  ( 3.960454120839856706, -6.376774720514402972, 18.17119035270509997 ) ) ;
#100349=ORIENTED_EDGE ( 'NONE', *, *, #79456, .F. ) ;
#100355=CARTESIAN_POINT ( 'NONE',  ( 22.81105451610979173, 8.475225279485572472, -18.46691820600746681 ) ) ;
#100356=ORIENTED_EDGE ( 'NONE', *, *, #41367, .F. ) ;
#100363=LINE ( 'NONE', #79047, #26008 ) ;
#100371=VECTOR ( 'NONE', #30976, 1000.000000000000000 ) ;
#100373=CARTESIAN_POINT ( 'NONE',  ( -5.891025641025637860, -5.876774720514426953, 21.75000000000000711 ) ) ;
#100374=CIRCLE ( 'NONE', #76052, 3.060000000000000053 ) ;
#100388=ADVANCED_FACE ( 'NONE', ( #41098 ), #87255, .F. ) ;
#100389=ORIENTED_EDGE ( 'NONE', *, *, #47630, .F. ) ;
#100399=VERTEX_POINT ( 'NONE', #32982 ) ;
#100403=CARTESIAN_POINT ( 'NONE',  ( 32.84232313084928023, -4.840274619472680229, -11.71291885348849782 ) ) ;
#100411=CARTESIAN_POINT ( 'NONE',  ( -1.001577508147789342, -6.376774720514411854, 19.87297243748311004 ) ) ;
#100448=COLOUR_RGB('Sky Blue', 0.40784314, 0.44705882, 0.49803922);
#100449=FILL_AREA_STYLE_COLOUR('',#100448);
#100450=FILL_AREA_STYLE('',(#100449));
#100451=SURFACE_STYLE_FILL_AREA(#100450);
#100452=SURFACE_SIDE_STYLE('',(#100451));
#100453=SURFACE_STYLE_USAGE(.BOTH.,#100452);
#100454=PRESENTATION_STYLE_ASSIGNMENT((#100453));
#100494=STYLED_ITEM('',(#100454),#44893);
#100495=MECHANICAL_DESIGN_GEOMETRIC_PRESENTATION_REPRESENTATION('',(#100494),#61811);
ENDSEC;
END-ISO-10303-21;
